ISO-10303-21;
HEADER;
FILE_DESCRIPTION (('STEP AP214'),
    '1' );
FILE_NAME ('MAS-673 Main Body.step',
    '2026-10-09T13:48:35',
    ( '' ),
    ( '' ),
    'SwSTEP 2.0',
    'SolidWorks 2026',
    '' );
FILE_SCHEMA (( 'AUTOMOTIVE_DESIGN' ));
ENDSEC;

DATA;
#1=VERTEX_POINT ( 'NONE', #550 ) ;
#2=CARTESIAN_POINT ( 'NONE',  ( -13.11728842303999976, -9.638936811879000643, -0.7309380707209000017 ) ) ;
#3=CIRCLE ( 'NONE', #13143, 12.50000000000000178 ) ;
#7=CARTESIAN_POINT ( 'NONE',  ( -10.64042603139669296, 15.44559798911979875, -1.499885078173281761 ) ) ;
#9=CARTESIAN_POINT ( 'NONE',  ( 14.76827916823049058, 9.002773128276517767, -5.059891690319244795 ) ) ;
#10=FACE_OUTER_BOUND ( 'NONE', #17299, .T. ) ;
#11=CARTESIAN_POINT ( 'NONE',  ( 19.46336793902999673, -11.08665823510999893, -1.415474986610000041 ) ) ;
#13=CARTESIAN_POINT ( 'NONE',  ( 14.10130024463479792, 4.527370814775449226, 7.815105637936889948 ) ) ;
#14=CARTESIAN_POINT ( 'NONE',  ( -6.552349917305206439, 15.43140745850629436, -1.524086724148710381 ) ) ;
#16=ADVANCED_FACE ( 'NONE', ( #18854 ), #20406, .T. ) ;
#17=VERTEX_POINT ( 'NONE', #2260 ) ;
#19=CARTESIAN_POINT ( 'NONE',  ( 24.50000000000000355, -10.15196322910628446, 1.570734485538005432 ) ) ;
#21=CARTESIAN_POINT ( 'NONE',  ( 11.82354270082560532, -9.054930663370594601, -3.446502399965523988 ) ) ;
#22=DIRECTION ( 'NONE',  ( -0.4719825803775118955, 0.1835218107899219686, 0.8622947226932178300 ) ) ;
#23=CARTESIAN_POINT ( 'NONE',  ( 18.51344355829000321, 13.93375672974000068, 0.000000000000000000 ) ) ;
#24=CARTESIAN_POINT ( 'NONE',  ( 19.10289643275000060, 0.6522580741204999644, 11.12207985314999803 ) ) ;
#26=CARTESIAN_POINT ( 'NONE',  ( -6.057596641756035183, 16.18429473919449890, 1.000000003976580842 ) ) ;
#29=ORIENTED_EDGE ( 'NONE', *, *, #18417, .F. ) ;
#30=CARTESIAN_POINT ( 'NONE',  ( -11.32728006584999925, -6.662114061867999482, 13.29187989938000136 ) ) ;
#34=CARTESIAN_POINT ( 'NONE',  ( -14.44097978627303469, 9.338505494776397242, 8.825220280766517433 ) ) ;
#35=CARTESIAN_POINT ( 'NONE',  ( 18.85240113949000218, -1.886779804701000041, 10.26112574610000117 ) ) ;
#36=B_SPLINE_CURVE_WITH_KNOTS ( 'NONE', 3,
 ( #18610, #11347, #22470, #18840, #2244, #6487, #13619, #2487, #661, #2741, #2366, #8067, #8431, #4429, #11583, #6112, #2611, #904 ),
 .UNSPECIFIED., .F., .F.,
 ( 4, 2, 2, 2, 2, 2, 2, 2, 4 ),
 ( 0.000000000000000000, 0.1250000000000000000, 0.2500000000000000000, 0.3750000000000000000, 0.5000000000000000000, 0.6250000000000000000, 0.7500000000000000000, 0.8750000000000000000, 1.000000000000000000 ),
 .UNSPECIFIED. ) ;
#38=CARTESIAN_POINT ( 'NONE',  ( 15.95305559329677436, -9.354823168593970451, -4.455688050559385438 ) ) ;
#39=CARTESIAN_POINT ( 'NONE',  ( -16.96748435807999655, 1.976003357569000141, -10.89472041289000082 ) ) ;
#41=CARTESIAN_POINT ( 'NONE',  ( -14.13294016288999977, 9.260019365940999947, -2.871107829034000414 ) ) ;
#42=EDGE_CURVE ( 'NONE', #6468, #23190, #12973, .T. ) ;
#44=VERTEX_POINT ( 'NONE', #7955 ) ;
#46=CARTESIAN_POINT ( 'NONE',  ( 19.50479438917271935, -10.32712268973978276, -1.911112615691448413 ) ) ;
#49=CARTESIAN_POINT ( 'NONE',  ( 4.864388344928220143, 14.50529179307395289, -3.789926123251598611 ) ) ;
#50=EDGE_CURVE ( 'NONE', #3196, #1114, #6484, .T. ) ;
#51=CARTESIAN_POINT ( 'NONE',  ( 11.28262625730999957, -8.806575700274999363, 0.9184129047361999643 ) ) ;
#53=B_SPLINE_CURVE_WITH_KNOTS ( 'NONE', 3,
 ( #23724, #16684, #11126, #22035, #20219, #20108, #94, #18511, #3517, #11252 ),
 .UNSPECIFIED., .F., .F.,
 ( 4, 2, 2, 2, 4 ),
 ( 0.000000000000000000, 0.1250000000000000000, 0.2500000000000000000, 0.4999999999999998890, 1.000000000000000000 ),
 .UNSPECIFIED. ) ;
#54=CARTESIAN_POINT ( 'NONE',  ( -14.25243324638999809, 7.716878364870000340, -11.63397459621999985 ) ) ;
#56=ORIENTED_EDGE ( 'NONE', *, *, #14846, .T. ) ;
#57=CARTESIAN_POINT ( 'NONE',  ( -15.49705420454666971, 1.186998013042136924, 9.068966667013654614 ) ) ;
#58=CARTESIAN_POINT ( 'NONE',  ( 3.983126710162000705, 12.34486698612999866, 2.717232713520998377 ) ) ;
#59=CARTESIAN_POINT ( 'NONE',  ( 12.00000000000000000, -1.960251216180438627, -9.262521325554040175 ) ) ;
#60=CARTESIAN_POINT ( 'NONE',  ( -15.96442470609999909, 5.230920372153000208, -8.223195615302000050 ) ) ;
#61=CARTESIAN_POINT ( 'NONE',  ( 18.86608333333332510, 2.396295210176243362, -8.917180031126768824 ) ) ;
#62=CARTESIAN_POINT ( 'NONE',  ( -23.39238510356613077, -5.190431350648047726, 9.217397525632280875 ) ) ;
#65=CARTESIAN_POINT ( 'NONE',  ( -5.500092053744999099, 15.58942091952000020, 2.547331119493998042 ) ) ;
#69=ADVANCED_FACE ( 'NONE', ( #11713 ), #19084, .F. ) ;
#71=CARTESIAN_POINT ( 'NONE',  ( 13.99789824808406102, 8.658198223038986896, -2.745508126827834516 ) ) ;
#72=CARTESIAN_POINT ( 'NONE',  ( -22.78638441723432706, -9.917706536484757862, -3.646566398122319530 ) ) ;
#74=B_SPLINE_CURVE_WITH_KNOTS ( 'NONE', 3,
 ( #8588, #12348, #14154, #1319, #8708, #1438, #3264, #4839, #5196, #6638 ),
 .UNSPECIFIED., .F., .F.,
 ( 4, 2, 2, 2, 4 ),
 ( 0.000000000000000000, 0.1249999999999999722, 0.2499999999999999445, 0.4999999999999998890, 1.000000000000000000 ),
 .UNSPECIFIED. ) ;
#76=CARTESIAN_POINT ( 'NONE',  ( 2.570568752299490445, 11.76159806634492000, 4.083892722200570091 ) ) ;
#78=CARTESIAN_POINT ( 'NONE',  ( -4.424293379393901660, 12.29270965195770771, -1.981197220050498808 ) ) ;
#80=CARTESIAN_POINT ( 'NONE',  ( 24.40278699097224901, 12.15528518867914620, 3.946428472716975833 ) ) ;
#85=CARTESIAN_POINT ( 'NONE',  ( 15.06487658531000129, -2.993859790429000078, 9.737735315623000432 ) ) ;
#86=CARTESIAN_POINT ( 'NONE',  ( 18.41753846593428889, 9.434636916628203807, -4.442455713531500372 ) ) ;
#89=CARTESIAN_POINT ( 'NONE',  ( -5.194121241778000275, 0.000000000000000000, 0.000000000000000000 ) ) ;
#93=VERTEX_POINT ( 'NONE', #21155 ) ;
#94=CARTESIAN_POINT ( 'NONE',  ( -24.37124162822892259, 12.10385983559126544, 4.035505227296849462 ) ) ;
#95=CARTESIAN_POINT ( 'NONE',  ( 22.24919044816000024, 10.13534249229999951, 5.028067520505000054 ) ) ;
#96=CARTESIAN_POINT ( 'NONE',  ( -24.02103270219855347, 2.506500440823137055, 9.528970304172808881 ) ) ;
#98=DIRECTION ( 'NONE',  ( 0.000000000000000000, 1.000000000000000000, 0.000000000000000000 ) ) ;
#99=CARTESIAN_POINT ( 'NONE',  ( 24.00016455292000117, -9.066063387507998783, 2.014468017461000127 ) ) ;
#100=CARTESIAN_POINT ( 'NONE',  ( -2.710948798071000088, 11.76207888428000103, 4.122880019904000548 ) ) ;
#107=CARTESIAN_POINT ( 'NONE',  ( 6.643062618671002006, 13.49901315086000686, 0.1224259533632999497 ) ) ;
#108=CARTESIAN_POINT ( 'NONE',  ( -4.371488211232004595, 13.35998688340998619, 5.531286660341000250 ) ) ;
#110=DIRECTION ( 'NONE',  ( 0.000000000000000000, -1.000000000000000000, 0.000000000000000000 ) ) ;
#112=CARTESIAN_POINT ( 'NONE',  ( 13.96800158531000058, -3.572926710108999870, -9.509691282521000488 ) ) ;
#113=CARTESIAN_POINT ( 'NONE',  ( -12.30476703115999904, 8.600742661000001732, -2.211712587549000020 ) ) ;
#114=CARTESIAN_POINT ( 'NONE',  ( 18.30262625730999915, -5.463569446885998993, 7.195226492777999638 ) ) ;
#117=ORIENTED_EDGE ( 'NONE', *, *, #18565, .T. ) ;
#118=CARTESIAN_POINT ( 'NONE',  ( -10.19274265977768579, 15.86535919139761219, -1.103256594710403160 ) ) ;
#119=B_SPLINE_CURVE_WITH_KNOTS ( 'NONE', 3,
 ( #6295, #17317, #2307, #720, #6416, #11875, #4485, #2421, #8128, #2671, #16960, #10062, #17075, #17447, #15493, #7994, #19128, #22524, #22758, #5931, #9575, #4122, #840, #15126, #13437, #8242, #11756, #15368, #13799, #21198, #11640, #11519, #6177, #359, #18898, #13563, #9694, #473, #7877, #15244, #22636, #20957 ),
 .UNSPECIFIED., .F., .F.,
 ( 4, 2, 1, 2, 2, 2, 1, 2, 2, 2, 2, 2, 2, 2, 2, 1, 2, 2, 2, 1, 2, 2, 4 ),
 ( 0.000000000000000000, 0.06250000000000149880, 0.09375000000000216493, 0.1093750000000024009, 0.1250000000000026368, 0.1875000000000031641, 0.2187500000000033307, 0.2343750000000034139, 0.2500000000000034972, 0.3125000000000032752, 0.3750000000000030531, 0.5000000000000025535, 0.5625000000000022204, 0.6250000000000019984, 0.6875000000000016653, 0.7187500000000015543, 0.7343750000000015543, 0.7500000000000014433, 0.8125000000000007772, 0.8437500000000005551, 0.8593750000000005551, 0.8750000000000004441, 1.000000000000000000 ),
 .UNSPECIFIED. ) ;
#121=CARTESIAN_POINT ( 'NONE',  ( 14.61520294907830220, 5.230627013449347551, -8.911388815577064193 ) ) ;
#123=CARTESIAN_POINT ( 'NONE',  ( 21.99610005449000028, 5.761042396082000749, -9.658588492111000789 ) ) ;
#125=CARTESIAN_POINT ( 'NONE',  ( 14.19049813593658982, 1.989872659937805599, 8.829286609355607496 ) ) ;
#126=CARTESIAN_POINT ( 'NONE',  ( -6.042815832213999983, 16.39253418350000047, -0.9999999878869999526 ) ) ;
#128=CARTESIAN_POINT ( 'NONE',  ( 19.17264246499999913, -10.17294749490999983, 5.068503378665999648 ) ) ;
#129=ORIENTED_EDGE ( 'NONE', *, *, #896, .T. ) ;
#131=CARTESIAN_POINT ( 'NONE',  ( -14.00000000000000000, -15.45000000000000107, 0.000000000000000000 ) ) ;
#132=EDGE_LOOP ( 'NONE', ( #5049, #12022, #23215, #18123, #9264, #7095, #5187 ) ) ;
#135=CARTESIAN_POINT ( 'NONE',  ( 14.44500238972999995, 0.2592567778176000370, -11.01108926215000139 ) ) ;
#136=CARTESIAN_POINT ( 'NONE',  ( -5.833999999999999631, 1.296092693409999996E-14, 0.000000000000000000 ) ) ;
#139=ORIENTED_EDGE ( 'NONE', *, *, #19795, .T. ) ;
#140=CARTESIAN_POINT ( 'NONE',  ( -11.21808363877000048, -14.99030728474000007, -2.625125111862999905 ) ) ;
#144=ORIENTED_EDGE ( 'NONE', *, *, #7334, .F. ) ;
#145=CARTESIAN_POINT ( 'NONE',  ( -14.48875655809282925, 10.17731420664813413, 7.372365177881404996 ) ) ;
#146=DIRECTION ( 'NONE',  ( 1.000000000000000000, 0.000000000000000000, 0.000000000000000000 ) ) ;
#147=CARTESIAN_POINT ( 'NONE',  ( -12.25000000000000000, 1.374666032043000015E-14, 0.000000000000000000 ) ) ;
#148=CARTESIAN_POINT ( 'NONE',  ( 15.93387064109369433, -9.634484427928969197, -3.804155515456032699 ) ) ;
#149=CARTESIAN_POINT ( 'NONE',  ( -15.52217783781999927, -9.820682682945999886, -5.027779166633999708 ) ) ;
#151=CIRCLE ( 'NONE', #16003, 10.59999999999999964 ) ;
#153=CARTESIAN_POINT ( 'NONE',  ( -13.60506528143999994, -10.72046298714999857, -0.8128029906560000351 ) ) ;
#156=ORIENTED_EDGE ( 'NONE', *, *, #22236, .T. ) ;
#158=CARTESIAN_POINT ( 'NONE',  ( 21.03695710696093002, -7.396588329481368795, 7.510079579479033818 ) ) ;
#159=CARTESIAN_POINT ( 'NONE',  ( -18.65919487842199231, 9.743618663561477433, -3.843173192191704501 ) ) ;
#163=CARTESIAN_POINT ( 'NONE',  ( -23.66121525787396962, 1.340508726618324875, -9.439414443187377657 ) ) ;
#164=CARTESIAN_POINT ( 'NONE',  ( 17.78062642131000004, 8.824178357484999680, -4.146495103786000058 ) ) ;
#167=DIRECTION ( 'NONE',  ( 0.000000000000000000, -1.000000000000000000, 0.000000000000000000 ) ) ;
#168=EDGE_CURVE ( 'NONE', #3985, #21240, #5700, .T. ) ;
#170=CARTESIAN_POINT ( 'NONE',  ( 23.00512270046333185, 8.092645076355477585, -4.664454223405380517 ) ) ;
#171=CARTESIAN_POINT ( 'NONE',  ( -4.740217193165002563, 12.61471626404000013, 0.1260612930167998857 ) ) ;
#172=CARTESIAN_POINT ( 'NONE',  ( -20.26299539000000038, -9.084714414767999457, 1.684552287285000061 ) ) ;
#173=CARTESIAN_POINT ( 'NONE',  ( 19.11258103379665130, 1.199143088786357669, -9.161748211282004561 ) ) ;
#174=CARTESIAN_POINT ( 'NONE',  ( -5.483292957314003679, 16.58400099841001918, -3.023963835265001343 ) ) ;
#175=CARTESIAN_POINT ( 'NONE',  ( -20.53578614557788384, 8.740101311720026800, -5.830131322368356628 ) ) ;
#183=CARTESIAN_POINT ( 'NONE',  ( 18.24195353945000164, -4.137305632263999833, 8.809128702420998991 ) ) ;
#184=CARTESIAN_POINT ( 'NONE',  ( 13.84234230361491136, 6.026165916141002832, -6.791106574337510970 ) ) ;
#185=CARTESIAN_POINT ( 'NONE',  ( -23.10770091748028321, -7.661184619407800156, 7.290997633578977677 ) ) ;
#188=CARTESIAN_POINT ( 'NONE',  ( 1.053140587386698135, 11.53014013154227335, 4.696634005027855885 ) ) ;
#191=CARTESIAN_POINT ( 'NONE',  ( -4.144738096053230514, 12.19662818091454426, -2.499798518877363485 ) ) ;
#194=ORIENTED_EDGE ( 'NONE', *, *, #3061, .T. ) ;
#198=CARTESIAN_POINT ( 'NONE',  ( 14.40675158531000122, 9.325397517960999139, -4.058504152148000088 ) ) ;
#199=AXIS2_PLACEMENT_3D ( 'NONE', #21129, #11572, #17500 ) ;
#200=CARTESIAN_POINT ( 'NONE',  ( -13.32870921828000021, 6.513713587124000171, -9.206748540250000445 ) ) ;
#202=CARTESIAN_POINT ( 'NONE',  ( 16.54676537306000128, 2.042383563461999785, -10.64749026856999947 ) ) ;
#203=CARTESIAN_POINT ( 'NONE',  ( 8.124934037954998800, 12.44999999999999929, 0.000000000000000000 ) ) ;
#204=CIRCLE ( 'NONE', #7166, 10.59999999999999964 ) ;
#207=CARTESIAN_POINT ( 'NONE',  ( 22.95738685678000124, -11.03983583171999960, 2.562588168388999943 ) ) ;
#211=CARTESIAN_POINT ( 'NONE',  ( -12.48243343204000055, 6.965111533508000718, -5.686492047758000545 ) ) ;
#212=CARTESIAN_POINT ( 'NONE',  ( 24.50000000000000000, -0.1464674377591403120, 10.48970002016351621 ) ) ;
#213=CARTESIAN_POINT ( 'NONE',  ( -1.985161156765999468, 11.61875206719000175, 4.524354049390001187 ) ) ;
#215=CARTESIAN_POINT ( 'NONE',  ( -21.47533412897999838, 2.576025989571999908, 10.78750342170000032 ) ) ;
#217=FACE_OUTER_BOUND ( 'NONE', #15939, .T. ) ;
#226=CARTESIAN_POINT ( 'NONE',  ( 17.17537674931000069, -4.906342569036000079, 9.567493125660998743 ) ) ;
#227=CARTESIAN_POINT ( 'NONE',  ( -16.44889015301999891, 10.17473773424000072, -3.711315847300999948 ) ) ;
#231=CARTESIAN_POINT ( 'NONE',  ( -10.33759248878110526, 15.67666494535818345, -1.227313276238695794 ) ) ;
#233=CARTESIAN_POINT ( 'NONE',  ( 13.88475961963752958, -9.356662177357431887, 4.335039568263141518 ) ) ;
#234=CARTESIAN_POINT ( 'NONE',  ( 24.50000000000000000, -2.116736914405999759, 10.36413001332999961 ) ) ;
#235=CARTESIAN_POINT ( 'NONE',  ( 23.83156968415000065, 6.491674009242999865, -9.245099637402999448 ) ) ;
#238=CARTESIAN_POINT ( 'NONE',  ( 14.09681483843687566, 4.646111251452054169, 7.745166602763706720 ) ) ;
#239=CARTESIAN_POINT ( 'NONE',  ( 17.04048089729959514, -1.953626282727659813, 10.24653127456325130 ) ) ;
#242=DIRECTION ( 'NONE',  ( 1.000000000000000000, 0.000000000000000000, 0.000000000000000000 ) ) ;
#243=CARTESIAN_POINT ( 'NONE',  ( 20.33214806635999850, 10.44200582290999968, 4.567853760350999437 ) ) ;
#245=CARTESIAN_POINT ( 'NONE',  ( 11.78693030657509588, -12.98156941795602215, 2.515258941348812005 ) ) ;
#247=CARTESIAN_POINT ( 'NONE',  ( -15.91866243917330870, 4.572869834151166657, -7.933744804850305421 ) ) ;
#250=CARTESIAN_POINT ( 'NONE',  ( 14.80590418541999931, 10.54075670043000024, -3.228249601621000497 ) ) ;
#258=CARTESIAN_POINT ( 'NONE',  ( 17.75645603379667037, 9.126947370999710429, 1.332864221464923560 ) ) ;
#259=VERTEX_POINT ( 'NONE', #12444 ) ;
#261=CARTESIAN_POINT ( 'NONE',  ( 20.92658103379664425, 1.205236576247646685, -9.208299026488377947 ) ) ;
#263=CARTESIAN_POINT ( 'NONE',  ( 15.75513086676498808, -10.05562620695802778, 2.464334981930285995 ) ) ;
#264=CARTESIAN_POINT ( 'NONE',  ( -15.91754618602999827, -1.832079236261000110, 10.89068162177000154 ) ) ;
#267=CARTESIAN_POINT ( 'NONE',  ( -19.46889333780000086, -9.261490887677000572, 5.613638565637999456 ) ) ;
#269=ORIENTED_EDGE ( 'NONE', *, *, #16936, .F. ) ;
#277=CARTESIAN_POINT ( 'NONE',  ( 24.32802197706151048, -3.549421024389301405, 12.49999999999999645 ) ) ;
#278=FACE_OUTER_BOUND ( 'NONE', #7793, .T. ) ;
#279=CARTESIAN_POINT ( 'NONE',  ( -23.58077218185689006, 2.644447661185095555, -9.069886164648769622 ) ) ;
#280=CARTESIAN_POINT ( 'NONE',  ( 12.26981375731000057, 8.958847990383999260, 1.572873132563999965 ) ) ;
#281=ORIENTED_EDGE ( 'NONE', *, *, #23157, .T. ) ;
#283=B_SPLINE_CURVE_WITH_KNOTS ( 'NONE', 3,
 ( #2361, #2125, #5763, #13373, #15188, #13148, #20776, #17138, #22466, #7940 ),
 .UNSPECIFIED., .F., .F.,
 ( 4, 2, 2, 2, 4 ),
 ( 0.000000000000000000, 0.2499999999999964473, 0.3749999999999970024, 0.4999999999999975575, 1.000000000000000000 ),
 .UNSPECIFIED. ) ;
#284=CARTESIAN_POINT ( 'NONE',  ( -4.438477777721789863, 15.42756752407910170, 4.222605013734312962 ) ) ;
#285=COLOUR_RGB ( '', 0.66274510, 0.83137255, 0.94901961) ;
#286=CARTESIAN_POINT ( 'NONE',  ( 23.99062354302999722, -13.93375672974000068, 0.8660254037843999608 ) ) ;
#287=B_SPLINE_SURFACE_WITH_KNOTS ( 'NONE', 3, 3, ( 
 ( #12787, #6851, #14366, #19939, #15924, #16045, #20175, #10379, #14247, #10738, #10621, #21642, #17769, #1171, #3238, #5058, #18007, #1411, #23683, #8804, #16167, #3360, #18130, #7091, #5283, #2110, #1762, #11084, #9619, #9270, #18702, #14817, #9500, #22568, #3935, #14710, #16527, #18818, #22211, #22102, #16753, #11212, #9151, #7435, #16875, #18469, #23914, #7324, #5512, #22329, #7684, #1881, #5625, #20640, #16645, #12890, #280, #20290, #5863, #4051, #5745, #15059, #18351, #3693, #3584, #22453, #51 ),
 ( #13008, #5975, #18592, #20409, #13136, #13247, #11444, #2226, #164, #1997, #20529, #3817, #13357, #17004, #9382, #403, #7801, #7555, #11329, #14934, #15173, #10967, #21248, #23041, #8411, #22801, #11922, #22682, #8040, #1007, #18941, #10222, #17238, #13482, #15649, #639, #19054, #2348, #6463, #15779, #9858, #766, #20884, #4291, #11800, #21120, #19177, #4660, #23168, #12046, #13845, #2586, #19430, #19307, #2840, #9738, #9975, #15289, #2719, #13722, #10101, #15414, #17365, #2467, #8286, #22920, #8166 ),
 ( #17489, #6588, #4531, #7922, #17123, #17614, #6218, #6090, #15534, #4407, #520, #13599, #883, #11680, #20997, #6339, #20758, #4167, #11563, #4900, #8648, #7383, #12288, #17738, #20238, #23287, #14092, #11146, #1143, #18531, #21487, #1260, #16012, #14765, #15895, #21365, #12843, #1940, #9328, #1703, #18413, #19677, #4781, #16702, #23406, #112, #6823, #14219, #3209, #6700, #2960, #3090, #12165, #9209, #5030, #10351, #13972, #19555, #9093, #12414, #10477, #16466, #21614, #10593, #3757, #11028, #1823 ),
 ( #19799, #5460, #17862, #17979, #8537, #23854, #7263, #14655, #22051, #16587, #3642, #23968, #22163, #5574, #12953, #20351, #11508, #7623, #226, #22508, #7862, #5918, #15355, #2526, #7983, #576, #13302, #17180, #6036, #22745, #20472, #20701, #2057, #22625, #460, #13424, #20582, #4110, #5809, #18996, #9681, #18882, #7747, #11627, #9447, #13191, #22273, #20824, #15230, #18650, #9797, #6161, #14999, #20944, #2291, #4234, #4349, #13546, #11740, #19114, #9562, #18759, #2406, #17062, #9918, #17304, #7499 ) ),
 .UNSPECIFIED., .F., .F., .F.,
 ( 4, 4 ),
 ( 4, 1, 1, 1, 1, 1, 1, 1, 1, 1, 1, 1, 1, 1, 1, 1, 1, 1, 1, 1, 1, 1, 1, 1, 1, 1, 1, 1, 1, 1, 1, 1, 1, 1, 1, 1, 1, 1, 1, 1, 1, 1, 1, 1, 1, 1, 1, 1, 1, 1, 1, 1, 1, 1, 1, 1, 1, 1, 1, 1, 1, 1, 1, 1, 4 ),
 ( -0.08331297109794000288, 1.083312971098000066 ),
 ( -0.02000000000000000042, -0.003749999999999999861, 0.01250000000000000069, 0.02875000000000000125, 0.04499999999999999833, 0.06124999999999999889, 0.07749999999999999944, 0.09375000000000000000, 0.1100000000000000006, 0.1262500000000000011, 0.1424999999999999878, 0.1587500000000000022, 0.1749999999999999889, 0.1912500000000000033, 0.2074999999999999900, 0.2237500000000000044, 0.2399999999999999911, 0.2562499999999999778, 0.2725000000000000200, 0.2887500000000000067, 0.3049999999999999933, 0.3212499999999999800, 0.3375000000000000222, 0.3537500000000000089, 0.3699999999999999956, 0.3862499999999999822, 0.4025000000000000244, 0.4187500000000000111, 0.4349999999999999978, 0.4512499999999999845, 0.4675000000000000266, 0.4837500000000000133, 0.5000000000000000000, 0.5162499999999999867, 0.5324999999999999734, 0.5487499999999999600, 0.5649999999999999467, 0.5812500000000000444, 0.5975000000000000311, 0.6137500000000000178, 0.6300000000000000044, 0.6462499999999999911, 0.6624999999999999778, 0.6787499999999999645, 0.6949999999999999512, 0.7112500000000000488, 0.7275000000000000355, 0.7437500000000000222, 0.7600000000000000089, 0.7762499999999999956, 0.7924999999999999822, 0.8087499999999999689, 0.8249999999999999556, 0.8412500000000000533, 0.8575000000000000400, 0.8737500000000000266, 0.8900000000000000133, 0.9062500000000000000, 0.9224999999999999867, 0.9387499999999999734, 0.9549999999999999600, 0.9712499999999999467, 0.9875000000000000444, 1.003749999999999920, 1.020000000000000018 ),
 .UNSPECIFIED. ) ;
#288=ORIENTED_EDGE ( 'NONE', *, *, #9109, .T. ) ;
#290=CARTESIAN_POINT ( 'NONE',  ( -23.29066724161056712, 1.115319073173602238, -9.351742763910808165 ) ) ;
#291=CARTESIAN_POINT ( 'NONE',  ( -2.623770339515000050, 11.96261007116998876, 4.059183977495999684 ) ) ;
#292=CARTESIAN_POINT ( 'NONE',  ( -21.81533334470000085, -7.216842995913999914, -6.341849293150000122 ) ) ;
#293=CARTESIAN_POINT ( 'NONE',  ( -14.46758741243325375, 9.725949910464320780, -8.154098604241012183 ) ) ;
#296=CARTESIAN_POINT ( 'NONE',  ( -4.750000000000000000, 22.00000000000000000, 0.000000000000000000 ) ) ;
#299=CARTESIAN_POINT ( 'NONE',  ( 23.70554140955999856, 3.449944951013000249, 9.831907654028000820 ) ) ;
#300=CARTESIAN_POINT ( 'NONE',  ( -3.800404330270033437, 13.28692498924355725, -5.638841271150126566 ) ) ;
#301=FACE_BOUND ( 'NONE', #15644, .T. ) ;
#302=CONICAL_SURFACE ( 'NONE', #14242, 13.23032192316000000, 1.235249617460683957 ) ;
#304=CARTESIAN_POINT ( 'NONE',  ( -21.71532941640836256, 6.478598051102530953, 8.484119408269807039 ) ) ;
#306=CARTESIAN_POINT ( 'NONE',  ( 24.50000000000000000, 9.974367097857467002, -1.221507673991182219E-15 ) ) ;
#307=ORIENTED_EDGE ( 'NONE', *, *, #7999, .T. ) ;
#309=CARTESIAN_POINT ( 'NONE',  ( -18.57752051073732247, 7.457970117013407396, -7.338587964615391535 ) ) ;
#310=CARTESIAN_POINT ( 'NONE',  ( 24.28255857085423131, 12.88093503250115290, 2.689566074712900434 ) ) ;
#312=FACE_OUTER_BOUND ( 'NONE', #13683, .T. ) ;
#313=ORIENTED_EDGE ( 'NONE', *, *, #11602, .F. ) ;
#316=CIRCLE ( 'NONE', #702, 0.09999999999999939493 ) ;
#317=CARTESIAN_POINT ( 'NONE',  ( 18.75768908530999823, -5.059016186635999723, 8.765201904772998986 ) ) ;
#318=CARTESIAN_POINT ( 'NONE',  ( 23.15628936713000030, 9.265517736846000219, 0.000000000000000000 ) ) ;
#320=CARTESIAN_POINT ( 'NONE',  ( 12.61921080085999947, 0.9513980104831999407, -10.33598124465999923 ) ) ;
#322=ADVANCED_FACE ( 'NONE', ( #21399 ), #12199, .T. ) ;
#324=CARTESIAN_POINT ( 'NONE',  ( 23.85409420549000004, -5.578683381639000238, -8.657878734822000766 ) ) ;
#326=CARTESIAN_POINT ( 'NONE',  ( 23.99062354302999722, 13.93375672974000068, 0.8660254037843999608 ) ) ;
#328=CARTESIAN_POINT ( 'NONE',  ( 12.10126773346000029, 4.413167110502000945, -7.952200573155999486 ) ) ;
#331=CARTESIAN_POINT ( 'NONE',  ( -4.229412747127002881, 12.27284885278998416, 2.242987681384999377 ) ) ;
#334=CARTESIAN_POINT ( 'NONE',  ( -19.61694117649999924, -4.574436835851999561, 10.04828037913000216 ) ) ;
#335=ORIENTED_EDGE ( 'NONE', *, *, #11923, .F. ) ;
#340=CARTESIAN_POINT ( 'NONE',  ( 5.083787571969999419, 13.95749297742998607, 4.279447512729996461 ) ) ;
#342=CARTESIAN_POINT ( 'NONE',  ( 16.76949770046334365, -9.101620074973595820, 1.191526229459673347 ) ) ;
#345=CIRCLE ( 'NONE', #18552, 7.000000000000000000 ) ;
#346=EDGE_CURVE ( 'NONE', #1455, #4875, #7182, .T. ) ;
#347=CARTESIAN_POINT ( 'NONE',  ( -12.61636557635000067, 8.538192823868000048, -4.467067395255999607 ) ) ;
#350=VECTOR ( 'NONE', #9545, 1000.000000000000000 ) ;
#351=CARTESIAN_POINT ( 'NONE',  ( -14.38789255204306983, 4.127795921197732198, 12.49979377836116967 ) ) ;
#353=CARTESIAN_POINT ( 'NONE',  ( 12.50448526289000029, -13.93375672974000068, -0.4329697263849999755 ) ) ;
#355=CARTESIAN_POINT ( 'NONE',  ( 13.81197141142692253, -8.026017885533216045, 6.503606596646131166 ) ) ;
#356=CARTESIAN_POINT ( 'NONE',  ( -18.10467920454667023, 2.391415452762288396, -8.898052290273778198 ) ) ;
#357=CARTESIAN_POINT ( 'NONE',  ( 22.21657238354000086, 10.93369321636999913, 2.658656121609999978 ) ) ;
#359=CARTESIAN_POINT ( 'NONE',  ( 11.55284350193499421, 3.530773253024809044, 12.49989659317028057 ) ) ;
#360=DIRECTION ( 'NONE',  ( 1.000000000000000000, 0.000000000000000000, 0.000000000000000000 ) ) ;
#361=DIRECTION ( 'NONE',  ( -1.000000000000000000, 0.000000000000000000, 0.000000000000000000 ) ) ;
#362=EDGE_CURVE ( 'NONE', #11065, #21095, #11524, .T. ) ;
#363=CARTESIAN_POINT ( 'NONE',  ( 11.78924557931191508, 8.668821331434422461, -9.985146724201950263 ) ) ;
#366=CARTESIAN_POINT ( 'NONE',  ( 11.59051697473728915, -12.65550321738646211, 3.079847693958680743 ) ) ;
#368=B_SPLINE_CURVE_WITH_KNOTS ( 'NONE', 3,
 ( #14625, #18275, #16435, #9625, #16880 ),
 .UNSPECIFIED., .F., .F.,
 ( 4, 1, 4 ),
 ( 0.000000000000000000, 0.5000000000000000000, 1.000000000000000000 ),
 .UNSPECIFIED. ) ;
#369=CARTESIAN_POINT ( 'NONE',  ( -16.25878743917330738, -5.585226852001683895, -7.267873252428181274 ) ) ;
#372=B_SPLINE_CURVE_WITH_KNOTS ( 'NONE', 3,
 ( #3482, #1297, #5064, #12446, #15814 ),
 .UNSPECIFIED., .F., .F.,
 ( 4, 1, 4 ),
 ( 0.000000000000000000, 0.5000000000000000000, 1.000000000000000000 ),
 .UNSPECIFIED. ) ;
#373=ORIENTED_EDGE ( 'NONE', *, *, #15908, .F. ) ;
#375=CARTESIAN_POINT ( 'NONE',  ( 16.42996226602999954, 6.392378590226999613, -9.036000841113999371 ) ) ;
#378=ADVANCED_FACE ( 'NONE', ( #13011 ), #8274, .F. ) ;
#379=VERTEX_POINT ( 'NONE', #22107 ) ;
#382=CARTESIAN_POINT ( 'NONE',  ( -14.00000000000000355, -7.644428321857049013, -6.387186174123134386 ) ) ;
#383=CARTESIAN_POINT ( 'NONE',  ( -10.90524221169000185, 10.44179980742999980, -11.54806271477999857 ) ) ;
#386=VERTEX_POINT ( 'NONE', #18474 ) ;
#387=CARTESIAN_POINT ( 'NONE',  ( -20.45951251414000183, -9.400720611274998362, 2.131946015016999763 ) ) ;
#388=CARTESIAN_POINT ( 'NONE',  ( -14.44633158889241287, 12.24656508597993465, 3.788310138426364215 ) ) ;
#389=CARTESIAN_POINT ( 'NONE',  ( 6.192588632250580538, 13.91017593417528708, 0.8180097329473892120 ) ) ;
#390=CARTESIAN_POINT ( 'NONE',  ( 15.71064099089155164, -9.557463844202629843, 3.988810051267251300 ) ) ;
#391=CARTESIAN_POINT ( 'NONE',  ( -14.07687131757000110, -7.628531263931999540, 7.915986703987999640 ) ) ;
#393=CARTESIAN_POINT ( 'NONE',  ( -15.83949910911000281, -2.044365629921999883, 10.61848174243000109 ) ) ;
#398=CARTESIAN_POINT ( 'NONE',  ( 24.00016455292000117, 0.000000000000000000, 0.000000000000000000 ) ) ;
#401=CARTESIAN_POINT ( 'NONE',  ( -5.600650454439005443, 15.08708793369000034, 2.809640077540999759 ) ) ;
#403=CARTESIAN_POINT ( 'NONE',  ( 17.01281392131000203, -9.720744103539999514, -0.4165551917177999774 ) ) ;
#405=CARTESIAN_POINT ( 'NONE',  ( -6.303284018220003837, 15.85635455589998344, -1.061654000538000409 ) ) ;
#407=ORIENTED_EDGE ( 'NONE', *, *, #646, .T. ) ;
#409=CARTESIAN_POINT ( 'NONE',  ( 21.43591666666666740, 2.413791263500860929, 8.981313434221711134 ) ) ;
#410=CARTESIAN_POINT ( 'NONE',  ( 3.263729719675002361, 12.11073175708999017, 3.451513885400003367 ) ) ;
#411=LINE ( 'NONE', #6349, #9892 ) ;
#413=CARTESIAN_POINT ( 'NONE',  ( 12.00000000000000355, -2.493385451254096719, -9.174917364955389232 ) ) ;
#415=CARTESIAN_POINT ( 'NONE',  ( 0.000000000000000000, 20.00000000000000000, 0.000000000000000000 ) ) ;
#416=CARTESIAN_POINT ( 'NONE',  ( -4.749997084077000054, 12.55000000011000161, -4.491085162427999259E-09 ) ) ;
#417=DIRECTION ( 'NONE',  ( 0.000000000000000000, -0.8660254037844288266, -0.5000000000000169864 ) ) ;
#422=CARTESIAN_POINT ( 'NONE',  ( 21.14071754283999738, 8.535971018086002005, -4.841000346350999628 ) ) ;
#423=CARTESIAN_POINT ( 'NONE',  ( 2.342532432829844691, 12.98933061754887497, -6.293791080244014680 ) ) ;
#425=CARTESIAN_POINT ( 'NONE',  ( -23.56289929282874240, 7.339383936488848903, 7.628101533612420937 ) ) ;
#428=ORIENTED_EDGE ( 'NONE', *, *, #18310, .F. ) ;
#432=DIRECTION ( 'NONE',  ( 1.000000000000000000, 0.000000000000000000, 0.000000000000000000 ) ) ;
#435=CARTESIAN_POINT ( 'NONE',  ( 14.76225174930999984, 10.68374474379000105, -0.3265774252310000292 ) ) ;
#438=CARTESIAN_POINT ( 'NONE',  ( -14.25243324638999809, 13.93375672974000068, 0.8660254037843999608 ) ) ;
#439=CARTESIAN_POINT ( 'NONE',  ( 17.96864037306000128, -10.01334466946000035, -4.258412611471999121 ) ) ;
#440=CARTESIAN_POINT ( 'NONE',  ( -12.35833339120999952, 6.571898948015506114, -13.37941417155348311 ) ) ;
#442=CARTESIAN_POINT ( 'NONE',  ( 24.47949698200000057, 5.955140450698999999, -7.767301070824998988 ) ) ;
#443=VECTOR ( 'NONE', #1417, 1000.000000000000000 ) ;
#448=CARTESIAN_POINT ( 'NONE',  ( -4.836833366243003418, 12.42306831226000874, 0.1266535678225001182 ) ) ;
#450=ADVANCED_FACE ( 'NONE', ( #1885 ), #12791, .T. ) ;
#451=CARTESIAN_POINT ( 'NONE',  ( -20.61944845118999936, 1.065297639031000054, -11.01620010679999950 ) ) ;
#452=ORIENTED_EDGE ( 'NONE', *, *, #7334, .T. ) ;
#453=DIRECTION ( 'NONE',  ( 0.000000000000000000, 0.000000000000000000, 1.000000000000000000 ) ) ;
#458=FACE_OUTER_BOUND ( 'NONE', #14382, .T. ) ;
#460=CARTESIAN_POINT ( 'NONE',  ( 15.42037674930999991, -6.716928621565999791, 8.336789182003000676 ) ) ;
#461=CARTESIAN_POINT ( 'NONE',  ( -19.53660345378999708, -7.531619525312000185, 7.381236299612999652 ) ) ;
#462=CARTESIAN_POINT ( 'NONE',  ( 17.20575125731000199, -0.07625726307336000431, -9.225306777752001253 ) ) ;
#463=CARTESIAN_POINT ( 'NONE',  ( -14.49454881829679920, -0.9069790025675873446, 12.49996723896235906 ) ) ;
#465=ORIENTED_EDGE ( 'NONE', *, *, #22112, .T. ) ;
#468=CARTESIAN_POINT ( 'NONE',  ( 13.74204473073353938, -6.236800112200524993, 8.214069492593580435 ) ) ;
#471=CARTESIAN_POINT ( 'NONE',  ( 20.52772435074999891, 11.05526862676000022, 1.831395270467999881 ) ) ;
#473=CARTESIAN_POINT ( 'NONE',  ( 11.83261479512707659, 4.444106517312727433, 12.50001436053427462 ) ) ;
#474=CARTESIAN_POINT ( 'NONE',  ( 18.40646359464608395, 10.24499631306186309, 2.163839732140223848 ) ) ;
#475=CARTESIAN_POINT ( 'NONE',  ( -4.394996721094583059, 13.55525068814215039, 5.016329272847380949 ) ) ;
#476=CARTESIAN_POINT ( 'NONE',  ( -6.533908178998216520, 15.44339042599172096, 1.502435935679650614 ) ) ;
#481=CARTESIAN_POINT ( 'NONE',  ( 12.28779254561781720, -13.65788853942738079, 1.343868873886420845 ) ) ;
#482=ORIENTED_EDGE ( 'NONE', *, *, #4216, .F. ) ;
#485=DIRECTION ( 'NONE',  ( 0.000000000000000000, 0.000000000000000000, -1.000000000000000000 ) ) ;
#490=CARTESIAN_POINT ( 'NONE',  ( -6.161940360818770834, 15.88536285935762038, 1.094220165152027135 ) ) ;
#491=EDGE_CURVE ( 'NONE', #13012, #9699, #7476, .T. ) ;
#493=ORIENTED_EDGE ( 'NONE', *, *, #6761, .F. ) ;
#494=EDGE_LOOP ( 'NONE', ( #4284, #23458, #17919 ) ) ;
#495=CARTESIAN_POINT ( 'NONE',  ( -13.99999999999999822, -8.587304723161174991, -5.250545313949140258 ) ) ;
#496=CARTESIAN_POINT ( 'NONE',  ( -11.00706471169000089, 4.728939151478000369, -14.83327577388999963 ) ) ;
#498=CARTESIAN_POINT ( 'NONE',  ( 18.17812270046333367, -0.3397639754939833501, 9.228485993081845251 ) ) ;
#499=EDGE_CURVE ( 'NONE', #17201, #19976, #8041, .T. ) ;
#500=ORIENTED_EDGE ( 'NONE', *, *, #19755, .T. ) ;
#501=CARTESIAN_POINT ( 'NONE',  ( -24.30210239110000003, -9.610041974782999930, 1.174637117329000002 ) ) ;
#503=CARTESIAN_POINT ( 'NONE',  ( -14.48092005499817247, 11.66846015894712707, 4.789644024569511771 ) ) ;
#505=CARTESIAN_POINT ( 'NONE',  ( 15.77750233183371265, -10.22258791821789536, 1.644876861122036349 ) ) ;
#509=CARTESIAN_POINT ( 'NONE',  ( -13.40193493347000064, -7.644751109369999575, -7.551345029496000727 ) ) ;
#517=CARTESIAN_POINT ( 'NONE',  ( -22.26176253788000281, -9.242562415387000740, 0.000000000000000000 ) ) ;
#518=CARTESIAN_POINT ( 'NONE',  ( -4.007822987411000959, 13.30559351321000783, 4.666582981500002170 ) ) ;
#520=CARTESIAN_POINT ( 'NONE',  ( 17.80706408530999951, 3.725969113535000155, -9.559170675091001712 ) ) ;
#521=ORIENTED_EDGE ( 'NONE', *, *, #17867, .T. ) ;
#522=CARTESIAN_POINT ( 'NONE',  ( -6.326119818082997170, 16.13697961988999552, -0.9718497405647000820 ) ) ;
#523=CARTESIAN_POINT ( 'NONE',  ( 24.00034722001000276, 6.716786535997999685, 12.21137788282999992 ) ) ;
#524=ORIENTED_EDGE ( 'NONE', *, *, #1140, .F. ) ;
#527=CARTESIAN_POINT ( 'NONE',  ( 3.924142709797999728, 12.31642185211999241, 2.670936164341001895 ) ) ;
#528=CARTESIAN_POINT ( 'NONE',  ( -14.00000000000000000, -4.143720316427557115, 9.101378173059835319 ) ) ;
#529=CARTESIAN_POINT ( 'NONE',  ( 18.34519826651710162, 8.005455623522196973, -6.676223990317056156 ) ) ;
#530=CARTESIAN_POINT ( 'NONE',  ( 11.99999999999999822, 4.923960526494110646, -7.557474118975338051 ) ) ;
#532=CARTESIAN_POINT ( 'NONE',  ( 22.24928936712999672, -9.242242329243000043, 0.000000000000000000 ) ) ;
#538=ORIENTED_EDGE ( 'NONE', *, *, #15854, .F. ) ;
#539=CARTESIAN_POINT ( 'NONE',  ( 23.65297967911999777, -3.219993159064999944, 9.343258505126000202 ) ) ;
#540=CARTESIAN_POINT ( 'NONE',  ( 2.127428512114412751, 12.95714030754093926, -6.359730179768805947 ) ) ;
#541=CARTESIAN_POINT ( 'NONE',  ( -23.65071241290791448, -9.336176072467093690, -1.519767395369341578 ) ) ;
#542=CARTESIAN_POINT ( 'NONE',  ( -21.15302554097793575, -10.13353536419278278, 2.834801739046542757 ) ) ;
#546=CARTESIAN_POINT ( 'NONE',  ( -19.24739020423550073, -10.46819004694524757, -0.4592041673053260387 ) ) ;
#550=CARTESIAN_POINT ( 'NONE',  ( -11.04281598264000053, 15.31903517167999951, 1.878299281558999834 ) ) ;
#553=CARTESIAN_POINT ( 'NONE',  ( 14.87193924930999955, 10.04572779547000039, 3.659788831486999960 ) ) ;
#554=CARTESIAN_POINT ( 'NONE',  ( -14.14123061016000094, -9.145880708538998149, 6.639339533417000005 ) ) ;
#555=DIRECTION ( 'NONE',  ( 1.000000000000000000, 0.000000000000000000, 0.000000000000000000 ) ) ;
#556=CARTESIAN_POINT ( 'NONE',  ( 14.10926537306000128, -9.926075755316000837, 4.188684833930999218 ) ) ;
#559=CARTESIAN_POINT ( 'NONE',  ( 24.20819240979999876, 6.272633220716000046, -8.181320936509997921 ) ) ;
#562=CARTESIAN_POINT ( 'NONE',  ( 11.84472065189999945, 4.409932236062999777, -7.946371848247000713 ) ) ;
#564=AXIS2_PLACEMENT_3D ( 'NONE', #17689, #4734, #3281 ) ;
#565=CARTESIAN_POINT ( 'NONE',  ( 3.627106408426999273, 12.14388422481000518, 3.038632416491001909 ) ) ;
#567=CARTESIAN_POINT ( 'NONE',  ( -22.45737845476999794, 0.1502580860940999907, -11.11644552567000055 ) ) ;
#569=CARTESIAN_POINT ( 'NONE',  ( -4.649999999999999467, 20.10000000000000142, 5.428583055299999740E-09 ) ) ;
#572=CARTESIAN_POINT ( 'NONE',  ( -24.33938584176924991, 2.815218398139987865, -12.49992678697366166 ) ) ;
#574=DIRECTION ( 'NONE',  ( 1.000000000000000000, 0.000000000000000000, 0.000000000000000000 ) ) ;
#576=CARTESIAN_POINT ( 'NONE',  ( 16.40756424930999913, 8.766565845128001300, -6.190543086277999763 ) ) ;
#577=CARTESIAN_POINT ( 'NONE',  ( -14.37682859208999986, 9.777980407524001549, -3.031781461267000211 ) ) ;
#579=B_SPLINE_CURVE_WITH_KNOTS ( 'NONE', 3,
 ( #6025, #20812, #13412, #20933 ),
 .UNSPECIFIED., .F., .F.,
 ( 4, 4 ),
 ( 0.000000000000000000, 0.6207796204815331231 ),
 .UNSPECIFIED. ) ;
#580=CARTESIAN_POINT ( 'NONE',  ( 13.91512625730999986, 8.379890869990997970, -3.647050788746000194 ) ) ;
#581=CARTESIAN_POINT ( 'NONE',  ( -14.48633704289819057, -1.427546401406459831, 12.50000676666411792 ) ) ;
#586=CARTESIAN_POINT ( 'NONE',  ( 4.418452478372458359, 14.62271791494141837, -4.243679542130283977 ) ) ;
#587=EDGE_LOOP ( 'NONE', ( #22612, #16356, #15446, #22262 ) ) ;
#588=CARTESIAN_POINT ( 'NONE',  ( 5.373625923053002573, 13.70222443717999816, -4.580663796643002605 ) ) ;
#590=CARTESIAN_POINT ( 'NONE',  ( -5.529771451991000397, 1.198997689148999791E-14, 1.310996564781999865E-13 ) ) ;
#591=CARTESIAN_POINT ( 'NONE',  ( 14.40647870685735832, -4.521102126905931939, 7.829235988601594975 ) ) ;
#592=CARTESIAN_POINT ( 'NONE',  ( 17.90467403235581045, 0.4259370903896579907, -10.44751290468639660 ) ) ;
#596=B_SPLINE_CURVE_WITH_KNOTS ( 'NONE', 3,
 ( #7719, #3848, #14965, #1789 ),
 .UNSPECIFIED., .F., .F.,
 ( 4, 4 ),
 ( 0.000000000000000000, 1.000000000000000000 ),
 .UNSPECIFIED. ) ;
#599=AXIS2_PLACEMENT_3D ( 'NONE', #6456, #6583, #635 ) ;
#601=ORIENTED_EDGE ( 'NONE', *, *, #20949, .F. ) ;
#602=EDGE_CURVE ( 'NONE', #12251, #21466, #20643, .T. ) ;
#604=CARTESIAN_POINT ( 'NONE',  ( -4.270778468753240631, 12.23941797836552148, 2.280178412471628668 ) ) ;
#605=CARTESIAN_POINT ( 'NONE',  ( -24.50000000000000000, 1.721664336791999924E-14, 0.000000000000000000 ) ) ;
#607=CARTESIAN_POINT ( 'NONE',  ( 17.11793655645000101, 6.716980213484000650, 8.821080241391998200 ) ) ;
#608=CARTESIAN_POINT ( 'NONE',  ( -20.82261444457166988, 6.350348985615495323, 6.750538350822437472 ) ) ;
#610=ORIENTED_EDGE ( 'NONE', *, *, #17195, .T. ) ;
#612=CARTESIAN_POINT ( 'NONE',  ( -14.00000000000000533, -1.777611135496285355, -9.431915595318816514 ) ) ;
#613=DIRECTION ( 'NONE',  ( -1.000000000000000000, 0.000000000000000000, 0.000000000000000000 ) ) ;
#614=CARTESIAN_POINT ( 'NONE',  ( -14.48875655809283103, -10.17731420665194797, -7.372365177876170073 ) ) ;
#617=CARTESIAN_POINT ( 'NONE',  ( -21.73160135699000151, 8.161745128470998978, -6.112658946955999539 ) ) ;
#621=CARTESIAN_POINT ( 'NONE',  ( 15.58141692657948596, -6.929050783388004398, 7.685657546460438638 ) ) ;
#623=CARTESIAN_POINT ( 'NONE',  ( -13.92238738939999898, -10.21016635782999948, -2.519686904309999864 ) ) ;
#625=CARTESIAN_POINT ( 'NONE',  ( -21.05048866052816692, -7.545730853300948837, -7.331750953782708358 ) ) ;
#626=CARTESIAN_POINT ( 'NONE',  ( -14.98621963600000129, -7.639996621784999498, -6.839520901588999280 ) ) ;
#629=VERTEX_POINT ( 'NONE', #20887 ) ;
#630=AXIS2_PLACEMENT_3D ( 'NONE', #13866, #4916, #21270 ) ;
#632=DIRECTION ( 'NONE',  ( 1.000000000000000000, 0.000000000000000000, 0.000000000000000000 ) ) ;
#635=DIRECTION ( 'NONE',  ( 0.000000000000000000, -0.8660254037844288266, 0.5000000000000169864 ) ) ;
#639=CARTESIAN_POINT ( 'NONE',  ( 14.81906392131000061, -2.842327771818999871, 9.244929856806999524 ) ) ;
#642=B_SPLINE_CURVE_WITH_KNOTS ( 'NONE', 3,
 ( #11380, #22500, #11501, #18876 ),
 .UNSPECIFIED., .F., .F.,
 ( 4, 4 ),
 ( 0.000000000000000000, 1.000000000000000000 ),
 .UNSPECIFIED. ) ;
#643=CARTESIAN_POINT ( 'NONE',  ( 21.34228936713000024, 9.218966921638999779, 0.000000000000000000 ) ) ;
#644=CARTESIAN_POINT ( 'NONE',  ( -11.99999999434999864, -6.999999994347000154, -4.083277946868999946E-09 ) ) ;
#646=EDGE_CURVE ( 'NONE', #14845, #21017, #6325, .T. ) ;
#649=CARTESIAN_POINT ( 'NONE',  ( 24.29420393214009977, -1.914062225345805501, 10.44982418693062343 ) ) ;
#650=DIRECTION ( 'NONE',  ( -1.000000000000000000, 0.000000000000000000, 0.000000000000000000 ) ) ;
#651=CARTESIAN_POINT ( 'NONE',  ( 17.97914201263965595, -3.906812565131978499, -9.711116240607633898 ) ) ;
#652=CARTESIAN_POINT ( 'NONE',  ( -23.74465998031000069, 6.216878364870000340, 12.50000000000000000 ) ) ;
#654=CARTESIAN_POINT ( 'NONE',  ( -4.094404611478998923, 14.04847595166999952, -4.434860849016999396 ) ) ;
#656=AXIS2_PLACEMENT_3D ( 'NONE', #17617, #2470, #8045 ) ;
#657=CARTESIAN_POINT ( 'NONE',  ( 4.829988586904999437, 14.79876397742000194, 3.766541904039999888 ) ) ;
#661=CARTESIAN_POINT ( 'NONE',  ( -17.01462077250666738, 1.192095737878705153, 9.107910416114240348 ) ) ;
#662=CARTESIAN_POINT ( 'NONE',  ( 24.77691953824000137, -11.46202743651999967, -1.149253455826999781 ) ) ;
#663=CARTESIAN_POINT ( 'NONE',  ( -2.692449147991668568, 13.04955071611749418, -6.167886193833035158 ) ) ;
#665=ADVANCED_FACE ( 'NONE', ( #19057 ), #6222, .T. ) ;
#666=CARTESIAN_POINT ( 'NONE',  ( -20.53716891550649493, 2.994023850388096708, -10.07133576860161739 ) ) ;
#669=VECTOR ( 'NONE', #2870, 1000.000000000000000 ) ;
#671=ORIENTED_EDGE ( 'NONE', *, *, #1856, .T. ) ;
#672=CARTESIAN_POINT ( 'NONE',  ( -17.65644968217466726, -7.789232886291271640, 6.951626983977684304 ) ) ;
#675=DIRECTION ( 'NONE',  ( -1.000000000000000000, 0.000000000000000000, 0.000000000000000000 ) ) ;
#676=CARTESIAN_POINT ( 'NONE',  ( 0.000000000000000000, -1.100000000000000089, 0.000000000000000000 ) ) ;
#679=CARTESIAN_POINT ( 'NONE',  ( 17.41195603379666323, 4.591934376281141539, -7.967326209410963145 ) ) ;
#680=CARTESIAN_POINT ( 'NONE',  ( 15.63975174930999934, -10.61757272617999881, 1.417689269007999853 ) ) ;
#681=CARTESIAN_POINT ( 'NONE',  ( -24.21952468797000080, 6.266457887630000556, -9.319163484501999051 ) ) ;
#682=CARTESIAN_POINT ( 'NONE',  ( -17.18818582970000008, -2.107320772642000239, -11.18988855195000021 ) ) ;
#684=CARTESIAN_POINT ( 'NONE',  ( 15.05671080085999947, 8.813937669080001314, 7.134837867725000393 ) ) ;
#685=PLANE ( 'NONE',  #6580 ) ;
#687=PLANE ( 'NONE',  #16444 ) ;
#688=CARTESIAN_POINT ( 'NONE',  ( 22.17785865399000045, -8.361523973907999618, -4.965137225652999753 ) ) ;
#692=CARTESIAN_POINT ( 'NONE',  ( 4.829988586904999437, 14.79876397742000016, 3.766541904039999888 ) ) ;
#694=CARTESIAN_POINT ( 'NONE',  ( 4.543963002250998251, 12.38829681527001370, 1.501761386921000696 ) ) ;
#696=CARTESIAN_POINT ( 'NONE',  ( -22.95863209211000111, -11.00291023332999885, 1.684196372985999890 ) ) ;
#701=CARTESIAN_POINT ( 'NONE',  ( 4.835177208035999818, 0.000000000000000000, 0.000000000000000000 ) ) ;
#702=AXIS2_PLACEMENT_3D ( 'NONE', #569, #19234, #6518 ) ;
#705=CARTESIAN_POINT ( 'NONE',  ( -16.20500172382000059, 9.665285290698001575, -3.525418390172999850 ) ) ;
#706=CARTESIAN_POINT ( 'NONE',  ( 16.54762625731000014, -6.940875756134999186, 6.051234330564000174 ) ) ;
#709=VERTEX_POINT ( 'NONE', #2844 ) ;
#710=CARTESIAN_POINT ( 'NONE',  ( 21.34228936713000024, 9.218966921638999779, 0.000000000000000000 ) ) ;
#714=CARTESIAN_POINT ( 'NONE',  ( 13.72851662033176545, -5.846715754974600721, 8.501542022457519110 ) ) ;
#717=CARTESIAN_POINT ( 'NONE',  ( 3.941498952056000871, 13.94384724320999602, -4.660668869226999078 ) ) ;
#719=FACE_OUTER_BOUND ( 'NONE', #14130, .T. ) ;
#720=CARTESIAN_POINT ( 'NONE',  ( 12.12543434885670557, -5.255139125142729739, 12.50003690309258353 ) ) ;
#721=CARTESIAN_POINT ( 'NONE',  ( 17.15198968891989395, -5.679900478530641728, 8.758236662128663141 ) ) ;
#723=VECTOR ( 'NONE', #21146, 1000.000000000000000 ) ;
#725=CARTESIAN_POINT ( 'NONE',  ( 11.83261479512603032, 8.603276725239243916, -10.09871632138033881 ) ) ;
#726=EDGE_LOOP ( 'NONE', ( #11462, #19788, #12642, #19276 ) ) ;
#727=CARTESIAN_POINT ( 'NONE',  ( 11.43887872962553054, -12.36312605252038033, 3.586317572276362942 ) ) ;
#730=DIRECTION ( 'NONE',  ( 0.000000000000000000, 0.4098987730065234425, -0.9121310190360518710 ) ) ;
#731=CARTESIAN_POINT ( 'NONE',  ( -0.2205931549149543758, 11.48217017896666015, 4.812798745242788279 ) ) ;
#733=CARTESIAN_POINT ( 'NONE',  ( 8.124934037954998800, 0.000000000000000000, 0.000000000000000000 ) ) ;
#740=CARTESIAN_POINT ( 'NONE',  ( -13.99999999999999645, -4.994886009442610408, -8.411685227471448201 ) ) ;
#741=TOROIDAL_SURFACE ( 'NONE', #11184, 16.43375672870000059, 1.000000000000000000 ) ;
#742=DIRECTION ( 'NONE',  ( 0.000000000000000000, 1.000000000000000000, 0.000000000000000000 ) ) ;
#743=CARTESIAN_POINT ( 'NONE',  ( -24.24003052283108062, -9.030352382187791349, -9.358674018439064213 ) ) ;
#744=VERTEX_POINT ( 'NONE', #12419 ) ;
#745=CARTESIAN_POINT ( 'NONE',  ( -21.31634619217999926, 9.651037232871999549, -0.4757113999236000090 ) ) ;
#746=CARTESIAN_POINT ( 'NONE',  ( -18.99854661335000117, -6.966878364870000340, 12.06698729810999993 ) ) ;
#748=CARTESIAN_POINT ( 'NONE',  ( 15.86493638691169750, -10.25014446212039587, -1.494075193881422514 ) ) ;
#749=CARTESIAN_POINT ( 'NONE',  ( -17.80271749694000150, -11.00587167721000093, 1.406230294539999814 ) ) ;
#753=CARTESIAN_POINT ( 'NONE',  ( -20.92181303178861285, -3.650616230715998611, -9.863665015250019152 ) ) ;
#756=ORIENTED_EDGE ( 'NONE', *, *, #12377, .F. ) ;
#757=B_SPLINE_CURVE_WITH_KNOTS ( 'NONE', 3,
 ( #4909, #19684, #9987, #9865, #17250, #649, #2727, #21128, #10109, #8051, #22810, #15658, #13608, #11808, #19186, #17374, #14692, #12533, #7301, #12768, #5493, #20038, #5264, #1389, #17987, #1626, #9130, #19921, #10484, #3338, #5039, #10948, #22084, #10716, #12872, #20158, #3099, #3565, #8782, #16020, #18335, #1744, #16505, #18108, #23414, #3220, #14226, #23894, #12422, #17871, #23663, #1269, #8656, #5380, #23777, #14458, #7074, #9015, #6833, #21621, #19806, #1514, #10602, #16144, #6957, #23546, #14348, #8905, #21739, #5152, #21853, #7183, #16271, #12650, #3456, #10841, #18225, #16385, #14573, #21966, #20622, #6286, #7418, #14917, #3677, #22312, #833, #14800, #2661, #1860, #15603, #11310, #18451, #22436, #18799, #22871, #13669, #9482, #3918, #5846, #22196, #7666, #1979, #5728, #12990, #15040, #13115, #16858, #10055, #16987, #8120, #8235, #5609, #21063, #35 ),
 .UNSPECIFIED., .F., .F.,
 ( 4, 2, 2, 2, 2, 2, 1, 2, 2, 2, 2, 2, 2, 2, 2, 2, 2, 2, 2, 2, 2, 2, 2, 2, 2, 2, 2, 2, 2, 1, 2, 2, 2, 2, 2, 2, 2, 2, 2, 2, 2, 2, 2, 2, 2, 2, 2, 2, 2, 2, 2, 2, 1, 2, 2, 2, 2, 2, 4 ),
 ( 0.000000000000000000, 0.01562500000000001041, 0.03125000000000002082, 0.04687500000000002776, 0.06250000000000004163, 0.07812500000000005551, 0.09375000000000005551, 0.1093750000000000694, 0.1250000000000000833, 0.1406250000000000833, 0.1562500000000001110, 0.1718750000000001110, 0.1875000000000001110, 0.2031250000000001110, 0.2187500000000000833, 0.2343750000000000833, 0.2500000000000000555, 0.2656250000000000555, 0.2812500000000000555, 0.2968750000000001110, 0.3125000000000001110, 0.3281250000000001110, 0.3437500000000001110, 0.3593750000000001110, 0.3750000000000001110, 0.3906250000000001110, 0.4062500000000000555, 0.4375000000000000000, 0.4687500000000000000, 0.4999999999999999445, 0.5312499999999998890, 0.5624999999999998890, 0.5937499999999998890, 0.6093749999999998890, 0.6249999999999998890, 0.6406249999999998890, 0.6562499999999998890, 0.6718749999999998890, 0.6874999999999998890, 0.7031249999999998890, 0.7187499999999998890, 0.7343749999999998890, 0.7499999999999998890, 0.7656250000000000000, 0.7812500000000000000, 0.7968750000000000000, 0.8125000000000000000, 0.8281250000000000000, 0.8437500000000000000, 0.8593750000000000000, 0.8750000000000000000, 0.8906250000000000000, 0.9062500000000000000, 0.9218750000000001110, 0.9375000000000001110, 0.9531250000000001110, 0.9687500000000001110, 0.9843750000000001110, 1.000000000000000000 ),
 .UNSPECIFIED. ) ;
#759=CARTESIAN_POINT ( 'NONE',  ( -15.73633831973462627, -9.927802218130974410, -3.384033804227659648 ) ) ;
#762=CARTESIAN_POINT ( 'NONE',  ( 5.670434974910000925, 13.86170818258000281, -2.692715480849998233 ) ) ;
#765=CARTESIAN_POINT ( 'NONE',  ( -19.54076253787999562, 9.172736192578000214, 0.000000000000000000 ) ) ;
#766=CARTESIAN_POINT ( 'NONE',  ( 14.16093892131000054, 8.852644193975999443, -3.852777470446999697 ) ) ;
#768=CARTESIAN_POINT ( 'NONE',  ( 18.55445603379666153, -8.961743277533855689, 2.117392749268326657 ) ) ;
#770=DIRECTION ( 'NONE',  ( -1.000000000000000000, 0.000000000000000000, 0.000000000000000000 ) ) ;
#772=FACE_OUTER_BOUND ( 'NONE', #7197, .T. ) ;
#774=CARTESIAN_POINT ( 'NONE',  ( -23.47393953383764398, 4.611284423866098159, -8.094624080708051395 ) ) ;
#775=LINE ( 'NONE', #13609, #20067 ) ;
#776=CARTESIAN_POINT ( 'NONE',  ( 18.32399750313075515, 7.510740577353477221, -7.220990934370560943 ) ) ;
#777=DIRECTION ( 'NONE',  ( 1.000000000000000000, 0.000000000000000000, 0.000000000000000000 ) ) ;
#778=ADVANCED_FACE ( 'NONE', ( #10481 ), #23508, .F. ) ;
#779=CARTESIAN_POINT ( 'NONE',  ( -14.49999965082560038, 10.56569440617048805, -6.699684590240016391 ) ) ;
#780=CARTESIAN_POINT ( 'NONE',  ( 21.18914133790000065, -7.515829758343000044, -8.336216767992999266 ) ) ;
#785=ORIENTED_EDGE ( 'NONE', *, *, #1811, .T. ) ;
#786=CARTESIAN_POINT ( 'NONE',  ( 23.19221516142773964, 4.107034334315931901, 8.330789669698718924 ) ) ;
#787=CARTESIAN_POINT ( 'NONE',  ( 20.08633540235999959, 9.945159233172001123, 4.350446449599000509 ) ) ;
#788=CARTESIAN_POINT ( 'NONE',  ( -2.719034288096889629, 13.05437085155837629, -6.157680525929839277 ) ) ;
#790=CARTESIAN_POINT ( 'NONE',  ( -20.10874691517809509, 10.28412968912246939, 2.114059615703416384 ) ) ;
#791=CARTESIAN_POINT ( 'NONE',  ( -24.50000000000000000, -10.82531754731000007, -6.250000000000000000 ) ) ;
#795=CARTESIAN_POINT ( 'NONE',  ( -16.95866875144658081, 1.228736841276851788, -10.34930314903842152 ) ) ;
#796=LINE ( 'NONE', #15448, #669 ) ;
#798=AXIS2_PLACEMENT_3D ( 'NONE', #12824, #11004, #5550 ) ;
#800=CARTESIAN_POINT ( 'NONE',  ( -14.09989322724901051, 9.032303263851988007, 3.309274488355915889E-05 ) ) ;
#803=CARTESIAN_POINT ( 'NONE',  ( 13.33631424930999998, 2.709556187140999661, 10.30084784107000040 ) ) ;
#804=CARTESIAN_POINT ( 'NONE',  ( -23.73776463305999940, 8.652042595619999332, 7.138803698541999587 ) ) ;
#805=EDGE_CURVE ( 'NONE', #12931, #15294, #3214, .T. ) ;
#806=CARTESIAN_POINT ( 'NONE',  ( -18.53906879230999749, -1.456153306622999910, 10.25029566457999941 ) ) ;
#807=CARTESIAN_POINT ( 'NONE',  ( 19.16841666666666555, 8.924639406612350001, -2.398560541756590059 ) ) ;
#809=CARTESIAN_POINT ( 'NONE',  ( 16.27687451746000136, -4.819963443980000761, 8.480589539771001384 ) ) ;
#810=DIRECTION ( 'NONE',  ( 0.000000000000000000, 0.000000000000000000, 1.000000000000000000 ) ) ;
#812=CARTESIAN_POINT ( 'NONE',  ( 21.37540677533000277, -2.698669465534999645, 9.869515643728000498 ) ) ;
#814=ORIENTED_EDGE ( 'NONE', *, *, #1841, .F. ) ;
#817=CARTESIAN_POINT ( 'NONE',  ( 4.780913943838003277, 12.47998338134000029, -0.02289341065286999363 ) ) ;
#819=CARTESIAN_POINT ( 'NONE',  ( -21.95612481742999833, 10.92660042548000021, 1.976132411670999955 ) ) ;
#820=EDGE_CURVE ( 'NONE', #14252, #3985, #10762, .T. ) ;
#822=CARTESIAN_POINT ( 'NONE',  ( -18.13088126894000141, 1.446686056264999920E-14, 0.000000000000000000 ) ) ;
#827=PLANE ( 'NONE',  #9206 ) ;
#828=CARTESIAN_POINT ( 'NONE',  ( -17.09903927815000202, -2.106860712391000146, -11.18744719158000045 ) ) ;
#829=CARTESIAN_POINT ( 'NONE',  ( 15.88950125731000007, 9.094565878156000593, 1.328064802524999921 ) ) ;
#832=ORIENTED_EDGE ( 'NONE', *, *, #21823, .T. ) ;
#833=CARTESIAN_POINT ( 'NONE',  ( 20.11733268653172857, 10.39601757465827525, -1.570891001574004742 ) ) ;
#835=CARTESIAN_POINT ( 'NONE',  ( 24.25008227645999881, 9.630770167580999797, -1.179429185905188964E-15 ) ) ;
#836=CARTESIAN_POINT ( 'NONE',  ( 4.236807648326396780, 14.55040135328094664, -4.423799120031906007 ) ) ;
#837=VERTEX_POINT ( 'NONE', #13850 ) ;
#838=CARTESIAN_POINT ( 'NONE',  ( -3.719979053892001453, 14.47850010422000366, -4.885491426500000678 ) ) ;
#840=CARTESIAN_POINT ( 'NONE',  ( 11.07373617191544568, 0.5001676860470258834, 12.49996440465858960 ) ) ;
#841=CARTESIAN_POINT ( 'NONE',  ( 16.45505974129427784, 10.04716483004630589, -2.764689303999621650 ) ) ;
#842=CARTESIAN_POINT ( 'NONE',  ( -15.61632910584000022, 9.072027496059000384, 0.000000000000000000 ) ) ;
#843=DIRECTION ( 'NONE',  ( 0.000000000000000000, -0.8660254037844288266, 0.5000000000000169864 ) ) ;
#845=ORIENTED_EDGE ( 'NONE', *, *, #12365, .T. ) ;
#847=CARTESIAN_POINT ( 'NONE',  ( 3.792011109391261403, 12.19794324411309105, -2.926137113678119128 ) ) ;
#849=CARTESIAN_POINT ( 'NONE',  ( -5.636695640436695243, 16.19553706042610841, -2.397992902333817344 ) ) ;
#851=CARTESIAN_POINT ( 'NONE',  ( -3.555098145900802198, 13.22760776865786170, 5.776756902176543917 ) ) ;
#853=CARTESIAN_POINT ( 'NONE',  ( 6.145626734707911432, 14.16193665001459223, -0.1742073854001389144 ) ) ;
#854=CARTESIAN_POINT ( 'NONE',  ( -19.54076253787999562, 9.172736192578000214, 0.000000000000000000 ) ) ;
#858=ORIENTED_EDGE ( 'NONE', *, *, #6254, .F. ) ;
#859=CARTESIAN_POINT ( 'NONE',  ( -13.99999999999999289, 1.810552339594545312, -9.225438086100725243 ) ) ;
#861=B_SPLINE_CURVE_WITH_KNOTS ( 'NONE', 3,
 ( #19771, #20125, #17948, #3533, #10915, #1353, #8744, #6919, #21705, #1597 ),
 .UNSPECIFIED., .F., .F.,
 ( 4, 1, 1, 2, 2, 4 ),
 ( 0.000000000000000000, 0.2500000000000001110, 0.3750000000000001665, 0.4375000000000002220, 0.5000000000000002220, 1.000000000000000000 ),
 .UNSPECIFIED. ) ;
#862=CARTESIAN_POINT ( 'NONE',  ( -6.838539683295000060, 15.31903503039000114, -1.878299264234999821 ) ) ;
#863=ORIENTED_EDGE ( 'NONE', *, *, #22126, .T. ) ;
#865=CARTESIAN_POINT ( 'NONE',  ( 6.227597389086636959, 13.75196057894610036, 1.343634751001441918 ) ) ;
#866=CARTESIAN_POINT ( 'NONE',  ( 14.97278813112675167, 10.13360311651370615, 2.016797930637777458 ) ) ;
#867=CARTESIAN_POINT ( 'NONE',  ( -19.42868733223000177, -9.644227811630997849, -5.575930749671000441 ) ) ;
#869=CARTESIAN_POINT ( 'NONE',  ( -20.89607790604070914, -2.753905224125297480, -10.15048530611613664 ) ) ;
#871=CARTESIAN_POINT ( 'NONE',  ( -15.88025719033000094, -8.846829628555999747, 7.110504558004000053 ) ) ;
#872=BREP_WITH_VOIDS ( 'NONE', #9631, ( #16413, #14644 ) );
#876=CARTESIAN_POINT ( 'NONE',  ( -16.72027023057977146, 10.39404030090816455, 0.6342462940522078929 ) ) ;
#879=CARTESIAN_POINT ( 'NONE',  ( 6.141155213800003843, 13.62012030888000069, -2.541026553239001284 ) ) ;
#880=CARTESIAN_POINT ( 'NONE',  ( 12.00000000000000000, -1.561535578790016476, -8.842512525458630535 ) ) ;
#883=CARTESIAN_POINT ( 'NONE',  ( 17.58768908531000008, -3.881224882977999613, -9.490963515925001204 ) ) ;
#885=CARTESIAN_POINT ( 'NONE',  ( -11.43647649291999890, 10.56401704806000019, 9.958020882561998022 ) ) ;
#886=CARTESIAN_POINT ( 'NONE',  ( -14.25243324638999809, -6.216878364870000340, 12.50000000000000000 ) ) ;
#887=DIRECTION ( 'NONE',  ( -1.000000000000000000, 0.000000000000000000, 0.000000000000000000 ) ) ;
#891=CARTESIAN_POINT ( 'NONE',  ( 21.47370833333333096, 1.207328351017924462, 9.222339391325609981 ) ) ;
#893=CARTESIAN_POINT ( 'NONE',  ( -14.00000000000000000, -5.950771400213850093, 8.190499872437872142 ) ) ;
#894=CARTESIAN_POINT ( 'NONE',  ( 18.38411873406448294, 8.826705673792748286, -5.540809837595687348 ) ) ;
#895=CARTESIAN_POINT ( 'NONE',  ( -6.250000012226999857, 15.73199627394999922, 1.185103398761000015 ) ) ;
#896=EDGE_CURVE ( 'NONE', #16467, #5788, #1395, .T. ) ;
#898=CARTESIAN_POINT ( 'NONE',  ( 24.08896737927999965, 6.587527820344000418, 9.185660392408999897 ) ) ;
#900=CARTESIAN_POINT ( 'NONE',  ( -3.861659623566732424, 14.00549260456081058, -4.847283716246065133 ) ) ;
#901=DIRECTION ( 'NONE',  ( 0.000000000000000000, 0.000000000000000000, -1.000000000000000000 ) ) ;
#904=CARTESIAN_POINT ( 'NONE',  ( -16.52332910583999848, -9.095302903661998783, 0.000000000000000000 ) ) ;
#905=CARTESIAN_POINT ( 'NONE',  ( 21.63234287083999874, 9.479527916586000913, -5.375967906524000028 ) ) ;
#906=CARTESIAN_POINT ( 'NONE',  ( 23.33520118364659623, -6.718265184276733137, -8.198908078898558216 ) ) ;
#909=CARTESIAN_POINT ( 'NONE',  ( 4.852652572476451098, 14.56096245632547692, 3.781519854356791832 ) ) ;
#910=CARTESIAN_POINT ( 'NONE',  ( -4.940724180147997302, 12.51283282727001556, 0.1567042536069999104 ) ) ;
#913=CARTESIAN_POINT ( 'NONE',  ( -16.48417771855191205, 10.21602491043049810, 1.967329235809863297 ) ) ;
#920=CARTESIAN_POINT ( 'NONE',  ( 14.98162674931000105, 7.974294229383000143, 7.126218918095000632 ) ) ;
#922=CARTESIAN_POINT ( 'NONE',  ( -20.84720430363000077, -3.223876527765000333, -10.66212759214000094 ) ) ;
#924=CARTESIAN_POINT ( 'NONE',  ( -15.28898322480000083, 9.440789260380000769, 4.024077471293999508 ) ) ;
#926=CARTESIAN_POINT ( 'NONE',  ( 14.85499951745999958, -9.268832152391000889, -2.910280560324999932 ) ) ;
#927=CARTESIAN_POINT ( 'NONE',  ( -14.25243324638999809, -13.93375672974000068, -0.8660254037843999608 ) ) ;
#928=PLANE ( 'NONE',  #23180 ) ;
#929=B_SPLINE_CURVE_WITH_KNOTS ( 'NONE', 3,
 ( #8824, #12092, #6629, #14018, #3250 ),
 .UNSPECIFIED., .F., .F.,
 ( 4, 1, 4 ),
 ( 0.000000000000000000, 0.5000000000000000000, 1.000000000000000000 ),
 .UNSPECIFIED. ) ;
#930=CARTESIAN_POINT ( 'NONE',  ( 24.42844379342591665, 9.716713767727441109, 2.075955529744581085 ) ) ;
#931=ORIENTED_EDGE ( 'NONE', *, *, #5430, .T. ) ;
#933=CARTESIAN_POINT ( 'NONE',  ( -0.1581195908683433182, 13.69161915620259151, 6.124206696172819875 ) ) ;
#935=CARTESIAN_POINT ( 'NONE',  ( 1.596228967263000786, 11.66853105775998678, 4.467123007223999132 ) ) ;
#937=CARTESIAN_POINT ( 'NONE',  ( -20.11353743917332082, -9.187434725425410065, -1.202759340935936061 ) ) ;
#939=DIRECTION ( 'NONE',  ( -0.9999999999999994449, 3.360583440989998554E-08, -4.120678714624997717E-09 ) ) ;
#940=CIRCLE ( 'NONE', #18358, 7.000000000000000000 ) ;
#941=ORIENTED_EDGE ( 'NONE', *, *, #17551, .T. ) ;
#943=ADVANCED_FACE ( 'NONE', ( #21849, #1742 ), #10714, .F. ) ;
#944=CARTESIAN_POINT ( 'NONE',  ( 2.921430590333649935, 11.94558362360630177, 3.795594775063057202 ) ) ;
#945=CARTESIAN_POINT ( 'NONE',  ( 4.106019081683001559, 14.61196862056002388, 4.606493351513002210 ) ) ;
#949=CARTESIAN_POINT ( 'NONE',  ( -9.310023045028000155, 13.82947516575999991, -6.440908831219999797 ) ) ;
#950=DIRECTION ( 'NONE',  ( 1.000000000000000000, 0.000000000000000000, 0.000000000000000000 ) ) ;
#951=CARTESIAN_POINT ( 'NONE',  ( 14.79262625730999936, -7.984278194804999451, 4.494107504349000415 ) ) ;
#955=CARTESIAN_POINT ( 'NONE',  ( -22.26703117493464745, -4.632470568168542968, 8.021466634618056091 ) ) ;
#957=CARTESIAN_POINT ( 'NONE',  ( -12.25000000000000000, 6.613190111079999767, -13.46349570337000046 ) ) ;
#958=CARTESIAN_POINT ( 'NONE',  ( 0.9835805066508525041, 13.73841607712214241, -6.045557612536501146 ) ) ;
#964=CARTESIAN_POINT ( 'NONE',  ( 15.81388418947362062, -8.259696827618725479, -6.316793570899937649 ) ) ;
#965=CARTESIAN_POINT ( 'NONE',  ( -4.322696709239871815, 13.59640335390094634, 4.972036931828690776 ) ) ;
#966=LINE ( 'NONE', #2675, #23567 ) ;
#969=FACE_OUTER_BOUND ( 'NONE', #3292, .T. ) ;
#970=CARTESIAN_POINT ( 'NONE',  ( -2.922221168653406309, 11.94577451725421646, -3.794953772402525516 ) ) ;
#972=CARTESIAN_POINT ( 'NONE',  ( -23.50032910583999879, 1.512442827330999945E-14, 0.000000000000000000 ) ) ;
#975=DIRECTION ( 'NONE',  ( 1.000000000000000000, 0.000000000000000000, 0.000000000000000000 ) ) ;
#976=AXIS2_PLACEMENT_3D ( 'NONE', #11607, #4453, #18978 ) ;
#977=CARTESIAN_POINT ( 'NONE',  ( 15.85478027152999836, -10.51359821371000081, 3.409925352663000009 ) ) ;
#981=ORIENTED_EDGE ( 'NONE', *, *, #7459, .F. ) ;
#985=CARTESIAN_POINT ( 'NONE',  ( -20.15132910583999859, -9.188404534074999574, 1.125025998286999896E-14 ) ) ;
#987=EDGE_CURVE ( 'NONE', #13362, #22144, #4263, .T. ) ;
#988=CARTESIAN_POINT ( 'NONE',  ( -23.00369019983000030, -5.232895320036999642, 9.395593148101001546 ) ) ;
#991=CARTESIAN_POINT ( 'NONE',  ( 14.97294087919659056, 10.13249089077432785, 2.022385466357334405 ) ) ;
#992=CARTESIAN_POINT ( 'NONE',  ( -16.75277932490000055, 10.95855636149000034, -1.542517388603999784 ) ) ;
#994=CARTESIAN_POINT ( 'NONE',  ( 4.834780805419000238, 12.45065217972999960, 0.000000000000000000 ) ) ;
#996=CARTESIAN_POINT ( 'NONE',  ( -4.630573125257002154, 12.42127774015998298, -1.209421156049999224 ) ) ;
#1000=EDGE_LOOP ( 'NONE', ( #8543, #22260, #1976, #4442, #2164 ) ) ;
#1002=CARTESIAN_POINT ( 'NONE',  ( -15.62058162434104425, -7.748628952019913640, -6.926152932935100814 ) ) ;
#1004=CARTESIAN_POINT ( 'NONE',  ( 5.435972110109003275, 14.69581070629001474, -2.844462854985000178 ) ) ;
#1005=CARTESIAN_POINT ( 'NONE',  ( -4.544340308300998998, 13.49051417780999884, -5.132142894851999593 ) ) ;
#1006=CARTESIAN_POINT ( 'NONE',  ( -24.49999999999999289, 1.631301440766486310, -10.29771265513020850 ) ) ;
#1007=CARTESIAN_POINT ( 'NONE',  ( 15.47718892131000068, -5.177634673800000975, -8.189908713891000502 ) ) ;
#1010=CARTESIAN_POINT ( 'NONE',  ( -6.250000000000000000, 16.31160201366999729, -1.000000000001000089 ) ) ;
#1014=VERTEX_POINT ( 'NONE', #20737 ) ;
#1016=CARTESIAN_POINT ( 'NONE',  ( -4.900699999999999612, 1.284663064832999817E-14, 0.000000000000000000 ) ) ;
#1017=CARTESIAN_POINT ( 'NONE',  ( -23.44629291275694172, 5.369329345814918497, -7.615845659716430127 ) ) ;
#1018=CARTESIAN_POINT ( 'NONE',  ( -14.00000000000000533, 0.8719941289985287947, 9.658611517165889282 ) ) ;
#1019=CARTESIAN_POINT ( 'NONE',  ( 17.16962222460619358, 0.4914365713909190081, 10.41567669192089873 ) ) ;
#1021=CARTESIAN_POINT ( 'NONE',  ( -14.42499036736162310, -9.146326703434620953, 9.158041868012015030 ) ) ;
#1022=CARTESIAN_POINT ( 'NONE',  ( 20.96866900885000007, -10.17611281151999947, 4.721347032623000040 ) ) ;
#1025=CARTESIAN_POINT ( 'NONE',  ( -3.899678468944780096, 13.96058569223144374, -4.846132543982858643 ) ) ;
#1026=DIRECTION ( 'NONE',  ( 0.000000000000000000, 0.000000000000000000, -1.000000000000000000 ) ) ;
#1027=ADVANCED_FACE ( 'NONE', ( #11423 ), #13339, .T. ) ;
#1030=CARTESIAN_POINT ( 'NONE',  ( 23.56485220644000123, 10.89047681322000116, -1.152164691522000073 ) ) ;
#1031=B_SPLINE_CURVE_WITH_KNOTS ( 'NONE', 3,
 ( #20391, #7536, #11544, #11309, #13341, #16986, #5956, #15272, #13463, #388, #20621, #11190, #6072, #7417, #503, #2208, #18573, #18924, #22435, #4031, #9599, #145, #16734, #7785, #4276, #19036, #13114, #15039, #34, #2333, #7665, #9722 ),
 .UNSPECIFIED., .F., .F.,
 ( 4, 2, 2, 2, 2, 2, 2, 2, 2, 2, 2, 2, 2, 2, 2, 4 ),
 ( 0.000000000000000000, 0.1250000000000003053, 0.1875000000000003331, 0.2187500000000004718, 0.2500000000000006106, 0.3125000000000006106, 0.3437500000000005551, 0.3750000000000004996, 0.5000000000000004441, 0.5625000000000004441, 0.5937500000000005551, 0.6250000000000006661, 0.6875000000000006661, 0.7187500000000006661, 0.7500000000000005551, 1.000000000000000000 ),
 .UNSPECIFIED. ) ;
#1032=CARTESIAN_POINT ( 'NONE',  ( 24.18640269352763639, 8.182940205309693127, 6.768123944646319501 ) ) ;
#1033=AXIS2_PLACEMENT_3D ( 'NONE', #4893, #17856, #19791 ) ;
#1036=CARTESIAN_POINT ( 'NONE',  ( -11.04281598264000053, 1.359882291614000008E-14, 0.000000000000000000 ) ) ;
#1037=CARTESIAN_POINT ( 'NONE',  ( -4.884003751836998752, 12.49132197575000092, -0.8076278545717995305 ) ) ;
#1039=CARTESIAN_POINT ( 'NONE',  ( -16.62373390469630863, 9.968533772034067653, -3.001379283816392185 ) ) ;
#1041=VECTOR ( 'NONE', #1026, 1000.000000000000000 ) ;
#1043=CIRCLE ( 'NONE', #4136, 12.50000000000000000 ) ;
#1044=DIRECTION ( 'NONE',  ( 0.000000000000000000, 1.000000000000000000, 0.000000000000000000 ) ) ;
#1048=CARTESIAN_POINT ( 'NONE',  ( -12.07716019469000024, 9.613013645102999050, -12.04164784824000023 ) ) ;
#1049=FACE_OUTER_BOUND ( 'NONE', #9713, .T. ) ;
#1050=CARTESIAN_POINT ( 'NONE',  ( -18.06675765898000208, -8.132406931018000051, 7.220925319278000742 ) ) ;
#1051=CARTESIAN_POINT ( 'NONE',  ( 22.15395833333332121, -7.388848214911551082, -5.678196526935670896 ) ) ;
#1052=CARTESIAN_POINT ( 'NONE',  ( 16.07374951746000136, 1.809993214902999803, 9.579455531516000377 ) ) ;
#1055=EDGE_CURVE ( 'NONE', #6663, #12473, #16944, .T. ) ;
#1058=CARTESIAN_POINT ( 'NONE',  ( 1.934504865404305329, 13.87243343662209583, 5.816204379626650933 ) ) ;
#1060=AXIS2_PLACEMENT_3D ( 'NONE', #2053, #22506, #20579 ) ;
#1062=CARTESIAN_POINT ( 'NONE',  ( -19.93064731917000287, 1.667734798046999867, 10.92226482541000010 ) ) ;
#1063=VECTOR ( 'NONE', #16789, 1000.000000000000000 ) ;
#1067=CARTESIAN_POINT ( 'NONE',  ( 4.649999999999999467, 20.00000000000000000, 0.000000000000000000 ) ) ;
#1068=CARTESIAN_POINT ( 'NONE',  ( 4.675391681975701097, 12.38404500047236567, -1.288137502435812820 ) ) ;
#1069=EDGE_CURVE ( 'NONE', #629, #17203, #20259, .T. ) ;
#1070=CARTESIAN_POINT ( 'NONE',  ( -0.4616800974773001554, 13.20162905315999957, 6.080923912729003789 ) ) ;
#1074=CARTESIAN_POINT ( 'NONE',  ( -14.25521440656999950, -2.679375877985999743, 10.98274110836000084 ) ) ;
#1075=VECTOR ( 'NONE', #23438, 1000.000000000000000 ) ;
#1076=CARTESIAN_POINT ( 'NONE',  ( 18.54843892131000160, -5.767951301206999837, 7.596080989717999721 ) ) ;
#1078=CARTESIAN_POINT ( 'NONE',  ( 18.92821040849097614, 2.505321190189683911, 10.13026339292191302 ) ) ;
#1080=B_SPLINE_CURVE_WITH_KNOTS ( 'NONE', 3,
 ( #21557, #2531, #23107, #15843, #13667, #6769, #6283, #21188, #6405, #14162, #19376, #13786 ),
 .UNSPECIFIED., .F., .F.,
 ( 4, 1, 1, 1, 1, 2, 2, 4 ),
 ( 0.000000000000000000, 0.2499999999999980016, 0.3749999999999969469, 0.4374999999999963918, 0.4687499999999962252, 0.4843749999999963363, 0.4999999999999964473, 1.000000000000000000 ),
 .UNSPECIFIED. ) ;
#1084=CARTESIAN_POINT ( 'NONE',  ( -2.511040024960635719, 13.99897430365290596, -5.586622607424842180 ) ) ;
#1085=ORIENTED_EDGE ( 'NONE', *, *, #23142, .F. ) ;
#1087=VECTOR ( 'NONE', #8395, 1000.000000000000000 ) ;
#1092=CARTESIAN_POINT ( 'NONE',  ( 15.45148061670815842, -8.690430497184191694, 5.949322236961282151 ) ) ;
#1095=CARTESIAN_POINT ( 'NONE',  ( -23.99212502903982980, -8.254180775415035143, 10.70333952211954198 ) ) ;
#1096=EDGE_LOOP ( 'NONE', ( #6511, #10471, #14338, #13387 ) ) ;
#1098=CARTESIAN_POINT ( 'NONE',  ( -4.143590529358013974, 12.32185200877851905, -2.404200284871922388 ) ) ;
#1099=AXIS2_PLACEMENT_3D ( 'NONE', #23876, #22181, #20021 ) ;
#1100=EDGE_LOOP ( 'NONE', ( #9009, #12037, #22729, #307, #8287, #5800, #13151, #4308, #8031, #1436 ) ) ;
#1102=CARTESIAN_POINT ( 'NONE',  ( 6.131904361748996557, 14.49481577323998494, -0.05944742189950995986 ) ) ;
#1103=EDGE_CURVE ( 'NONE', #23793, #12304, #11219, .T. ) ;
#1104=CARTESIAN_POINT ( 'NONE',  ( -2.937971692690656944, 13.09510414649091103, 6.070550775144435640 ) ) ;
#1105=CARTESIAN_POINT ( 'NONE',  ( 6.228968653373813780, 13.74531475821428472, -1.369654784524615421 ) ) ;
#1108=LINE ( 'NONE', #7040, #6688 ) ;
#1109=VERTEX_POINT ( 'NONE', #4029 ) ;
#1110=CYLINDRICAL_SURFACE ( 'NONE', #20496, 10.59999999999999964 ) ;
#1113=CARTESIAN_POINT ( 'NONE',  ( 6.125000000000000000, 22.00000000000000000, 0.000000000000000000 ) ) ;
#1114=VERTEX_POINT ( 'NONE', #15150 ) ;
#1115=CARTESIAN_POINT ( 'NONE',  ( -18.87548909685999732, -9.583084618030000001, 1.668392796240999898 ) ) ;
#1116=DIRECTION ( 'NONE',  ( 0.000000000000000000, -0.5000000000000169864, 0.8660254037844288266 ) ) ;
#1118=CARTESIAN_POINT ( 'NONE',  ( 15.23231850497268525, 4.710292849053081099, 9.203326907294682613 ) ) ;
#1120=DIRECTION ( 'NONE',  ( 0.000000000000000000, -1.000000000000000000, 0.000000000000000000 ) ) ;
#1122=CARTESIAN_POINT ( 'NONE',  ( 4.834782059083999606, 12.44497316928999808, -0.3759403457470999466 ) ) ;
#1125=CARTESIAN_POINT ( 'NONE',  ( -4.736748033549996073, 12.61325905412998871, 0.1514502988820001228 ) ) ;
#1127=CARTESIAN_POINT ( 'NONE',  ( 8.124934037954998800, -12.44999999999999929, 0.000000000000000000 ) ) ;
#1132=CARTESIAN_POINT ( 'NONE',  ( -16.54663518748942153, 8.347930828672053494, 6.471747366174584570 ) ) ;
#1133=AXIS2_PLACEMENT_3D ( 'NONE', #9306, #16563, #21795 ) ;
#1135=ORIENTED_EDGE ( 'NONE', *, *, #7163, .T. ) ;
#1137=CARTESIAN_POINT ( 'NONE',  ( 6.223523631586996174, 13.71390417251999949, -0.8158110508759003343 ) ) ;
#1139=CARTESIAN_POINT ( 'NONE',  ( 11.99999999999999822, -4.059331642145825647, -8.012115679970065685 ) ) ;
#1140=EDGE_CURVE ( 'NONE', #22006, #14445, #17840, .T. ) ;
#1142=CARTESIAN_POINT ( 'NONE',  ( -20.03205420454666452, -1.202231731695348138, -9.185343705029872297 ) ) ;
#1143=CARTESIAN_POINT ( 'NONE',  ( 15.83268908530999930, -1.865934471007999917, -10.03576702404999921 ) ) ;
#1144=ORIENTED_EDGE ( 'NONE', *, *, #1797, .F. ) ;
#1145=DIRECTION ( 'NONE',  ( 0.000000000000000000, 0.9981468999026679167, -0.06085035919937799298 ) ) ;
#1148=VECTOR ( 'NONE', #13158, 1000.000000000000114 ) ;
#1150=CARTESIAN_POINT ( 'NONE',  ( 11.72559253311346339, 12.88358093003557592, 2.684900464144857501 ) ) ;
#1152=CARTESIAN_POINT ( 'NONE',  ( -14.00000000000000178, 7.084868190922404274, 5.933636879945280995 ) ) ;
#1154=CARTESIAN_POINT ( 'NONE',  ( 16.65500885062994740, 10.07209838378439670, -2.687555505311734816 ) ) ;
#1156=DIRECTION ( 'NONE',  ( 0.000000000000000000, -0.9704651937236938863, -0.2412411817472984998 ) ) ;
#1157=CARTESIAN_POINT ( 'NONE',  ( -14.47125383376745589, -9.790219516174829550, 8.042794959434482749 ) ) ;
#1158=CARTESIAN_POINT ( 'NONE',  ( -4.059709635163400776, 13.79591589661956164, -4.865803654251010357 ) ) ;
#1162=CARTESIAN_POINT ( 'NONE',  ( 21.19327927328000172, 3.892238382344999970, -9.590411839331999033 ) ) ;
#1163=CARTESIAN_POINT ( 'NONE',  ( 24.04453577521502794, 10.40724578197013805, 2.113084592499416381 ) ) ;
#1165=ORIENTED_EDGE ( 'NONE', *, *, #10326, .T. ) ;
#1167=CARTESIAN_POINT ( 'NONE',  ( -24.17970357211695287, -12.87935348060794460, -2.692294542481509012 ) ) ;
#1168=CARTESIAN_POINT ( 'NONE',  ( -0.6105871316501998436, 11.54226242508000233, -4.935054442950004727 ) ) ;
#1170=CARTESIAN_POINT ( 'NONE',  ( -16.70746761638316968, 8.693072922700327609, -5.728755917543943532 ) ) ;
#1171=CARTESIAN_POINT ( 'NONE',  ( 16.98637625730999900, -6.405805545913000110, -6.631092424295999876 ) ) ;
#1172=VERTEX_POINT ( 'NONE', #15989 ) ;
#1173=AXIS2_PLACEMENT_3D ( 'NONE', #9633, #9751, #11343 ) ;
#1178=CARTESIAN_POINT ( 'NONE',  ( 12.45881424931000048, -1.641155845125999768, -10.50071198764000080 ) ) ;
#1179=CARTESIAN_POINT ( 'NONE',  ( -23.89835131802999868, 11.12127188689000157, 1.495067083984999989 ) ) ;
#1180=CARTESIAN_POINT ( 'NONE',  ( -16.23858452724999779, -8.437247725758000527, 6.781230591525000406 ) ) ;
#1181=CARTESIAN_POINT ( 'NONE',  ( 22.26733333333332254, -4.654919140148669143, -8.076101565712940911 ) ) ;
#1182=CARTESIAN_POINT ( 'NONE',  ( 15.80244494526000132, 1.908725879256999880, 10.10239154523000060 ) ) ;
#1185=CARTESIAN_POINT ( 'NONE',  ( 15.61599999999999966, 9.072019050554999353, 0.000000000000000000 ) ) ;
#1186=VERTEX_POINT ( 'NONE', #10453 ) ;
#1187=CARTESIAN_POINT ( 'NONE',  ( 23.72055893949304561, -3.444828185086491690, 8.695936745105788290 ) ) ;
#1188=CARTESIAN_POINT ( 'NONE',  ( 2.820196252569187934, 14.07833607265465758, 5.437106381143619771 ) ) ;
#1191=CARTESIAN_POINT ( 'NONE',  ( -14.13652826923847883, 9.034860340956925029, -1.094524698571601506 ) ) ;
#1192=CARTESIAN_POINT ( 'NONE',  ( -22.24936801119999785, 10.93443063335000076, 1.977547908896999829 ) ) ;
#1193=CARTESIAN_POINT ( 'NONE',  ( -4.196763389404418731, 12.21402715469226763, 2.415977519593344169 ) ) ;
#1194=ORIENTED_EDGE ( 'NONE', *, *, #14275, .F. ) ;
#1195=FACE_OUTER_BOUND ( 'NONE', #23097, .T. ) ;
#1197=CARTESIAN_POINT ( 'NONE',  ( 0.7693602595439000824, 13.21609357992999456, 6.056548692576001258 ) ) ;
#1198=CARTESIAN_POINT ( 'NONE',  ( -21.27917920454665790, 8.977395928926879876, 2.412738463204236794 ) ) ;
#1199=CARTESIAN_POINT ( 'NONE',  ( -10.04281598263999875, 20.50000000000000000, 1.000000000000000000 ) ) ;
#1201=DIRECTION ( 'NONE',  ( 0.000000000000000000, 0.000000000000000000, -1.000000000000000000 ) ) ;
#1202=CARTESIAN_POINT ( 'NONE',  ( -16.69277858220999988, 10.68419017778999880, -3.897213304429000491 ) ) ;
#1203=CARTESIAN_POINT ( 'NONE',  ( 16.13531392131000075, 9.604728693984000643, 1.402583754804999971 ) ) ;
#1205=ORIENTED_EDGE ( 'NONE', *, *, #11724, .F. ) ;
#1206=CARTESIAN_POINT ( 'NONE',  ( 5.262221487413253129, 13.84847638346749044, 4.167423381671452098 ) ) ;
#1208=CARTESIAN_POINT ( 'NONE',  ( -15.57853743917333311, 9.071057687409222581, 1.187525622282655124 ) ) ;
#1209=DIRECTION ( 'NONE',  ( 0.000000000000000000, -0.5795667693381943986, 0.8149247571885935848 ) ) ;
#1210=B_SPLINE_CURVE_WITH_KNOTS ( 'NONE', 3,
 ( #17375, #17133, #21259, #893, #22578, #4671, #15660, #528, #6472, #19063, #13367, #13856, #20768, #22690, #20039, #14349, #10231, #1018, #1516, #8906, #19685, #21740, #21854, #23296, #1271, #3340, #12423, #5154, #8783, #1152, #23547, #5265, #10717, #18109, #8657, #6834, #23179 ),
 .UNSPECIFIED., .F., .F.,
 ( 4, 2, 1, 2, 2, 1, 1, 2, 2, 1, 2, 2, 1, 1, 1, 1, 2, 2, 1, 1, 1, 2, 2, 4 ),
 ( 0.000000000000000000, 0.1250000000000004996, 0.1875000000000006106, 0.2187500000000006106, 0.2500000000000006106, 0.3125000000000004996, 0.3437500000000004996, 0.3593750000000004996, 0.3750000000000004996, 0.4375000000000005551, 0.4687500000000006661, 0.5000000000000006661, 0.6250000000000009992, 0.6875000000000013323, 0.7187500000000014433, 0.7343750000000013323, 0.7421875000000014433, 0.7500000000000014433, 0.8125000000000011102, 0.8437500000000009992, 0.8593750000000008882, 0.8671875000000007772, 0.8750000000000006661, 1.000000000000000000 ),
 .UNSPECIFIED. ) ;
#1214=ADVANCED_FACE ( 'NONE', ( #4636 ), #4506, .T. ) ;
#1216=CARTESIAN_POINT ( 'NONE',  ( 15.39572622089800014, -7.354054053997821860, 7.547009246631161794 ) ) ;
#1217=CARTESIAN_POINT ( 'NONE',  ( -4.076854769385132471, 13.78041422864121479, 4.870052410342037064 ) ) ;
#1218=CARTESIAN_POINT ( 'NONE',  ( -21.77637077250666309, -7.380920199195522002, -5.672421320939294631 ) ) ;
#1219=CARTESIAN_POINT ( 'NONE',  ( 20.35970603379665889, -8.954414562724045012, 2.406562392635347436 ) ) ;
#1220=VERTEX_POINT ( 'NONE', #6564 ) ;
#1221=DIRECTION ( 'NONE',  ( 0.000000000000000000, -0.01045465616390956094, 0.9999453485888589732 ) ) ;
#1222=CARTESIAN_POINT ( 'NONE',  ( 12.28022044534097645, -7.993836135614808214, 11.15426966573714473 ) ) ;
#1223=B_SPLINE_CURVE_WITH_KNOTS ( 'NONE', 3,
 ( #5114, #12495, #12612, #5571 ),
 .UNSPECIFIED., .F., .F.,
 ( 4, 4 ),
 ( 0.000000000000000000, 1.000000000000000000 ),
 .UNSPECIFIED. ) ;
#1227=CARTESIAN_POINT ( 'NONE',  ( -1.425181558570351115, 12.87128047289576216, 6.531978145723615903 ) ) ;
#1228=CARTESIAN_POINT ( 'NONE',  ( 12.50000000000000000, 13.93375672974000068, 0.000000000000000000 ) ) ;
#1231=LINE ( 'NONE', #15984, #14039 ) ;
#1235=DIRECTION ( 'NONE',  ( 1.000000000000000000, 0.000000000000000000, 0.000000000000000000 ) ) ;
#1236=VERTEX_POINT ( 'NONE', #12142 ) ;
#1237=CARTESIAN_POINT ( 'NONE',  ( -23.76167883585000240, 10.79930063205999957, 3.320022971283000501 ) ) ;
#1238=LINE ( 'NONE', #8629, #11857 ) ;
#1239=CARTESIAN_POINT ( 'NONE',  ( 15.12422319296440065, 7.823096909157138512, 6.778400638252913168 ) ) ;
#1240=DIRECTION ( 'NONE',  ( 0.000000000000000000, 0.000000000000000000, -1.000000000000000000 ) ) ;
#1242=ADVANCED_FACE ( 'NONE', ( #23141 ), #3276, .F. ) ;
#1244=CARTESIAN_POINT ( 'NONE',  ( -4.775989160958999058, 12.47797649990998359, -0.3237615643668999010 ) ) ;
#1245=ORIENTED_EDGE ( 'NONE', *, *, #4475, .T. ) ;
#1246=DIRECTION ( 'NONE',  ( 0.000000000000000000, -1.000000000000000000, 0.000000000000000000 ) ) ;
#1251=CARTESIAN_POINT ( 'NONE',  ( -16.31512179670237472, 1.090436056802820852, 10.50050333464076147 ) ) ;
#1252=EDGE_CURVE ( 'NONE', #18988, #11301, #21592, .T. ) ;
#1255=CARTESIAN_POINT ( 'NONE',  ( 5.513483907770004855, 14.23393714730998560, -2.574004873080997680 ) ) ;
#1257=CARTESIAN_POINT ( 'NONE',  ( 16.82469336267999793, 6.712115241498000096, 8.814690082545999061 ) ) ;
#1258=EDGE_CURVE ( 'NONE', #9228, #1109, #20726, .T. ) ;
#1260=CARTESIAN_POINT ( 'NONE',  ( 15.50362658531000193, -9.889101471244000408, -2.495492728532000104 ) ) ;
#1263=CARTESIAN_POINT ( 'NONE',  ( -11.02918649291999920, -11.29156741745999959, 9.124755533559000042 ) ) ;
#1265=DIRECTION ( 'NONE',  ( 0.9996708941621519351, 0.02565352539210875166, 3.160978645759844973E-14 ) ) ;
#1267=CARTESIAN_POINT ( 'NONE',  ( -24.05821396189999817, -9.114349543487000105, 1.114048544447999944 ) ) ;
#1268=CARTESIAN_POINT ( 'NONE',  ( 11.66614181939630512, 12.78577920083404429, 2.854240613876971366 ) ) ;
#1269=CARTESIAN_POINT ( 'NONE',  ( 22.23518289557183181, 6.552653103078741381, 8.300818614678858509 ) ) ;
#1271=CARTESIAN_POINT ( 'NONE',  ( -14.00000000000000178, 5.717788174535797019, 7.417575028664895598 ) ) ;
#1272=CARTESIAN_POINT ( 'NONE',  ( 16.31493751112632040, 1.365414610549234631, -10.28867410738198629 ) ) ;
#1273=DIRECTION ( 'NONE',  ( -1.000000000000000000, 0.000000000000000000, 0.000000000000000000 ) ) ;
#1275=EDGE_CURVE ( 'NONE', #3898, #15294, #15523, .T. ) ;
#1282=CARTESIAN_POINT ( 'NONE',  ( 19.94564619923999871, 6.840494197459999981, -9.103015306854999267 ) ) ;
#1283=CARTESIAN_POINT ( 'NONE',  ( 22.59749320841400433, 1.050738802132360705, 10.52673552388134581 ) ) ;
#1286=CYLINDRICAL_SURFACE ( 'NONE', #2168, 10.59999999999999964 ) ;
#1287=DIRECTION ( 'NONE',  ( 0.000000000000000000, 0.9999453485888588622, 0.01045465616390955921 ) ) ;
#1289=CARTESIAN_POINT ( 'NONE',  ( 1.437939696344002316, 11.60874954011002025, -4.772587024640002618 ) ) ;
#1291=CARTESIAN_POINT ( 'NONE',  ( -16.65164514192520429, 9.627632571596107525, -3.955004559287954358 ) ) ;
#1292=FACE_OUTER_BOUND ( 'NONE', #3662, .T. ) ;
#1294=DIRECTION ( 'NONE',  ( -1.000000000000000000, 0.000000000000000000, 0.000000000000000000 ) ) ;
#1295=CARTESIAN_POINT ( 'NONE',  ( -14.25243324638999809, -6.216878364870000340, -12.50000000000000000 ) ) ;
#1297=CARTESIAN_POINT ( 'NONE',  ( -10.04561490871999929, 16.32684872328999859, -1.000000000000000000 ) ) ;
#1298=CARTESIAN_POINT ( 'NONE',  ( 12.56850174931000019, 2.370728120151999629, -10.36336111974000040 ) ) ;
#1299=CARTESIAN_POINT ( 'NONE',  ( -22.40107856874000092, 10.65649927505999806, -0.3310050493610999789 ) ) ;
#1300=CARTESIAN_POINT ( 'NONE',  ( -14.20728104755000132, -10.73719763778000136, -0.8140697014076999638 ) ) ;
#1304=CARTESIAN_POINT ( 'NONE',  ( 19.32374951746000136, 9.811947351814998441, 0.7349391902708000135 ) ) ;
#1306=PRODUCT_DEFINITION_FORMATION_WITH_SPECIFIED_SOURCE ( 'ANY', '', #20806, .NOT_KNOWN. ) ;
#1309=ORIENTED_EDGE ( 'NONE', *, *, #8194, .T. ) ;
#1310=CARTESIAN_POINT ( 'NONE',  ( -17.08430420454666887, -5.598425178770643384, 7.284634173358401021 ) ) ;
#1311=DIRECTION ( 'NONE',  ( -1.000000000000000000, 0.000000000000000000, 0.000000000000000000 ) ) ;
#1315=CARTESIAN_POINT ( 'NONE',  ( -19.48508853042000055, -10.46451423961999794, 1.868989650143999981 ) ) ;
#1316=CARTESIAN_POINT ( 'NONE',  ( -2.142505351569140792, 11.67753982942237378, 4.317242088958800572 ) ) ;
#1319=CARTESIAN_POINT ( 'NONE',  ( -24.47970833437514671, -1.023963593989784870, -12.49997010189743563 ) ) ;
#1321=CARTESIAN_POINT ( 'NONE',  ( -20.59892920454666410, -8.038787966541713459, 4.633122357395726532 ) ) ;
#1323=ORIENTED_EDGE ( 'NONE', *, *, #10262, .T. ) ;
#1324=( BOUNDED_SURFACE ( )  B_SPLINE_SURFACE ( 3, 3, ( 
 ( #17242, #9621, #7686, #4293, #6341, #17126 ),
 ( #20886, #15416, #17006, #19056, #405, #5865 ),
 ( #7925, #13251, #11682, #2469, #20642, #522 ),
 ( #15176, #4053, #7804, #9740, #9860, #15292 ) ),
 .UNSPECIFIED., .F., .F., .T. ) 
 B_SPLINE_SURFACE_WITH_KNOTS ( ( 4, 4 ),
 ( 4, 1, 1, 4 ),
 ( 0.000000000000000000, 1.000000000000000000 ),
 ( 0.9657854881572999206, 0.9726412705193000496, 0.9856983999281999642, 0.9888385341825000063 ),
 .UNSPECIFIED. ) 
 GEOMETRIC_REPRESENTATION_ITEM ( )  RATIONAL_B_SPLINE_SURFACE ( (
 ( 1.047483055770999982, 1.047483055770999982, 1.047483055770999982, 1.047483055770999982, 1.047483055770999982, 1.047483055770999982),
 ( 0.9841723147430000429, 0.9841723147430000429, 0.9841723147430000429, 0.9841723147430000429, 0.9841723147430000429, 0.9841723147430000429),
 ( 0.9841723147430000429, 0.9841723147430000429, 0.9841723147430000429, 0.9841723147430000429, 0.9841723147430000429, 0.9841723147430000429),
 ( 1.047483055770999982, 1.047483055770999982, 1.047483055770999982, 1.047483055770999982, 1.047483055770999982, 1.047483055770999982) ) ) 
 REPRESENTATION_ITEM ( '' )  SURFACE ( )  );
#1325=DIRECTION ( 'NONE',  ( -1.000000000000000000, 0.000000000000000000, 0.000000000000000000 ) ) ;
#1326=CARTESIAN_POINT ( 'NONE',  ( -15.06773579844999844, 6.079600582824999933, -9.557752359651999541 ) ) ;
#1327=CARTESIAN_POINT ( 'NONE',  ( 15.58687642131000040, -1.771707419409999984, -9.528874100789000323 ) ) ;
#1328=CARTESIAN_POINT ( 'NONE',  ( 18.45452326807764720, 9.933489636791392741, -3.151000111601911069 ) ) ;
#1330=CARTESIAN_POINT ( 'NONE',  ( 12.52688711657000020, -13.93375672974000068, -0.8660254037843999608 ) ) ;
#1333=B_SPLINE_CURVE_WITH_KNOTS ( 'NONE', 3,
 ( #18317, #11286, #20365, #18663, #23872, #3776, #11044, #7055, #9225, #18550, #14439, #5246, #14, #16715, #7398, #22176, #19259, #5932, #15127, #4006 ),
 .UNSPECIFIED., .F., .F.,
 ( 4, 2, 2, 1, 1, 2, 2, 2, 2, 2, 4 ),
 ( 0.000000000000000000, 0.2499999999999911737, 0.3749999999999851785, 0.4374999999999799050, 0.4687499999999784062, 0.4843749999999780176, 0.4999999999999776845, 0.6249999999999839018, 0.6874999999999863443, 0.7499999999999887867, 1.000000000000000000 ),
 .UNSPECIFIED. ) ;
#1334=CARTESIAN_POINT ( 'NONE',  ( -14.89828743917333398, -7.239954394872571974, 5.563771113903599463 ) ) ;
#1335=CARTESIAN_POINT ( 'NONE',  ( 3.128306947727627740, 14.16607981661443461, -5.265925022374893238 ) ) ;
#1337=DIRECTION ( 'NONE',  ( 1.000000000000000000, 0.000000000000000000, 0.000000000000000000 ) ) ;
#1338=CARTESIAN_POINT ( 'NONE',  ( -24.11803009775520934, -13.00903097537756992, 2.467105211282460964 ) ) ;
#1339=CARTESIAN_POINT ( 'NONE',  ( 16.14508333333333212, -2.378018344083014490, 8.849171197995115534 ) ) ;
#1340=FACE_OUTER_BOUND ( 'NONE', #2755, .T. ) ;
#1342=CARTESIAN_POINT ( 'NONE',  ( 0.8370874130355989706, 11.55651838240000195, 4.900516244706000890 ) ) ;
#1343=EDGE_CURVE ( 'NONE', #19206, #4168, #8387, .T. ) ;
#1344=CARTESIAN_POINT ( 'NONE',  ( -12.25000000000000355, 7.259277535838063677, -12.86049852923413539 ) ) ;
#1346=DIRECTION ( 'NONE',  ( 0.000000000000000000, -1.000000000000000000, 0.000000000000000000 ) ) ;
#1350=CARTESIAN_POINT ( 'NONE',  ( -19.10482910584000038, 1.458613477275000161E-14, 0.000000000000000000 ) ) ;
#1351=CARTESIAN_POINT ( 'NONE',  ( 12.52688711657000020, 6.216878364870000340, -12.50000000000000000 ) ) ;
#1353=CARTESIAN_POINT ( 'NONE',  ( 13.49999999999999645, -1.222753220167238863, 10.22419479022183708 ) ) ;
#1354=DIRECTION ( 'NONE',  ( -0.7071067811866525998, 0.000000000000000000, -0.7071067811864425456 ) ) ;
#1355=EDGE_LOOP ( 'NONE', ( #7560, #5400, #15054, #407 ) ) ;
#1356=DIRECTION ( 'NONE',  ( 1.000000000000000000, 0.000000000000000000, 0.000000000000000000 ) ) ;
#1357=AXIS2_PLACEMENT_3D ( 'NONE', #18081, #21470, #8753 ) ;
#1358=LINE ( 'NONE', #21591, #9002 ) ;
#1361=CARTESIAN_POINT ( 'NONE',  ( -21.38886788576999720, 8.715394838837001501, 5.275457124725000391 ) ) ;
#1363=CARTESIAN_POINT ( 'NONE',  ( 15.23219685105820709, 4.714089901989198417, 9.201376909055083431 ) ) ;
#1367=CARTESIAN_POINT ( 'NONE',  ( 13.50000000000000000, 4.517872873748999929, -7.804362139085999850 ) ) ;
#1368=CARTESIAN_POINT ( 'NONE',  ( 3.118557983420002344, 12.06593937194998922, -3.608953852771001447 ) ) ;
#1370=CARTESIAN_POINT ( 'NONE',  ( -22.18617920454664727, -9.000065539970952599, -2.418830751902067533 ) ) ;
#1375=EDGE_LOOP ( 'NONE', ( #7092, #3096, #7354, #23291 ) ) ;
#1376=CARTESIAN_POINT ( 'NONE',  ( 12.52688711657000020, -13.93375672974000068, -0.8660254037843999608 ) ) ;
#1377=CARTESIAN_POINT ( 'NONE',  ( 12.00000000000000000, -6.717641695603743024, -5.958818398439713171 ) ) ;
#1378=B_SPLINE_CURVE_WITH_KNOTS ( 'NONE', 3,
 ( #13207, #2184, #22177, #5589, #15128, #9696, #9462, #4255, #16837, #20598, #476, #22526, #5933, #11643 ),
 .UNSPECIFIED., .F., .F.,
 ( 4, 2, 2, 2, 2, 2, 4 ),
 ( 0.000000000000000000, 0.1249999999999985290, 0.1874999999999984734, 0.2499999999999984457, 0.3749999999999983347, 0.4999999999999983347, 1.000000000000000000 ),
 .UNSPECIFIED. ) ;
#1379=CARTESIAN_POINT ( 'NONE',  ( 15.77581727657000066, -6.549303922337999850, -8.900682842320000177 ) ) ;
#1383=FACE_OUTER_BOUND ( 'NONE', #11764, .T. ) ;
#1384=CARTESIAN_POINT ( 'NONE',  ( 13.50000000000000178, 9.568802105555617388, -0.1296229622023596650 ) ) ;
#1385=SURFACE_STYLE_FILL_AREA ( #15784 ) ;
#1386=VERTEX_POINT ( 'NONE', #11152 ) ;
#1387=CARTESIAN_POINT ( 'NONE',  ( -23.03001354826000124, 9.280677558483001022, 2.853289170403999986 ) ) ;
#1388=CARTESIAN_POINT ( 'NONE',  ( 11.36448692219687651, 9.446283672483898997, 8.638507912450332782 ) ) ;
#1389=CARTESIAN_POINT ( 'NONE',  ( 23.47059551751145179, 4.797115948774011152, -9.456088267976967998 ) ) ;
#1390=CIRCLE ( 'NONE', #5627, 12.44999999999999574 ) ;
#1392=CARTESIAN_POINT ( 'NONE',  ( 16.27550863102649359, -0.04483518904284756329, -10.36594529132968923 ) ) ;
#1393=EDGE_CURVE ( 'NONE', #22764, #1513, #151, .T. ) ;
#1395=B_SPLINE_CURVE_WITH_KNOTS ( 'NONE', 3,
 ( #3563, #18223, #7534, #18333, #5490 ),
 .UNSPECIFIED., .F., .F.,
 ( 4, 1, 4 ),
 ( 0.000000000000000000, 0.5000000000000000000, 1.000000000000000000 ),
 .UNSPECIFIED. ) ;
#1397=CARTESIAN_POINT ( 'NONE',  ( -15.59561067990999916, -1.941903525450000112, 10.08593956198000008 ) ) ;
#1401=CARTESIAN_POINT ( 'NONE',  ( 11.09594815123491074, 11.32305097982894182, -5.387897831827406669 ) ) ;
#1402=CARTESIAN_POINT ( 'NONE',  ( 23.61893502027211511, 3.101547904345725915, -10.14056206740493593 ) ) ;
#1405=CARTESIAN_POINT ( 'NONE',  ( 11.01624327026000039, 12.44999999999999929, 0.000000000000000000 ) ) ;
#1407=CIRCLE ( 'NONE', #8349, 4.649999999999999467 ) ;
#1408=CARTESIAN_POINT ( 'NONE',  ( 3.883475859697001376, 12.07688333241999068, -3.051465999718002475 ) ) ;
#1409=ORIENTED_EDGE ( 'NONE', *, *, #14537, .T. ) ;
#1411=CARTESIAN_POINT ( 'NONE',  ( 16.54762625731000014, -6.940875756134999186, 6.051234330564000174 ) ) ;
#1415=CARTESIAN_POINT ( 'NONE',  ( -23.75701756399666209, -13.93375672974000068, -0.3849425590144652243 ) ) ;
#1417=DIRECTION ( 'NONE',  ( -1.000000000000000000, 0.000000000000000000, 0.000000000000000000 ) ) ;
#1418=CARTESIAN_POINT ( 'NONE',  ( -4.032879115117613544, 14.96244278679635187, -4.610086244949046730 ) ) ;
#1419=CARTESIAN_POINT ( 'NONE',  ( -22.18849929921000097, -0.6770054873877999757, 10.11404905110999941 ) ) ;
#1420=CARTESIAN_POINT ( 'NONE',  ( -13.86707078901000045, 5.903954493066000175, -8.344675977248000365 ) ) ;
#1421=CARTESIAN_POINT ( 'NONE',  ( -5.403725322399998809, 14.30357683451000739, -5.155213201826003733 ) ) ;
#1422=CARTESIAN_POINT ( 'NONE',  ( -23.62400123529080176, 3.021837668578921221, 10.14788162303472596 ) ) ;
#1426=DIRECTION ( 'NONE',  ( -1.000000000000000000, 0.000000000000000000, 0.000000000000000000 ) ) ;
#1432=CARTESIAN_POINT ( 'NONE',  ( 3.957520350577631074, 14.44398668127747953, 4.674802188335122288 ) ) ;
#1436=ORIENTED_EDGE ( 'NONE', *, *, #987, .T. ) ;
#1438=CARTESIAN_POINT ( 'NONE',  ( -24.41904027020278534, -2.048447027932289721, -12.49998758062248072 ) ) ;
#1440=DIRECTION ( 'NONE',  ( 1.000000000000000000, 0.000000000000000000, 0.000000000000000000 ) ) ;
#1441=EDGE_CURVE ( 'NONE', #9887, #10277, #1709, .T. ) ;
#1442=AXIS2_PLACEMENT_3D ( 'NONE', #8505, #8620, #21815 ) ;
#1443=CARTESIAN_POINT ( 'NONE',  ( -20.97684587121333166, 2.410473131623945608, 8.969936553441268501 ) ) ;
#1444=ORIENTED_EDGE ( 'NONE', *, *, #5542, .T. ) ;
#1447=CARTESIAN_POINT ( 'NONE',  ( 17.78062642131000004, 8.824178357484999680, -4.146495103786000058 ) ) ;
#1448=CARTESIAN_POINT ( 'NONE',  ( 18.51438200485527474, 10.36799380519708613, -1.084925629257029511 ) ) ;
#1455=VERTEX_POINT ( 'NONE', #9099 ) ;
#1460=CARTESIAN_POINT ( 'NONE',  ( -23.91865653299513994, -2.798222612723384906, 9.337377610831497421 ) ) ;
#1462=CARTESIAN_POINT ( 'NONE',  ( 24.50000000000000711, -4.607483203864474852, 9.612698788763484714 ) ) ;
#1463=CARTESIAN_POINT ( 'NONE',  ( -3.972370958142942055, 13.88120499530448271, 4.850339516680738150 ) ) ;
#1464=CARTESIAN_POINT ( 'NONE',  ( -12.24999999999999645, 9.514185716142288030, -11.72205336956529820 ) ) ;
#1466=CARTESIAN_POINT ( 'NONE',  ( -18.33732910583999853, -9.141853718868999223, 0.000000000000000000 ) ) ;
#1468=DIRECTION ( 'NONE',  ( 0.000000000000000000, -0.9999453485888588622, -0.01045465616390954186 ) ) ;
#1473=CARTESIAN_POINT ( 'NONE',  ( 11.09594815121217337, 0.9954690943758390809, -12.49999871279053920 ) ) ;
#1475=CARTESIAN_POINT ( 'NONE',  ( 6.243179886996583328, 13.64542961362179518, -1.868502116970985671 ) ) ;
#1480=DIRECTION ( 'NONE',  ( 0.000000000000000000, 0.4408793407386908392, -0.8975663802247816347 ) ) ;
#1484=CARTESIAN_POINT ( 'NONE',  ( -20.18930073651999990, -0.1331888895339000123, -10.15414876350000029 ) ) ;
#1485=CARTESIAN_POINT ( 'NONE',  ( 20.56670833333332382, -1.204281607287327249, -9.199063983722616911 ) ) ;
#1486=CARTESIAN_POINT ( 'NONE',  ( 14.65490855118977720, 6.368553073539274578, -8.126428349890224112 ) ) ;
#1487=DIRECTION ( 'NONE',  ( 0.000000000000000000, 0.000000000000000000, 1.000000000000000000 ) ) ;
#1488=CARTESIAN_POINT ( 'NONE',  ( 23.90542041631999837, 10.75005818520000034, 3.477932657473000067 ) ) ;
#1490=CARTESIAN_POINT ( 'NONE',  ( -22.45139694715554768, -7.393363156508755196, 5.681353437585703325 ) ) ;
#1491=CARTESIAN_POINT ( 'NONE',  ( 2.320742031598997279, 11.86997853088999655, -4.174612069706000739 ) ) ;
#1493=B_SPLINE_CURVE_WITH_KNOTS ( 'NONE', 3,
 ( #3469, #23790, #23909, #1993, #11208 ),
 .UNSPECIFIED., .F., .F.,
 ( 4, 1, 4 ),
 ( 0.000000000000000000, 0.5000000000000000000, 1.000000000000000000 ),
 .UNSPECIFIED. ) ;
#1496=ORIENTED_EDGE ( 'NONE', *, *, #16640, .T. ) ;
#1498=CARTESIAN_POINT ( 'NONE',  ( -14.20256210577654166, -8.310917263278849276, 6.177374401935199266 ) ) ;
#1501=CIRCLE ( 'NONE', #4196, 3.000000000000000000 ) ;
#1502=DIRECTION ( 'NONE',  ( -1.000000000000000000, 0.000000000000000000, 0.000000000000000000 ) ) ;
#1503=CARTESIAN_POINT ( 'NONE',  ( 11.85409292834168049, -13.07924560384158852, -2.346130611933173071 ) ) ;
#1504=CARTESIAN_POINT ( 'NONE',  ( 12.00000000000000355, 3.355345449857968454, -8.329183830964261404 ) ) ;
#1508=CARTESIAN_POINT ( 'NONE',  ( -11.62537363877000018, -0.5797963012832000329, 15.20738078243999958 ) ) ;
#1510=CARTESIAN_POINT ( 'NONE',  ( 13.50000000000000178, 9.112083061060197053, -2.440520083675369101 ) ) ;
#1512=ADVANCED_FACE ( 'NONE', ( #16470 ), #18202, .T. ) ;
#1513=VERTEX_POINT ( 'NONE', #3427 ) ;
#1514=CARTESIAN_POINT ( 'NONE',  ( 21.26450154976144802, -8.294907895047991531, -6.779548171067567353 ) ) ;
#1515=B_SPLINE_CURVE_WITH_KNOTS ( 'NONE', 3,
 ( #765, #19176, #20996, #12044, #4290, #13598, #12163, #2584, #17737, #1142, #22919, #2839, #6462, #17235, #19053, #4780, #15413, #22800 ),
 .UNSPECIFIED., .F., .F.,
 ( 4, 2, 2, 2, 2, 2, 2, 2, 4 ),
 ( 0.000000000000000000, 0.1250000000000000278, 0.2500000000000000555, 0.3750000000000001110, 0.5000000000000001110, 0.6250000000000001110, 0.7500000000000000000, 0.8750000000000001110, 1.000000000000000000 ),
 .UNSPECIFIED. ) ;
#1516=CARTESIAN_POINT ( 'NONE',  ( -13.99999999999999822, 1.087951517378483279, 9.623364086261211980 ) ) ;
#1517=CARTESIAN_POINT ( 'NONE',  ( 17.31322874800178369, -4.549943461054996696, 9.392757792553869223 ) ) ;
#1518=CARTESIAN_POINT ( 'NONE',  ( -17.00152607621999934, -4.780068549123999588, -9.988549307159999557 ) ) ;
#1521=CARTESIAN_POINT ( 'NONE',  ( -12.50789737913000010, 5.572872693153001045, -7.876595158781000805 ) ) ;
#1522=EDGE_CURVE ( 'NONE', #11301, #1186, #10138, .T. ) ;
#1524=VERTEX_POINT ( 'NONE', #7268 ) ;
#1525=CARTESIAN_POINT ( 'NONE',  ( 23.58884305931480796, -7.417893891498020587, 5.701350536648257972 ) ) ;
#1526=CARTESIAN_POINT ( 'NONE',  ( 19.75239526568000059, -0.2837697319328000289, -11.37783472723000067 ) ) ;
#1527=CARTESIAN_POINT ( 'NONE',  ( 19.76015484213748152, -5.065527522992182341, -9.203031659326928349 ) ) ;
#1532=CARTESIAN_POINT ( 'NONE',  ( 4.985850635142116793, 14.19104587639733772, -3.879869294806315594 ) ) ;
#1533=CARTESIAN_POINT ( 'NONE',  ( -4.632032373251000479, 12.33312095925000307, -1.660520014003999512 ) ) ;
#1542=ORIENTED_EDGE ( 'NONE', *, *, #20251, .T. ) ;
#1543=CARTESIAN_POINT ( 'NONE',  ( -19.54076253787999562, 9.172736192578000214, 0.000000000000000000 ) ) ;
#1545=CARTESIAN_POINT ( 'NONE',  ( -21.59814514390000184, -9.834866976764999436, 4.060023984597999736 ) ) ;
#1547=CARTESIAN_POINT ( 'NONE',  ( -5.135907502119001045, 13.92753848266001349, -5.532842021099998675 ) ) ;
#1548=CARTESIAN_POINT ( 'NONE',  ( -22.23430444492038305, 10.49227087223982302, -1.974901390299137915 ) ) ;
#1552=EDGE_CURVE ( 'NONE', #22092, #13026, #22167, .T. ) ;
#1555=DIRECTION ( 'NONE',  ( 1.000000000000000000, 0.000000000000000000, 0.000000000000000000 ) ) ;
#1556=CARTESIAN_POINT ( 'NONE',  ( 3.872051077439735423, 14.41258966728797120, 4.746043954005092047 ) ) ;
#1558=B_SPLINE_CURVE_WITH_KNOTS ( 'NONE', 3,
 ( #5315, #8955, #20647, #22575, #16323, #23824, #3392, #12586, #7235, #20210, #22023, #4056, #5981, #11451, #18825, #5436, #2232, #9182 ),
 .UNSPECIFIED., .F., .F.,
 ( 4, 2, 2, 2, 2, 2, 2, 2, 4 ),
 ( 0.000000000000000000, 0.1249999999999999167, 0.2499999999999998890, 0.3749999999999998335, 0.4999999999999998890, 0.6249999999999998890, 0.7499999999999998890, 0.8750000000000000000, 1.000000000000000000 ),
 .UNSPECIFIED. ) ;
#1561=CARTESIAN_POINT ( 'NONE',  ( 1.472357546044718912, 11.57346035306418663, 4.589515119174757629 ) ) ;
#1562=ORIENTED_EDGE ( 'NONE', *, *, #6602, .F. ) ;
#1563=CARTESIAN_POINT ( 'NONE',  ( 17.73233333333332595, 4.596309454924390359, 7.974412893977484096 ) ) ;
#1564=CARTESIAN_POINT ( 'NONE',  ( 4.801955413365184278, 12.43156791562425489, -0.6979716084022052902 ) ) ;
#1565=CARTESIAN_POINT ( 'NONE',  ( -10.53807879897562394, 15.50632097202035098, 1.406271040994186761 ) ) ;
#1566=CARTESIAN_POINT ( 'NONE',  ( -21.20359587121333433, 8.052249294577444871, 4.641171550773364629 ) ) ;
#1567=ORIENTED_EDGE ( 'NONE', *, *, #2903, .F. ) ;
#1570=CARTESIAN_POINT ( 'NONE',  ( -11.00000000000000000, 10.59999999999999964, 0.000000000000000000 ) ) ;
#1572=CARTESIAN_POINT ( 'NONE',  ( 11.96718892131000089, -1.481964887125999830, -9.481920936164000224 ) ) ;
#1573=CARTESIAN_POINT ( 'NONE',  ( 18.45432512885125576, 9.931295749172702969, -3.157890530097379411 ) ) ;
#1577=CARTESIAN_POINT ( 'NONE',  ( 18.51344355829000321, 6.966878364870000340, -12.06698729810999993 ) ) ;
#1578=B_SPLINE_CURVE_WITH_KNOTS ( 'NONE', 3,
 ( #16341, #7138, #13063, #20339, #3870 ),
 .UNSPECIFIED., .F., .F.,
 ( 4, 1, 4 ),
 ( 0.000000000000000000, 0.5000000000000000000, 1.000000000000000000 ),
 .UNSPECIFIED. ) ;
#1579=ORIENTED_EDGE ( 'NONE', *, *, #8821, .T. ) ;
#1581=CARTESIAN_POINT ( 'NONE',  ( 19.86475848803999966, -8.290923745122999122, -6.795056182818000501 ) ) ;
#1585=CARTESIAN_POINT ( 'NONE',  ( 13.80672594031167399, -10.34511788736346638, 0.1683342567789284094 ) ) ;
#1586=CARTESIAN_POINT ( 'NONE',  ( -4.277841172294765570, 13.62415523807033324, 4.947054612845048993 ) ) ;
#1587=CARTESIAN_POINT ( 'NONE',  ( -2.715077639162999823, 11.83540306990998481, 4.154853624383998856 ) ) ;
#1588=CARTESIAN_POINT ( 'NONE',  ( -12.25000000000000178, 8.353912356140339668, -12.24351521210916438 ) ) ;
#1592=ORIENTED_EDGE ( 'NONE', *, *, #22403, .F. ) ;
#1594=FACE_OUTER_BOUND ( 'NONE', #3534, .T. ) ;
#1595=CARTESIAN_POINT ( 'NONE',  ( 4.146132389986815880, 13.37806292782055984, 5.418534502940187458 ) ) ;
#1596=CARTESIAN_POINT ( 'NONE',  ( 12.50448233770999984, 13.93375672974000068, 0.4328756433527000680 ) ) ;
#1597=CARTESIAN_POINT ( 'NONE',  ( 13.50000000000000000, -4.865356088987999428, 9.073685197596999430 ) ) ;
#1598=CARTESIAN_POINT ( 'NONE',  ( 8.124934037954998800, 14.44999999999999929, 0.000000000000000000 ) ) ;
#1599=ORIENTED_EDGE ( 'NONE', *, *, #23855, .T. ) ;
#1600=CARTESIAN_POINT ( 'NONE',  ( -15.35172225070999907, -1.839441420978000119, 9.553397381538999866 ) ) ;
#1603=DIRECTION ( 'NONE',  ( 1.000000000000000000, 0.000000000000000000, 0.000000000000000000 ) ) ;
#1605=CARTESIAN_POINT ( 'NONE',  ( -10.38832047382276613, 15.62395172623501871, -1.271871094456791473 ) ) ;
#1607=CARTESIAN_POINT ( 'NONE',  ( 14.77055141664746429, 9.043857732850597131, -4.985902765646755164 ) ) ;
#1609=CARTESIAN_POINT ( 'NONE',  ( 18.98657778229999948, -9.749946538104000027, 5.437902738275999681 ) ) ;
#1611=CARTESIAN_POINT ( 'NONE',  ( 13.69869376140666972, 8.478391648451442109, -3.082568484730727310 ) ) ;
#1612=CARTESIAN_POINT ( 'NONE',  ( 4.220193709370997581, 12.42420947506999873, -2.355922916967998049 ) ) ;
#1618=CARTESIAN_POINT ( 'NONE',  ( 17.27883333333331706, 7.964244026804120580, -4.590448486402081585 ) ) ;
#1620=CARTESIAN_POINT ( 'NONE',  ( 18.30212984639999974, 10.73999106964999939, 2.881100424796000148 ) ) ;
#1622=CARTESIAN_POINT ( 'NONE',  ( -9.087185065846002274, 6.105045399203000045, -13.55681854251999852 ) ) ;
#1623=CARTESIAN_POINT ( 'NONE',  ( 13.49999999999999822, 9.355385045509903463, 2.879371244180602307 ) ) ;
#1626=CARTESIAN_POINT ( 'NONE',  ( 23.38235175880183192, 1.726590010014731336, -10.45918579154710315 ) ) ;
#1627=CARTESIAN_POINT ( 'NONE',  ( 12.51792796885999870, -13.93375672974000068, 0.7216006907722000152 ) ) ;
#1628=CARTESIAN_POINT ( 'NONE',  ( 16.10298205229174329, -5.908803289076222320, -8.512465605292881321 ) ) ;
#1629=CARTESIAN_POINT ( 'NONE',  ( -18.82862077250666744, 1.198189225339994612, 9.154461231320610182 ) ) ;
#1630=VECTOR ( 'NONE', #19185, 1000.000000000000114 ) ;
#1632=CARTESIAN_POINT ( 'NONE',  ( -13.11728842303999976, -9.638936811879000643, -0.7309380707209000017 ) ) ;
#1635=CARTESIAN_POINT ( 'NONE',  ( 23.70216531585290909, -8.985547010004388824, 2.405992734474589945 ) ) ;
#1636=CARTESIAN_POINT ( 'NONE',  ( 22.51237305742672135, 4.065799934601714405, 9.766473785554790510 ) ) ;
#1637=CARTESIAN_POINT ( 'NONE',  ( -12.48243343204000055, 6.965111533508000718, -5.686492047758000545 ) ) ;
#1642=CARTESIAN_POINT ( 'NONE',  ( 4.854249925572221791, 14.55265595715461124, -3.782643825661391457 ) ) ;
#1643=CARTESIAN_POINT ( 'NONE',  ( -4.263501161146997731, 12.20307014857999839, -2.457753744994997547 ) ) ;
#1644=ORIENTED_EDGE ( 'NONE', *, *, #4507, .T. ) ;
#1646=ORIENTED_EDGE ( 'NONE', *, *, #7863, .T. ) ;
#1650=ORIENTED_EDGE ( 'NONE', *, *, #10005, .T. ) ;
#1651=CARTESIAN_POINT ( 'NONE',  ( -12.49414447734999989, 6.965344330034999309, -5.686682108691999638 ) ) ;
#1652=CARTESIAN_POINT ( 'NONE',  ( -23.47319277894999701, -9.624513788245998569, -3.290287683043000122 ) ) ;
#1653=CARTESIAN_POINT ( 'NONE',  ( -18.60511922971000232, -7.342831292577000291, 6.519673310378999886 ) ) ;
#1654=CARTESIAN_POINT ( 'NONE',  ( -6.378350646088002840, 15.10313706270000189, -3.204455250576998981 ) ) ;
#1655=LINE ( 'NONE', #18481, #14678 ) ;
#1659=ORIENTED_EDGE ( 'NONE', *, *, #14309, .F. ) ;
#1660=CARTESIAN_POINT ( 'NONE',  ( -18.33732910583999853, -9.141853718868999223, 0.000000000000000000 ) ) ;
#1662=CARTESIAN_POINT ( 'NONE',  ( 13.93567587029640364, 7.873185683027793758, -4.525993401469360577 ) ) ;
#1664=EDGE_CURVE ( 'NONE', #3791, #12959, #10926, .T. ) ;
#1666=CARTESIAN_POINT ( 'NONE',  ( 2.899766981581773706, 11.83721411937113821, 3.858556422892893245 ) ) ;
#1668=CARTESIAN_POINT ( 'NONE',  ( 0.4089070776637447335, 11.48994554096019982, -4.794126951967982997 ) ) ;
#1669=CARTESIAN_POINT ( 'NONE',  ( 24.27836688955406430, 7.477364734544921454, -6.207148011325140047 ) ) ;
#1675=CARTESIAN_POINT ( 'NONE',  ( 17.25862658530999738, -10.23584709072999921, -0.4386478486912999686 ) ) ;
#1676=CARTESIAN_POINT ( 'NONE',  ( 18.58956004406604023, 10.30724957857451329, 1.570066827172868607 ) ) ;
#1680=CARTESIAN_POINT ( 'NONE',  ( -12.50349985809999964, 6.524880561163000081, -6.187457173207999261 ) ) ;
#1681=CARTESIAN_POINT ( 'NONE',  ( 13.49999999999999822, -8.267279161049540193, 5.671028086302140281 ) ) ;
#1684=EDGE_CURVE ( 'NONE', #14929, #16467, #10917, .T. ) ;
#1685=CARTESIAN_POINT ( 'NONE',  ( 4.835177208035999818, 0.000000000000000000, 0.000000000000000000 ) ) ;
#1686=CARTESIAN_POINT ( 'NONE',  ( 23.13443595893999927, -10.50750968058000012, -4.259898950046999921 ) ) ;
#1687=LINE ( 'NONE', #9076, #350 ) ;
#1688=CARTESIAN_POINT ( 'NONE',  ( 13.69521714869160967, -9.517818908541695322, 4.057451185538291760 ) ) ;
#1692=EDGE_CURVE ( 'NONE', #8826, #10857, #17559, .T. ) ;
#1693=CARTESIAN_POINT ( 'NONE',  ( -23.31326413257000141, 3.475863815851999661, 10.58457578842000046 ) ) ;
#1694=EDGE_LOOP ( 'NONE', ( #8143, #22988, #19930, #23524, #16581, #9411, #11945, #14595, #20479, #9039, #14531 ) ) ;
#1700=CARTESIAN_POINT ( 'NONE',  ( 11.43887872963225938, 3.075720902665963763, -12.49994001780840058 ) ) ;
#1701=FACE_OUTER_BOUND ( 'NONE', #726, .T. ) ;
#1703=CARTESIAN_POINT ( 'NONE',  ( 14.62612658531000243, 9.561303730670999812, 3.483288127948000135 ) ) ;
#1706=ORIENTED_EDGE ( 'NONE', *, *, #13562, .F. ) ;
#1707=CARTESIAN_POINT ( 'NONE',  ( -18.13088126894000141, 1.446686056264999920E-14, 0.000000000000000000 ) ) ;
#1709=LINE ( 'NONE', #11035, #17167 ) ;
#1710=ORIENTED_EDGE ( 'NONE', *, *, #14895, .T. ) ;
#1711=CARTESIAN_POINT ( 'NONE',  ( -10.58090218245767389, 15.47935404656033853, -1.445406436927922700 ) ) ;
#1713=CARTESIAN_POINT ( 'NONE',  ( 14.54031634975408949, 2.702827404106709075, -9.961777166465550337 ) ) ;
#1715=CARTESIAN_POINT ( 'NONE',  ( -17.72676253787999912, 9.126185377371999863, 0.000000000000000000 ) ) ;
#1716=CARTESIAN_POINT ( 'NONE',  ( 20.93174364276999810, -5.383988185498999712, 9.840443131421999112 ) ) ;
#1718=CARTESIAN_POINT ( 'NONE',  ( 14.09937895178651956, 4.578329686716531732, 7.785341728062208588 ) ) ;
#1719=CARTESIAN_POINT ( 'NONE',  ( -3.588253153925999417, 12.21993382980000931, -3.223409665062000329 ) ) ;
#1720=B_SPLINE_CURVE_WITH_KNOTS ( 'NONE', 3,
 ( #19359, #2765, #930, #17904, #10396, #17787 ),
 .UNSPECIFIED., .F., .F.,
 ( 4, 2, 4 ),
 ( 0.7901839888852105753, 0.8950919944426052322, 1.000000000000000000 ),
 .UNSPECIFIED. ) ;
#1722=EDGE_CURVE ( 'NONE', #1842, #7244, #14041, .T. ) ;
#1723=ORIENTED_EDGE ( 'NONE', *, *, #16063, .F. ) ;
#1724=EDGE_CURVE ( 'NONE', #1220, #14845, #1080, .T. ) ;
#1725=AXIS2_PLACEMENT_3D ( 'NONE', #21645, #5061, #12442 ) ;
#1726=CARTESIAN_POINT ( 'NONE',  ( -14.69275774687465486, -4.229081981004126689, -8.019797593851203388 ) ) ;
#1727=CARTESIAN_POINT ( 'NONE',  ( 24.49999999999999289, -10.07254353310004369, -1.427226065814861000 ) ) ;
#1730=CARTESIAN_POINT ( 'NONE',  ( 11.55284350194278531, -12.59061462088587646, -3.192208964457393439 ) ) ;
#1731=DIRECTION ( 'NONE',  ( -0.000000000000000000, 1.000000000000000000, 0.000000000000000000 ) ) ;
#1733=CARTESIAN_POINT ( 'NONE',  ( 24.32802197706165259, 3.549421024388790258, -12.50000000000000355 ) ) ;
#1734=CARTESIAN_POINT ( 'NONE',  ( -15.31190575492827044, -4.623917834005626837, -9.292808272911738499 ) ) ;
#1740=CARTESIAN_POINT ( 'NONE',  ( -9.596297565846001021, -14.72535623507000047, 2.054682120933999823 ) ) ;
#1741=CARTESIAN_POINT ( 'NONE',  ( 13.50000000000000000, 9.582599390072616075, 0.7345775502715846672 ) ) ;
#1742=FACE_OUTER_BOUND ( 'NONE', #7598, .T. ) ;
#1743=EDGE_LOOP ( 'NONE', ( #21400, #18889, #3660, #23863 ) ) ;
#1744=CARTESIAN_POINT ( 'NONE',  ( 22.67640168912134513, -8.018325136500161321, 6.902805651056266534 ) ) ;
#1745=DIRECTION ( 'NONE',  ( -1.000000000000000000, 0.000000000000000000, 0.000000000000000000 ) ) ;
#1746=CARTESIAN_POINT ( 'NONE',  ( 16.01635173159208492, -8.104727441204580884, -6.451229416688261331 ) ) ;
#1750=CARTESIAN_POINT ( 'NONE',  ( -17.58615607838000372, 9.339993809354998788, 2.937842867551999859 ) ) ;
#1754=CARTESIAN_POINT ( 'NONE',  ( 22.22863922079730514, 10.51474377966081875, 2.086151727073547679 ) ) ;
#1758=CARTESIAN_POINT ( 'NONE',  ( -6.378247030388997985, 15.10307864196000516, 3.204776768353000183 ) ) ;
#1760=CARTESIAN_POINT ( 'NONE',  ( 2.361827492105001536, 11.73717613017002037, -4.198437883487004640 ) ) ;
#1762=CARTESIAN_POINT ( 'NONE',  ( 15.56043875731000092, 5.001549981505999831, -7.700678710662999471 ) ) ;
#1763=EDGE_LOOP ( 'NONE', ( #22179, #4490, #19938 ) ) ;
#1767=CARTESIAN_POINT ( 'NONE',  ( -14.50000017815840891, 0.2596243778658171020, -12.49999897408938310 ) ) ;
#1768=ORIENTED_EDGE ( 'NONE', *, *, #4821, .T. ) ;
#1770=CARTESIAN_POINT ( 'NONE',  ( -25.34824041399999928, -4.583299861329000358, -7.994677941742001082 ) ) ;
#1772=CARTESIAN_POINT ( 'NONE',  ( 12.12543434885914095, -8.197779943747480758, -10.80110243434621431 ) ) ;
#1773=CARTESIAN_POINT ( 'NONE',  ( -5.600699945962000825, 15.08715837589000053, -2.809455428781000297 ) ) ;
#1774=CARTESIAN_POINT ( 'NONE',  ( -23.85561736702028313, 9.397789499121957491, 4.882708127867132042 ) ) ;
#1778=ORIENTED_EDGE ( 'NONE', *, *, #22021, .T. ) ;
#1780=CARTESIAN_POINT ( 'NONE',  ( 14.21567657034085208, 8.191001517356450989, 3.937144643937185773 ) ) ;
#1782=CARTESIAN_POINT ( 'NONE',  ( 5.818132659865536738, 14.45536608084069208, -1.914417212635753929 ) ) ;
#1785=CARTESIAN_POINT ( 'NONE',  ( 4.254626796002882294, 12.23359600459727758, 2.313684877474057267 ) ) ;
#1786=EDGE_LOOP ( 'NONE', ( #15697, #16611, #15498, #7312, #19793, #10078, #15131, #16394, #6992, #18684 ) ) ;
#1787=CARTESIAN_POINT ( 'NONE',  ( -4.339621077386181192, 12.26288397286404575, -2.157489521576238634 ) ) ;
#1789=CARTESIAN_POINT ( 'NONE',  ( 4.835083642289389694, 12.44448910615697912, 0.3758261001295359338 ) ) ;
#1795=CARTESIAN_POINT ( 'NONE',  ( 14.73581408531000037, 7.589869243736000470, 6.782654363299000622 ) ) ;
#1796=CARTESIAN_POINT ( 'NONE',  ( 18.45416163448745195, 9.929482224075606211, -3.163580258347401308 ) ) ;
#1797=EDGE_CURVE ( 'NONE', #12884, #21421, #1941, .T. ) ;
#1799=FACE_OUTER_BOUND ( 'NONE', #14293, .T. ) ;
#1801=CARTESIAN_POINT ( 'NONE',  ( 13.50000000000000355, -8.034537072252554424, 6.023462719563941192 ) ) ;
#1804=CARTESIAN_POINT ( 'NONE',  ( 24.82213334836999863, -5.577735010582999919, 8.534839029212999861 ) ) ;
#1808=CARTESIAN_POINT ( 'NONE',  ( 24.50000000000000711, 2.053173317924622765, 10.18216561726737091 ) ) ;
#1809=CARTESIAN_POINT ( 'NONE',  ( -4.776861987225999862, 12.47838630334000065, -0.1510726511063999189 ) ) ;
#1811=EDGE_CURVE ( 'NONE', #2201, #11805, #6261, .T. ) ;
#1812=CARTESIAN_POINT ( 'NONE',  ( -20.63991140007999903, -5.133906642417999322, -9.805448442688000199 ) ) ;
#1816=ORIENTED_EDGE ( 'NONE', *, *, #14709, .T. ) ;
#1818=CARTESIAN_POINT ( 'NONE',  ( 4.822430994633001511, 14.15577629170999430, 4.015704910791001225 ) ) ;
#1819=CARTESIAN_POINT ( 'NONE',  ( 4.267029504470329471, 13.41085527056981697, 5.337432762833688393 ) ) ;
#1820=B_SPLINE_CURVE_WITH_KNOTS ( 'NONE', 3,
 ( #17083, #9466, #481, #5593, #11408, #12975, #18669, #13095, #245, #9581, #366, #21081, #21451, #22886, #727, #4372, #11763, #21330, #17828, #23251, #15862, #4866, #13808, #6550, #6665, #15499, #10188, #19393, #8372, #17454, #4493, #13686, #4745, #12254, #15617, #6183, #23006, #13934, #10069, #12130, #1222, #19518 ),
 .UNSPECIFIED., .F., .F.,
 ( 4, 2, 1, 2, 2, 2, 1, 2, 2, 2, 2, 2, 2, 2, 2, 1, 2, 2, 2, 1, 2, 2, 4 ),
 ( 0.000000000000000000, 0.06250000000000002776, 0.09375000000000012490, 0.1093750000000000555, 0.1249999999999999722, 0.1874999999999998890, 0.2187499999999998335, 0.2343749999999998057, 0.2499999999999997502, 0.3124999999999997224, 0.3749999999999997780, 0.4999999999999996669, 0.5624999999999997780, 0.6249999999999998890, 0.6875000000000001110, 0.7187500000000004441, 0.7343750000000007772, 0.7500000000000011102, 0.8125000000000013323, 0.8437500000000013323, 0.8593750000000013323, 0.8750000000000014433, 1.000000000000000000 ),
 .UNSPECIFIED. ) ;
#1823=CARTESIAN_POINT ( 'NONE',  ( 11.77425158531000093, -9.807789133420998340, 1.022826625653000088 ) ) ;
#1826=DIRECTION ( 'NONE',  ( -1.000000000000000000, 0.000000000000000000, 0.000000000000000000 ) ) ;
#1827=DIRECTION ( 'NONE',  ( 1.000000000000000000, 0.000000000000000000, 0.000000000000000000 ) ) ;
#1830=CARTESIAN_POINT ( 'NONE',  ( -10.24525051287397304, 15.78812810035701908, -1.147541437844174839 ) ) ;
#1831=AXIS2_PLACEMENT_3D ( 'NONE', #4906, #22804, #2722 ) ;
#1833=CARTESIAN_POINT ( 'NONE',  ( 14.42230551843989339, -1.412630712418221357, -10.22074767084959213 ) ) ;
#1834=CARTESIAN_POINT ( 'NONE',  ( -18.02909587121333956, 4.600144771116639220, -7.981067224362968560 ) ) ;
#1835=CARTESIAN_POINT ( 'NONE',  ( 24.72504754407999883, -9.523234606517998913, 5.134017250187000059 ) ) ;
#1837=CARTESIAN_POINT ( 'NONE',  ( 14.10065998436765611, 4.544368654919230366, 7.805219334371307660 ) ) ;
#1841=EDGE_CURVE ( 'NONE', #10857, #7090, #3, .T. ) ;
#1842=VERTEX_POINT ( 'NONE', #12240 ) ;
#1843=CARTESIAN_POINT ( 'NONE',  ( 24.49999999999998934, -10.18003712748733314, 1.238246424670434775 ) ) ;
#1846=CARTESIAN_POINT ( 'NONE',  ( -15.80528743917331269, 7.258566966576419865, -5.578074939302383406 ) ) ;
#1848=PLANE ( 'NONE',  #18900 ) ;
#1849=CARTESIAN_POINT ( 'NONE',  ( 18.95627483587000128, 0.6520233587864000535, 11.11807124853999973 ) ) ;
#1853=CARTESIAN_POINT ( 'NONE',  ( -11.22545756585000021, -11.56411535172999905, 9.345002482406000510 ) ) ;
#1856=EDGE_CURVE ( 'NONE', #13583, #3987, #13535, .T. ) ;
#1857=VERTEX_POINT ( 'NONE', #18175 ) ;
#1858=ADVANCED_FACE ( 'NONE', ( #3734 ), #3279, .T. ) ;
#1859=DIRECTION ( 'NONE',  ( -1.000000000000000000, 0.000000000000000000, 0.000000000000000000 ) ) ;
#1860=CARTESIAN_POINT ( 'NONE',  ( 19.97025975534796771, 8.314106973087666219, -6.433823374046138355 ) ) ;
#1862=CARTESIAN_POINT ( 'NONE',  ( 15.98099710151175756, -8.853047632443667325, -5.378228472014759731 ) ) ;
#1863=CIRCLE ( 'NONE', #19664, 4.750000000000000000 ) ;
#1864=CARTESIAN_POINT ( 'NONE',  ( -19.64339236541000133, -7.798846739588999100, 6.943248922331999751 ) ) ;
#1866=B_SPLINE_CURVE_WITH_KNOTS ( 'NONE', 3,
 ( #19014, #11761, #6419, #17200, #13805, #20718, #6052, #13441, #21202, #18776, #16964, #20844 ),
 .UNSPECIFIED., .F., .F.,
 ( 4, 1, 1, 1, 1, 2, 2, 4 ),
 ( 0.000000000000000000, 0.2500000000000006106, 0.3750000000000012768, 0.4375000000000013323, 0.4687500000000012768, 0.4843750000000014433, 0.5000000000000016653, 1.000000000000000000 ),
 .UNSPECIFIED. ) ;
#1867=CARTESIAN_POINT ( 'NONE',  ( -15.35172225070999907, -1.839441420978000119, 9.553397381538999866 ) ) ;
#1873=EDGE_CURVE ( 'NONE', #629, #3985, #10896, .T. ) ;
#1874=CARTESIAN_POINT ( 'NONE',  ( 19.70340807481104406, -6.760929761475917843, -8.039421042557430397 ) ) ;
#1878=CARTESIAN_POINT ( 'NONE',  ( -6.370760730814999384, 15.09911243606998177, 3.226444468181998815 ) ) ;
#1880=CARTESIAN_POINT ( 'NONE',  ( 4.833494560126003314, 12.42175294347999071, 0.1521608003744000515 ) ) ;
#1881=CARTESIAN_POINT ( 'NONE',  ( 12.81825125731000092, -4.388733341911000174, 7.983506680731000671 ) ) ;
#1882=ORIENTED_EDGE ( 'NONE', *, *, #15760, .T. ) ;
#1885=FACE_OUTER_BOUND ( 'NONE', #18910, .T. ) ;
#1886=VECTOR ( 'NONE', #18982, 1000.000000000000000 ) ;
#1887=ORIENTED_EDGE ( 'NONE', *, *, #2096, .F. ) ;
#1888=CARTESIAN_POINT ( 'NONE',  ( 22.32487270046334160, -9.003629214848199780, -2.419527782799394178 ) ) ;
#1891=CARTESIAN_POINT ( 'NONE',  ( 11.99999999999999822, -1.778133311928435933, -9.288411946047254730 ) ) ;
#1892=CARTESIAN_POINT ( 'NONE',  ( 11.59051697471232600, -8.994977951464667498, -9.420063436902960774 ) ) ;
#1894=CARTESIAN_POINT ( 'NONE',  ( -24.39605500772391622, 1.877234304591530289, -10.43857512010684196 ) ) ;
#1897=CARTESIAN_POINT ( 'NONE',  ( -6.382298667867003950, 15.08199981258001010, 3.360745759041997793 ) ) ;
#1899=ORIENTED_EDGE ( 'NONE', *, *, #13827, .F. ) ;
#1901=CARTESIAN_POINT ( 'NONE',  ( 14.68234440374828331, -4.311926369740707976, 8.013692814287820099 ) ) ;
#1902=AXIS2_PLACEMENT_3D ( 'NONE', #23294, #14101, #21495 ) ;
#1903=CARTESIAN_POINT ( 'NONE',  ( -21.17980191599842854, -9.824981607888839008, 3.766868870501678401 ) ) ;
#1906=CARTESIAN_POINT ( 'NONE',  ( 3.689409531404894249, 12.05188896767502627, 3.123460345082171408 ) ) ;
#1908=CARTESIAN_POINT ( 'NONE',  ( -1.842032823788972928, 11.62708128007210817, -4.451304217208804204 ) ) ;
#1909=CARTESIAN_POINT ( 'NONE',  ( 24.31126325372243357, 8.589904588849305966, -4.641259051888694920 ) ) ;
#1912=VERTEX_POINT ( 'NONE', #18048 ) ;
#1913=CARTESIAN_POINT ( 'NONE',  ( -23.76320766698999876, 13.93375672974000068, 0.0006662677302622000038 ) ) ;
#1914=CARTESIAN_POINT ( 'NONE',  ( 13.96800158531000058, -3.572926710108999870, -9.509691282521000488 ) ) ;
#1915=CARTESIAN_POINT ( 'NONE',  ( 18.28194284694450644, 6.412433293717898941, -8.218262321110563207 ) ) ;
#1916=AXIS2_PLACEMENT_3D ( 'NONE', #16614, #22, #8137 ) ;
#1919=CARTESIAN_POINT ( 'NONE',  ( 19.11921080085999947, -6.083244085703999993, 8.615239357168999135 ) ) ;
#1920=CARTESIAN_POINT ( 'NONE',  ( -24.50000000000000000, -1.873582633960999999, -10.39897383761999983 ) ) ;
#1921=AXIS2_PLACEMENT_3D ( 'NONE', #17760, #13992, #14359 ) ;
#1922=ORIENTED_EDGE ( 'NONE', *, *, #11094, .F. ) ;
#1924=CARTESIAN_POINT ( 'NONE',  ( 22.34344591821000137, 10.66184160259999913, -1.641226805065000072 ) ) ;
#1927=CARTESIAN_POINT ( 'NONE',  ( 24.50000000000000000, -5.768522138344023276, 8.866799569317205254 ) ) ;
#1928=CARTESIAN_POINT ( 'NONE',  ( 6.124999911758999716, 14.37502625872000195, -0.0001546258496581000123 ) ) ;
#1929=CARTESIAN_POINT ( 'NONE',  ( -3.235268519333999393, 11.88803707044000824, 3.615098393403000099 ) ) ;
#1933=VERTEX_POINT ( 'NONE', #9308 ) ;
#1936=CARTESIAN_POINT ( 'NONE',  ( 5.081323529022999885, 13.95840221409999771, 4.282381695897004015 ) ) ;
#1937=CARTESIAN_POINT ( 'NONE',  ( 16.42937270046333254, -2.379927906264107662, 8.856276743063176582 ) ) ;
#1940=CARTESIAN_POINT ( 'NONE',  ( 14.84550158531000008, 4.534570621724000716, 9.116298118718001220 ) ) ;
#1941=B_SPLINE_CURVE_WITH_KNOTS ( 'NONE', 3,
 ( #9921, #21061, #13916, #4971, #4725, #11991, #19117, #4474, #11863, #6531, #21312, #12113, #19499, #2908, #10290, #1078, #23232, #6645, #4847, #21906, #14284, #12707, #8957, #9184, #3510, #23951, #19857, #21791, #14743, #19745, #16325, #9066, #6891, #5438, #16081, #14399, #16209, #16561, #12588, #8844, #7358, #21679, #5206, #18170, #19975, #7122, #14512, #7237, #16437, #10655, #11000, #12471, #14628, #10891, #3272, #1676, #22136, #18277, #3394, #5091, #22025, #3155, #12819, #20212, #3617, #8717, #1448, #17923, #12356, #10538, #23606, #18385, #7011, #23828, #10778, #23716, #1328, #1573, #1796, #23480, #5317, #18043, #20099, #19320, #86, #6228, #6350, #14855, #3853, #7470, #17501, #18624, #20894, #22932, #894, #17252, #11246, #13733, #529, #5660, #8177, #21130, #776, #20441, #15300, #15545, #8297, #15426, #11119, #4300, #18505, #1915, #3730, #4541, #8053, #22812, #16678, #9304, #19188, #11934, #2031, #9421, #16791, #2729, #10111, #15661, #5547, #7933, #22691, #22243, #12925, #651, #9989, #6101, #13494, #20322, #11690, #13045, #19064, #2478, #9867, #13610, #21008, #4420, #11811, #2597, #17377, #3341, #17625, #5155, #12536, #18110, #14103, #4672, #19923, #23548, #12298, #1517, #19686, #6710, #8658, #1019, #23417, #3102, #10718, #14227, #8907, #6598, #8548, #23051, #6473, #10487, #19808, #8421, #16146, #2851, #1154, #2970, #13857, #23297, #19566, #12056, #15789, #15905, #4910, #21498, #17873, #1272, #17990, #3223, #21374, #21741, #23181, #1392, #21623, #13982, #12424, #21261, #5042, #16022, #4790, #19442, #10232, #8784, #6959, #14350, #12175, #10360, #17749, #6835, #10605, #5382, #11193, #10951, #12993, #14694, #20275, #5266, #22086, #5730, #13117, #12652, #3679, #9251, #12770, #23779, #14460, #1628, #21968, #7186, #7303, #9018, #3458, #14920, #16387, #20515, #3920, #21855, #11070, #11312, #1746, #18576, #20394, #18453, #16628, #10843, #7076, #5495, #16508, #20040, #12875, #1862, #18227, #9133, #14575, #20160, #3567, #18337, #23896, #38, #7420, #14803, #18688, #148, #9364, #2094, #16273, #22198, #5611, #1981, #23665, #3799, #16738, #7540, #22314, #17344, #13706, #16861, #19158, #11783, #748, #7787, #2568, #20982, #19287, #2448, #8152, #505, #9959, #16989, #21099, #13586, #4034, #20624, #15274, #263, #22438, #13465, #9841, #5958, #390, #17222, #15517, #18802, #15157, #11428, #4513, #22552, #7905, #22905, #11904, #20868, #13343, #6321, #4150, #9602, #9484, #4392, #4278, #621, #6074, #7668, #15042, #19038, #5848, #22665, #13231, #2211, #20742, #11546, #11666, #8023, #18926, #2335, #22785, #9724, #15395, #6201, #17106, #21347, #12148, #15993, #6569, #19781, #17721, #1118, #1363, #6442, #23148, #23268, #8393, #23025, #3191, #4641, #10573, #17846, #12508, #17472, #21596, #8520, #15634, #8630, #10204, #1239, #8270, #5125, #23386, #13953, #10457, #14074, #2701, #19658, #17959, #15878, #12397, #17597, #14327, #6805, #21228, #13830, #6682, #12029, #21469, #3072, #4762, #991, #866, #19410, #15758, #19536, #4882, #2824, #2942, #8752, #10331, #23519, #6930, #12271, #14199, #21715, #5011, #16118, #10085, #7273, #20247, #16475, #10815, #16363, #12964, #1951, #14891, #22171, #1607, #5351, #7049, #16709, #14665, #9, #18206, #12740, #22282, #10925, #11039, #8992, #14546, #20134, #10690, #1486, #22060, #3769, #5469, #21941, #121, #14432, #9337, #7508, #5697, #18312, #8880, #19893, #20360, #3309, #18080, #14775, #1713, #16250, #21827, #3653, #23866, #23643, #18422, #5240, #3431, #3542, #12625, #20010, #12851, #16598, #23752, #11157, #7156, #1833, #9103, #9219, #7392, #5582, #18543, #22408, #15123, #18892, #20709, #7871, #15239, #7990, #9806, #11397, #11750, #13199, #15362, #11636, #4001, #16829, #7636, #4358, #16955, #20953, #17312, #20482, #22753, #6172, #19122, #9455, #2177, #18658, #2064, #4118, #233, #15010, #11281, #13555, #22632, #17189, #18767, #22518, #15487, #11516, #5817, #2535, #2303, #9689, #9570, #2415, #355, #9927, #17070, #468, #714, #20592, #7755, #6043, #5927, #13432, #13311, #8123, #22873, #20833 ),
 .UNSPECIFIED., .F., .F.,
 ( 4, 2, 2, 2, 1, 1, 2, 2, 1, 1, 2, 2, 2, 1, 2, 2, 1, 2, 2, 2, 2, 2, 1, 1, 1, 1, 1, 2, 2, 2, 2, 2, 1, 1, 2, 2, 1, 1, 2, 2, 2, 2, 2, 2, 1, 1, 2, 2, 1, 2, 2, 2, 2, 1, 1, 2, 2, 2, 2, 2, 2, 2, 1, 1, 1, 2, 2, 2, 2, 2, 2, 2, 2, 1, 2, 2, 1, 1, 2, 2, 2, 2, 1, 1, 1, 1, 1, 1, 1, 1, 2, 2, 2, 2, 2, 2, 2, 2, 2, 2, 2, 2, 2, 2, 2, 2, 2, 2, 2, 2, 2, 2, 2, 2, 2, 1, 1, 1, 1, 1, 1, 2, 2, 2, 2, 1, 1, 1, 1, 1, 2, 2, 2, 2, 2, 1, 1, 1, 1, 1, 2, 2, 2, 2, 2, 1, 1, 1, 1, 2, 2, 2, 2, 1, 1, 1, 2, 2, 2, 2, 2, 1, 2, 2, 2, 2, 1, 1, 2, 2, 2, 2, 2, 2, 2, 1, 1, 1, 1, 1, 2, 2, 2, 2, 2, 1, 1, 1, 2, 2, 2, 2, 1, 1, 1, 1, 1, 2, 2, 2, 2, 2, 2, 2, 2, 2, 1, 1, 1, 1, 1, 2, 2, 2, 2, 2, 1, 1, 1, 1, 1, 2, 2, 2, 2, 2, 1, 1, 1, 2, 2, 2, 2, 1, 1, 1, 1, 1, 1, 2, 2, 2, 2, 2, 1, 1, 1, 1, 1, 2, 2, 2, 2, 2, 1, 1, 2, 2, 1, 1, 2, 2, 2, 2, 2, 2, 2, 2, 2, 2, 1, 1, 1, 1, 1, 2, 2, 2, 2, 2, 2, 1, 2, 2, 1, 1, 1, 2, 2, 2, 2, 2, 2, 2, 1, 1, 1, 1, 2, 2, 2, 2, 2, 2, 2, 2, 2, 2, 2, 1, 1, 1, 1, 2, 2, 2, 2, 2, 2, 2, 2, 4 ),
 ( 0.000000000000000000, 0.007812499999996756067, 0.01562499999999351213, 0.01953124999999188843, 0.02050781249999149639, 0.02075195312499140618, 0.02081298828124138883, 0.02087402343749137149, 0.02099609374999134720, 0.02148437499999125699, 0.02343749999999087535, 0.03124999999998935574, 0.03906249999998783612, 0.04101562499998746142, 0.04150390624998735734, 0.04174804687498730876, 0.04199218749998725325, 0.04296874999998700345, 0.04687499999998599731, 0.05468749999998395034, 0.05859374999998293726, 0.06054687499998243072, 0.06152343749998217398, 0.06201171874998204214, 0.06225585937498197969, 0.06237792968748194500, 0.06243896484373193806, 0.06246948242185692418, 0.06249999999998190336, 0.07031249999997722655, 0.07812499999997254974, 0.08203124999997023215, 0.08300781249996963540, 0.08325195312496949662, 0.08331298828121945499, 0.08337402343746941336, 0.08349609374996934397, 0.08398437499996899702, 0.08593749999996766475, 0.09374999999996232181, 0.09570312499996098954, 0.09765624999995964339, 0.1015624999999569789, 0.1054687499999543143, 0.1064453124999536482, 0.1069335937499533151, 0.1070556640624532319, 0.1071777343749531486, 0.1074218749999530514, 0.1093749999999521771, 0.1132812499999504147, 0.1171874999999486522, 0.1181640624999482220, 0.1186523437499479999, 0.1188964843749478889, 0.1190185546874478195, 0.1191406249999477501, 0.1210937499999469313, 0.1249999999999452799, 0.1289062499999436562, 0.1308593749999428235, 0.1309814453124427958, 0.1311035156249427402, 0.1313476562499426015, 0.1318359374999423239, 0.1328124999999417688, 0.1406249999999372169, 0.1484374999999326650, 0.1562499999999281408, 0.1640624999999235889, 0.1718749999999190370, 0.1757812499999167610, 0.1777343749999156231, 0.1782226562499153455, 0.1784667968749151790, 0.1785888671874150957, 0.1787109374999150124, 0.1796874999999144296, 0.1874999999999097111, 0.2031249999999002742, 0.2187499999998908651, 0.2343749999998814282, 0.2421874999998767097, 0.2460937499998743505, 0.2480468749998731848, 0.2490234374998726019, 0.2495117187498722966, 0.2497558593748721578, 0.2498779296873720746, 0.2499389648436220468, 0.2499694824217470190, 0.2499999999998720190, 0.2578124999998676059, 0.2656249999998631095, 0.2734374999998586686, 0.2812499999998541722, 0.2890624999998497313, 0.2968749999998452349, 0.3046874999998407940, 0.3124999999998363531, 0.3203124999998318567, 0.3281249999998274158, 0.3437499999998185340, 0.3515624999998140376, 0.3593749999998096523, 0.3749999999998007705, 0.3906249999997918887, 0.4062499999997830069, 0.4218749999997741251, 0.4374999999997652989, 0.4531249999997564171, 0.4687499999997475353, 0.4843749999997386535, 0.4921874999997341571, 0.4960937499997319367, 0.4980468749997308819, 0.4990234374997302713, 0.4995117187497300493, 0.4997558593747298827, 0.4998779296872298272, 0.4999389648434798272, 0.4999694824216048827, 0.4999999999997299382, 0.5078124999997339906, 0.5117187499997359890, 0.5136718749997369882, 0.5146484374997374323, 0.5151367187497376543, 0.5153808593747377653, 0.5155029296872378763, 0.5155639648434878763, 0.5156249999997378763, 0.5234374999997412070, 0.5273437499997429834, 0.5292968749997437605, 0.5302734374997442046, 0.5307617187497444267, 0.5310058593747445377, 0.5311279296872446487, 0.5311889648434945377, 0.5312194824216195377, 0.5312499999997445377, 0.5390624999997504219, 0.5429687499997533084, 0.5449218749997548628, 0.5458984374997555289, 0.5463867187497559730, 0.5466308593747561950, 0.5467529296872561950, 0.5468139648435063060, 0.5468749999997564171, 0.5507812499997595257, 0.5527343749997611910, 0.5537109374997619682, 0.5541992187497623013, 0.5544433593747625233, 0.5545654296872626343, 0.5546874999997626343, 0.5585937499997662981, 0.5605468749997680744, 0.5615234374997689626, 0.5620117187497694067, 0.5622558593747696287, 0.5624999999997698508, 0.5664062499997735145, 0.5683593749997752909, 0.5693359374997762901, 0.5698242187497767341, 0.5700683593747769562, 0.5703124999997771782, 0.5742187499997807310, 0.5781249999997843947, 0.5859374999997915001, 0.5898437499997950528, 0.5917968749997968292, 0.5927734374997977174, 0.5932617187497981615, 0.5935058593747983835, 0.5936279296872984945, 0.5936889648435486055, 0.5937194824216734945, 0.5937499999997984945, 0.6015624999998055999, 0.6054687499998091527, 0.6074218749998108180, 0.6083984374998118172, 0.6088867187498122613, 0.6091308593748124833, 0.6092529296873124833, 0.6093749999998125944, 0.6171874999998200328, 0.6210937499998236966, 0.6230468749998255840, 0.6240234374998264721, 0.6245117187498269162, 0.6247558593748271383, 0.6248779296873273603, 0.6249389648435774713, 0.6249999999998274713, 0.6406249999998402389, 0.6562499999998530065, 0.6640624999998593347, 0.6718749999998657740, 0.6796874999998722133, 0.6835937499998753220, 0.6855468749998769873, 0.6865234374998777644, 0.6870117187498782085, 0.6872558593748784306, 0.6873779296873784306, 0.6874389648436285416, 0.6874694824217535416, 0.6874999999998785416, 0.6953124999998835376, 0.6992187499998859801, 0.7011718749998873124, 0.7021484374998878675, 0.7026367187498882005, 0.7028808593748883116, 0.7030029296873884226, 0.7030639648436385336, 0.7030944824217634226, 0.7031249999998884226, 0.7109374999998898659, 0.7148437499998905320, 0.7167968749998908651, 0.7177734374998910871, 0.7182617187498911981, 0.7185058593748911981, 0.7186279296873911981, 0.7187499999998913092, 0.7265624999998921973, 0.7304687499998925304, 0.7324218749998927525, 0.7333984374998928635, 0.7338867187498928635, 0.7341308593748928635, 0.7342529296873929745, 0.7343139648436429745, 0.7343444824217679745, 0.7343749999998928635, 0.7421874999998934186, 0.7460937499998937517, 0.7480468749998938627, 0.7490234374998939737, 0.7495117187498939737, 0.7497558593748939737, 0.7498779296873939737, 0.7499389648436439737, 0.7499694824217689737, 0.7499999999998939737, 0.7578124999998957501, 0.7656249999998975264, 0.7695312499998984146, 0.7705078124998986366, 0.7707519531248986366, 0.7708129882811486366, 0.7708740234373986366, 0.7709960937498986366, 0.7714843749998987477, 0.7734374999998988587, 0.7812499999998996358, 0.7890624999999004130, 0.7910156249999006350, 0.7919921874999006350, 0.7929687499999006350, 0.7968749999999010791, 0.8046874999999016342, 0.8085937499999020783, 0.8105468749999023004, 0.8115234374999023004, 0.8120117187499023004, 0.8122558593749023004, 0.8123779296874023004, 0.8124389648436521894, 0.8124694824217771894, 0.8124999999999021894, 0.8203124999999076294, 0.8281249999999130695, 0.8320312499999157341, 0.8330078124999165112, 0.8332519531249166223, 0.8333129882811666223, 0.8333435058592916223, 0.8333740234374166223, 0.8334960937499167333, 0.8339843749999170663, 0.8359374999999186207, 0.8437499999999246159, 0.8515624999999307221, 0.8593749999999368283, 0.8671874999999429345, 0.8710937499999459321, 0.8730468749999474865, 0.8740234374999481526, 0.8745117187499484857, 0.8747558593749487077, 0.8748779296874488187, 0.8749389648436989297, 0.8749999999999489297, 0.8828124999999543698, 0.8906249999999598099, 0.8984374999999652500, 0.9062499999999706901, 0.9140624999999760192, 0.9218749999999814593, 0.9296874999999868994, 0.9335937499999895639, 0.9355468749999910072, 0.9365234374999916733, 0.9370117187499921174, 0.9372558593749922284, 0.9373779296874923395, 0.9374389648437423395, 0.9374999999999923395, 0.9531249999999942268, 0.9609374999999952260, 0.9687499999999962252, 0.9765624999999972244, 0.9843749999999981126, 0.9921874999999991118, 1.000000000000000000 ),
 .UNSPECIFIED. ) ;
#1942=VERTEX_POINT ( 'NONE', #1920 ) ;
#1943=CARTESIAN_POINT ( 'NONE',  ( -12.50789737913000010, 5.572872693153001045, -7.876595158781000805 ) ) ;
#1945=CARTESIAN_POINT ( 'NONE',  ( 0.000000000000000000, 17.00000000000000000, 0.000000000000000000 ) ) ;
#1948=EDGE_CURVE ( 'NONE', #16694, #16650, #11470, .T. ) ;
#1949=CARTESIAN_POINT ( 'NONE',  ( -6.250000000000000000, 16.31160201366999729, -1.000000000001000089 ) ) ;
#1951=CARTESIAN_POINT ( 'NONE',  ( 14.77879143498036285, 9.187885709464108430, -4.717911039109739413 ) ) ;
#1952=CARTESIAN_POINT ( 'NONE',  ( -18.44480420454666714, -7.312553030913967689, -5.619880916868769560 ) ) ;
#1953=CARTESIAN_POINT ( 'NONE',  ( 23.31785416133999789, -6.911498531077999274, -8.917763646754000462 ) ) ;
#1955=CARTESIAN_POINT ( 'NONE',  ( 13.69882080557875881, 8.479719668256132437, -3.078924866922988279 ) ) ;
#1956=CARTESIAN_POINT ( 'NONE',  ( -4.810356821045001396, 12.64187851441000454, -0.3304506023919999147 ) ) ;
#1958=CARTESIAN_POINT ( 'NONE',  ( 22.26465740196000098, 7.788096699281999769, 8.394476371801001591 ) ) ;
#1964=CARTESIAN_POINT ( 'NONE',  ( -16.48553743917331360, -9.094333095012673951, -1.190572366013357586 ) ) ;
#1965=CARTESIAN_POINT ( 'NONE',  ( 24.18393254356834277, 8.381833107684220963, 10.48223919692640393 ) ) ;
#1966=CARTESIAN_POINT ( 'NONE',  ( 22.17370603379667671, -8.999753784811684199, 2.418746970030813959 ) ) ;
#1967=CARTESIAN_POINT ( 'NONE',  ( 15.52770777679999981, -6.525431417549000024, 8.909778109634999055 ) ) ;
#1969=FACE_OUTER_BOUND ( 'NONE', #5237, .T. ) ;
#1973=CARTESIAN_POINT ( 'NONE',  ( -10.81079363876999899, 4.622502607133999852, -14.49941598755999905 ) ) ;
#1975=CARTESIAN_POINT ( 'NONE',  ( -14.49454820080683781, -11.34301321103862215, -5.353338751774003867 ) ) ;
#1976=ORIENTED_EDGE ( 'NONE', *, *, #7285, .F. ) ;
#1978=DIRECTION ( 'NONE',  ( 0.000000000000000000, 0.000000000000000000, -1.000000000000000000 ) ) ;
#1979=CARTESIAN_POINT ( 'NONE',  ( 19.38196803061413576, -9.569877228560322635, -4.561946182171338293 ) ) ;
#1980=CARTESIAN_POINT ( 'NONE',  ( 24.38510397947347386, 9.380175294669545139, -8.753059805729597187 ) ) ;
#1981=CARTESIAN_POINT ( 'NONE',  ( 15.92416512556680352, -9.758728831869941445, -3.476723394276768797 ) ) ;
#1982=CARTESIAN_POINT ( 'NONE',  ( -19.46272905036999745, -11.08280635929999924, 1.130260105365999967 ) ) ;
#1984=CARTESIAN_POINT ( 'NONE',  ( -16.65202050098999820, 5.360250747359000201, -9.417511137717001546 ) ) ;
#1985=EDGE_CURVE ( 'NONE', #16663, #13308, #14974, .T. ) ;
#1987=ORIENTED_EDGE ( 'NONE', *, *, #12666, .T. ) ;
#1989=CARTESIAN_POINT ( 'NONE',  ( 20.69647650300873210, 4.117193616373135967, 9.695396857088221410 ) ) ;
#1990=CARTESIAN_POINT ( 'NONE',  ( -18.22510727069612102, 4.477738147576441285, 9.453292167412891800 ) ) ;
#1991=VERTEX_POINT ( 'NONE', #22724 ) ;
#1993=CARTESIAN_POINT ( 'NONE',  ( 12.50897733419000168, 7.466846271614999253, 11.77833069256000087 ) ) ;
#1994=CARTESIAN_POINT ( 'NONE',  ( -5.310415759193001684, 14.71388207620999466, 3.630273082683998176 ) ) ;
#1996=DIRECTION ( 'NONE',  ( -1.000000000000000000, 0.000000000000000000, 0.000000000000000000 ) ) ;
#1997=CARTESIAN_POINT ( 'NONE',  ( 17.67093892131000032, 6.655236401869999874, -7.121176743063999837 ) ) ;
#2001=CARTESIAN_POINT ( 'NONE',  ( -14.39391695409897665, 4.126581034334551035, -12.49998949086425526 ) ) ;
#2005=CARTESIAN_POINT ( 'NONE',  ( 22.62720603379666073, -2.421793114379757750, -9.011088590333773851 ) ) ;
#2006=CARTESIAN_POINT ( 'NONE',  ( -4.736789979881001145, 12.61336825782000481, -0.1514565667017998829 ) ) ;
#2007=CARTESIAN_POINT ( 'NONE',  ( -21.65474665972999802, -2.779264633183000210, -9.192073190559000295 ) ) ;
#2008=DIRECTION ( 'NONE',  ( 0.000000000000000000, 1.000000000000000000, 0.000000000000000000 ) ) ;
#2010=CARTESIAN_POINT ( 'NONE',  ( -20.61299152281980085, 6.891406388424135443, -7.933605387358306338 ) ) ;
#2013=CARTESIAN_POINT ( 'NONE',  ( -6.002899204263999700, 16.48938829593000222, 1.302400215941999617 ) ) ;
#2015=ORIENTED_EDGE ( 'NONE', *, *, #17636, .T. ) ;
#2016=CARTESIAN_POINT ( 'NONE',  ( 23.26647781200000153, 8.343268572584999987, 5.276840896087999333 ) ) ;
#2017=CARTESIAN_POINT ( 'NONE',  ( 4.950289441944255131, 13.61399942321605927, -4.797373584915786360 ) ) ;
#2018=CARTESIAN_POINT ( 'NONE',  ( -23.48257016776725337, 4.959647080842567668, 9.349265232667463010 ) ) ;
#2021=AXIS2_PLACEMENT_3D ( 'NONE', #8540, #21962, #19802 ) ;
#2022=DIRECTION ( 'NONE',  ( 0.000000000000000000, -1.000000000000000000, 0.000000000000000000 ) ) ;
#2024=CARTESIAN_POINT ( 'NONE',  ( -3.348221499849736826, 11.95344782507623194, -3.481183559751760637 ) ) ;
#2025=DIRECTION ( 'NONE',  ( 0.000000000000000000, 0.9512662730843030046, -0.3083706822840010520 ) ) ;
#2029=CARTESIAN_POINT ( 'NONE',  ( 24.00034722001000276, -6.716786536054000223, 12.21137788280000080 ) ) ;
#2030=CARTESIAN_POINT ( 'NONE',  ( 17.14893908531000122, -9.665900270332999256, 3.387665420544000217 ) ) ;
#2031=CARTESIAN_POINT ( 'NONE',  ( 18.07779827556542074, -0.4281578631263728285, -10.40548960717138272 ) ) ;
#2032=CARTESIAN_POINT ( 'NONE',  ( -24.47970833437514315, 1.023963593981846776, 12.49997010189808044 ) ) ;
#2034=CARTESIAN_POINT ( 'NONE',  ( 13.63483580085999947, -5.096719188837999681, 10.08552589914000031 ) ) ;
#2036=AXIS2_PLACEMENT_3D ( 'NONE', #3244, #1859, #13886 ) ;
#2037=VERTEX_POINT ( 'NONE', #203 ) ;
#2039=CARTESIAN_POINT ( 'NONE',  ( 20.57295489666000066, 10.73902819488999860, -0.02183603347782999901 ) ) ;
#2040=CARTESIAN_POINT ( 'NONE',  ( -24.12340887139987089, 7.182491261854132780, 6.898148839887506156 ) ) ;
#2041=EDGE_LOOP ( 'NONE', ( #19969, #19071, #19671, #2961 ) ) ;
#2042=CARTESIAN_POINT ( 'NONE',  ( 12.26599830533000102, 1.737683063983999965, -9.170090943151999241 ) ) ;
#2043=LINE ( 'NONE', #3742, #15291 ) ;
#2044=CARTESIAN_POINT ( 'NONE',  ( -4.821039626244001397, 12.41688405863999378, 0.4163202411090001220 ) ) ;
#2046=CARTESIAN_POINT ( 'NONE',  ( -23.14617958678999798, -2.878374533911999933, 10.75773347001999802 ) ) ;
#2049=ORIENTED_EDGE ( 'NONE', *, *, #9059, .F. ) ;
#2053=CARTESIAN_POINT ( 'NONE',  ( 0.000000000000000000, -1.100000000000000089, 0.000000000000000000 ) ) ;
#2055=DIRECTION ( 'NONE',  ( -1.000000000000000000, 0.000000000000000000, 0.000000000000000000 ) ) ;
#2056=CARTESIAN_POINT ( 'NONE',  ( 11.00000000000000000, 0.000000000000000000, 0.000000000000000000 ) ) ;
#2057=CARTESIAN_POINT ( 'NONE',  ( 15.63975174930999934, -10.61757272617999881, 1.417689269007999853 ) ) ;
#2058=CARTESIAN_POINT ( 'NONE',  ( -18.64256589945999920, -8.356153348075000764, -6.118136038720999537 ) ) ;
#2060=CARTESIAN_POINT ( 'NONE',  ( -14.48091997122308783, 1.686280348617847258, 12.50000494027669262 ) ) ;
#2061=ORIENTED_EDGE ( 'NONE', *, *, #22831, .F. ) ;
#2062=CARTESIAN_POINT ( 'NONE',  ( -21.87664474417000093, 9.621532986476999838, 5.823833470188000128 ) ) ;
#2064=CARTESIAN_POINT ( 'NONE',  ( 13.91722143161700487, -9.787662134382348000, 3.259115714080555559 ) ) ;
#2065=LINE ( 'NONE', #14776, #23782 ) ;
#2066=CARTESIAN_POINT ( 'NONE',  ( 24.56575753602000134, -0.1539563260370000186, 11.31598377959000068 ) ) ;
#2067=EDGE_CURVE ( 'NONE', #22434, #744, #7596, .T. ) ;
#2069=CARTESIAN_POINT ( 'NONE',  ( 13.80188479459891404, 9.025291018604240989, 0.006585034666644948471 ) ) ;
#2070=CARTESIAN_POINT ( 'NONE',  ( 4.811303266717004590, 12.64225230711998549, 0.1541639457764001631 ) ) ;
#2073=CARTESIAN_POINT ( 'NONE',  ( 22.07140646839999931, 11.31094428649000072, 1.749821515072000011 ) ) ;
#2074=ORIENTED_EDGE ( 'NONE', *, *, #499, .T. ) ;
#2078=AXIS2_PLACEMENT_3D ( 'NONE', #8810, #19713, #14251 ) ;
#2081=CARTESIAN_POINT ( 'NONE',  ( 18.05402034664000155, -0.4689034603063000350, -11.10308750183000015 ) ) ;
#2086=CARTESIAN_POINT ( 'NONE',  ( -12.53440221169000068, 2.913425087080000253, -14.82027568206000012 ) ) ;
#2092=CARTESIAN_POINT ( 'NONE',  ( 20.58645603379664379, -8.038508279625668607, -4.632961155938045472 ) ) ;
#2093=DIRECTION ( 'NONE',  ( 0.000000000000000000, 0.000000000000000000, 1.000000000000000000 ) ) ;
#2094=CARTESIAN_POINT ( 'NONE',  ( 15.93110892925370159, -9.670762698854872497, -3.710595638575625355 ) ) ;
#2095=CARTESIAN_POINT ( 'NONE',  ( -18.05146424826999763, 4.664330861219999846, 10.07481800594999832 ) ) ;
#2096=EDGE_CURVE ( 'NONE', #7720, #2709, #13864, .T. ) ;
#2098=AXIS2_PLACEMENT_3D ( 'NONE', #6220, #15061, #20760 ) ;
#2099=CARTESIAN_POINT ( 'NONE',  ( -14.57995894006000093, 5.497579849475999758, -8.642519878353001062 ) ) ;
#2103=CARTESIAN_POINT ( 'NONE',  ( 19.16431378521849993, -5.700780802628737653, 8.808059238752626641 ) ) ;
#2104=CIRCLE ( 'NONE', #6368, 10.59999999999999964 ) ;
#2105=CARTESIAN_POINT ( 'NONE',  ( -17.84889801066703541, -7.935400264423112304, 6.802475617916535988 ) ) ;
#2107=CARTESIAN_POINT ( 'NONE',  ( 24.36414987671881605, -3.145589772712558574, 12.49999999999999822 ) ) ;
#2110=CARTESIAN_POINT ( 'NONE',  ( 15.67012625730999886, 7.503068644359999873, -5.298384255253999697 ) ) ;
#2112=CARTESIAN_POINT ( 'NONE',  ( -5.047512558650118386, 15.90113563435273392, 3.469625691324551120 ) ) ;
#2113=ADVANCED_FACE ( 'NONE', ( #4452 ), #17013, .T. ) ;
#2114=DIRECTION ( 'NONE',  ( 0.000000000000000000, 1.000000000000000000, 0.000000000000000000 ) ) ;
#2116=CARTESIAN_POINT ( 'NONE',  ( -22.97657263213626067, 8.792444840933823613, -3.354899762457558499 ) ) ;
#2117=CARTESIAN_POINT ( 'NONE',  ( 0.7954828832003001393, 11.65690288844000122, 4.699030088164001917 ) ) ;
#2120=CARTESIAN_POINT ( 'NONE',  ( 12.00000000000000000, -3.904004055809709328, -8.760530875779460658 ) ) ;
#2122=CARTESIAN_POINT ( 'NONE',  ( -14.38789256606429312, 8.761241120844390551, -9.824672794992732605 ) ) ;
#2125=CARTESIAN_POINT ( 'NONE',  ( 5.302306457911683424, 13.74700690846063722, -4.399542679587089111 ) ) ;
#2129=CARTESIAN_POINT ( 'NONE',  ( -17.92162077250666030, -1.195142481609338336, -9.131185823717723693 ) ) ;
#2130=CARTESIAN_POINT ( 'NONE',  ( 24.28529421024000001, -10.38286454550999949, -1.040937569600999923 ) ) ;
#2131=CARTESIAN_POINT ( 'NONE',  ( 13.65567517025193922, 0.7181510411685014805, -9.045400155240761464 ) ) ;
#2133=CARTESIAN_POINT ( 'NONE',  ( -23.91099216809519490, 9.753959700133281174, -4.141585236787074464 ) ) ;
#2137=VERTEX_POINT ( 'NONE', #10030 ) ;
#2138=CARTESIAN_POINT ( 'NONE',  ( -1.692126093021008471, 11.60421557973431383, -4.510750546857305920 ) ) ;
#2140=CARTESIAN_POINT ( 'NONE',  ( 24.24531177150999994, 0.000000000000000000, 0.000000000000000000 ) ) ;
#2141=EDGE_LOOP ( 'NONE', ( #9313, #22325, #20795, #1922, #9033, #14452, #2349 ) ) ;
#2142=DIRECTION ( 'NONE',  ( -0.9989428060277519839, 0.000000000000000000, 0.04597031961386779941 ) ) ;
#2143=CARTESIAN_POINT ( 'NONE',  ( 13.09050158531000108, 2.578416522421000057, 9.802228185182000786 ) ) ;
#2146=CARTESIAN_POINT ( 'NONE',  ( -18.40696791751999584, 10.89439442848000006, 3.426539622133999874 ) ) ;
#2147=FACE_OUTER_BOUND ( 'NONE', #21896, .T. ) ;
#2149=CARTESIAN_POINT ( 'NONE',  ( 14.44733580085999947, 1.586710932958000031, -11.21110614856999987 ) ) ;
#2153=CARTESIAN_POINT ( 'NONE',  ( 23.32294689903000062, -6.854607272587000644, 7.667868601460999578 ) ) ;
#2155=VERTEX_POINT ( 'NONE', #19475 ) ;
#2158=CARTESIAN_POINT ( 'NONE',  ( -4.779708402705001191, 12.47950863541999311, -0.05972554645062000400 ) ) ;
#2159=DIRECTION ( 'NONE',  ( -0.9996708941621511579, -0.02565352539213875543, 0.000000000000000000 ) ) ;
#2160=CARTESIAN_POINT ( 'NONE',  ( -20.95361754275000266, -9.668541804323000477, -5.404777570993999802 ) ) ;
#2161=ORIENTED_EDGE ( 'NONE', *, *, #5383, .T. ) ;
#2162=ADVANCED_FACE ( 'NONE', ( #12208, #17533, #19597 ), #685, .T. ) ;
#2163=EDGE_CURVE ( 'NONE', #19254, #13362, #7210, .T. ) ;
#2164=ORIENTED_EDGE ( 'NONE', *, *, #16063, .T. ) ;
#2165=CARTESIAN_POINT ( 'NONE',  ( 5.186887866327001717, 13.91948403396000344, 4.156460832888996926 ) ) ;
#2168=AXIS2_PLACEMENT_3D ( 'NONE', #21753, #12667, #21512 ) ;
#2169=CARTESIAN_POINT ( 'NONE',  ( 24.00034722001000276, -13.93375672974000068, 0.2887811717300000081 ) ) ;
#2170=CARTESIAN_POINT ( 'NONE',  ( -14.00000000000000000, 1.396097351027999937E-14, 0.000000000000000000 ) ) ;
#2171=( NAMED_UNIT ( * ) PLANE_ANGLE_UNIT ( ) SI_UNIT ( $, .RADIAN. ) );
#2172=CARTESIAN_POINT ( 'NONE',  ( -13.40193493347000064, -7.644751109369999575, -7.551345029496000727 ) ) ;
#2173=CARTESIAN_POINT ( 'NONE',  ( 8.124934037954998800, 0.000000000000000000, 0.000000000000000000 ) ) ;
#2174=CARTESIAN_POINT ( 'NONE',  ( -14.49454818139149559, 1.035381146816525266, 12.50000698751844297 ) ) ;
#2177=CARTESIAN_POINT ( 'NONE',  ( 13.95888961830255859, -10.15714629801752444, 1.812660213858063862 ) ) ;
#2178=CARTESIAN_POINT ( 'NONE',  ( -17.80234587121333689, 8.890592914788218337, -2.389150121181911501 ) ) ;
#2179=CARTESIAN_POINT ( 'NONE',  ( 23.68494808727000134, 6.489360873926000473, -9.241806053444001634 ) ) ;
#2181=CARTESIAN_POINT ( 'NONE',  ( 14.53764925629900873, -7.579119239074397107, 5.000770392501714845 ) ) ;
#2182=FACE_OUTER_BOUND ( 'NONE', #19800, .T. ) ;
#2183=AXIS2_PLACEMENT_3D ( 'NONE', #972, #17326, #730 ) ;
#2184=CARTESIAN_POINT ( 'NONE',  ( -6.809815940849730076, 15.32358591363257361, 1.841184338583090829 ) ) ;
#2187=CARTESIAN_POINT ( 'NONE',  ( -14.50561062189895267, 1.530330873916638801, -8.911763648040071928 ) ) ;
#2193=VECTOR ( 'NONE', #17019, 1000.000000000000000 ) ;
#2195=CARTESIAN_POINT ( 'NONE',  ( 19.07657543443000137, -3.766769386410000031, 9.975653420128997695 ) ) ;
#2198=PRODUCT_DEFINITION ( 'UNKNOWN', '', #1306, #11213 ) ;
#2200=ORIENTED_EDGE ( 'NONE', *, *, #9489, .F. ) ;
#2201=VERTEX_POINT ( 'NONE', #17784 ) ;
#2202=CIRCLE ( 'NONE', #20008, 12.89775331292476857 ) ;
#2203=CARTESIAN_POINT ( 'NONE',  ( -13.99999999999999467, 1.266994025276806379, -9.342908241774937395 ) ) ;
#2204=CARTESIAN_POINT ( 'NONE',  ( -12.33813113877000056, 2.847851204958999460, -14.48670849514999937 ) ) ;
#2206=DIRECTION ( 'NONE',  ( -0.000000000000000000, 0.5000000000000169864, 0.8660254037844288266 ) ) ;
#2208=CARTESIAN_POINT ( 'NONE',  ( -14.49454820080683426, 11.34301321103429494, 5.353338751784230354 ) ) ;
#2210=CARTESIAN_POINT ( 'NONE',  ( 6.146042104385863070, 14.15896049273807300, 0.1829400497938399317 ) ) ;
#2211=CARTESIAN_POINT ( 'NONE',  ( 15.47072016145524742, -3.491802273154016589, 9.789331991493677165 ) ) ;
#2212=CARTESIAN_POINT ( 'NONE',  ( -13.74958640564999968, -10.81015631786999975, 1.945342028014000135 ) ) ;
#2214=VECTOR ( 'NONE', #16785, 1000.000000000000000 ) ;
#2215=CARTESIAN_POINT ( 'NONE',  ( -18.11469101799999848, 6.086102628551000038, 9.654141096248000764 ) ) ;
#2217=EDGE_LOOP ( 'NONE', ( #14711, #832, #15805, #13513, #16578, #452, #4323, #22133, #17526, #4127 ) ) ;
#2220=CARTESIAN_POINT ( 'NONE',  ( 19.27780731986851137, -8.649574563187062637, 5.948916446097893385 ) ) ;
#2222=ORIENTED_EDGE ( 'NONE', *, *, #22126, .F. ) ;
#2223=CARTESIAN_POINT ( 'NONE',  ( 6.642147790651000250, 13.49920969778000135, 0.06640950685239001283 ) ) ;
#2224=CARTESIAN_POINT ( 'NONE',  ( -13.99999999999999645, -9.587150838885284188, 3.957974977218785551 ) ) ;
#2226=CARTESIAN_POINT ( 'NONE',  ( 17.89031392131000331, 9.735558222862998434, -0.5785200253907000212 ) ) ;
#2230=CARTESIAN_POINT ( 'NONE',  ( 24.36165043081783921, -12.41271798542465810, 3.500541789220333211 ) ) ;
#2232=CARTESIAN_POINT ( 'NONE',  ( -16.78197087121331421, -9.101940161118450945, -1.191568128638077928 ) ) ;
#2233=CARTESIAN_POINT ( 'NONE',  ( 21.70045833333333007, -5.671044614236272707, 7.379541929059594274 ) ) ;
#2234=CARTESIAN_POINT ( 'NONE',  ( -1.890114362710001217, 11.79193194378000342, 4.373319237984003571 ) ) ;
#2235=CARTESIAN_POINT ( 'NONE',  ( -23.10002682443999689, 8.026624707145000315, -5.342598563384999721 ) ) ;
#2236=EDGE_CURVE ( 'NONE', #379, #2137, #16244, .T. ) ;
#2238=CARTESIAN_POINT ( 'NONE',  ( -4.544324455327999779, 13.49053734526000170, 5.132126114358000812 ) ) ;
#2240=CARTESIAN_POINT ( 'NONE',  ( 4.903707650242860261, 14.76847038361531794, 3.672007579896967577 ) ) ;
#2244=CARTESIAN_POINT ( 'NONE',  ( -17.24137077250667005, 7.287857340677485141, 5.600902193946013519 ) ) ;
#2245=CARTESIAN_POINT ( 'NONE',  ( 22.93253767531999898, 1.313452474455999885, -10.31494984694000117 ) ) ;
#2246=CARTESIAN_POINT ( 'NONE',  ( 3.397923753680991421, 13.19211977465199581, -5.856784336400644442 ) ) ;
#2247=LINE ( 'NONE', #19201, #23507 ) ;
#2249=CARTESIAN_POINT ( 'NONE',  ( -21.55467116628538804, 1.019337657976560729, 10.62255827922021112 ) ) ;
#2251=LINE ( 'NONE', #16902, #21276 ) ;
#2252=VERTEX_POINT ( 'NONE', #22223 ) ;
#2253=AXIS2_PLACEMENT_3D ( 'NONE', #21946, #5588, #13090 ) ;
#2254=EDGE_CURVE ( 'NONE', #12473, #8479, #9295, .T. ) ;
#2256=CARTESIAN_POINT ( 'NONE',  ( 24.39431354042982747, 9.829649394705615606, 2.587219325858395311E-05 ) ) ;
#2258=CONICAL_SURFACE ( 'NONE', #11158, 9.136555860486998526, 0.02565634000431304615 ) ;
#2260=CARTESIAN_POINT ( 'NONE',  ( 6.243179582884000212, 13.63342035941999875, -1.952365010387999922 ) ) ;
#2261=CARTESIAN_POINT ( 'NONE',  ( 0.000000000000000000, 20.10000000000000142, 0.000000000000000000 ) ) ;
#2263=CARTESIAN_POINT ( 'NONE',  ( 17.28506424931000041, -8.106780832215999766, 7.067619055798999739 ) ) ;
#2265=CARTESIAN_POINT ( 'NONE',  ( -15.76627339390999971, -11.34295740443999989, -0.3014791613419999794 ) ) ;
#2267=CARTESIAN_POINT ( 'NONE',  ( 13.02546080085999947, 11.25441903210000127, -0.8115343024272000383 ) ) ;
#2269=CARTESIAN_POINT ( 'NONE',  ( -6.042815635770000249, 16.39253429789999927, 0.9999999720525000191 ) ) ;
#2270=CARTESIAN_POINT ( 'NONE',  ( 19.33361118158000025, -4.341085640097999132, 9.785006935544998896 ) ) ;
#2272=CARTESIAN_POINT ( 'NONE',  ( 24.50000000000000711, -10.56912816078165562, 6.693733033818888956 ) ) ;
#2274=CARTESIAN_POINT ( 'NONE',  ( 12.12827354077999864, -2.665947717100999981, -8.940798416249000624 ) ) ;
#2277=CARTESIAN_POINT ( 'NONE',  ( 4.874073134685000142, 12.42371922698999853, 0.6764121694032001475 ) ) ;
#2278=EDGE_CURVE ( 'NONE', #19420, #2511, #13558, .T. ) ;
#2280=CARTESIAN_POINT ( 'NONE',  ( -20.76607004806999868, 1.065680277943000132, -11.02016022475999968 ) ) ;
#2281=EDGE_LOOP ( 'NONE', ( #7740, #14456, #10120, #8642 ) ) ;
#2286=CARTESIAN_POINT ( 'NONE',  ( 4.622963014007718918, 12.49839699622550349, 1.256155413754589167 ) ) ;
#2288=CARTESIAN_POINT ( 'NONE',  ( 24.50000000000000000, 0.000000000000000000, 0.000000000000000000 ) ) ;
#2289=EDGE_CURVE ( 'NONE', #20328, #13328, #20422, .T. ) ;
#2290=DIRECTION ( 'NONE',  ( 1.000000000000000000, 0.000000000000000000, 0.000000000000000000 ) ) ;
#2291=CARTESIAN_POINT ( 'NONE',  ( 13.22662674931000204, 6.334720884006999952, 8.559150566242998082 ) ) ;
#2292=CIRCLE ( 'NONE', #1916, 0.9999989211906009645 ) ;
#2293=CARTESIAN_POINT ( 'NONE',  ( -12.79254388956000099, 9.568035197138000214, -2.460455418527999871 ) ) ;
#2294=AXIS2_PLACEMENT_3D ( 'NONE', #15694, #23084, #6509 ) ;
#2297=CARTESIAN_POINT ( 'NONE',  ( -14.33281117769207569, -5.151946275727822488, 12.49999999999962697 ) ) ;
#2298=ORIENTED_EDGE ( 'NONE', *, *, #3038, .T. ) ;
#2299=EDGE_CURVE ( 'NONE', #6464, #386, #4181, .T. ) ;
#2303=CARTESIAN_POINT ( 'NONE',  ( 13.84539632146338128, -8.680774802907970766, 5.550785524995694331 ) ) ;
#2304=EDGE_LOOP ( 'NONE', ( #3750, #2061, #10700, #16455 ) ) ;
#2305=CARTESIAN_POINT ( 'NONE',  ( -2.461267912185001183, 12.87788887804001803, -6.662423917068999835 ) ) ;
#2307=CARTESIAN_POINT ( 'NONE',  ( 12.28779254564781986, -5.665119685639886882, 12.50001287414623619 ) ) ;
#2308=CARTESIAN_POINT ( 'NONE',  ( 18.71311277160243947, 3.105602819214801080, 10.00188426715560297 ) ) ;
#2309=CARTESIAN_POINT ( 'NONE',  ( -12.25000000000000000, 1.374666032043000015E-14, 0.000000000000000000 ) ) ;
#2310=CARTESIAN_POINT ( 'NONE',  ( 11.85409292833900707, 8.571431512452234003, -10.15389364929188609 ) ) ;
#2316=CARTESIAN_POINT ( 'NONE',  ( -9.042815982636001948, 20.50000000000000000, -1.000000000000000000 ) ) ;
#2319=AXIS2_PLACEMENT_3D ( 'NONE', #1577, #3400, #11124 ) ;
#2320=CARTESIAN_POINT ( 'NONE',  ( 15.88860957249000094, -10.52205501482999850, -3.386765196271000367 ) ) ;
#2321=DIRECTION ( 'NONE',  ( 0.000000000000000000, 0.8660254037844288266, -0.5000000000000169864 ) ) ;
#2322=CARTESIAN_POINT ( 'NONE',  ( 24.40278699097224901, -2.659935282767429854, -12.50000000000000178 ) ) ;
#2324=VERTEX_POINT ( 'NONE', #18713 ) ;
#2325=CARTESIAN_POINT ( 'NONE',  ( -14.00000000000000178, -1.971496140865625302, -9.404298541413128376 ) ) ;
#2326=CARTESIAN_POINT ( 'NONE',  ( -10.39612971169000133, 4.211105248640000021, 14.98851321108000079 ) ) ;
#2329=DIRECTION ( 'NONE',  ( 6.613961328593999866E-09, -8.164805666996911273E-09, 1.000000000000000000 ) ) ;
#2332=CARTESIAN_POINT ( 'NONE',  ( -23.10253524184999918, 6.427000661414000504, 7.964584163192999000 ) ) ;
#2333=CARTESIAN_POINT ( 'NONE',  ( -14.39391696178813262, 8.762017990479289864, 9.823718642491295228 ) ) ;
#2335=CARTESIAN_POINT ( 'NONE',  ( 15.31019486909626082, 2.146509511632994638, 10.14207265829758597 ) ) ;
#2337=CARTESIAN_POINT ( 'NONE',  ( -14.00878788127999997, -9.282977100841998563, -4.456265381222999977 ) ) ;
#2339=CARTESIAN_POINT ( 'NONE',  ( -14.82384736926000102, 5.788590216149999357, -9.100136119003000346 ) ) ;
#2343=CARTESIAN_POINT ( 'NONE',  ( -19.52737009387375267, -10.18506149564973207, 2.517846037059293440 ) ) ;
#2344=ORIENTED_EDGE ( 'NONE', *, *, #3639, .F. ) ;
#2346=CARTESIAN_POINT ( 'NONE',  ( -4.108124441661001214, 14.09331144393998692, 4.413805377952999542 ) ) ;
#2347=CARTESIAN_POINT ( 'NONE',  ( 18.33699999999999974, -9.141845273363999880, 1.095420050962999850E-14 ) ) ;
#2348=CARTESIAN_POINT ( 'NONE',  ( 14.59968892130999940, 4.304969983318999383, 8.654667617400001234 ) ) ;
#2349=ORIENTED_EDGE ( 'NONE', *, *, #11203, .T. ) ;
#2354=DIRECTION ( 'NONE',  ( 0.000000000000000000, -1.000000000000000000, 0.000000000000000000 ) ) ;
#2355=CARTESIAN_POINT ( 'NONE',  ( -4.724251990381001853, 12.60843673673999810, 0.4143338360902000250 ) ) ;
#2357=CARTESIAN_POINT ( 'NONE',  ( -21.17298660481999661, 9.406917137533000073, -1.865098543902999895 ) ) ;
#2358=DIRECTION ( 'NONE',  ( 0.000000000000000000, -1.000000000000000000, 0.000000000000000000 ) ) ;
#2359=CARTESIAN_POINT ( 'NONE',  ( -3.317489423066998455, 13.45101538807001873, -5.148797630174996698 ) ) ;
#2360=CARTESIAN_POINT ( 'NONE',  ( 5.972539995960000070, 13.70650976685000089, 2.690923256664000007 ) ) ;
#2361=CARTESIAN_POINT ( 'NONE',  ( 5.302309017544000191, 13.73032573480000096, -4.450985556070999216 ) ) ;
#2366=CARTESIAN_POINT ( 'NONE',  ( -16.90124577250666604, -2.383332030605061380, 8.867973604693034417 ) ) ;
#2367=CARTESIAN_POINT ( 'NONE',  ( 18.82170634012999955, -6.238070653312000502, -7.492020000904000554 ) ) ;
#2368=CARTESIAN_POINT ( 'NONE',  ( 3.914845617362098018, 13.31586473120900393, -5.570899607885616334 ) ) ;
#2370=CARTESIAN_POINT ( 'NONE',  ( -22.86671354229583031, -10.53743997464867732, -0.7811924423727086841 ) ) ;
#2372=B_SPLINE_CURVE_WITH_KNOTS ( 'NONE', 3,
 ( #6836, #20044, #21624, #17874, #23298, #18228, #4911, #10952, #14351, #10488 ),
 .UNSPECIFIED., .F., .F.,
 ( 4, 2, 2, 2, 4 ),
 ( 0.000000000000000000, 0.2500000000000000000, 0.5000000000000000000, 0.7500000000000000000, 1.000000000000000000 ),
 .UNSPECIFIED. ) ;
#2375=CARTESIAN_POINT ( 'NONE',  ( -17.90765081723635177, 0.2656351261378813722, 10.58437225064310816 ) ) ;
#2376=EDGE_CURVE ( 'NONE', #7890, #4095, #20895, .T. ) ;
#2377=DIRECTION ( 'NONE',  ( -1.000000000000000000, 0.000000000000000000, 0.000000000000000000 ) ) ;
#2379=CARTESIAN_POINT ( 'NONE',  ( -14.03310205518379128, 8.843032913246654303, 2.087261342718107482 ) ) ;
#2380=VERTEX_POINT ( 'NONE', #5875 ) ;
#2381=CARTESIAN_POINT ( 'NONE',  ( 17.44974770046333390, 5.604008867033932972, -7.292312980387861465 ) ) ;
#2382=CARTESIAN_POINT ( 'NONE',  ( 16.40756424930999913, 8.766565845128001300, -6.190543086277999763 ) ) ;
#2383=CARTESIAN_POINT ( 'NONE',  ( -16.17253408984999652, -2.147297115180999860, 11.15346350841000067 ) ) ;
#2385=CARTESIAN_POINT ( 'NONE',  ( 12.89051537305999950, 0.9064800472110999818, -9.847992809938999059 ) ) ;
#2388=CARTESIAN_POINT ( 'NONE',  ( 22.26065228610000091, 1.952640354001999867, -10.06840971000000096 ) ) ;
#2392=VERTEX_POINT ( 'NONE', #21012 ) ;
#2393=FACE_OUTER_BOUND ( 'NONE', #1763, .T. ) ;
#2395=CARTESIAN_POINT ( 'NONE',  ( 2.814154119931001841, 11.91260811072999104, 3.809416604937000184 ) ) ;
#2397=CARTESIAN_POINT ( 'NONE',  ( -22.43691550588000183, 6.205779378985000427, -9.223551109405999426 ) ) ;
#2400=EDGE_LOOP ( 'NONE', ( #6111, #10554, #8252, #16567, #10570 ) ) ;
#2403=EDGE_CURVE ( 'NONE', #4084, #18848, #2605, .T. ) ;
#2404=CARTESIAN_POINT ( 'NONE',  ( 2.428345707995998470, 12.87484077716998598, 6.668354174382002064 ) ) ;
#2406=CARTESIAN_POINT ( 'NONE',  ( 12.34912674931000076, -5.416870430593999863, -9.140812312194999123 ) ) ;
#2407=CARTESIAN_POINT ( 'NONE',  ( -16.81439276773000202, -8.006006257143999605, -6.488443847660000152 ) ) ;
#2409=CARTESIAN_POINT ( 'NONE',  ( 14.46356375731000021, 0.7465905146449000052, 9.123040730097999429 ) ) ;
#2411=CARTESIAN_POINT ( 'NONE',  ( -14.49284521823309824, -1.036537809018404310, 12.49997544921124337 ) ) ;
#2415=CARTESIAN_POINT ( 'NONE',  ( 13.83037995398642295, -8.404022434966693211, 5.981951882901380024 ) ) ;
#2417=CARTESIAN_POINT ( 'NONE',  ( -3.448929114309002397, 13.22474374734999003, -5.490345264048999141 ) ) ;
#2419=EDGE_CURVE ( 'NONE', #6719, #259, #2482, .T. ) ;
#2420=CARTESIAN_POINT ( 'NONE',  ( -19.10482910584000038, 1.458613477275000161E-14, 0.000000000000000000 ) ) ;
#2421=CARTESIAN_POINT ( 'NONE',  ( 11.90008533512006572, -4.641570061506480549, 12.50003962888516895 ) ) ;
#2423=CARTESIAN_POINT ( 'NONE',  ( 18.04406002188076741, 5.225631352894819059, -9.061601784925585434 ) ) ;
#2426=CARTESIAN_POINT ( 'NONE',  ( 11.72559253309100313, 8.766982473631962591, -9.815058144992619305 ) ) ;
#2427=ORIENTED_EDGE ( 'NONE', *, *, #22115, .T. ) ;
#2432=CARTESIAN_POINT ( 'NONE',  ( -3.066980279242876861, 11.87898535859614135, 3.727226793947211014 ) ) ;
#2435=FACE_OUTER_BOUND ( 'NONE', #12405, .T. ) ;
#2436=DIRECTION ( 'NONE',  ( -1.000000000000000000, 0.000000000000000000, 0.000000000000000000 ) ) ;
#2437=CARTESIAN_POINT ( 'NONE',  ( -7.135193656722003119, 15.40309895115001737, -1.043051061229000265 ) ) ;
#2439=ORIENTED_EDGE ( 'NONE', *, *, #21974, .F. ) ;
#2441=CARTESIAN_POINT ( 'NONE',  ( -13.99999999999999645, 1.449170934955976486, -9.306736692574475001 ) ) ;
#2443=CARTESIAN_POINT ( 'NONE',  ( -14.48633706258206288, -10.11155074088070371, -7.486293916572105189 ) ) ;
#2444=ORIENTED_EDGE ( 'NONE', *, *, #3636, .F. ) ;
#2445=CARTESIAN_POINT ( 'NONE',  ( -22.24570156380999819, -7.689645674130000330, -6.718150816083000798 ) ) ;
#2446=CARTESIAN_POINT ( 'NONE',  ( -24.16119556689726977, 8.771053125571407705, 9.807567373710691427 ) ) ;
#2447=CARTESIAN_POINT ( 'NONE',  ( 6.230117939712608965, 13.73923584163333800, 1.395535972837913308 ) ) ;
#2448=CARTESIAN_POINT ( 'NONE',  ( 15.79764610807505143, -10.31663114728906905, 0.9025345700017101125 ) ) ;
#2449=CARTESIAN_POINT ( 'NONE',  ( -18.34470744204000070, 4.667706239444999738, 10.08210694793999984 ) ) ;
#2452=CARTESIAN_POINT ( 'NONE',  ( -18.66670768690667614, -9.150306222430156566, 1.044069867951560981 ) ) ;
#2453=EDGE_CURVE ( 'NONE', #14911, #6411, #12164, .T. ) ;
#2454=CARTESIAN_POINT ( 'NONE',  ( -13.15804650426999878, -7.258886979407000339, -7.170289537978000283 ) ) ;
#2458=CARTESIAN_POINT ( 'NONE',  ( -19.18010000769303502, -6.003056531568853771, -8.588473314997994379 ) ) ;
#2459=VERTEX_POINT ( 'NONE', #15794 ) ;
#2464=EDGE_CURVE ( 'NONE', #9388, #17324, #13862, .T. ) ;
#2466=VECTOR ( 'NONE', #17383, 1000.000000000000000 ) ;
#2467=CARTESIAN_POINT ( 'NONE',  ( 11.74781392131000146, -7.601052271439000307, -5.849495945765999849 ) ) ;
#2469=CARTESIAN_POINT ( 'NONE',  ( -6.230543946801002875, 16.13931437111000733, -0.9718497405647000820 ) ) ;
#2470=DIRECTION ( 'NONE',  ( -1.280113743563924749E-07, -4.045642977578689132E-08, -0.9999999999999911182 ) ) ;
#2472=ORIENTED_EDGE ( 'NONE', *, *, #2718, .T. ) ;
#2476=CARTESIAN_POINT ( 'NONE',  ( -1.058805613176999616, 11.70499902296001160, 4.728261420812001958 ) ) ;
#2477=CARTESIAN_POINT ( 'NONE',  ( -12.50000000000000000, 6.992973968623999781, -5.709239639804999378 ) ) ;
#2478=CARTESIAN_POINT ( 'NONE',  ( 17.68641176306230989, -10.25162057640060631, -1.802399854559492587 ) ) ;
#2479=FACE_OUTER_BOUND ( 'NONE', #15038, .T. ) ;
#2480=CARTESIAN_POINT ( 'NONE',  ( -14.25243324638999809, 7.716878364870000340, -11.63397459621999985 ) ) ;
#2481=CARTESIAN_POINT ( 'NONE',  ( -4.724624249661752984, 13.39762491672413525, 5.370412594684863095 ) ) ;
#2482=LINE ( 'NONE', #13614, #6338 ) ;
#2483=CARTESIAN_POINT ( 'NONE',  ( 5.896080086043998136, 14.43358657436269432, 1.669016364038776956 ) ) ;
#2486=ORIENTED_EDGE ( 'NONE', *, *, #17155, .F. ) ;
#2487=CARTESIAN_POINT ( 'NONE',  ( -17.05241243917333804, 2.384112843373643820, 8.871849034729358152 ) ) ;
#2488=CARTESIAN_POINT ( 'NONE',  ( 20.56096474217000036, -7.987351613630001346, -5.673264839440999907 ) ) ;
#2489=CARTESIAN_POINT ( 'NONE',  ( 2.198509335874302195, 12.96754872753050769, -6.338474540310088834 ) ) ;
#2492=LINE ( 'NONE', #11707, #1148 ) ;
#2493=ORIENTED_EDGE ( 'NONE', *, *, #14178, .T. ) ;
#2495=FACE_OUTER_BOUND ( 'NONE', #23239, .T. ) ;
#2499=ORIENTED_EDGE ( 'NONE', *, *, #4500, .T. ) ;
#2500=CARTESIAN_POINT ( 'NONE',  ( 17.07183103379666633, -5.598228470880529883, -7.284378211082013443 ) ) ;
#2502=CARTESIAN_POINT ( 'NONE',  ( 17.83350174931000254, -4.076359992019000344, -9.968186170592000295 ) ) ;
#2503=CARTESIAN_POINT ( 'NONE',  ( -23.84635873346000068, 3.413845864946000397, 10.14151937845999996 ) ) ;
#2505=CARTESIAN_POINT ( 'NONE',  ( 24.00016455292000117, -6.692834685703999753, -6.438753808737999407 ) ) ;
#2506=CARTESIAN_POINT ( 'NONE',  ( 19.32280703972000069, -3.872993065167000371, 9.573872678542000969 ) ) ;
#2508=FACE_OUTER_BOUND ( 'NONE', #19005, .T. ) ;
#2509=CARTESIAN_POINT ( 'NONE',  ( 19.48688301901000131, -0.05922813441184000827, 9.759376508132000083 ) ) ;
#2511=VERTEX_POINT ( 'NONE', #6603 ) ;
#2514=AXIS2_PLACEMENT_3D ( 'NONE', #3192, #17961, #1240 ) ;
#2515=CARTESIAN_POINT ( 'NONE',  ( 4.488154563753997905, 12.44456933786999286, 1.490167364050000609 ) ) ;
#2517=CARTESIAN_POINT ( 'NONE',  ( -21.93566186853000133, 8.065990246855999857, 7.630410654556999184 ) ) ;
#2519=B_SPLINE_CURVE_WITH_KNOTS ( 'NONE', 3,
 ( #6893, #19859, #4849, #21559, #14288, #6534, #1206, #10420, #14164, #15845 ),
 .UNSPECIFIED., .F., .F.,
 ( 4, 2, 2, 2, 4 ),
 ( 0.000000000000000000, 0.2499999999999942268, 0.3749999999999960032, 0.4999999999999977796, 1.000000000000000000 ),
 .UNSPECIFIED. ) ;
#2522=DIRECTION ( 'NONE',  ( -1.000000000000000000, 0.000000000000000000, 0.000000000000000000 ) ) ;
#2523=CARTESIAN_POINT ( 'NONE',  ( 2.400996485352273613, 11.81767763009764316, 4.145245190034037464 ) ) ;
#2524=CARTESIAN_POINT ( 'NONE',  ( -2.688159063712002084, 13.03541276042999364, 5.879976109452004884 ) ) ;
#2526=CARTESIAN_POINT ( 'NONE',  ( 16.62693924930999856, 10.62505432564000074, 1.551621659364999850 ) ) ;
#2527=EDGE_CURVE ( 'NONE', #12621, #23059, #22959, .T. ) ;
#2528=CARTESIAN_POINT ( 'NONE',  ( -16.24575980504999606, 10.15426072268999924, 3.750674035441000420 ) ) ;
#2530=CARTESIAN_POINT ( 'NONE',  ( 11.61168875731000050, -4.628380041800000733, -7.810153319783999848 ) ) ;
#2531=CARTESIAN_POINT ( 'NONE',  ( 24.49999999999999645, 0.5123787730663634798, 12.50000000000000000 ) ) ;
#2532=ORIENTED_EDGE ( 'NONE', *, *, #10996, .F. ) ;
#2535=CARTESIAN_POINT ( 'NONE',  ( 13.84544698529813367, -8.681709169862820374, 5.549329201613704576 ) ) ;
#2536=ORIENTED_EDGE ( 'NONE', *, *, #1522, .T. ) ;
#2537=CARTESIAN_POINT ( 'NONE',  ( -0.7159621321844995556, 13.80975668258999178, -6.133614306996999943 ) ) ;
#2538=CARTESIAN_POINT ( 'NONE',  ( -23.97728971654279917, 13.40084515676303312, -1.788539470789224595 ) ) ;
#2541=CARTESIAN_POINT ( 'NONE',  ( -11.04281598264000053, 15.43375672974000068, 0.000000000000000000 ) ) ;
#2542=CARTESIAN_POINT ( 'NONE',  ( 18.32283200093110054, 10.42794303851333737, -0.8528220165487894189 ) ) ;
#2550=CARTESIAN_POINT ( 'NONE',  ( -6.042815832213999983, 16.39253418350000047, -0.9999999878869999526 ) ) ;
#2551=CARTESIAN_POINT ( 'NONE',  ( -4.446287379418881969, 12.30056135601858713, 1.928247084751353535 ) ) ;
#2554=CARTESIAN_POINT ( 'NONE',  ( 14.77207488446000028, 6.658492172936999687, -8.784828455393000723 ) ) ;
#2555=CARTESIAN_POINT ( 'NONE',  ( -5.981181950157998806, 15.11060635804999741, -2.632465999322001426 ) ) ;
#2558=VERTEX_POINT ( 'NONE', #22301 ) ;
#2560=CARTESIAN_POINT ( 'NONE',  ( -14.00000000000000178, -4.872638669815645862, -8.474582696947910776 ) ) ;
#2563=ORIENTED_EDGE ( 'NONE', *, *, #19487, .F. ) ;
#2564=CARTESIAN_POINT ( 'NONE',  ( -18.57447842246000036, -9.039081325395999400, -0.2073323074504999919 ) ) ;
#2566=AXIS2_PLACEMENT_3D ( 'NONE', #18094, #1502, #16262 ) ;
#2567=CARTESIAN_POINT ( 'NONE',  ( 6.146311545762546125, 14.15705020831570593, 0.1884214613589945964 ) ) ;
#2568=CARTESIAN_POINT ( 'NONE',  ( 15.84391418034966215, -10.32692765650489797, -0.7703782186506803464 ) ) ;
#2569=AXIS2_PLACEMENT_3D ( 'NONE', #11576, #9749, #2008 ) ;
#2570=CARTESIAN_POINT ( 'NONE',  ( -14.91210445643999982, 9.869058056742000318, 4.894649932895999811 ) ) ;
#2573=CARTESIAN_POINT ( 'NONE',  ( -19.60932161866278278, -9.094709918404200621, 5.216993370950443243 ) ) ;
#2579=CARTESIAN_POINT ( 'NONE',  ( -14.31831880116688538, -5.229320062394984703, 8.931164432586227164 ) ) ;
#2581=VERTEX_POINT ( 'NONE', #20502 ) ;
#2583=CARTESIAN_POINT ( 'NONE',  ( 6.626584110769001335, 13.50257275877999064, -0.5067788187794998178 ) ) ;
#2584=CARTESIAN_POINT ( 'NONE',  ( -19.91867920454665608, 2.403600030157754919, -8.943391512361417384 ) ) ;
#2585=ADVANCED_FACE ( 'NONE', ( #18788 ), #15261, .F. ) ;
#2586=CARTESIAN_POINT ( 'NONE',  ( 13.06406392131000160, -4.637122060904999898, 8.435305548789999719 ) ) ;
#2588=ORIENTED_EDGE ( 'NONE', *, *, #16504, .T. ) ;
#2589=CARTESIAN_POINT ( 'NONE',  ( 18.45420603379666247, -7.704153391283862007, 5.039298146494758157 ) ) ;
#2594=CARTESIAN_POINT ( 'NONE',  ( 12.52688711657000020, 7.716878364870000340, 11.63397459621999985 ) ) ;
#2595=CARTESIAN_POINT ( 'NONE',  ( 4.813190031656002787, 12.64298052023998586, 0.2515842787466999186 ) ) ;
#2596=DIRECTION ( 'NONE',  ( 0.000000000000000000, 1.000000000000000000, 0.000000000000000000 ) ) ;
#2597=CARTESIAN_POINT ( 'NONE',  ( 17.66152877879916261, -10.36100141562122268, -0.9108117703243313601 ) ) ;
#2601=CARTESIAN_POINT ( 'NONE',  ( 22.10687615272999906, 7.216905606319000022, 8.629172509395999668 ) ) ;
#2604=EDGE_CURVE ( 'NONE', #18376, #10732, #23071, .T. ) ;
#2605=LINE ( 'NONE', #22937, #14697 ) ;
#2606=CARTESIAN_POINT ( 'NONE',  ( 5.801373033572341242, 14.45988999510258388, 1.973196774158483935 ) ) ;
#2611=CARTESIAN_POINT ( 'NONE',  ( -16.56112077250667269, -9.096272712312636344, 1.190572366013356698 ) ) ;
#2612=CARTESIAN_POINT ( 'NONE',  ( 18.35893224774000032, 0.1033670869143000076, 9.766723590596999571 ) ) ;
#2613=CARTESIAN_POINT ( 'NONE',  ( 0.8106507644720812866, 12.82603987343919094, -6.620134064058884604 ) ) ;
#2614=DIRECTION ( 'NONE',  ( 0.000000000000000000, 0.000000000000000000, 1.000000000000000000 ) ) ;
#2615=CARTESIAN_POINT ( 'NONE',  ( -20.91203816579346508, -8.901941407118242111, -5.604029123285282132 ) ) ;
#2622=CARTESIAN_POINT ( 'NONE',  ( -19.13574525531997494, -9.517642123610587035, -4.380541451279561294 ) ) ;
#2627=ORIENTED_EDGE ( 'NONE', *, *, #18310, .T. ) ;
#2628=CARTESIAN_POINT ( 'NONE',  ( 16.84508103379666721, -9.103559692274046711, -1.191526229459736408 ) ) ;
#2629=CARTESIAN_POINT ( 'NONE',  ( 13.55568924931000119, -5.133899498893999436, 9.338903284905999413 ) ) ;
#2630=CARTESIAN_POINT ( 'NONE',  ( -24.05893800299999796, 10.23807085788999949, -4.603936266037999658 ) ) ;
#2632=DIRECTION ( 'NONE',  ( 0.000000000000000000, 0.000000000000000000, 1.000000000000000000 ) ) ;
#2633=CARTESIAN_POINT ( 'NONE',  ( 15.39619494526000132, 10.26707030725000003, -0.2369671920225999984 ) ) ;
#2637=CARTESIAN_POINT ( 'NONE',  ( 22.35490775615000203, -3.982320853531000182, -8.877099480003998622 ) ) ;
#2638=B_SPLINE_SURFACE_WITH_KNOTS ( 'NONE', 3, 3, ( 
 ( #6861, #9248, #4701, #14012 ),
 ( #19717, #12447, #19831, #15930 ),
 ( #19591, #6738, #14132, #16625 ),
 ( #14254, #21289, #1048, #6504 ) ),
 .UNSPECIFIED., .F., .F., .F.,
 ( 4, 4 ),
 ( 4, 4 ),
 ( -0.09148521614644000710, 0.2147869640759000054 ),
 ( 0.9473429275995000065, 1.001032491615999831 ),
 .UNSPECIFIED. ) ;
#2641=CARTESIAN_POINT ( 'NONE',  ( 18.64355344916001300, -1.808540911500012838, 9.835923363989143908 ) ) ;
#2643=CARTESIAN_POINT ( 'NONE',  ( -0.1141952544650000068, 11.49080619599998876, 4.810811492839003556 ) ) ;
#2647=CARTESIAN_POINT ( 'NONE',  ( -20.11819481384999975, 10.67730650337000142, 2.861074714015000353 ) ) ;
#2649=CIRCLE ( 'NONE', #9995, 10.59999999999999964 ) ;
#2650=ORIENTED_EDGE ( 'NONE', *, *, #14392, .T. ) ;
#2651=CARTESIAN_POINT ( 'NONE',  ( 15.14445603379664895, -7.916481873543318670, -4.562629533669052329 ) ) ;
#2652=CARTESIAN_POINT ( 'NONE',  ( -19.78832264027077059, -9.441231315352206721, 3.364601191696911631 ) ) ;
#2653=CARTESIAN_POINT ( 'NONE',  ( 3.118723778390000589, 14.26802845704001754, 5.330537660070998385 ) ) ;
#2656=CARTESIAN_POINT ( 'NONE',  ( -6.250000000000000000, 15.73203524433000311, -1.185075242810999852 ) ) ;
#2657=CARTESIAN_POINT ( 'NONE',  ( 17.64450125731000085, 9.220888413547999818, -0.5479559280035000146 ) ) ;
#2661=CARTESIAN_POINT ( 'NONE',  ( 20.02908892782178540, 9.445433025424275542, -4.628470371599332722 ) ) ;
#2665=CARTESIAN_POINT ( 'NONE',  ( 3.425434194794530818, 14.25881501014746888, -5.078536901545239068 ) ) ;
#2667=ORIENTED_EDGE ( 'NONE', *, *, #7066, .F. ) ;
#2668=CARTESIAN_POINT ( 'NONE',  ( 5.752440845993000096, 13.85430232992000299, -4.060540161502004253 ) ) ;
#2669=CARTESIAN_POINT ( 'NONE',  ( 20.34417738779000473, 9.978297411703000108, -5.088582451532000839 ) ) ;
#2671=CARTESIAN_POINT ( 'NONE',  ( 11.70388046502320201, -4.051054454411410433, 12.49994163046800288 ) ) ;
#2672=DIRECTION ( 'NONE',  ( -0.9996708941621509359, 0.02565352539214875091, 1.648348900435920369E-14 ) ) ;
#2675=CARTESIAN_POINT ( 'NONE',  ( -18.63376253787999914, -9.149460784975000038, 0.000000000000000000 ) ) ;
#2676=EDGE_CURVE ( 'NONE', #20521, #6064, #21068, .T. ) ;
#2682=TOROIDAL_SURFACE ( 'NONE', #8888, 13.91261088316000105, 1.521145846583000116 ) ;
#2683=FACE_OUTER_BOUND ( 'NONE', #21589, .T. ) ;
#2685=CARTESIAN_POINT ( 'NONE',  ( 3.958466783697788038, 13.32814196193950984, 5.540440575617210150 ) ) ;
#2687=CYLINDRICAL_SURFACE ( 'NONE', #18834, 7.000000000000000000 ) ;
#2691=ADVANCED_FACE ( 'NONE', ( #11179, #1969 ), #9352, .F. ) ;
#2692=EDGE_LOOP ( 'NONE', ( #19556, #23252 ) ) ;
#2694=CARTESIAN_POINT ( 'NONE',  ( 7.124999988904000325, 14.37502327612999942, -5.687882594960999921E-06 ) ) ;
#2695=AXIS2_PLACEMENT_3D ( 'NONE', #398, #632, #5740 ) ;
#2697=CARTESIAN_POINT ( 'NONE',  ( -6.517755120876246089, 15.19342473677416727, -2.753401504715822679 ) ) ;
#2701=CARTESIAN_POINT ( 'NONE',  ( 15.06374514717642477, 9.021709532834009337, 5.042244869155494413 ) ) ;
#2702=CARTESIAN_POINT ( 'NONE',  ( -14.18945119630999940, -10.82201390087000092, 1.947477006705999880 ) ) ;
#2705=CARTESIAN_POINT ( 'NONE',  ( -19.81520262463921611, -3.472309042968596771, 9.897195304290566042 ) ) ;
#2706=CARTESIAN_POINT ( 'NONE',  ( -14.05208405859999843, -9.143870435873997948, 6.637879840603000403 ) ) ;
#2709=VERTEX_POINT ( 'NONE', #5834 ) ;
#2711=CARTESIAN_POINT ( 'NONE',  ( -17.27011453369921057, -2.826153282971739511, -10.04434318468920573 ) ) ;
#2714=CARTESIAN_POINT ( 'NONE',  ( -23.75391236596000155, 7.467096437641000506, -11.77818625913999817 ) ) ;
#2715=CARTESIAN_POINT ( 'NONE',  ( 5.625313445317996930, 13.77071113236998379, -3.543115536436998170 ) ) ;
#2716=CARTESIAN_POINT ( 'NONE',  ( 12.00000000000000000, -3.611861960331876897, -8.220758729215566163 ) ) ;
#2718=EDGE_CURVE ( 'NONE', #22144, #6663, #13217, .T. ) ;
#2719=CARTESIAN_POINT ( 'NONE',  ( 12.29625142131000004, 8.002767958507000401, -5.312704480003000995 ) ) ;
#2720=ORIENTED_EDGE ( 'NONE', *, *, #12795, .F. ) ;
#2721=DIRECTION ( 'NONE',  ( 0.000000000000000000, 1.000000000000000000, 0.000000000000000000 ) ) ;
#2722=DIRECTION ( 'NONE',  ( 1.000000000000000000, 0.000000000000000000, 0.000000000000000000 ) ) ;
#2724=ORIENTED_EDGE ( 'NONE', *, *, #14550, .T. ) ;
#2725=DIRECTION ( 'NONE',  ( 0.000000000000000000, 1.000000000000000000, 0.000000000000000000 ) ) ;
#2726=CARTESIAN_POINT ( 'NONE',  ( -23.74465998031000069, -13.93375672974000068, -0.8660254037843999608 ) ) ;
#2727=CARTESIAN_POINT ( 'NONE',  ( 24.26478934590349468, -0.8345397459580851107, 10.59477908038717686 ) ) ;
#2728=CARTESIAN_POINT ( 'NONE',  ( -12.48243343204000055, 6.965111533508000718, -5.686492047758000545 ) ) ;
#2729=CARTESIAN_POINT ( 'NONE',  ( 18.06179173045719821, -1.003953116814803481, -10.36291011014150065 ) ) ;
#2731=CARTESIAN_POINT ( 'NONE',  ( 12.00000000000000178, -5.648153558507000405, -7.896738249884089456 ) ) ;
#2732=CARTESIAN_POINT ( 'NONE',  ( -14.37382047448982192, -8.632461983038391296, 10.04764370666022444 ) ) ;
#2733=CARTESIAN_POINT ( 'NONE',  ( 18.80303081932999731, -4.612880036109999082, 10.15984863128999827 ) ) ;
#2734=DIRECTION ( 'NONE',  ( -1.000000000000000000, 0.000000000000000000, 0.000000000000000000 ) ) ;
#2735=CARTESIAN_POINT ( 'NONE',  ( -3.998638495880459498, 13.85419791046053994, -4.853578403047964507 ) ) ;
#2741=CARTESIAN_POINT ( 'NONE',  ( -16.93903743917333315, -1.192095737878614781, 9.105970798813979528 ) ) ;
#2742=CARTESIAN_POINT ( 'NONE',  ( 18.87426807056999678, -10.06611063169999909, -2.115216155665999853 ) ) ;
#2743=CARTESIAN_POINT ( 'NONE',  ( 3.177045621698409317, 13.14387179043593079, -5.964232631809895935 ) ) ;
#2746=CARTESIAN_POINT ( 'NONE',  ( -24.41904027017961454, -11.84953030590303591, -4.475986625628626925 ) ) ;
#2747=CARTESIAN_POINT ( 'NONE',  ( -4.282263979383000851, 12.27659869337001552, -2.483328958996001479 ) ) ;
#2749=CARTESIAN_POINT ( 'NONE',  ( -18.74498793411180131, 2.216523406432389098, -10.23078730626788158 ) ) ;
#2750=EDGE_CURVE ( 'NONE', #9910, #6464, #5568, .T. ) ;
#2751=DIRECTION ( 'NONE',  ( 0.000000000000000000, -1.000000000000000000, 0.000000000000000000 ) ) ;
#2755=EDGE_LOOP ( 'NONE', ( #1706, #2222, #5122, #12171, #3062 ) ) ;
#2757=CARTESIAN_POINT ( 'NONE',  ( 17.63870603379666946, 8.886405729592773639, -2.388285526542218040 ) ) ;
#2758=CARTESIAN_POINT ( 'NONE',  ( 19.00350174931000069, -5.312632942934000013, 9.204603991398000673 ) ) ;
#2759=CARTESIAN_POINT ( 'NONE',  ( -14.02955537940998809, 6.411209705375615187, -6.427717830503866026 ) ) ;
#2760=CARTESIAN_POINT ( 'NONE',  ( -17.25423626710000136, 5.368550673722999989, -9.432097563122999517 ) ) ;
#2761=CARTESIAN_POINT ( 'NONE',  ( -6.044422725124001694, 15.62653472375999542, 1.260791734048000379 ) ) ;
#2762=CARTESIAN_POINT ( 'NONE',  ( 14.98994494525999954, 1.437436215449000132, -10.15727603318000050 ) ) ;
#2765=CARTESIAN_POINT ( 'NONE',  ( 24.41097397878344921, 9.853094029288689271, 1.034144647742462508 ) ) ;
#2766=VERTEX_POINT ( 'NONE', #20970 ) ;
#2767=CARTESIAN_POINT ( 'NONE',  ( 2.541770361367480913, 14.00639520368903312, 5.573038258459499517 ) ) ;
#2769=CARTESIAN_POINT ( 'NONE',  ( -4.607457922294000419, 12.49060724118000110, 1.057233348562000685 ) ) ;
#2771=CARTESIAN_POINT ( 'NONE',  ( -20.24435346183999940, 7.375945635487999752, 8.237836394566999232 ) ) ;
#2773=B_SPLINE_CURVE_WITH_KNOTS ( 'NONE', 3,
 ( #15195, #8189, #541, #18961, #9758, #5769, #16898, #7946, #3958, #4311 ),
 .UNSPECIFIED., .F., .F.,
 ( 4, 2, 2, 2, 4 ),
 ( 0.000000000000000000, 0.2500000000000000000, 0.5000000000000000000, 0.7500000000000000000, 1.000000000000000000 ),
 .UNSPECIFIED. ) ;
#2778=CARTESIAN_POINT ( 'NONE',  ( -4.005628047234999656, 13.41105388907000417, 5.056273175647006290 ) ) ;
#2779=EDGE_CURVE ( 'NONE', #14211, #3898, #9531, .T. ) ;
#2780=DIRECTION ( 'NONE',  ( 0.000000000000000000, 1.000000000000000000, 0.000000000000000000 ) ) ;
#2782=CARTESIAN_POINT ( 'NONE',  ( -12.43257971169000164, 9.053737661458001185, -12.66555795296999953 ) ) ;
#2784=CARTESIAN_POINT ( 'NONE',  ( 17.86387625731000028, 7.066414026761999700, 5.957971218261000956 ) ) ;
#2788=CARTESIAN_POINT ( 'NONE',  ( -22.00241225129201794, -9.233902645863798497, 1.209007217019692604 ) ) ;
#2790=B_SPLINE_CURVE_WITH_KNOTS ( 'NONE', 3,
 ( #8895, #8768, #18095, #1618, #9117, #7063, #16376, #16131, #14447, #5254, #16491, #23880, #12638, #21610, #20026, #3444, #23533, #9006 ),
 .UNSPECIFIED., .F., .F.,
 ( 4, 2, 2, 2, 2, 2, 2, 2, 4 ),
 ( 0.000000000000000000, 0.1250000000000000000, 0.2500000000000000000, 0.3750000000000000555, 0.5000000000000000000, 0.6250000000000000000, 0.7500000000000000000, 0.8750000000000000000, 1.000000000000000000 ),
 .UNSPECIFIED. ) ;
#2792=CARTESIAN_POINT ( 'NONE',  ( 3.099532833261116949, 14.15752231852028231, -5.282866363571895540 ) ) ;
#2793=ORIENTED_EDGE ( 'NONE', *, *, #5676, .T. ) ;
#2794=CARTESIAN_POINT ( 'NONE',  ( 5.704330172568996105, 13.83477387354001031, -4.128797533092996019 ) ) ;
#2796=B_SPLINE_SURFACE_WITH_KNOTS ( 'NONE', 3, 3, ( 
 ( #1919, #10782, #18174, #23720, #14403, #22141, #14858, #7127, #22247, #14516, #21909, #3514, #18739, #15459, #4328, #18627, #13640, #6137, #9540, #13282, #14973, #684, #15210, #7962, #2149, #20681, #6257, #18861, #2034, #11719, #11486, #2267, #16917, #17041, #320 ),
 ( #9660, #2506, #7595, #7726, #19094, #22371, #5896, #4090, #439, #5786, #16796, #13169, #9424, #22723, #7841, #202, #9895, #22607, #15091, #22487, #20559, #6016, #13401, #20802, #3857, #11249, #4211, #556, #3973, #20924, #11366, #11605, #13526, #18976, #2385 ),
 ( #9775, #17161, #15334, #17284, #8091, #22844, #15820, #15935, #17783, #19355, #19721, #21163, #23329, #19596, #11966, #10391, #16057, #21530, #14138, #12090, #1182, #4946, #2633, #6742, #2762, #3134, #3006, #4822, #8208, #8453, #15575, #11840, #19474, #21293, #19221 ),
 ( #12330, #21406, #17653, #10518, #1304, #4705, #13761, #2882, #23452, #17901, #23211, #8693, #6866, #21036, #4451, #10029, #10265, #10146, #17414, #809, #1052, #22963, #6378, #4574, #17532, #6627, #926, #8326, #8575, #15691, #23082, #6506, #14016, #13890, #12207 ) ),
 .UNSPECIFIED., .F., .F., .F.,
 ( 4, 4 ),
 ( 4, 1, 1, 1, 1, 1, 1, 1, 1, 1, 1, 1, 1, 1, 1, 1, 1, 1, 1, 1, 1, 1, 1, 1, 1, 1, 1, 1, 1, 1, 1, 1, 4 ),
 ( -0.08331297109794000288, 1.083312971098000066 ),
 ( -0.01851851851851999894, 0.01157407407407000030, 0.04166666666667000196, 0.07175925925925999427, 0.1018518518519000021, 0.1319444444444000109, 0.1620370370369999813, 0.1921296296295999795, 0.2222222222222000054, 0.2523148148148000036, 0.2824074074074000018, 0.3125000000000000000, 0.3425925925925999982, 0.3726851851851999964, 0.4027777777777999946, 0.4328703703703999928, 0.4629629629629999910, 0.4930555555555999891, 0.5231481481480999562, 0.5532407407406999544, 0.5833333333333000637, 0.6134259259259000618, 0.6435185185185000600, 0.6736111111111000582, 0.7037037037036999454, 0.7337962962962999436, 0.7638888888888999418, 0.7939814814814999400, 0.8240740740740999382, 0.8541666666667000474, 0.8842592592593000456, 0.9143518518519000438, 0.9444444444444000109 ),
 .UNSPECIFIED. ) ;
#2798=CARTESIAN_POINT ( 'NONE',  ( -12.50000000000000000, 6.868132469527897577, -5.843449823281533284 ) ) ;
#2799=CARTESIAN_POINT ( 'NONE',  ( 14.53153308584223247, 8.264717062064972808, -6.255766661236222603 ) ) ;
#2802=LINE ( 'NONE', #10183, #10804 ) ;
#2803=CARTESIAN_POINT ( 'NONE',  ( 20.05737270046332910, -2.404297061055042040, 8.946955187238454954 ) ) ;
#2805=CARTESIAN_POINT ( 'NONE',  ( 19.19268716888089443, -6.541906309961956545, 8.200137938995508691 ) ) ;
#2807=ORIENTED_EDGE ( 'NONE', *, *, #2676, .T. ) ;
#2810=FACE_OUTER_BOUND ( 'NONE', #20935, .T. ) ;
#2813=CARTESIAN_POINT ( 'NONE',  ( -5.384399873003000714, 15.53476682087999805, -2.763068870761999030 ) ) ;
#2814=CARTESIAN_POINT ( 'NONE',  ( 24.38510397947347741, -2.890284505278647664, -12.49999999999999822 ) ) ;
#2815=ORIENTED_EDGE ( 'NONE', *, *, #13967, .T. ) ;
#2816=ORIENTED_EDGE ( 'NONE', *, *, #7137, .T. ) ;
#2823=CARTESIAN_POINT ( 'NONE',  ( 20.68008333333332160, 2.408479787571709441, -8.962519253214404458 ) ) ;
#2824=CARTESIAN_POINT ( 'NONE',  ( 14.91301520687590099, 10.33462043395056007, -0.1764324625305463967 ) ) ;
#2825=CARTESIAN_POINT ( 'NONE',  ( -15.12680948961000027, 7.749013830361000110, -7.838259309650000617 ) ) ;
#2827=CARTESIAN_POINT ( 'NONE',  ( -21.51372092398854363, -7.149116854185205483, 7.905589411838503722 ) ) ;
#2828=CARTESIAN_POINT ( 'NONE',  ( -3.843096720568998315, 12.21397984018998351, -2.758463352735002427 ) ) ;
#2829=CONICAL_SURFACE ( 'NONE', #16351, 9.161549281532000322, 0.02565634000431304615 ) ;
#2832=VERTEX_POINT ( 'NONE', #854 ) ;
#2834=CARTESIAN_POINT ( 'NONE',  ( -14.81028475658608912, 9.567064880699621909, 4.004655637193650364 ) ) ;
#2835=ORIENTED_EDGE ( 'NONE', *, *, #23758, .F. ) ;
#2837=CARTESIAN_POINT ( 'NONE',  ( 5.578854890061005101, 14.64920222439000419, -2.552219347586000886 ) ) ;
#2838=CARTESIAN_POINT ( 'NONE',  ( 12.00000000000000000, -6.865294675837238181, -5.791300988468927713 ) ) ;
#2839=CARTESIAN_POINT ( 'NONE',  ( -20.14542920454665520, -4.627261388873439962, -8.028619099368466294 ) ) ;
#2840=CARTESIAN_POINT ( 'NONE',  ( 12.73500142131000068, 5.721315692782000362, 7.730289442163000402 ) ) ;
#2841=ORIENTED_EDGE ( 'NONE', *, *, #1985, .T. ) ;
#2842=CARTESIAN_POINT ( 'NONE',  ( -11.84376649291999861, 8.442406968109999355, -11.81034824682000028 ) ) ;
#2844=CARTESIAN_POINT ( 'NONE',  ( -12.50000000000000000, -10.59999999999999964, 0.000000000000000000 ) ) ;
#2846=EDGE_LOOP ( 'NONE', ( #5654, #20814, #22515, #3675, #21747, #1882, #23557, #7256, #1650, #1496 ) ) ;
#2848=CARTESIAN_POINT ( 'NONE',  ( 12.28022044530303347, 13.65679895895511109, 1.345730334339762857 ) ) ;
#2850=DIRECTION ( 'NONE',  ( -1.000000000000000000, 0.000000000000000000, 0.000000000000000000 ) ) ;
#2851=CARTESIAN_POINT ( 'NONE',  ( 16.68568461312300499, 10.32051225367915492, -1.596948730429063046 ) ) ;
#2852=CARTESIAN_POINT ( 'NONE',  ( 12.00000000000000355, -5.410480646876911770, -8.043393307973820683 ) ) ;
#2853=DIRECTION ( 'NONE',  ( 1.000000000000000000, 0.000000000000000000, 0.000000000000000000 ) ) ;
#2854=CARTESIAN_POINT ( 'NONE',  ( 22.25349774961999927, 7.219487340945000220, 8.632260055193999193 ) ) ;
#2856=CARTESIAN_POINT ( 'NONE',  ( -3.845736221939690225, 14.02535984897294696, -4.848784559987059595 ) ) ;
#2857=ADVANCED_FACE ( 'NONE', ( #23258 ), #20344, .F. ) ;
#2860=CARTESIAN_POINT ( 'NONE',  ( 21.00002833972000005, -2.896904163262000065, -9.930905325560999586 ) ) ;
#2863=CARTESIAN_POINT ( 'NONE',  ( -19.84098316496925918, 4.513343901832210570, 9.564988471992716512 ) ) ;
#2864=CARTESIAN_POINT ( 'NONE',  ( 4.888224998722219716, 14.41767836092300215, 3.807294520224770551 ) ) ;
#2868=CARTESIAN_POINT ( 'NONE',  ( -14.64203606142728908, 9.931845001584829191, 2.940492112398142233 ) ) ;
#2870=DIRECTION ( 'NONE',  ( -0.7071067811865969777, 0.7071067811864980568, 2.474839539219989905E-09 ) ) ;
#2877=CARTESIAN_POINT ( 'NONE',  ( 12.02006424930999984, -10.30839584998999925, 1.075033486111000025 ) ) ;
#2879=CARTESIAN_POINT ( 'NONE',  ( -23.20401199359000088, -10.10894130240999900, -3.455853891913000187 ) ) ;
#2880=CARTESIAN_POINT ( 'NONE',  ( -15.62919348333999991, -1.476505563563000001, -10.70629720786000050 ) ) ;
#2881=DIRECTION ( 'NONE',  ( 0.000000000000000000, -1.000000000000000000, 0.000000000000000000 ) ) ;
#2882=CARTESIAN_POINT ( 'NONE',  ( 18.71437451746000136, -4.405870748760999156, -8.778983313941999711 ) ) ;
#2884=B_SPLINE_CURVE_WITH_KNOTS ( 'NONE', 3,
 ( #1185, #5073, #4825, #15938, #2887, #19601, #12211, #3009, #8578, #23333, #14141, #21536, #4949, #12334, #10637, #18024, #8213, #5298 ),
 .UNSPECIFIED., .F., .F.,
 ( 4, 2, 2, 2, 2, 2, 2, 2, 4 ),
 ( 0.000000000000000000, 0.1250000000000000278, 0.2500000000000000555, 0.3750000000000001110, 0.5000000000000001110, 0.6250000000000001110, 0.7500000000000002220, 0.8750000000000001110, 1.000000000000000000 ),
 .UNSPECIFIED. ) ;
#2885=CARTESIAN_POINT ( 'NONE',  ( 20.40736763244999707, -7.483925214229000034, -6.133533836256000349 ) ) ;
#2886=EDGE_CURVE ( 'NONE', #11065, #22774, #5000, .T. ) ;
#2887=CARTESIAN_POINT ( 'NONE',  ( 15.42704166666666055, 7.250625443680725368, -5.572289352991960598 ) ) ;
#2888=ORIENTED_EDGE ( 'NONE', *, *, #15839, .T. ) ;
#2890=CARTESIAN_POINT ( 'NONE',  ( -2.131540934788977548, 13.91340213905352918, 5.742140983464480541 ) ) ;
#2894=AXIS2_PLACEMENT_3D ( 'NONE', #10555, #1346, #17939 ) ;
#2897=DIRECTION ( 'NONE',  ( 0.000000000000000000, -0.9999999999994555466, 1.043416718096953418E-06 ) ) ;
#2898=CARTESIAN_POINT ( 'NONE',  ( 3.297306448684705682, 11.93904864444474789, -3.531362723138341320 ) ) ;
#2902=DIRECTION ( 'NONE',  ( -0.6979779633370118974, 0.000000000000000000, -0.7161192377641567575 ) ) ;
#2903=EDGE_CURVE ( 'NONE', #4084, #5502, #17574, .T. ) ;
#2904=EDGE_CURVE ( 'NONE', #21421, #16694, #861, .T. ) ;
#2905=CARTESIAN_POINT ( 'NONE',  ( -12.33075721169000083, 13.48257539618999878, -7.785259987329999909 ) ) ;
#2907=CARTESIAN_POINT ( 'NONE',  ( 15.69656392131000011, 1.888996749216000026, -9.509257592937000680 ) ) ;
#2908=CARTESIAN_POINT ( 'NONE',  ( 18.93485879530803118, 2.282263698320222911, 10.18192374699490799 ) ) ;
#2913=CARTESIAN_POINT ( 'NONE',  ( -2.531476009669907601, 14.00394004275433524, -5.577390614649326395 ) ) ;
#2921=CARTESIAN_POINT ( 'NONE',  ( 14.61516467955725851, 9.713890784730681460, -3.635657044371410684 ) ) ;
#2922=CARTESIAN_POINT ( 'NONE',  ( -4.414959355983806510, 13.54502321037925228, 5.029880799536921465 ) ) ;
#2926=CARTESIAN_POINT ( 'NONE',  ( 4.143262790852083377, 12.32174769774581868, -2.404817559472536725 ) ) ;
#2930=CARTESIAN_POINT ( 'NONE',  ( -0.5794485495992535151, 12.81494912436375877, 6.641564743694956974 ) ) ;
#2934=EDGE_LOOP ( 'NONE', ( #4494, #13395, #1567, #14429 ) ) ;
#2939=CARTESIAN_POINT ( 'NONE',  ( -19.84656726529999915, 9.357477915406001046, -3.920807637256999989 ) ) ;
#2940=DIRECTION ( 'NONE',  ( -1.000000000000000000, 0.000000000000000000, 0.000000000000000000 ) ) ;
#2941=CARTESIAN_POINT ( 'NONE',  ( 23.99062354302999722, 6.216878364870000340, -12.50000000000000000 ) ) ;
#2942=CARTESIAN_POINT ( 'NONE',  ( 14.90675817089161903, 10.32645797258115472, -0.4027543523436388218 ) ) ;
#2946=DIRECTION ( 'NONE',  ( 0.000000000000000000, 1.000000000000000000, 0.000000000000000000 ) ) ;
#2947=CARTESIAN_POINT ( 'NONE',  ( -3.583888380590997347, 12.05920279233998649, -3.176321221271000361 ) ) ;
#2950=CARTESIAN_POINT ( 'NONE',  ( -6.249999999916000526, 15.09564573669999987, 3.212813967733000098 ) ) ;
#2954=CARTESIAN_POINT ( 'NONE',  ( -17.44374957678954985, -8.022022119424356390, -6.684027340921669946 ) ) ;
#2955=ORIENTED_EDGE ( 'NONE', *, *, #22482, .T. ) ;
#2957=CARTESIAN_POINT ( 'NONE',  ( 5.640389443970001970, 14.19524044333999058, -2.282071340294998585 ) ) ;
#2959=CARTESIAN_POINT ( 'NONE',  ( 24.28455689590321498, 3.990707743056026935, -12.50000000000000000 ) ) ;
#2960=CARTESIAN_POINT ( 'NONE',  ( 13.41956408531000022, -7.835164430201999153, 6.443409769539999665 ) ) ;
#2961=ORIENTED_EDGE ( 'NONE', *, *, #2419, .T. ) ;
#2964=FACE_OUTER_BOUND ( 'NONE', #7028, .T. ) ;
#2965=CARTESIAN_POINT ( 'NONE',  ( -18.13088126894000141, 1.446686056264999920E-14, 0.000000000000000000 ) ) ;
#2966=ORIENTED_EDGE ( 'NONE', *, *, #14275, .T. ) ;
#2967=CARTESIAN_POINT ( 'NONE',  ( 11.59051697470852460, 8.994977951493066115, 9.420063436870602658 ) ) ;
#2969=CARTESIAN_POINT ( 'NONE',  ( -5.340660509843405457, 14.27930097228464135, -5.055472689471347536 ) ) ;
#2970=CARTESIAN_POINT ( 'NONE',  ( 16.59721451432771033, 9.337922582797750337, -4.634226228450162743 ) ) ;
#2971=CARTESIAN_POINT ( 'NONE',  ( -24.50000000000000000, 1.721664336791999924E-14, 0.000000000000000000 ) ) ;
#2972=CARTESIAN_POINT ( 'NONE',  ( -14.48633711635905819, -11.53909476760599873, 5.013715100885081988 ) ) ;
#2974=CARTESIAN_POINT ( 'NONE',  ( -3.889659136885874613, 13.97224236195846636, -4.846263912825002684 ) ) ;
#2975=CARTESIAN_POINT ( 'NONE',  ( 12.52688711657000020, 7.716878364870000340, -11.63397459621999985 ) ) ;
#2979=CARTESIAN_POINT ( 'NONE',  ( 21.38653020683999983, 9.007749467335999682, -5.108484126438000317 ) ) ;
#2980=CARTESIAN_POINT ( 'NONE',  ( 23.44869471829550278, -3.059739909190946960, -10.14852769068212268 ) ) ;
#2981=CONICAL_SURFACE ( 'NONE', #21158, 9.157130689899000586, 0.02565634000431304615 ) ;
#2986=CARTESIAN_POINT ( 'NONE',  ( 4.829988586904999437, 14.79876397742000016, 3.766541904039999888 ) ) ;
#2988=CARTESIAN_POINT ( 'NONE',  ( -3.701981919174000435, 12.09302152519998330, -3.290687922835001000 ) ) ;
#2989=VERTEX_POINT ( 'NONE', #12842 ) ;
#2990=CARTESIAN_POINT ( 'NONE',  ( -16.03759792288471075, -1.727053351349761900, 10.25380015627600905 ) ) ;
#2999=ORIENTED_EDGE ( 'NONE', *, *, #5856, .T. ) ;
#3000=LINE ( 'NONE', #8570, #20563 ) ;
#3001=AXIS2_PLACEMENT_3D ( 'NONE', #15537, #14095, #19433 ) ;
#3002=CARTESIAN_POINT ( 'NONE',  ( -4.517065591395176938, 15.49914285584037899, -4.136658920617758639 ) ) ;
#3003=CARTESIAN_POINT ( 'NONE',  ( -23.04342530862000160, -6.757663101931999705, -8.268912786219999589 ) ) ;
#3004=CARTESIAN_POINT ( 'NONE',  ( -17.86362731101000278, -10.86714433699999915, 0.2447078565204000022 ) ) ;
#3006=CARTESIAN_POINT ( 'NONE',  ( 14.58369494525999954, -9.776545566456000813, -3.069771413624999834 ) ) ;
#3009=CARTESIAN_POINT ( 'NONE',  ( 15.23808333333332676, 2.371926055385309429, -8.826501586951490452 ) ) ;
#3010=VERTEX_POINT ( 'NONE', #7746 ) ;
#3011=CARTESIAN_POINT ( 'NONE',  ( 2.798004395824331247, 14.07234475661186046, 5.448569188702180988 ) ) ;
#3013=CIRCLE ( 'NONE', #12299, 14.43375672973999890 ) ;
#3016=CARTESIAN_POINT ( 'NONE',  ( -20.26481641072999906, 10.68114957034000057, 2.862104170669000247 ) ) ;
#3018=CARTESIAN_POINT ( 'NONE',  ( -4.273318845158264878, 12.24029060234036237, 2.275484052468874197 ) ) ;
#3019=EDGE_LOOP ( 'NONE', ( #12858, #20645, #20176, #19727 ) ) ;
#3021=CARTESIAN_POINT ( 'NONE',  ( 4.519733411219042374, 12.32701741422152431, -1.748064119505302161 ) ) ;
#3022=CARTESIAN_POINT ( 'NONE',  ( -2.460016173531001549, 13.49435256317998366, 5.562971390105002634 ) ) ;
#3023=CARTESIAN_POINT ( 'NONE',  ( -20.48555420454666987, -9.196981408831147675, 1.203755103560655515 ) ) ;
#3024=FACE_OUTER_BOUND ( 'NONE', #17593, .T. ) ;
#3025=EDGE_CURVE ( 'NONE', #12095, #21674, #7227, .T. ) ;
#3026=DIRECTION ( 'NONE',  ( -1.000000000000000000, 0.000000000000000000, 0.000000000000000000 ) ) ;
#3029=CARTESIAN_POINT ( 'NONE',  ( 12.73500142131000068, 5.721315692782000362, 7.730289442163000402 ) ) ;
#3035=DIRECTION ( 'NONE',  ( -1.000000000000000000, 0.000000000000000000, 0.000000000000000000 ) ) ;
#3036=B_SPLINE_CURVE_WITH_KNOTS ( 'NONE', 3,
 ( #23366, #1344, #1588, #18292, #5677, #8970, #23843, #7253, #11017 ),
 .UNSPECIFIED., .F., .F.,
 ( 4, 1, 2, 2, 4 ),
 ( 0.000000000000000000, 0.2499999999999994449, 0.3749999999999993894, 0.4999999999999993339, 1.000000000000000000 ),
 .UNSPECIFIED. ) ;
#3037=ORIENTED_EDGE ( 'NONE', *, *, #13978, .T. ) ;
#3038=EDGE_CURVE ( 'NONE', #3318, #17201, #12428, .T. ) ;
#3041=CARTESIAN_POINT ( 'NONE',  ( -24.50000000000000000, 2.324045842668999493E-14, 12.50000000000000000 ) ) ;
#3042=FACE_OUTER_BOUND ( 'NONE', #13242, .T. ) ;
#3043=CARTESIAN_POINT ( 'NONE',  ( -11.72636993442999831, 14.27363006556999991, 0.000000000000000000 ) ) ;
#3044=CARTESIAN_POINT ( 'NONE',  ( 16.81746331405949135, 5.745323216197852467, 8.703258724007747915 ) ) ;
#3045=CARTESIAN_POINT ( 'NONE',  ( -4.177414563858471652, 13.69652605315409488, 4.902318025240887778 ) ) ;
#3046=DIRECTION ( 'NONE',  ( -1.000000000000000000, 0.000000000000000000, 0.000000000000000000 ) ) ;
#3047=EDGE_CURVE ( 'NONE', #1220, #19976, #1043, .T. ) ;
#3052=CARTESIAN_POINT ( 'NONE',  ( 2.920483249375370960, 11.94533022032288727, -3.796384527241723816 ) ) ;
#3053=ORIENTED_EDGE ( 'NONE', *, *, #7068, .T. ) ;
#3056=CARTESIAN_POINT ( 'NONE',  ( -0.4175917513579801565, 12.80961402668161142, 6.651874616197407164 ) ) ;
#3057=CARTESIAN_POINT ( 'NONE',  ( 6.215921278351865809, 13.80668456282085366, -1.138992957140015250 ) ) ;
#3060=CARTESIAN_POINT ( 'NONE',  ( -6.043487373412999908, 16.34784519966000005, -1.000000006055999924 ) ) ;
#3061=EDGE_CURVE ( 'NONE', #14234, #16706, #3385, .T. ) ;
#3062=ORIENTED_EDGE ( 'NONE', *, *, #12245, .T. ) ;
#3064=TOROIDAL_SURFACE ( 'NONE', #20832, 5.625000000000000000, 0.5000000000000000000 ) ;
#3065=CARTESIAN_POINT ( 'NONE',  ( -14.00000000000000533, -10.15903121243555773, -1.673958311142742073 ) ) ;
#3066=CONICAL_SURFACE ( 'NONE', #20068, 13.23032192316000000, 1.235249617460683957 ) ;
#3069=VERTEX_POINT ( 'NONE', #16942 ) ;
#3070=CARTESIAN_POINT ( 'NONE',  ( -23.93304557145999922, 10.81351501108999891, -3.289488343111999669 ) ) ;
#3072=CARTESIAN_POINT ( 'NONE',  ( 14.97401178964219959, 10.12462245865840949, 2.061518227450690244 ) ) ;
#3073=CONICAL_SURFACE ( 'NONE', #13481, 9.136555860486998526, 0.02565634000431304615 ) ;
#3075=CARTESIAN_POINT ( 'NONE',  ( 13.59694017449214165, 6.847023289163344018, -5.872291703794573436 ) ) ;
#3076=CARTESIAN_POINT ( 'NONE',  ( -4.665938679690996516, 12.51338962337001703, -0.7728731416223998396 ) ) ;
#3077=ORIENTED_EDGE ( 'NONE', *, *, #7041, .T. ) ;
#3081=ORIENTED_EDGE ( 'NONE', *, *, #14325, .T. ) ;
#3082=LINE ( 'NONE', #12280, #14568 ) ;
#3083=CARTESIAN_POINT ( 'NONE',  ( -16.37300014439912133, 3.220437795823801075, 10.06239832674213552 ) ) ;
#3085=ORIENTED_EDGE ( 'NONE', *, *, #18004, .F. ) ;
#3086=CARTESIAN_POINT ( 'NONE',  ( 6.265924793058000652, 13.58761645048999966, -2.214804771343001910 ) ) ;
#3087=CARTESIAN_POINT ( 'NONE',  ( 11.99999999999999822, -1.594904923283001263, -8.836587722619364982 ) ) ;
#3089=CARTESIAN_POINT ( 'NONE',  ( 17.00514426052999895, 0.2856091294997000207, 11.08057831931000159 ) ) ;
#3090=CARTESIAN_POINT ( 'NONE',  ( 13.30987658531000051, -4.885510779899000511, 8.887104416848000454 ) ) ;
#3092=VERTEX_POINT ( 'NONE', #12952 ) ;
#3093=CARTESIAN_POINT ( 'NONE',  ( -9.196381492921000600, -10.96796587088999964, -9.511275453079001352 ) ) ;
#3096=ORIENTED_EDGE ( 'NONE', *, *, #2750, .T. ) ;
#3097=CARTESIAN_POINT ( 'NONE',  ( -23.71548049068999831, -4.708188689841001029, -8.512973244356000890 ) ) ;
#3099=CARTESIAN_POINT ( 'NONE',  ( 22.88230379277824511, -10.58571745970539624, -0.03397870593635089059 ) ) ;
#3100=DIRECTION ( 'NONE',  ( 1.000000000000000000, 0.000000000000000000, 0.000000000000000000 ) ) ;
#3101=VECTOR ( 'NONE', #14379, 1000.000000000000000 ) ;
#3102=CARTESIAN_POINT ( 'NONE',  ( 17.10182080017775519, 2.899594746005321966, 10.01006028584902197 ) ) ;
#3103=VECTOR ( 'NONE', #21801, 1000.000000000000000 ) ;
#3104=CARTESIAN_POINT ( 'NONE',  ( -18.71524577250666965, -2.395516608000527015, 8.913312826780673603 ) ) ;
#3107=CARTESIAN_POINT ( 'NONE',  ( -3.782540744202022243, 14.10894914716129556, -4.859551560401516035 ) ) ;
#3110=ORIENTED_EDGE ( 'NONE', *, *, #20635, .T. ) ;
#3112=CARTESIAN_POINT ( 'NONE',  ( 24.90575349395000160, -9.343402930240999993, -5.725328257854999769 ) ) ;
#3113=CARTESIAN_POINT ( 'NONE',  ( 22.73936012672840690, -4.034463466300610257, 9.782371928200333855 ) ) ;
#3115=ORIENTED_EDGE ( 'NONE', *, *, #168, .T. ) ;
#3116=FACE_OUTER_BOUND ( 'NONE', #11330, .T. ) ;
#3117=CARTESIAN_POINT ( 'NONE',  ( 4.894061048423400173, 14.39961068744026562, 3.811571210762304318 ) ) ;
#3118=CARTESIAN_POINT ( 'NONE',  ( 4.925062053240003124, 12.50686037410001639, -0.5310971773938999441 ) ) ;
#3119=ORIENTED_EDGE ( 'NONE', *, *, #3366, .F. ) ;
#3120=CARTESIAN_POINT ( 'NONE',  ( -14.80950348480317658, 9.924210800638553209, -2.985472924579720910 ) ) ;
#3121=DIRECTION ( 'NONE',  ( -2.945128176746998816E-08, 0.9999999999999996669, -2.371622976689998485E-09 ) ) ;
#3122=ORIENTED_EDGE ( 'NONE', *, *, #23465, .F. ) ;
#3128=CARTESIAN_POINT ( 'NONE',  ( -19.00198616926667228, -2.679675940451125893, 8.823058184319245711 ) ) ;
#3129=CARTESIAN_POINT ( 'NONE',  ( -3.940066807388778791, 14.83395602534511148, -4.689820734438498562 ) ) ;
#3130=CARTESIAN_POINT ( 'NONE',  ( -24.70589367413000303, 9.599129830737000546, 1.290551844122999725 ) ) ;
#3132=CARTESIAN_POINT ( 'NONE',  ( -18.47301835491999711, 5.805793625715000239, 9.209612613527001557 ) ) ;
#3133=CARTESIAN_POINT ( 'NONE',  ( 22.11616666666665409, -8.072809104850792394, -4.652730915293407321 ) ) ;
#3134=CARTESIAN_POINT ( 'NONE',  ( 14.78681994525999954, -5.472050788572000002, -8.670468866855999934 ) ) ;
#3136=FACE_OUTER_BOUND ( 'NONE', #21640, .T. ) ;
#3137=CARTESIAN_POINT ( 'NONE',  ( 5.607952975149999908, 13.81675705620000016, -3.376495290877999711 ) ) ;
#3139=CARTESIAN_POINT ( 'NONE',  ( -17.68897087121334977, 9.125215568721371184, 1.194614872368663372 ) ) ;
#3140=CARTESIAN_POINT ( 'NONE',  ( 0.08622555209230960138, 13.69124592427118969, 6.124469631175590401 ) ) ;
#3147=VERTEX_POINT ( 'NONE', #5459 ) ;
#3148=FACE_OUTER_BOUND ( 'NONE', #6184, .T. ) ;
#3149=CARTESIAN_POINT ( 'NONE',  ( 4.420750779110104389, 12.29170844221592951, -1.979016023043961736 ) ) ;
#3150=CARTESIAN_POINT ( 'NONE',  ( -10.86679200004126677, 15.33979541265035174, 1.708982890173643909 ) ) ;
#3153=CARTESIAN_POINT ( 'NONE',  ( -14.45834475453999879, 5.064797291421999859, 10.11313827054000036 ) ) ;
#3154=CARTESIAN_POINT ( 'NONE',  ( 17.23218892130999791, -6.764005061571999988, -7.001918906472000437 ) ) ;
#3155=CARTESIAN_POINT ( 'NONE',  ( 18.58051607384739867, 10.35305503824381645, 1.237856399541606311 ) ) ;
#3157=VERTEX_POINT ( 'NONE', #15112 ) ;
#3158=CARTESIAN_POINT ( 'NONE',  ( -22.68286091209157362, 7.357512616696472385, 5.643998677357938476 ) ) ;
#3161=CARTESIAN_POINT ( 'NONE',  ( -3.644450799678000230, 14.33206891749000000, -4.922778709793999674 ) ) ;
#3164=FACE_OUTER_BOUND ( 'NONE', #5617, .T. ) ;
#3167=CARTESIAN_POINT ( 'NONE',  ( 15.22846303346806707, -2.020663429760869878, 10.33544534940901194 ) ) ;
#3169=CARTESIAN_POINT ( 'NONE',  ( -3.284923493671003669, 11.90416970545999931, 3.676126646792003960 ) ) ;
#3171=CARTESIAN_POINT ( 'NONE',  ( 20.17074770046333043, -5.646920343229677286, 7.348150695498397056 ) ) ;
#3173=PLANE ( 'NONE',  #2894 ) ;
#3177=CARTESIAN_POINT ( 'NONE',  ( 4.818326428766001257, 14.92945012152000928, 3.793178214860002839 ) ) ;
#3179=CARTESIAN_POINT ( 'NONE',  ( 6.183697154463740020, 13.95082363276063653, -0.7065469572563792822 ) ) ;
#3180=CARTESIAN_POINT ( 'NONE',  ( -5.857053599681002254, 15.76999461102998445, -1.550034662246998929 ) ) ;
#3182=CARTESIAN_POINT ( 'NONE',  ( -6.046837210729000489, 16.30334039894000142, -1.000000000000000000 ) ) ;
#3185=CARTESIAN_POINT ( 'NONE',  ( 13.21250000000000036, 0.000000000000000000, 0.000000000000000000 ) ) ;
#3187=EDGE_CURVE ( 'NONE', #15169, #4052, #6454, .T. ) ;
#3189=CARTESIAN_POINT ( 'NONE',  ( -21.80412305057999944, 10.70889992142000047, -0.5279559311888000206 ) ) ;
#3191=CARTESIAN_POINT ( 'NONE',  ( 15.16527071506006941, 6.736440203948466099, 7.842709918793921098 ) ) ;
#3192=CARTESIAN_POINT ( 'NONE',  ( -12.24999999459000044, 1.554281285377000029E-14, 0.000000000000000000 ) ) ;
#3194=CARTESIAN_POINT ( 'NONE',  ( -22.50811508569069730, -6.110212329431499612, 6.967324166022520693 ) ) ;
#3195=CARTESIAN_POINT ( 'NONE',  ( -3.848016993207002301, 12.29094384469000012, -2.779960707798002417 ) ) ;
#3196=VERTEX_POINT ( 'NONE', #22744 ) ;
#3197=B_SPLINE_CURVE_WITH_KNOTS ( 'NONE', 3,
 ( #21602, #19163, #8398, #8526, #6327, #12277, #13710, #13835, #19666, #12154 ),
 .UNSPECIFIED., .F., .F.,
 ( 4, 2, 2, 2, 4 ),
 ( 0.2414086770563061979, 0.4310565077922296484, 0.6207043385281530989, 0.8103521692640764940, 1.000000000000000000 ),
 .UNSPECIFIED. ) ;
#3198=CARTESIAN_POINT ( 'NONE',  ( 24.25008227645999881, -9.630770167580999797, 0.000000000000000000 ) ) ;
#3205=CARTESIAN_POINT ( 'NONE',  ( 11.12576011241361940, -11.44859199040162068, -5.170472096576233412 ) ) ;
#3206=CARTESIAN_POINT ( 'NONE',  ( -4.814895406027281055, 13.26421056701085099, -5.692049281717411091 ) ) ;
#3207=CARTESIAN_POINT ( 'NONE',  ( 17.76077715286999847, -0.4685653280873000037, -11.09506330460999912 ) ) ;
#3209=CARTESIAN_POINT ( 'NONE',  ( 13.63893908531000143, -10.12407100975999974, -0.7263252697377000633 ) ) ;
#3211=B_SPLINE_CURVE_WITH_KNOTS ( 'NONE', 3,
 ( #9233, #11885, #22646, #849, #17580, #15254, #4375, #6304, #11529, #6056, #11765, #11649, #2550 ),
 .UNSPECIFIED., .F., .F.,
 ( 4, 2, 1, 1, 1, 2, 2, 4 ),
 ( 0.000000000000000000, 0.2500000000000019429, 0.3750000000000021649, 0.4375000000000027200, 0.4687500000000027756, 0.4843750000000025535, 0.5000000000000023315, 1.000000000000000000 ),
 .UNSPECIFIED. ) ;
#3212=CARTESIAN_POINT ( 'NONE',  ( -9.909138992921000977, 9.357018744401999655, 11.09985848640999961 ) ) ;
#3213=CARTESIAN_POINT ( 'NONE',  ( 13.49999999999999822, 8.294162734344720178, -4.272258766888964665 ) ) ;
#3214=LINE ( 'NONE', #17744, #8830 ) ;
#3219=CARTESIAN_POINT ( 'NONE',  ( 11.31235608934058412, 9.572705071893905071, 8.419524251273594828 ) ) ;
#3220=CARTESIAN_POINT ( 'NONE',  ( 22.49991417170085484, -2.603443972844405874, 10.25004708077911708 ) ) ;
#3222=CARTESIAN_POINT ( 'NONE',  ( -4.917862031230266773, 13.52432712154163141, -5.676368724613010563 ) ) ;
#3223=CARTESIAN_POINT ( 'NONE',  ( 16.29049680864105198, 0.4916202364665146485, -10.35987764636037056 ) ) ;
#3224=CARTESIAN_POINT ( 'NONE',  ( 12.00000000000000000, 0.000000000000000000, 1.045589212608000028E-14 ) ) ;
#3226=CARTESIAN_POINT ( 'NONE',  ( 18.62128936713000371, -9.149140698829999252, 0.000000000000000000 ) ) ;
#3230=CARTESIAN_POINT ( 'NONE',  ( 11.45478115326000612, 12.39608915219456442, -3.529209591797321632 ) ) ;
#3235=CARTESIAN_POINT ( 'NONE',  ( -4.954596429287999371, 13.56914355584999754, 5.779622067328999080 ) ) ;
#3236=CARTESIAN_POINT ( 'NONE',  ( 4.911774765700998913, 12.43823212697000535, 0.1548528812091000406 ) ) ;
#3238=CARTESIAN_POINT ( 'NONE',  ( 16.87668875730999929, -8.405545991651999671, -3.781450583054000170 ) ) ;
#3239=ORIENTED_EDGE ( 'NONE', *, *, #17155, .T. ) ;
#3243=LINE ( 'NONE', #10628, #443 ) ;
#3244=CARTESIAN_POINT ( 'NONE',  ( 5.699442596042000098, 1.578914512950999657E-14, 0.000000000000000000 ) ) ;
#3245=CARTESIAN_POINT ( 'NONE',  ( -23.31260609398000128, -6.433678087575999349, -7.872534309770998995 ) ) ;
#3246=CARTESIAN_POINT ( 'NONE',  ( -16.71089566058999765, -1.947775803553999818, 10.11646046336000104 ) ) ;
#3247=CARTESIAN_POINT ( 'NONE',  ( 19.24399999999999977, 9.165120680968000144, 0.000000000000000000 ) ) ;
#3248=CARTESIAN_POINT ( 'NONE',  ( -23.05782846884435955, -10.51579617812587131, -1.069715151266978692 ) ) ;
#3250=CARTESIAN_POINT ( 'NONE',  ( -14.25243324638999809, 13.93375672974000068, 0.8660254037843999608 ) ) ;
#3253=FACE_OUTER_BOUND ( 'NONE', #6502, .T. ) ;
#3256=VECTOR ( 'NONE', #5978, 1000.000000000000000 ) ;
#3259=CARTESIAN_POINT ( 'NONE',  ( -23.75312892322000025, 3.479588606389999672, 10.59591538551999790 ) ) ;
#3260=CARTESIAN_POINT ( 'NONE',  ( -4.747617524593668925, 12.41110054352763292, 0.9834176323472247905 ) ) ;
#3261=EDGE_LOOP ( 'NONE', ( #16125, #20060, #20371, #9649, #15436 ) ) ;
#3264=CARTESIAN_POINT ( 'NONE',  ( -24.37124162822026463, -2.557079873875873322, -12.50000271512792871 ) ) ;
#3265=CARTESIAN_POINT ( 'NONE',  ( -10.29381500303638930, 15.72616211534351471, 1.189143564266787578 ) ) ;
#3266=CARTESIAN_POINT ( 'NONE',  ( 11.82347178278407718, 0.1432880675219483646, -8.999235042547903518 ) ) ;
#3271=CARTESIAN_POINT ( 'NONE',  ( 16.46437642130999990, 2.740937500800999960, 9.320585551182000827 ) ) ;
#3272=CARTESIAN_POINT ( 'NONE',  ( 18.59037132503243228, 10.30267188619290408, 1.600077239284419806 ) ) ;
#3274=CARTESIAN_POINT ( 'NONE',  ( -22.56945280195751735, 4.659483922790810695, 8.084632350547995117 ) ) ;
#3276=CONICAL_SURFACE ( 'NONE', #23355, 9.161549281532000322, 0.02565634000431304615 ) ;
#3278=CARTESIAN_POINT ( 'NONE',  ( 0.000000000000000000, -7.216878364870000340, -12.50000000000000000 ) ) ;
#3279=PLANE ( 'NONE',  #2319 ) ;
#3280=ORIENTED_EDGE ( 'NONE', *, *, #6602, .T. ) ;
#3281=DIRECTION ( 'NONE',  ( 0.000000000000000000, 0.000000000000000000, -1.000000000000000000 ) ) ;
#3282=CARTESIAN_POINT ( 'NONE',  ( -24.24003052285332416, -12.62002563673716082, 3.141177558950714488 ) ) ;
#3283=CARTESIAN_POINT ( 'NONE',  ( 16.48520833333332547, -9.094324649508100933, 1.190571260499372785 ) ) ;
#3285=CARTESIAN_POINT ( 'NONE',  ( 14.11337511726693528, -5.197435860462716661, -8.961902679360624902 ) ) ;
#3287=CARTESIAN_POINT ( 'NONE',  ( -4.927853318462999788, 12.50793478510998646, 0.4287087720616001296 ) ) ;
#3288=CARTESIAN_POINT ( 'NONE',  ( 23.99062354302999722, 13.93375672974000068, -0.8660254037843999608 ) ) ;
#3289=EDGE_LOOP ( 'NONE', ( #18203, #18809 ) ) ;
#3292=EDGE_LOOP ( 'NONE', ( #8266, #3711, #23634, #7882 ) ) ;
#3296=CARTESIAN_POINT ( 'NONE',  ( 11.36448692216918310, 2.758025466607516130, -12.49997558795211994 ) ) ;
#3299=LINE ( 'NONE', #5001, #8636 ) ;
#3300=ORIENTED_EDGE ( 'NONE', *, *, #7355, .F. ) ;
#3302=VECTOR ( 'NONE', #15662, 1000.000000000000000 ) ;
#3307=CARTESIAN_POINT ( 'NONE',  ( -22.83232346421999992, -9.588805902508001466, 4.859514279198000608 ) ) ;
#3308=CARTESIAN_POINT ( 'NONE',  ( 20.45333333333332249, -4.631475266059001505, -8.035426097018820712 ) ) ;
#3309=CARTESIAN_POINT ( 'NONE',  ( 14.54181763333886224, 2.757009540540801940, -9.946943164393594827 ) ) ;
#3312=CARTESIAN_POINT ( 'NONE',  ( 18.61948385635999870, 2.167412405366000439, 10.19942539954999994 ) ) ;
#3315=CARTESIAN_POINT ( 'NONE',  ( 4.156984850324001890, 12.39561475064999385, -2.315346335006999823 ) ) ;
#3318=VERTEX_POINT ( 'NONE', #23474 ) ;
#3319=CARTESIAN_POINT ( 'NONE',  ( -6.045495691042000352, 16.31816057295000277, 1.000000020649999932 ) ) ;
#3321=FACE_OUTER_BOUND ( 'NONE', #21911, .T. ) ;
#3322=EDGE_LOOP ( 'NONE', ( #601, #9624, #5976 ) ) ;
#3323=B_SPLINE_CURVE_WITH_KNOTS ( 'NONE', 3,
 ( #3247, #17413, #807, #12564, #21882, #14827, #8820, #61, #7100, #3371, #5522, #14490, #8933, #16180, #20301, #22221, #23692, #14604 ),
 .UNSPECIFIED., .F., .F.,
 ( 4, 2, 2, 2, 2, 2, 2, 2, 4 ),
 ( 0.000000000000000000, 0.1250000000000000278, 0.2500000000000000555, 0.3750000000000001110, 0.5000000000000001110, 0.6250000000000001110, 0.7500000000000002220, 0.8750000000000001110, 1.000000000000000000 ),
 .UNSPECIFIED. ) ;
#3324=EDGE_CURVE ( 'NONE', #8938, #93, #23943, .T. ) ;
#3326=CARTESIAN_POINT ( 'NONE',  ( 11.07373617191559845, -11.07537056389462649, -5.816824279993104696 ) ) ;
#3328=ADVANCED_BREP_SHAPE_REPRESENTATION ( '', ( #872, #4390 ), #7088 ) ;
#3329=CARTESIAN_POINT ( 'NONE',  ( 13.12920410816999883, 3.893241004392999915, 9.759185651010000129 ) ) ;
#3330=ORIENTED_EDGE ( 'NONE', *, *, #15329, .F. ) ;
#3332=CARTESIAN_POINT ( 'NONE',  ( 13.50000000000000000, 7.504433909277588022, 6.535239850074254342 ) ) ;
#3336=EDGE_CURVE ( 'NONE', #12931, #3365, #10140, .T. ) ;
#3338=CARTESIAN_POINT ( 'NONE',  ( 23.20586424138126702, -4.586665969535743237, -9.551222875646683264 ) ) ;
#3340=CARTESIAN_POINT ( 'NONE',  ( -14.00000000000000000, 5.799910849219894082, 7.344702494732569420 ) ) ;
#3341=CARTESIAN_POINT ( 'NONE',  ( 17.66124667370037571, -10.36187076387821726, -0.9006624543728345422 ) ) ;
#3342=CARTESIAN_POINT ( 'NONE',  ( -17.18218939125000233, -9.729142757502000194, -5.298450458072998970 ) ) ;
#3344=B_SPLINE_CURVE_WITH_KNOTS ( 'NONE', 3,
 ( #14337, #11050, #1727, #5363, #9230, #1843, #16608, #9114, #19, #8891, #3551, #9003 ),
 .UNSPECIFIED., .F., .F.,
 ( 4, 1, 1, 1, 1, 2, 2, 4 ),
 ( 0.000000000000000000, 0.2500000000000002220, 0.3750000000000003331, 0.4375000000000003886, 0.4687500000000004441, 0.4843750000000004441, 0.5000000000000004441, 1.000000000000000000 ),
 .UNSPECIFIED. ) ;
#3346=CARTESIAN_POINT ( 'NONE',  ( -15.14859190273999801, -7.578844389069999465, 6.091136938512000221 ) ) ;
#3349=CARTESIAN_POINT ( 'NONE',  ( 11.36448692217191336, 12.20430913916406723, -3.861467675590581017 ) ) ;
#3350=CARTESIAN_POINT ( 'NONE',  ( 23.25008103265993853, -8.808711889959772279, -5.889380441415137390 ) ) ;
#3355=CARTESIAN_POINT ( 'NONE',  ( 4.853323543749686664, 14.55746228791980812, -3.781984119402277855 ) ) ;
#3357=CIRCLE ( 'NONE', #599, 12.50000000000000178 ) ;
#3358=CARTESIAN_POINT ( 'NONE',  ( -0.6021973048112005955, 11.45120988776001347, -4.827765333209999454 ) ) ;
#3360=CARTESIAN_POINT ( 'NONE',  ( 16.10887625731000128, 5.681759715831000257, 7.231772086132999711 ) ) ;
#3365=VERTEX_POINT ( 'NONE', #5779 ) ;
#3366=EDGE_CURVE ( 'NONE', #9620, #7062, #596, .T. ) ;
#3367=DIRECTION ( 'NONE',  ( 0.9996708941621513800, -0.02565352539212875996, 0.000000000000000000 ) ) ;
#3369=CARTESIAN_POINT ( 'NONE',  ( -19.83169160925000085, -8.995645751853000860, 5.591779661146000002 ) ) ;
#3370=CARTESIAN_POINT ( 'NONE',  ( -14.94877296625000085, -7.864110397542998676, 5.708624538612000698 ) ) ;
#3371=CARTESIAN_POINT ( 'NONE',  ( 18.75270833333332376, -1.198188119826038678, -9.152513168516252406 ) ) ;
#3372=CARTESIAN_POINT ( 'NONE',  ( -23.77841198977664661, 7.775167525423574588, 7.193020863907117146 ) ) ;
#3378=DIRECTION ( 'NONE',  ( 0.000000000000000000, -0.8660254037844288266, 0.5000000000000169864 ) ) ;
#3380=CARTESIAN_POINT ( 'NONE',  ( 5.836855219999685929, 14.45009295325265697, -1.856713035812031620 ) ) ;
#3383=CARTESIAN_POINT ( 'NONE',  ( 3.731864964225694692, 12.06477785729058283, 3.073113330803231236 ) ) ;
#3385=CIRCLE ( 'NONE', #7608, 7.000000000000000000 ) ;
#3386=CARTESIAN_POINT ( 'NONE',  ( 3.623732334858088322, 12.03139012425049970, -3.204893096957067922 ) ) ;
#3387=CARTESIAN_POINT ( 'NONE',  ( -10.05747503393159903, 16.19757463933138553, 1.000000000003420819 ) ) ;
#3390=VERTEX_POINT ( 'NONE', #11242 ) ;
#3392=CARTESIAN_POINT ( 'NONE',  ( -16.21509587121331819, 4.576700897026971582, -7.940391755668851914 ) ) ;
#3393=CARTESIAN_POINT ( 'NONE',  ( 18.10968892130999919, 7.460570333748000493, 6.290326521484000288 ) ) ;
#3394=CARTESIAN_POINT ( 'NONE',  ( 18.58888770137535573, 10.31100517592262555, 1.545193600490515573 ) ) ;
#3396=EDGE_LOOP ( 'NONE', ( #12792, #9859, #16166, #20728 ) ) ;
#3399=FACE_OUTER_BOUND ( 'NONE', #494, .T. ) ;
#3400=DIRECTION ( 'NONE',  ( 0.000000000000000000, 0.5000000000000169864, -0.8660254037844288266 ) ) ;
#3404=CARTESIAN_POINT ( 'NONE',  ( 24.37377967401999612, 0.3913942306882999822, 11.36483370893999911 ) ) ;
#3408=CARTESIAN_POINT ( 'NONE',  ( -3.748176061208841947, 14.15044768785049101, 4.861384448517857670 ) ) ;
#3409=CARTESIAN_POINT ( 'NONE',  ( -12.25000000000000000, 12.86886241750721105, -7.894071469735785662 ) ) ;
#3411=CARTESIAN_POINT ( 'NONE',  ( -19.30323503384000361, -9.318276757531000598, 5.904625933860000231 ) ) ;
#3414=DIRECTION ( 'NONE',  ( -1.000000000000000000, 0.000000000000000000, 0.000000000000000000 ) ) ;
#3415=ORIENTED_EDGE ( 'NONE', *, *, #13696, .T. ) ;
#3418=CARTESIAN_POINT ( 'NONE',  ( 11.92450592358142636, 4.711271677195460583, -12.50004466714985618 ) ) ;
#3421=CARTESIAN_POINT ( 'NONE',  ( 19.24399999999999977, 9.165120680968000144, 0.000000000000000000 ) ) ;
#3426=DIRECTION ( 'NONE',  ( -0.3292854386466978478, 0.9442304273297127404, 0.000000000000000000 ) ) ;
#3427=CARTESIAN_POINT ( 'NONE',  ( 11.00000000000000000, -10.59999999999999964, 0.000000000000000000 ) ) ;
#3428=EDGE_LOOP ( 'NONE', ( #8749, #10212 ) ) ;
#3429=CARTESIAN_POINT ( 'NONE',  ( -10.64917158021815879, 15.44101125622223947, -1.507928438456294096 ) ) ;
#3431=CARTESIAN_POINT ( 'NONE',  ( 14.44670397028254172, -0.5670727829898102312, -10.31211031097369002 ) ) ;
#3433=CARTESIAN_POINT ( 'NONE',  ( 20.82204741195999986, -10.17246175326000035, 4.719653495980000280 ) ) ;
#3434=ADVANCED_FACE ( 'NONE', ( #9178 ), #23470, .T. ) ;
#3437=CARTESIAN_POINT ( 'NONE',  ( 4.701265373510000956, 12.59995792350999189, -1.092434317656999054 ) ) ;
#3438=CARTESIAN_POINT ( 'NONE',  ( -22.11059587121331305, -8.072587028924724351, -4.652893487818362317 ) ) ;
#3444=CARTESIAN_POINT ( 'NONE',  ( 16.59858333333331970, -8.860506003517219398, -2.381064488431900994 ) ) ;
#3448=CARTESIAN_POINT ( 'NONE',  ( 18.26830054543999893, 10.39455046184000153, -3.947462618599999917 ) ) ;
#3450=CARTESIAN_POINT ( 'NONE',  ( -9.290830065846000352, -6.196630076247999774, -13.51516600793999956 ) ) ;
#3451=AXIS2_PLACEMENT_3D ( 'NONE', #3986, #17426, #10160 ) ;
#3452=CARTESIAN_POINT ( 'NONE',  ( 13.50000000000000000, 9.141558265356509949, -2.348328869579741518 ) ) ;
#3453=CARTESIAN_POINT ( 'NONE',  ( -14.41332674684390369, -12.63239273137551777, -3.119888754839689415 ) ) ;
#3456=CARTESIAN_POINT ( 'NONE',  ( 20.64679523879173928, -1.188210788644911142, 10.46129133059315564 ) ) ;
#3458=CARTESIAN_POINT ( 'NONE',  ( 16.10203026881945121, -5.935666563581813548, -8.493690021681720381 ) ) ;
#3463=CARTESIAN_POINT ( 'NONE',  ( -14.53920085882999835, -1.325901587985999885, -9.615240848067001522 ) ) ;
#3465=ORIENTED_EDGE ( 'NONE', *, *, #1684, .T. ) ;
#3466=CARTESIAN_POINT ( 'NONE',  ( 21.20719740893701655, -10.32741046810345509, 2.129377785346741714 ) ) ;
#3468=ORIENTED_EDGE ( 'NONE', *, *, #23142, .T. ) ;
#3469=CARTESIAN_POINT ( 'NONE',  ( 12.52688711657000020, 6.216878364870000340, 12.50000000000000000 ) ) ;
#3470=CARTESIAN_POINT ( 'NONE',  ( 4.855310581006569315, 14.54728511032672422, -3.783400810746735399 ) ) ;
#3472=CARTESIAN_POINT ( 'NONE',  ( 1.394400747533001361, 11.57446794508000742, -4.613298798923998412 ) ) ;
#3475=CARTESIAN_POINT ( 'NONE',  ( 12.50897833293000083, -6.466896515026999914, -12.35565195369999891 ) ) ;
#3476=ORIENTED_EDGE ( 'NONE', *, *, #10113, .F. ) ;
#3482=CARTESIAN_POINT ( 'NONE',  ( -10.04701370327999932, 16.31160201366999729, -1.000000000000000000 ) ) ;
#3483=CARTESIAN_POINT ( 'NONE',  ( -24.11553951883000124, 3.250485078146000184, 9.656343706050000364 ) ) ;
#3484=ADVANCED_FACE ( 'NONE', ( #23947 ), #8790, .F. ) ;
#3485=CARTESIAN_POINT ( 'NONE',  ( 12.52688711657000020, -7.716878364870000340, -11.63397459621999985 ) ) ;
#3486=CARTESIAN_POINT ( 'NONE',  ( -6.294318966394004455, 15.05816953584999851, -3.444806853728002327 ) ) ;
#3487=ADVANCED_FACE ( 'NONE', ( #312 ), #22019, .T. ) ;
#3488=CARTESIAN_POINT ( 'NONE',  ( -24.29311450473293021, 5.407626218985153166, -9.123098698783515204 ) ) ;
#3500=DIRECTION ( 'NONE',  ( -1.000000000000000000, 0.000000000000000000, 0.000000000000000000 ) ) ;
#3501=ORIENTED_EDGE ( 'NONE', *, *, #10008, .F. ) ;
#3502=CARTESIAN_POINT ( 'NONE',  ( -4.040251331918567779, 12.16185153434827093, -2.666099664634059341 ) ) ;
#3503=CARTESIAN_POINT ( 'NONE',  ( 24.13033325080091274, -0.1217589085045256286, -9.517347760093475273 ) ) ;
#3505=ORIENTED_EDGE ( 'NONE', *, *, #15253, .F. ) ;
#3508=B_SPLINE_CURVE_WITH_KNOTS ( 'NONE', 3,
 ( #15476, #17176, #21177, #2651, #19237, #22860, #15590, #21052, #13777, #22503, #11982, #4104, #5913, #11503, #17915, #8468, #8587, #17669 ),
 .UNSPECIFIED., .F., .F.,
 ( 4, 2, 2, 2, 2, 2, 2, 2, 4 ),
 ( 0.000000000000000000, 0.1250000000000000278, 0.2500000000000000555, 0.3750000000000001110, 0.5000000000000001110, 0.6250000000000001110, 0.7500000000000002220, 0.8750000000000002220, 1.000000000000000000 ),
 .UNSPECIFIED. ) ;
#3509=CARTESIAN_POINT ( 'NONE',  ( 11.74781392131000146, -7.601052271439000307, -5.849495945765999849 ) ) ;
#3510=CARTESIAN_POINT ( 'NONE',  ( 18.81959018942939466, 6.044305804050750019, 8.501725326887493495 ) ) ;
#3514=CARTESIAN_POINT ( 'NONE',  ( 17.08796080085999947, 1.565451709191000074, 11.28839175225999902 ) ) ;
#3515=CARTESIAN_POINT ( 'NONE',  ( 13.50000000000000355, -9.490788312992085807, -1.343451305609774993 ) ) ;
#3517=CARTESIAN_POINT ( 'NONE',  ( -23.99212502904700983, 13.39645431917582030, 1.796660477929257427 ) ) ;
#3518=CARTESIAN_POINT ( 'NONE',  ( 21.18689583523000053, -11.25120934773000059, 0.8723638986538000406 ) ) ;
#3521=DIRECTION ( 'NONE',  ( 1.000000000000000000, 0.000000000000000000, 0.000000000000000000 ) ) ;
#3522=CARTESIAN_POINT ( 'NONE',  ( 1.673502882357000177, 11.64651242530998410, 4.674820881733997346 ) ) ;
#3530=CARTESIAN_POINT ( 'NONE',  ( 6.598144805745005392, 13.50878560842000020, 0.7964734107506996619 ) ) ;
#3531=CARTESIAN_POINT ( 'NONE',  ( 11.97297107870701893, 4.846971342257544002, -12.50004942866563340 ) ) ;
#3533=CARTESIAN_POINT ( 'NONE',  ( 13.50000000000000355, -0.4765265073848649058, 10.29322485242600571 ) ) ;
#3534=EDGE_LOOP ( 'NONE', ( #15704, #13656, #6150, #14286 ) ) ;
#3535=CARTESIAN_POINT ( 'NONE',  ( -16.16424364259000157, 4.823843515939000071, -8.474820356344999084 ) ) ;
#3536=VECTOR ( 'NONE', #7475, 1000.000000000000114 ) ;
#3539=ORIENTED_EDGE ( 'NONE', *, *, #12093, .F. ) ;
#3542=CARTESIAN_POINT ( 'NONE',  ( 14.43179268012507954, -1.084526859950961875, -10.26172237758129846 ) ) ;
#3543=CARTESIAN_POINT ( 'NONE',  ( 0.000000000000000000, 22.00000000000000000, 0.000000000000000000 ) ) ;
#3544=CARTESIAN_POINT ( 'NONE',  ( 20.01400882793000235, 5.003195029065000021, -10.01125156252000004 ) ) ;
#3546=CARTESIAN_POINT ( 'NONE',  ( 13.69548965135293450, 8.444355585795914720, -3.174683004369278194 ) ) ;
#3549=ORIENTED_EDGE ( 'NONE', *, *, #5216, .F. ) ;
#3550=CARTESIAN_POINT ( 'NONE',  ( -14.89767593716247163, -8.438677071178334543, -3.297102474276865092 ) ) ;
#3551=CARTESIAN_POINT ( 'NONE',  ( 24.50000000000000711, -9.325532229573614273, 5.118943956174335952 ) ) ;
#3553=CARTESIAN_POINT ( 'NONE',  ( 19.51605026741271232, -1.735679401533887001, 9.439139126610488262 ) ) ;
#3556=CARTESIAN_POINT ( 'NONE',  ( 15.23446458303000028, -6.520685359936000403, 8.903299142152000911 ) ) ;
#3557=CARTESIAN_POINT ( 'NONE',  ( -14.30710121467889273, 1.268344841054370065, 10.26973291966113599 ) ) ;
#3561=CARTESIAN_POINT ( 'NONE',  ( -8.917480899178999110, 13.20694165471999959, -6.150971466210000571 ) ) ;
#3563=CARTESIAN_POINT ( 'NONE',  ( -14.25243324638999809, -6.216878364870000340, 12.50000000000000000 ) ) ;
#3564=ORIENTED_EDGE ( 'NONE', *, *, #20949, .T. ) ;
#3565=CARTESIAN_POINT ( 'NONE',  ( 22.85288920654172173, -10.53285308750527705, 1.051356703202095844 ) ) ;
#3567=CARTESIAN_POINT ( 'NONE',  ( 15.97156973469264152, -9.031727242954262991, -5.071998056861781734 ) ) ;
#3568=CARTESIAN_POINT ( 'NONE',  ( -17.72417933634999798, -2.118794415358999927, 10.88897014444000177 ) ) ;
#3569=AXIS2_PLACEMENT_3D ( 'NONE', #19879, #12610, #17944 ) ;
#3575=CARTESIAN_POINT ( 'NONE',  ( 21.12207725794927526, -9.259445203091740240, 5.038593002177021773 ) ) ;
#3579=CARTESIAN_POINT ( 'NONE',  ( 13.21250000000000036, 0.000000000000000000, 0.000000000000000000 ) ) ;
#3580=CARTESIAN_POINT ( 'NONE',  ( 4.871792852526525053, 14.47489112828897362, -3.795289058065452803 ) ) ;
#3581=CARTESIAN_POINT ( 'NONE',  ( -2.718451692004000275, 11.82335083566999323, -3.948280308763997493 ) ) ;
#3584=CARTESIAN_POINT ( 'NONE',  ( 11.39231375731000107, -8.729484032481000355, -2.472142458034000345 ) ) ;
#3586=CIRCLE ( 'NONE', #10935, 12.50000000000000178 ) ;
#3590=VERTEX_POINT ( 'NONE', #19711 ) ;
#3591=DIRECTION ( 'NONE',  ( 0.000000000000000000, 0.5000000000000169864, -0.8660254037844288266 ) ) ;
#3592=CARTESIAN_POINT ( 'NONE',  ( -20.42204576454999909, 0.9856272077188000802, 10.04066030219000005 ) ) ;
#3594=CARTESIAN_POINT ( 'NONE',  ( -16.57381575000999874, -9.759477557600000353, -0.2595777249469000125 ) ) ;
#3595=CARTESIAN_POINT ( 'NONE',  ( -5.431150319964994644, 14.88403208498999142, -3.316913632744003415 ) ) ;
#3596=CARTESIAN_POINT ( 'NONE',  ( -22.28577469641619402, 9.959647916863344719, -3.842436443305321081 ) ) ;
#3601=CARTESIAN_POINT ( 'NONE',  ( 23.75578739169031550, -4.482660184358483235, 8.204279979722965521 ) ) ;
#3602=DIRECTION ( 'NONE',  ( 0.000000000000000000, -1.000000000000000000, 0.000000000000000000 ) ) ;
#3603=CARTESIAN_POINT ( 'NONE',  ( 13.71789754803960193, 2.629260093309664814, -8.685948811178583640 ) ) ;
#3604=EDGE_CURVE ( 'NONE', #1114, #12621, #21520, .T. ) ;
#3606=CARTESIAN_POINT ( 'NONE',  ( 3.022862379614798645, 11.86775895167101247, 3.763016671309872496 ) ) ;
#3609=CARTESIAN_POINT ( 'NONE',  ( -3.943681128674290992, 12.13065354962336428, -2.803234342281037961 ) ) ;
#3610=CARTESIAN_POINT ( 'NONE',  ( -10.30414807049024972, 15.71393056377423036, 1.198114258386445696 ) ) ;
#3612=ORIENTED_EDGE ( 'NONE', *, *, #16285, .T. ) ;
#3613=CARTESIAN_POINT ( 'NONE',  ( 24.00034722001000276, -7.216970193741999218, 11.92259671338999993 ) ) ;
#3614=CARTESIAN_POINT ( 'NONE',  ( -18.13088126894000141, 1.446686056264999920E-14, 0.000000000000000000 ) ) ;
#3616=CARTESIAN_POINT ( 'NONE',  ( 16.38112658530999610, 10.11489150981000051, 1.477102707085000022 ) ) ;
#3617=CARTESIAN_POINT ( 'NONE',  ( 18.52789202429464410, 10.40670619203928915, -0.6213187097667132175 ) ) ;
#3618=EDGE_CURVE ( 'NONE', #5775, #12558, #17583, .T. ) ;
#3621=CARTESIAN_POINT ( 'NONE',  ( -12.49883338062999805, 6.877492854395000244, -5.798745594989999752 ) ) ;
#3622=CARTESIAN_POINT ( 'NONE',  ( 13.49999999999999645, -8.661498127773935352, -3.738203993960828253 ) ) ;
#3623=ORIENTED_EDGE ( 'NONE', *, *, #11153, .T. ) ;
#3626=CARTESIAN_POINT ( 'NONE',  ( 18.94427387461000123, -0.06533020399979999615, 10.75972831271999830 ) ) ;
#3627=CARTESIAN_POINT ( 'NONE',  ( -24.20872234573575099, 9.568575771055293444, 3.051701187166265594 ) ) ;
#3628=CARTESIAN_POINT ( 'NONE',  ( 13.94611192983668246, -9.250779629793038694, -4.651112269942151656 ) ) ;
#3630=CARTESIAN_POINT ( 'NONE',  ( -12.25000000000000000, 6.613190111079999767, -13.46349570337000046 ) ) ;
#3632=CARTESIAN_POINT ( 'NONE',  ( -21.97658776632000155, 10.22865322212999928, -4.322346676424000833 ) ) ;
#3636=EDGE_CURVE ( 'NONE', #12346, #1991, #18352, .T. ) ;
#3638=CARTESIAN_POINT ( 'NONE',  ( 11.45478115325884083, 3.141659414319641463, -12.49993290927501199 ) ) ;
#3639=EDGE_CURVE ( 'NONE', #23059, #12621, #11389, .T. ) ;
#3641=CARTESIAN_POINT ( 'NONE',  ( 23.99478584076000232, -13.93375672974000068, -0.6736217020456000126 ) ) ;
#3642=CARTESIAN_POINT ( 'NONE',  ( 18.05287674931000197, 3.913226583351999910, -10.03953908883999979 ) ) ;
#3645=CARTESIAN_POINT ( 'NONE',  ( -13.32041877100999905, -7.827390682981001824, 5.681961735881999154 ) ) ;
#3650=DIRECTION ( 'NONE',  ( -1.000000000000000000, 0.000000000000000000, 2.461955262174999944E-13 ) ) ;
#3651=EDGE_CURVE ( 'NONE', #9820, #21250, #4659, .T. ) ;
#3653=CARTESIAN_POINT ( 'NONE',  ( 14.53584632513973851, 2.541295010820454614, -10.00545943804216620 ) ) ;
#3654=CARTESIAN_POINT ( 'NONE',  ( -18.59597087121333558, -9.148490976324819002, -1.197661616099367166 ) ) ;
#3655=CARTESIAN_POINT ( 'NONE',  ( 23.64802272119000293, -0.2661318661629999971, -11.28844956766999985 ) ) ;
#3657=CARTESIAN_POINT ( 'NONE',  ( 13.61354498824686843, 7.183912508121929719, -5.456131416217646191 ) ) ;
#3658=CARTESIAN_POINT ( 'NONE',  ( -2.712275836624000291, 11.98432359369998856, -3.994273073785000072 ) ) ;
#3659=CARTESIAN_POINT ( 'NONE',  ( -21.39255420454665213, 9.220256816434664771, -1.206801847291320229 ) ) ;
#3660=ORIENTED_EDGE ( 'NONE', *, *, #15591, .T. ) ;
#3662=EDGE_LOOP ( 'NONE', ( #11373, #8035, #6815, #21382, #13079, #9124, #18751, #10439 ) ) ;
#3664=CARTESIAN_POINT ( 'NONE',  ( 11.29022434644324235, -12.01543594605075782, -4.188602139406581770 ) ) ;
#3665=DIRECTION ( 'NONE',  ( -1.000000000000000000, 0.000000000000000000, 0.000000000000000000 ) ) ;
#3667=CARTESIAN_POINT ( 'NONE',  ( 13.39612630362000090, -0.4383194471242999879, 10.97614716848999983 ) ) ;
#3672=CARTESIAN_POINT ( 'NONE',  ( -9.792568638769999723, -15.07240962404999962, 2.103107733322999717 ) ) ;
#3675=ORIENTED_EDGE ( 'NONE', *, *, #11768, .T. ) ;
#3676=CARTESIAN_POINT ( 'NONE',  ( -4.927443545268737068, 15.82417552330234223, -3.638606983025983510 ) ) ;
#3677=CARTESIAN_POINT ( 'NONE',  ( 20.20557644524101804, 10.39545583923814753, 1.631852776342430866 ) ) ;
#3678=CARTESIAN_POINT ( 'NONE',  ( 24.28255857085268943, 8.769700062105057370, -9.810433925293667201 ) ) ;
#3679=CARTESIAN_POINT ( 'NONE',  ( 16.11492084001121228, -5.561606119988664609, -8.744802779703126916 ) ) ;
#3680=CARTESIAN_POINT ( 'NONE',  ( -15.34151452278999983, -5.012687067889999959, -9.822839049446999482 ) ) ;
#3687=CARTESIAN_POINT ( 'NONE',  ( 20.61135635202220939, 6.753515711663456322, 8.075049422923598286 ) ) ;
#3690=CARTESIAN_POINT ( 'NONE',  ( 24.28455689590299826, -3.990707743057282819, 12.50000000000000355 ) ) ;
#3691=CARTESIAN_POINT ( 'NONE',  ( 5.065664929567285313, 14.06852716411717630, -3.939930271556426167 ) ) ;
#3692=CARTESIAN_POINT ( 'NONE',  ( 4.776902136988002923, 12.47834512453000144, 0.1510561884015998724 ) ) ;
#3693=CARTESIAN_POINT ( 'NONE',  ( 11.50200125730999900, -7.192471199227000511, -5.535041905695000430 ) ) ;
#3694=ORIENTED_EDGE ( 'NONE', *, *, #18513, .F. ) ;
#3698=CARTESIAN_POINT ( 'NONE',  ( -14.33281117768507507, 5.151946275820663779, -12.49999999999962874 ) ) ;
#3700=CARTESIAN_POINT ( 'NONE',  ( -15.91276253787999728, 9.079634562165001199, 0.000000000000000000 ) ) ;
#3701=CARTESIAN_POINT ( 'NONE',  ( -24.22413361922000163, -2.219501623213000485, 9.414378356634001577 ) ) ;
#3702=CARTESIAN_POINT ( 'NONE',  ( -15.15190331421999836, -2.304711170240999696, 9.446210836873998318 ) ) ;
#3703=DIRECTION ( 'NONE',  ( 0.000000000000000000, 1.000000000000000000, 0.000000000000000000 ) ) ;
#3704=CARTESIAN_POINT ( 'NONE',  ( -22.59459620538663316, 1.415938697088058307, -10.58759565406335135 ) ) ;
#3709=AXIS2_PLACEMENT_3D ( 'NONE', #21622, #3100, #17989 ) ;
#3711=ORIENTED_EDGE ( 'NONE', *, *, #4507, .F. ) ;
#3714=CARTESIAN_POINT ( 'NONE',  ( 4.436745834877500627, 13.45903375662160073, -5.214346380604272468 ) ) ;
#3715=AXIS2_PLACEMENT_3D ( 'NONE', #11917, #23037, #19302 ) ;
#3716=CARTESIAN_POINT ( 'NONE',  ( -21.82243491649035505, 9.089534782749435493, 5.598433407583303989 ) ) ;
#3721=CARTESIAN_POINT ( 'NONE',  ( -4.658304025590487285, 12.37774214680684892, -1.339611838526547416 ) ) ;
#3723=CARTESIAN_POINT ( 'NONE',  ( -24.12232999016000079, 1.520060141252000183E-14, 0.000000000000000000 ) ) ;
#3726=CARTESIAN_POINT ( 'NONE',  ( 23.99062354302999722, -7.716878364870000340, 11.63397459621999985 ) ) ;
#3727=AXIS2_PLACEMENT_3D ( 'NONE', #22979, #2522, #15350 ) ;
#3729=CARTESIAN_POINT ( 'NONE',  ( 14.18737658531000001, 3.962519675866999602, -9.360324180111000203 ) ) ;
#3730=CARTESIAN_POINT ( 'NONE',  ( 18.25830969247345337, 5.725820681186363004, -8.709654033915940730 ) ) ;
#3734=FACE_OUTER_BOUND ( 'NONE', #23498, .T. ) ;
#3737=CARTESIAN_POINT ( 'NONE',  ( 24.64508424622000149, 0.3734825580707000214, 10.84342182217999984 ) ) ;
#3738=EDGE_CURVE ( 'NONE', #21095, #4782, #17080, .T. ) ;
#3740=VERTEX_POINT ( 'NONE', #7438 ) ;
#3741=DIRECTION ( 'NONE',  ( 0.000000000000000000, 0.9899013191676121481, -0.1417581684074016302 ) ) ;
#3742=CARTESIAN_POINT ( 'NONE',  ( -23.74465998031000069, 6.216878364870000340, -12.50000000000000000 ) ) ;
#3743=CARTESIAN_POINT ( 'NONE',  ( 1.673168206979000594, 11.57251234639000970, 4.644218459094000551 ) ) ;
#3744=AXIS2_PLACEMENT_3D ( 'NONE', #15710, #9917, #2780 ) ;
#3748=AXIS2_PLACEMENT_3D ( 'NONE', #15505, #2436, #4498 ) ;
#3749=DIRECTION ( 'NONE',  ( 0.000000000000000000, 6.254606381427999609E-11, 1.000000000000000000 ) ) ;
#3750=ORIENTED_EDGE ( 'NONE', *, *, #17334, .T. ) ;
#3752=CARTESIAN_POINT ( 'NONE',  ( 4.972623340256002500, 14.42132507220000015, 3.509556516286003625 ) ) ;
#3754=CARTESIAN_POINT ( 'NONE',  ( 5.752357458139003121, 13.85427084562999589, 4.060679559109004799 ) ) ;
#3755=CARTESIAN_POINT ( 'NONE',  ( -16.85755420454665554, -9.103879778418416890, 1.191568128638077262 ) ) ;
#3757=CARTESIAN_POINT ( 'NONE',  ( 11.88393908531000065, -9.721606288483000569, -2.753149205743999683 ) ) ;
#3758=DIRECTION ( 'NONE',  ( 1.000000000000000000, 0.000000000000000000, 0.000000000000000000 ) ) ;
#3759=ORIENTED_EDGE ( 'NONE', *, *, #13773, .F. ) ;
#3760=CARTESIAN_POINT ( 'NONE',  ( -12.91415807507000046, -6.873022849445000304, -6.789234046460999927 ) ) ;
#3761=AXIS2_PLACEMENT_3D ( 'NONE', #4996, #975, #15504 ) ;
#3764=CARTESIAN_POINT ( 'NONE',  ( -10.04281598263999875, 1.347635823622999967E-14, 0.000000000000000000 ) ) ;
#3766=CARTESIAN_POINT ( 'NONE',  ( -10.71135110314821404, 15.41046848462710983, -1.565338808390349445 ) ) ;
#3769=CARTESIAN_POINT ( 'NONE',  ( 14.65012636277685587, 6.238725812500826251, -8.226221173691849131 ) ) ;
#3770=CARTESIAN_POINT ( 'NONE',  ( -5.194121241700999647, -12.44999999995000017, -4.899859737990999515E-10 ) ) ;
#3771=CARTESIAN_POINT ( 'NONE',  ( 19.09627401310000039, -4.616208307064000316, 10.16717727690999951 ) ) ;
#3774=CARTESIAN_POINT ( 'NONE',  ( 13.80174867965053664, 9.025293717818129835, 0.002229559405347460773 ) ) ;
#3776=CARTESIAN_POINT ( 'NONE',  ( -6.442648543447514697, 15.51394528351816327, -1.396635598960656921 ) ) ;
#3777=CARTESIAN_POINT ( 'NONE',  ( -14.00000000000000000, -10.59999999999999964, 0.000000000000000000 ) ) ;
#3778=CARTESIAN_POINT ( 'NONE',  ( 21.29840273415999619, -9.313682482016000463, -6.615575153290000010 ) ) ;
#3779=ORIENTED_EDGE ( 'NONE', *, *, #16205, .F. ) ;
#3781=CIRCLE ( 'NONE', #18111, 7.500000000000000000 ) ;
#3783=CARTESIAN_POINT ( 'NONE',  ( -15.69191243917330780, 8.837844618163940069, -2.374974410327074903 ) ) ;
#3786=CARTESIAN_POINT ( 'NONE',  ( 22.21149770046333671, -9.241272520592698214, 1.209806691843540838 ) ) ;
#3787=ADVANCED_FACE ( 'NONE', ( #22923 ), #21000, .F. ) ;
#3788=CARTESIAN_POINT ( 'NONE',  ( 13.93747899715999949, -10.35476673622000021, -3.712727401404000371 ) ) ;
#3791=VERTEX_POINT ( 'NONE', #11447 ) ;
#3792=CARTESIAN_POINT ( 'NONE',  ( -9.113751972103999677, 13.51820841023999975, -6.295940148715000184 ) ) ;
#3794=CARTESIAN_POINT ( 'NONE',  ( -14.47793701804645927, -11.73188619686388812, -4.679765522767608488 ) ) ;
#3797=CARTESIAN_POINT ( 'NONE',  ( 20.69983103379664868, -5.655443772474994191, -7.358828497896286791 ) ) ;
#3798=CARTESIAN_POINT ( 'NONE',  ( 6.241905009026717188, 13.66125922203571363, 1.775230544922867582 ) ) ;
#3799=CARTESIAN_POINT ( 'NONE',  ( 15.90676250867264052, -9.944674072179898516, -2.897521108056326344 ) ) ;
#3801=CARTESIAN_POINT ( 'NONE',  ( -13.93024972067999911, -7.625744536618999092, 7.913094424807001204 ) ) ;
#3803=CARTESIAN_POINT ( 'NONE',  ( -17.22065346366999705, -7.714380452752999773, 6.849660182178999968 ) ) ;
#3804=AXIS2_PLACEMENT_3D ( 'NONE', #590, #19509, #15608 ) ;
#3808=CARTESIAN_POINT ( 'NONE',  ( 20.78159665399543243, 1.123289875192744480, 10.47162823820594468 ) ) ;
#3810=CIRCLE ( 'NONE', #22754, 0.8000000000000003775 ) ;
#3813=ADVANCED_FACE ( 'NONE', ( #22455 ), #1324, .F. ) ;
#3817=CARTESIAN_POINT ( 'NONE',  ( 17.45156392131000089, -0.08049851871593999286, -9.740865876825999692 ) ) ;
#3818=EDGE_LOOP ( 'NONE', ( #17214, #17518, #7752, #6892 ) ) ;
#3819=CARTESIAN_POINT ( 'NONE',  ( -4.142610502493168312, 15.10207515396060352, 4.511673133457231089 ) ) ;
#3821=AXIS2_PLACEMENT_3D ( 'NONE', #8561, #21392, #21147 ) ;
#3823=CARTESIAN_POINT ( 'NONE',  ( 22.51383103379667361, -5.684051423272225456, -7.396053641303423909 ) ) ;
#3824=CARTESIAN_POINT ( 'NONE',  ( 4.738540299664001587, 12.61405493002000711, 0.2471290196958000063 ) ) ;
#3826=CARTESIAN_POINT ( 'NONE',  ( -20.53063986495000037, -4.235883636776000216, 8.584601015509999655 ) ) ;
#3827=CARTESIAN_POINT ( 'NONE',  ( 19.03699770046332418, -1.199143088786338796, -9.159808593981743741 ) ) ;
#3830=CARTESIAN_POINT ( 'NONE',  ( -24.50000000000000000, 1.524685264937999788E-14, 0.000000000000000000 ) ) ;
#3831=VECTOR ( 'NONE', #20193, 1000.000000000000000 ) ;
#3832=CARTESIAN_POINT ( 'NONE',  ( 15.61599999999999966, 9.072019050554999353, 0.000000000000000000 ) ) ;
#3833=CARTESIAN_POINT ( 'NONE',  ( 18.51344355829000321, 6.966878364870000340, 12.06698729810999993 ) ) ;
#3835=EDGE_LOOP ( 'NONE', ( #1409, #16851, #12026, #2074, #23143 ) ) ;
#3837=CARTESIAN_POINT ( 'NONE',  ( 14.09123181476553910, 9.084527387259015541, 0.1472698650368901852 ) ) ;
#3839=CARTESIAN_POINT ( 'NONE',  ( -23.16125366752128656, -6.188651670778435587, 8.573940610315684552 ) ) ;
#3842=CIRCLE ( 'NONE', #8504, 15.45000000000000107 ) ;
#3843=CARTESIAN_POINT ( 'NONE',  ( 4.690616603563839249, 12.38867937097142757, 1.313715200103743763 ) ) ;
#3845=CARTESIAN_POINT ( 'NONE',  ( -1.948370167467705638, 11.64426098586311831, -4.406099265893608674 ) ) ;
#3846=CARTESIAN_POINT ( 'NONE',  ( 24.37173283531059909, 12.35285683711744653, 3.604224339486718609 ) ) ;
#3848=CARTESIAN_POINT ( 'NONE',  ( 4.834857269758976450, 12.45115135844470622, 0.1243267821587187988 ) ) ;
#3852=CARTESIAN_POINT ( 'NONE',  ( 16.27143908530999639, 9.938600131338999333, -2.378686727414999869 ) ) ;
#3853=CARTESIAN_POINT ( 'NONE',  ( 18.39512765608887435, 9.038824569696712885, -5.186684426708589868 ) ) ;
#3857=CARTESIAN_POINT ( 'NONE',  ( 14.71864037305999950, 1.512073574203999904, -10.68419109087999885 ) ) ;
#3862=CARTESIAN_POINT ( 'NONE',  ( 24.76311698098999869, -3.832248145790000393, 9.673750008746999640 ) ) ;
#3864=CARTESIAN_POINT ( 'NONE',  ( -24.10634617653294498, 6.505742320928646016, 7.512631181061424357 ) ) ;
#3865=ORIENTED_EDGE ( 'NONE', *, *, #18114, .T. ) ;
#3866=CARTESIAN_POINT ( 'NONE',  ( -12.49585571294465325, 6.729692068040215247, -5.965106315427219918 ) ) ;
#3868=CARTESIAN_POINT ( 'NONE',  ( 3.358145790808003905, 11.92291747373999478, 3.495386131071001934 ) ) ;
#3870=CARTESIAN_POINT ( 'NONE',  ( 12.52688711657000020, 13.93375672974000068, -0.8660254037843999608 ) ) ;
#3877=CARTESIAN_POINT ( 'NONE',  ( 16.61833103379667165, -7.275071925230092162, 5.591076558181078404 ) ) ;
#3879=CARTESIAN_POINT ( 'NONE',  ( -12.25000000000000000, 1.374666032043000015E-14, 0.000000000000000000 ) ) ;
#3881=EDGE_CURVE ( 'NONE', #9228, #23352, #14481, .T. ) ;
#3883=CARTESIAN_POINT ( 'NONE',  ( -18.98111647941000157, -8.384220026111998791, 5.081857170174999716 ) ) ;
#3884=B_SPLINE_CURVE_WITH_KNOTS ( 'NONE', 3,
 ( #2986, #6612, #19337, #4687, #12073, #19456, #4926, #14118, #909, #19702, #12312, #6848, #14241, #2864, #3117, #15676, #8191, #17639, #6363, #10501, #21513, #8437 ),
 .UNSPECIFIED., .F., .F.,
 ( 4, 2, 2, 1, 1, 2, 2, 2, 2, 2, 2, 4 ),
 ( 0.000000000000000000, 0.1250000000000900391, 0.1875000000001351697, 0.2187500000001618428, 0.2343750000001749989, 0.2421875000001745271, 0.2500000000001740830, 0.3750000000001458278, 0.4375000000001291744, 0.4687500000001231792, 0.5000000000001172396, 1.000000000000000000 ),
 .UNSPECIFIED. ) ;
#3887=ORIENTED_EDGE ( 'NONE', *, *, #11874, .F. ) ;
#3888=CARTESIAN_POINT ( 'NONE',  ( -21.36254453733999981, -7.691211596171000586, 8.186677943368000143 ) ) ;
#3890=CARTESIAN_POINT ( 'NONE',  ( 4.495027222853295257, 14.65432717051509037, -4.161727442053731352 ) ) ;
#3892=CARTESIAN_POINT ( 'NONE',  ( 21.29883756869999800, -11.00028630601000046, -2.245331027877000007 ) ) ;
#3894=EDGE_CURVE ( 'NONE', #12304, #20918, #14472, .T. ) ;
#3895=CARTESIAN_POINT ( 'NONE',  ( 13.80113244728332234, 9.025301755077943966, -0.01720271198835989293 ) ) ;
#3897=CARTESIAN_POINT ( 'NONE',  ( 12.40357033522255037, 13.79529643152775797, -1.105845675118900084 ) ) ;
#3898=VERTEX_POINT ( 'NONE', #4533 ) ;
#3900=EDGE_CURVE ( 'NONE', #22764, #1513, #8294, .T. ) ;
#3901=VERTEX_POINT ( 'NONE', #10103 ) ;
#3903=DIRECTION ( 'NONE',  ( -1.000000000000000000, 0.000000000000000000, 0.000000000000000000 ) ) ;
#3904=DIRECTION ( 'NONE',  ( -1.000000000000000000, 0.000000000000000000, 0.000000000000000000 ) ) ;
#3905=CARTESIAN_POINT ( 'NONE',  ( 18.41492214233000269, 10.39830466543000043, -3.948887927675999165 ) ) ;
#3906=AXIS2_PLACEMENT_3D ( 'NONE', #1350, #15865, #8977 ) ;
#3913=CARTESIAN_POINT ( 'NONE',  ( -10.81816756584999872, -7.700301352277000078, -12.71861605121999972 ) ) ;
#3915=CARTESIAN_POINT ( 'NONE',  ( -14.45529025083969898, -9.532921455384554932, -8.488438081456083140 ) ) ;
#3916=ORIENTED_EDGE ( 'NONE', *, *, #4864, .F. ) ;
#3917=CARTESIAN_POINT ( 'NONE',  ( 20.11758333333333226, -9.187538551043507695, 1.063519409932076609 ) ) ;
#3918=CARTESIAN_POINT ( 'NONE',  ( 19.58787013427168233, -4.214981502252697076, -9.617786801466230884 ) ) ;
#3919=PLANE ( 'NONE',  #17237 ) ;
#3920=CARTESIAN_POINT ( 'NONE',  ( 16.03245491809901324, -7.736135533815227561, -6.891731924576589563 ) ) ;
#3921=CARTESIAN_POINT ( 'NONE',  ( -19.49677076852000113, -7.796036496380999381, 6.940746985983999195 ) ) ;
#3924=CARTESIAN_POINT ( 'NONE',  ( -17.66767224083000087, -1.527991571549000005, 10.75645198264999891 ) ) ;
#3929=CARTESIAN_POINT ( 'NONE',  ( -18.91964744305752077, 3.100836465720866020, -10.17440793236460728 ) ) ;
#3930=VERTEX_POINT ( 'NONE', #15781 ) ;
#3931=FACE_OUTER_BOUND ( 'NONE', #6802, .T. ) ;
#3933=CARTESIAN_POINT ( 'NONE',  ( -13.99999999999999822, -9.930093542707636445, 2.724120365425963364 ) ) ;
#3935=CARTESIAN_POINT ( 'NONE',  ( 14.68293875730999964, -5.746474821545000111, 7.132383943660999925 ) ) ;
#3936=EDGE_CURVE ( 'NONE', #1186, #2766, #16780, .T. ) ;
#3941=EDGE_LOOP ( 'NONE', ( #9150, #19213, #9707, #22563, #521 ) ) ;
#3942=B_SPLINE_CURVE_WITH_KNOTS ( 'NONE', 3,
 ( #7537, #2788, #10173, #11993, #16083, #15960, #23353, #955, #19378, #19624, #6771, #12237, #17560, #3274, #4605, #12115, #3158, #23482, #8353, #8480, #21191, #12474 ),
 .UNSPECIFIED., .F., .F.,
 ( 4, 2, 2, 2, 2, 2, 2, 2, 2, 2, 4 ),
 ( 0.000000000000000000, 0.07385965502458807785, 0.1477193100491761557, 0.1846491375614701946, 0.2215789650737642613, 0.2954386200983524224, 0.3692982751229405558, 0.4431579301475287447, 0.4800877576598228669, 0.5170175851721169336, 0.5908772401967050669 ),
 .UNSPECIFIED. ) ;
#3944=CARTESIAN_POINT ( 'NONE',  ( -1.044905824211999734, 11.67616894756002033, 4.654497658188999409 ) ) ;
#3945=CARTESIAN_POINT ( 'NONE',  ( 12.00000000000000000, 0.3610762368853280280, -9.315579937737750171 ) ) ;
#3946=CARTESIAN_POINT ( 'NONE',  ( -14.44633174692086008, 9.404057468167051681, -8.711677720880402376 ) ) ;
#3947=CARTESIAN_POINT ( 'NONE',  ( -4.014472954888002043, 13.57154522720001744, -4.599265107325998692 ) ) ;
#3948=ADVANCED_FACE ( 'NONE', ( #8539 ), #23762, .T. ) ;
#3951=VECTOR ( 'NONE', #17436, 999.9999999999998863 ) ;
#3955=ORIENTED_EDGE ( 'NONE', *, *, #4832, .F. ) ;
#3958=CARTESIAN_POINT ( 'NONE',  ( -23.51536743654689943, -5.893785232171476984, -7.219491138192441149 ) ) ;
#3959=CARTESIAN_POINT ( 'NONE',  ( -23.75033391797219906, 10.46611617202711031, 1.634913018610795632 ) ) ;
#3962=AXIS2_PLACEMENT_3D ( 'NONE', #21933, #6799, #14193 ) ;
#3965=CARTESIAN_POINT ( 'NONE',  ( -3.261050669804293811, 11.92957528164763126, -3.562551734304618911 ) ) ;
#3970=CARTESIAN_POINT ( 'NONE',  ( 13.30987658531000051, -4.885510779899000511, 8.887104416848000454 ) ) ;
#3971=CARTESIAN_POINT ( 'NONE',  ( -19.42261965736999940, -11.41835772389999981, 0.8203659406909000751 ) ) ;
#3973=CARTESIAN_POINT ( 'NONE',  ( 13.90614037306000128, -4.856636860576000636, 9.610582908496999366 ) ) ;
#3977=CARTESIAN_POINT ( 'NONE',  ( 20.39590579450999996, 8.765676152204999738, -6.195664695497000274 ) ) ;
#3981=CARTESIAN_POINT ( 'NONE',  ( 24.50000000000000000, -1.131740379468156865, 10.47946835040394298 ) ) ;
#3982=CARTESIAN_POINT ( 'NONE',  ( 4.673640587513999023, 12.34837631718999340, 1.539931574126999880 ) ) ;
#3984=CARTESIAN_POINT ( 'NONE',  ( -19.33846693354000124, -10.46074197849999976, 1.868315815290999993 ) ) ;
#3985=VERTEX_POINT ( 'NONE', #12417 ) ;
#3986=CARTESIAN_POINT ( 'NONE',  ( 12.00000000000000000, 0.000000000000000000, 0.000000000000000000 ) ) ;
#3987=VERTEX_POINT ( 'NONE', #1010 ) ;
#3989=CARTESIAN_POINT ( 'NONE',  ( 6.273729641689004488, 13.70226080931000467, -0.03746541131887003856 ) ) ;
#3991=FACE_OUTER_BOUND ( 'NONE', #21871, .T. ) ;
#3992=CARTESIAN_POINT ( 'NONE',  ( 11.31235608929908665, 2.505169353248475783, -12.49996790082812659 ) ) ;
#3993=CARTESIAN_POINT ( 'NONE',  ( 23.99478584076000232, -13.93375672974000068, 0.6736217021363000157 ) ) ;
#3995=CARTESIAN_POINT ( 'NONE',  ( -13.80819562941000100, -8.705043851576000691, 6.319240472362000816 ) ) ;
#3997=CARTESIAN_POINT ( 'NONE',  ( -14.44097977831989255, -2.973612400777547737, 12.49999313495312414 ) ) ;
#4001=CARTESIAN_POINT ( 'NONE',  ( 14.19326017626335279, -8.265447570964310486, -6.165922807610080270 ) ) ;
#4003=CARTESIAN_POINT ( 'NONE',  ( 19.31674634214999742, -11.08266600408999913, -1.414964896437999942 ) ) ;
#4005=CARTESIAN_POINT ( 'NONE',  ( 13.79403029713875561, 9.023035438857904822, -0.2363099913121846085 ) ) ;
#4006=CARTESIAN_POINT ( 'NONE',  ( -6.838539683295000060, 15.31903503039000114, -1.878299264234999821 ) ) ;
#4008=ADVANCED_FACE ( 'NONE', ( #1383 ), #8811, .F. ) ;
#4009=CARTESIAN_POINT ( 'NONE',  ( 11.18574820343221710, 9.950120879851732880, -7.765924039707254423 ) ) ;
#4010=EDGE_LOOP ( 'NONE', ( #13966, #3564, #428 ) ) ;
#4014=CARTESIAN_POINT ( 'NONE',  ( 19.28343529110456700, -1.811640167859055017, 9.852238740839766251 ) ) ;
#4016=DIRECTION ( 'NONE',  ( 0.000000000000000000, 1.000000000000000000, 0.000000000000000000 ) ) ;
#4019=CARTESIAN_POINT ( 'NONE',  ( 13.21567540576999988, 5.680959247587999528, 8.577876493359001486 ) ) ;
#4020=DIRECTION ( 'NONE',  ( -1.000000000000000000, 0.000000000000000000, 0.000000000000000000 ) ) ;
#4023=VERTEX_POINT ( 'NONE', #22544 ) ;
#4024=ORIENTED_EDGE ( 'NONE', *, *, #2604, .F. ) ;
#4025=CARTESIAN_POINT ( 'NONE',  ( -14.00000000000000355, 3.517902211551271474, -8.602570206292373456 ) ) ;
#4027=LINE ( 'NONE', #5724, #21372 ) ;
#4029=CARTESIAN_POINT ( 'NONE',  ( -6.838539683295000060, 15.31903503039000114, -1.878299264234999821 ) ) ;
#4030=ORIENTED_EDGE ( 'NONE', *, *, #18897, .F. ) ;
#4031=CARTESIAN_POINT ( 'NONE',  ( -14.49454882815140522, 10.37180012737163359, 7.035449704349444389 ) ) ;
#4032=CARTESIAN_POINT ( 'NONE',  ( 21.26670603379664470, 8.977084173768046682, -2.412654681333150197 ) ) ;
#4033=CARTESIAN_POINT ( 'NONE',  ( 6.154060171291465764, 14.10599882039383779, 0.3200240209268620517 ) ) ;
#4034=CARTESIAN_POINT ( 'NONE',  ( 15.75691745686210510, -10.07139243573377030, 2.399251823897887714 ) ) ;
#4035=CARTESIAN_POINT ( 'NONE',  ( -16.06416778292000203, -1.832745140302000086, 10.89464230799999989 ) ) ;
#4038=CARTESIAN_POINT ( 'NONE',  ( -18.72408206190999991, 5.159378177076999528, -10.19862909758999869 ) ) ;
#4043=CARTESIAN_POINT ( 'NONE',  ( -24.50000000000000355, -6.320988460424660893, -8.473731186276276972 ) ) ;
#4044=AXIS2_PLACEMENT_3D ( 'NONE', #17253, #21262, #23052 ) ;
#4045=CARTESIAN_POINT ( 'NONE',  ( 5.302309017544000191, 13.73032573480000096, -4.450985556070999216 ) ) ;
#4046=EDGE_LOOP ( 'NONE', ( #20719, #17660 ) ) ;
#4049=CARTESIAN_POINT ( 'NONE',  ( -23.74228231688656976, 8.693394395448456762E-05, -9.522797051439189531 ) ) ;
#4051=CARTESIAN_POINT ( 'NONE',  ( 11.94075125730999964, 5.167059442038000050, -7.475232529384999047 ) ) ;
#4052=VERTEX_POINT ( 'NONE', #10414 ) ;
#4053=CARTESIAN_POINT ( 'NONE',  ( -5.989773396780996961, 16.41865079481998890, -1.007191989855000358 ) ) ;
#4054=CARTESIAN_POINT ( 'NONE',  ( 24.45564077607145492, -11.85537957198067005, 4.465880238315118156 ) ) ;
#4056=CARTESIAN_POINT ( 'NONE',  ( -16.51742920454665509, -4.580373640694110016, -7.947268161980230339 ) ) ;
#4058=CARTESIAN_POINT ( 'NONE',  ( 1.613427892151998666, 11.77489200500998834, 4.557952326475001925 ) ) ;
#4059=AXIS2_PLACEMENT_3D ( 'NONE', #9220, #22061, #20484 ) ;
#4061=CARTESIAN_POINT ( 'NONE',  ( -24.38472030418999736, 3.087124291345999971, 9.171168033639998995 ) ) ;
#4062=CARTESIAN_POINT ( 'NONE',  ( 18.65908103379666372, -9.150110507480414768, -1.197619716921026090 ) ) ;
#4063=CARTESIAN_POINT ( 'NONE',  ( -4.796844195024712043, 13.32315443175082414, 5.553764072526095497 ) ) ;
#4065=CARTESIAN_POINT ( 'NONE',  ( 5.690494692575421176, 14.49221151649372352, 2.273377197464830246 ) ) ;
#4067=ADVANCED_FACE ( 'NONE', ( #23712 ), #16533, .F. ) ;
#4069=VERTEX_POINT ( 'NONE', #21554 ) ;
#4070=EDGE_CURVE ( 'NONE', #14850, #18988, #6887, .T. ) ;
#4071=CARTESIAN_POINT ( 'NONE',  ( 19.59471007437000267, 8.951466053687999747, 3.915631828095000877 ) ) ;
#4072=CARTESIAN_POINT ( 'NONE',  ( -0.5533348865729804666, 12.81413901064252236, -6.643174729024203806 ) ) ;
#4073=DIRECTION ( 'NONE',  ( 0.000000000000000000, -1.000000000000000000, -2.763496998553999776E-10 ) ) ;
#4074=CARTESIAN_POINT ( 'NONE',  ( -22.70605529217283447, -8.531959713363267639, -6.226904222294471936 ) ) ;
#4077=CYLINDRICAL_SURFACE ( 'NONE', #7723, 11.50000000000000000 ) ;
#4079=CARTESIAN_POINT ( 'NONE',  ( -17.15404741204965688, -5.529600172785069212, -8.836923940253553766 ) ) ;
#4080=ADVANCED_FACE ( 'NONE', ( #18167 ), #7248, .T. ) ;
#4081=FACE_OUTER_BOUND ( 'NONE', #13883, .T. ) ;
#4084=VERTEX_POINT ( 'NONE', #1570 ) ;
#4085=CARTESIAN_POINT ( 'NONE',  ( 23.99478584078000054, -6.383504859171999612, 12.40379814865999997 ) ) ;
#4086=CARTESIAN_POINT ( 'NONE',  ( 18.49162674931000083, 10.23722398798000022, 3.399059637929999766 ) ) ;
#4087=AXIS2_PLACEMENT_3D ( 'NONE', #4391, #17471, #11782 ) ;
#4088=CARTESIAN_POINT ( 'NONE',  ( -17.39131617766999938, -8.850658443533001574, -7.172809675466000456 ) ) ;
#4089=CARTESIAN_POINT ( 'NONE',  ( 23.77835672501372599, -9.281039036324623126, -1.918975276430111748E-05 ) ) ;
#4090=CARTESIAN_POINT ( 'NONE',  ( 18.17176537305999773, -4.883153369406000088, -9.730320138885000247 ) ) ;
#4091=CARTESIAN_POINT ( 'NONE',  ( -6.042815982636000172, 21.50000000000000000, -1.000000000000000000 ) ) ;
#4093=CARTESIAN_POINT ( 'NONE',  ( 23.67704510333999579, -9.540510436538999883, -3.867765119376000094 ) ) ;
#4094=CARTESIAN_POINT ( 'NONE',  ( 23.99999963380662749, 13.93375672974000068, 0.09624782602625137073 ) ) ;
#4095=VERTEX_POINT ( 'NONE', #8713 ) ;
#4096=CARTESIAN_POINT ( 'NONE',  ( 12.35781481503000023, 4.416401984941999537, -7.958029298064000834 ) ) ;
#4098=CARTESIAN_POINT ( 'NONE',  ( 0.8375093185100999094, 11.48200882685999780, 4.871193163113003877 ) ) ;
#4100=CARTESIAN_POINT ( 'NONE',  ( -22.93816914322000144, -10.13184090208999955, -4.608035378405999971 ) ) ;
#4104=CARTESIAN_POINT ( 'NONE',  ( 15.59795603379665074, 4.568490502191478342, -7.926650740716842058 ) ) ;
#4105=CARTESIAN_POINT ( 'NONE',  ( -2.400843557866978006, 11.81756170137088269, 4.145428949226574566 ) ) ;
#4110=CARTESIAN_POINT ( 'NONE',  ( 15.09131424931000076, 4.764171260128000185, 9.577928620034999341 ) ) ;
#4111=CARTESIAN_POINT ( 'NONE',  ( -12.99567423753000028, 6.199143636224999199, -8.762012042742998830 ) ) ;
#4112=CARTESIAN_POINT ( 'NONE',  ( 24.00016455292000117, -6.692834685703999753, -6.438753808737999407 ) ) ;
#4113=CARTESIAN_POINT ( 'NONE',  ( 24.07420734439604004, 13.66464621573615190, -1.332138486891153217 ) ) ;
#4114=ORIENTED_EDGE ( 'NONE', *, *, #4700, .F. ) ;
#4118=CARTESIAN_POINT ( 'NONE',  ( 13.89455729310778942, -9.502394204169668512, 4.016926027372820229 ) ) ;
#4119=CARTESIAN_POINT ( 'NONE',  ( 0.6559879769048997389, 12.68326117563999667, -7.060560187867004345 ) ) ;
#4122=CARTESIAN_POINT ( 'NONE',  ( 11.06626444616512828, 0.2510812432465111543, 12.49999588481644608 ) ) ;
#4123=DIRECTION ( 'NONE',  ( -1.000000000000000000, 0.000000000000000000, 0.000000000000000000 ) ) ;
#4127=ORIENTED_EDGE ( 'NONE', *, *, #20478, .T. ) ;
#4128=CARTESIAN_POINT ( 'NONE',  ( -24.50000000000000000, 0.000000000000000000, -12.50000000000000000 ) ) ;
#4134=CARTESIAN_POINT ( 'NONE',  ( 13.75702809931000026, -10.56473829713000079, 3.046569488393000125 ) ) ;
#4135=CARTESIAN_POINT ( 'NONE',  ( -23.76320755544999841, -6.968962349015999536, 12.06578410929999912 ) ) ;
#4136=AXIS2_PLACEMENT_3D ( 'NONE', #7262, #22050, #22507 ) ;
#4138=ORIENTED_EDGE ( 'NONE', *, *, #17780, .F. ) ;
#4141=DIRECTION ( 'NONE',  ( 7.994189964398003696E-07, -1.682414072936945643E-07, 0.9999999999996664890 ) ) ;
#4142=CARTESIAN_POINT ( 'NONE',  ( -10.19248471168999970, -8.520788371486000656, 13.03016121583000064 ) ) ;
#4144=CARTESIAN_POINT ( 'NONE',  ( -4.849997028045999414, 12.54999874207999966, 2.403882053831000161E-08 ) ) ;
#4146=EDGE_LOOP ( 'NONE', ( #18444, #7488, #18540, #18510 ) ) ;
#4147=CARTESIAN_POINT ( 'NONE',  ( -24.24498014590000139, -9.840995202723000546, -0.7269391992499000255 ) ) ;
#4148=CARTESIAN_POINT ( 'NONE',  ( 19.81683333333332797, -3.716106903173100662, 8.461018381044933534 ) ) ;
#4150=CARTESIAN_POINT ( 'NONE',  ( 15.60735436316270253, -7.610950483687727086, 7.015716127438307304 ) ) ;
#4151=CARTESIAN_POINT ( 'NONE',  ( -18.59345419335999949, 8.208879709517999501, -7.496806360130000790 ) ) ;
#4154=CARTESIAN_POINT ( 'NONE',  ( -17.46454189286000158, -8.119858849493999386, 7.209780893148999503 ) ) ;
#4155=B_SPLINE_CURVE_WITH_KNOTS ( 'NONE', 3,
 ( #2238, #20652, #9750, #22340, #2481, #4063, #13497, #11693 ),
 .UNSPECIFIED., .F., .F.,
 ( 4, 2, 2, 4 ),
 ( 0.000000000000000000, 0.2499999999999997780, 0.4999999999999995559, 1.000000000000000000 ),
 .UNSPECIFIED. ) ;
#4156=ADVANCED_FACE ( 'NONE', ( #14396 ), #23492, .F. ) ;
#4160=B_SPLINE_CURVE_WITH_KNOTS ( 'NONE', 3,
 ( #5178, #16298, #7096, #14486, #21879, #5288, #10864, #18248, #23801, #57, #20415, #9157, #18598, #9507, #14823, #14601, #10975, #3700 ),
 .UNSPECIFIED., .F., .F.,
 ( 4, 2, 2, 2, 2, 2, 2, 2, 4 ),
 ( 0.000000000000000000, 0.1249999999999999722, 0.2500000000000000000, 0.3750000000000000555, 0.5000000000000001110, 0.6250000000000001110, 0.7500000000000000000, 0.8750000000000000000, 1.000000000000000000 ),
 .UNSPECIFIED. ) ;
#4162=CARTESIAN_POINT ( 'NONE',  ( -17.96465470606060677, -4.640328617862117255, 9.358849047281662337 ) ) ;
#4165=CARTESIAN_POINT ( 'NONE',  ( -5.553896923315000400, 15.03366893909998581, 2.958514830663998563 ) ) ;
#4167=CARTESIAN_POINT ( 'NONE',  ( 17.03925158531000150, -7.718145806856000490, 6.728824147386999854 ) ) ;
#4168=VERTEX_POINT ( 'NONE', #21787 ) ;
#4170=CARTESIAN_POINT ( 'NONE',  ( 18.38737270046332739, -6.348145805352896076, 6.664696905531276805 ) ) ;
#4173=EDGE_LOOP ( 'NONE', ( #15223, #4270, #10172, #11478 ) ) ;
#4174=CARTESIAN_POINT ( 'NONE',  ( -7.034000000000000696, -10.69999999999999929, 6.692380538630998849E-10 ) ) ;
#4176=CARTESIAN_POINT ( 'NONE',  ( 4.691862310626997434, 12.59647401853998971, 1.107358546619999773 ) ) ;
#4177=LINE ( 'NONE', #4299, #20717 ) ;
#4178=CARTESIAN_POINT ( 'NONE',  ( 12.00000000000000178, -0.06551022104711376470, -9.358750515500020128 ) ) ;
#4179=CARTESIAN_POINT ( 'NONE',  ( 19.33933103379666463, 7.330909640340940392, -5.633988034377063414 ) ) ;
#4180=PLANE ( 'NONE',  #15425 ) ;
#4181=LINE ( 'NONE', #20303, #11613 ) ;
#4187=CARTESIAN_POINT ( 'NONE',  ( 20.36771380861000225, -9.778663773954999527, 0.5067347920774000203 ) ) ;
#4188=CARTESIAN_POINT ( 'NONE',  ( -0.4177920217811221804, 12.80953346229017242, -6.652087608309179778 ) ) ;
#4189=DIRECTION ( 'NONE',  ( -1.000000000000000000, 0.000000000000000000, 0.000000000000000000 ) ) ;
#4191=CARTESIAN_POINT ( 'NONE',  ( -23.26835916760327905, -2.655106138931690563, 10.24194253716867031 ) ) ;
#4196=AXIS2_PLACEMENT_3D ( 'NONE', #6385, #8581, #1311 ) ;
#4197=CARTESIAN_POINT ( 'NONE',  ( -18.88454412025865992, -2.787382164252126593, -10.08993089778954122 ) ) ;
#4203=EDGE_CURVE ( 'NONE', #22775, #6561, #17037, .T. ) ;
#4204=VERTEX_POINT ( 'NONE', #18502 ) ;
#4206=DIRECTION ( 'NONE',  ( 0.000000000000000000, -0.3557256971724915284, 0.9345904067403778548 ) ) ;
#4208=CARTESIAN_POINT ( 'NONE',  ( 17.50443924930999984, -10.75095007791999890, -0.4607405056646999841 ) ) ;
#4209=CARTESIAN_POINT ( 'NONE',  ( -13.73496991422000058, -8.032382890017998989, -7.934146143239000359 ) ) ;
#4210=CARTESIAN_POINT ( 'NONE',  ( 22.60745833333331589, 5.685348439634987372, -7.398154500763331143 ) ) ;
#4211=CARTESIAN_POINT ( 'NONE',  ( 14.31239037306000128, -10.28425898052000065, -3.229262266925000180 ) ) ;
#4212=CARTESIAN_POINT ( 'NONE',  ( 13.50000000000000178, -6.755876297955836662, -6.302790169812603871 ) ) ;
#4213=DIRECTION ( 'NONE',  ( -1.000000000000000000, 0.000000000000000000, 0.000000000000000000 ) ) ;
#4214=CARTESIAN_POINT ( 'NONE',  ( 23.49999600117999776, -10.02335684408000027, 2.326734473723000018 ) ) ;
#4216=EDGE_CURVE ( 'NONE', #3157, #7720, #14740, .T. ) ;
#4218=ORIENTED_EDGE ( 'NONE', *, *, #22021, .F. ) ;
#4219=CARTESIAN_POINT ( 'NONE',  ( 12.66027015143999890, 5.546622252611999926, -7.082799009680999625 ) ) ;
#4221=CARTESIAN_POINT ( 'NONE',  ( -1.083921081176000056, 11.48516387305999764, 4.746390725385002618 ) ) ;
#4223=CARTESIAN_POINT ( 'NONE',  ( -22.79154754632999769, -10.12821918160999957, -4.606388536657999744 ) ) ;
#4228=ORIENTED_EDGE ( 'NONE', *, *, #10961, .F. ) ;
#4229=FACE_OUTER_BOUND ( 'NONE', #18655, .T. ) ;
#4230=CARTESIAN_POINT ( 'NONE',  ( -4.143437947609855954, 12.32179185387261100, 2.404511302189828559 ) ) ;
#4232=CARTESIAN_POINT ( 'NONE',  ( -0.5536789215616996218, 12.68198336050999231, 7.063110854946003769 ) ) ;
#4234=CARTESIAN_POINT ( 'NONE',  ( 13.11693924931000055, 9.054732109491999026, 5.598051111924999823 ) ) ;
#4238=CARTESIAN_POINT ( 'NONE',  ( -16.00187137585000130, 9.645521962609000965, 3.562832264799999926 ) ) ;
#4240=CARTESIAN_POINT ( 'NONE',  ( 17.09606375731000227, -3.490954664894000192, -8.536518206589999380 ) ) ;
#4241=AXIS2_PLACEMENT_3D ( 'NONE', #16181, #5069, #9161 ) ;
#4246=CARTESIAN_POINT ( 'NONE',  ( 4.778395690722049061, 14.77598124633097498, -3.832701201829089577 ) ) ;
#4247=ORIENTED_EDGE ( 'NONE', *, *, #1393, .T. ) ;
#4249=CARTESIAN_POINT ( 'NONE',  ( 20.71127131372000107, 7.811385099584000180, 8.041652894164000642 ) ) ;
#4251=CARTESIAN_POINT ( 'NONE',  ( 14.40078967323709946, -4.362328053288525354, 7.919021186112042088 ) ) ;
#4253=CARTESIAN_POINT ( 'NONE',  ( 18.21132320931108239, 9.336834288664581649, -4.723061267702502342 ) ) ;
#4255=CARTESIAN_POINT ( 'NONE',  ( -6.638602398571264551, 15.38275018475912326, 1.627931652404663199 ) ) ;
#4260=CYLINDRICAL_SURFACE ( 'NONE', #17265, 0.9999999999999991118 ) ;
#4263=B_SPLINE_CURVE_WITH_KNOTS ( 'NONE', 3,
 ( #18105, #8902, #7298, #22082, #14571, #20035, #3453, #10837, #21963, #5378, #20155, #12870, #18448, #3794, #16622, #1975, #5149, #7415, #5606, #12986, #18571, #614, #2443, #8018, #20508, #6197, #3915, #18795, #15391, #4387, #17340, #22779 ),
 .UNSPECIFIED., .F., .F.,
 ( 4, 2, 2, 2, 2, 2, 2, 2, 2, 2, 2, 2, 2, 2, 2, 4 ),
 ( 0.000000000000000000, 0.1249999999999978351, 0.1874999999999967526, 0.2187499999999963363, 0.2499999999999959477, 0.3124999999999953371, 0.3437499999999952816, 0.3749999999999951705, 0.4999999999999955591, 0.5624999999999955591, 0.5937499999999956701, 0.6249999999999957812, 0.6874999999999963363, 0.7187499999999965583, 0.7499999999999967804, 1.000000000000000000 ),
 .UNSPECIFIED. ) ;
#4266=CARTESIAN_POINT ( 'NONE',  ( 16.03523116938000115, -10.52587742755999933, -3.387995920261000382 ) ) ;
#4267=CARTESIAN_POINT ( 'NONE',  ( -6.595625688791005636, 15.16860556014002448, -2.934141294233998387 ) ) ;
#4268=CARTESIAN_POINT ( 'NONE',  ( 24.15736593520906794, -5.143174366503609818, -12.50000000000000355 ) ) ;
#4270=ORIENTED_EDGE ( 'NONE', *, *, #7181, .F. ) ;
#4271=CARTESIAN_POINT ( 'NONE',  ( -23.99212502900741129, 8.254180775344659438, -10.70333952224147112 ) ) ;
#4272=CARTESIAN_POINT ( 'NONE',  ( -24.50000000000000000, 1.524685264937999788E-14, 0.000000000000000000 ) ) ;
#4275=CARTESIAN_POINT ( 'NONE',  ( -23.78800218427999980, 0.9048305059418999541, -10.21290675204000031 ) ) ;
#4276=CARTESIAN_POINT ( 'NONE',  ( -14.47158024777374763, 9.790304928774279603, 8.042633409149424040 ) ) ;
#4277=CARTESIAN_POINT ( 'NONE',  ( 6.179554688491347036, 13.96940086483144228, 0.6559343789280690507 ) ) ;
#4278=CARTESIAN_POINT ( 'NONE',  ( 15.58288198016115444, -6.969638865288424689, 7.648956436886991561 ) ) ;
#4279=CARTESIAN_POINT ( 'NONE',  ( -14.22349291444999864, -7.631317991244999988, 7.918878983168999852 ) ) ;
#4281=CARTESIAN_POINT ( 'NONE',  ( -21.66813167847034194, -2.121835831585393795, 10.44917271204820253 ) ) ;
#4282=CARTESIAN_POINT ( 'NONE',  ( -16.85515084895999749, -2.006433207287000364, -10.65451757797000099 ) ) ;
#4284=ORIENTED_EDGE ( 'NONE', *, *, #8942, .F. ) ;
#4286=CARTESIAN_POINT ( 'NONE',  ( -19.49843092002534917, -10.39128334678671450, 1.480522605369253286 ) ) ;
#4288=ADVANCED_FACE ( 'NONE', ( #18857 ), #19233, .T. ) ;
#4290=CARTESIAN_POINT ( 'NONE',  ( -19.72972087121333118, 7.339100371923414023, -5.639965138420785173 ) ) ;
#4291=CARTESIAN_POINT ( 'NONE',  ( 13.94156392131000111, 3.761510884484999817, -8.885545664707001023 ) ) ;
#4293=CARTESIAN_POINT ( 'NONE',  ( -6.234717296507000128, 15.63949533431998873, -1.260321238843998604 ) ) ;
#4294=CARTESIAN_POINT ( 'NONE',  ( 23.99062354302999722, 7.716878364870000340, 11.63397459621999985 ) ) ;
#4295=EDGE_LOOP ( 'NONE', ( #12553, #12999 ) ) ;
#4297=CARTESIAN_POINT ( 'NONE',  ( 21.96499999999999986, -9.234946903777000671, 0.000000000000000000 ) ) ;
#4298=CARTESIAN_POINT ( 'NONE',  ( -3.981022404528000269, 12.34392304552999597, 2.724439042342001294 ) ) ;
#4299=CARTESIAN_POINT ( 'NONE',  ( -12.25000000000000000, -13.93375672974000068, 0.000000000000000000 ) ) ;
#4300=CARTESIAN_POINT ( 'NONE',  ( 18.30891208659113545, 7.138339280091794414, -7.593585127964508352 ) ) ;
#4301=CARTESIAN_POINT ( 'NONE',  ( -23.75391653307000084, 7.466983940307000189, 11.77825120950999960 ) ) ;
#4302=FACE_OUTER_BOUND ( 'NONE', #11346, .T. ) ;
#4308=ORIENTED_EDGE ( 'NONE', *, *, #15366, .T. ) ;
#4309=CARTESIAN_POINT ( 'NONE',  ( 20.94746660927999926, 3.688233682878999886, -9.087913520545999546 ) ) ;
#4310=CARTESIAN_POINT ( 'NONE',  ( 1.231503247170836257, 12.85502785828538919, -6.563768214206104012 ) ) ;
#4311=CARTESIAN_POINT ( 'NONE',  ( -23.50032910583999879, -5.270462733209999584, -7.631233524726999562 ) ) ;
#4312=EDGE_CURVE ( 'NONE', #7164, #15500, #23428, .T. ) ;
#4313=CARTESIAN_POINT ( 'NONE',  ( -19.57321941476413940, -4.900126282342609940, 9.269928300904794582 ) ) ;
#4317=CARTESIAN_POINT ( 'NONE',  ( -17.54480473325896028, -9.830998375515614285, 3.491180853190327227 ) ) ;
#4321=ORIENTED_EDGE ( 'NONE', *, *, #9786, .F. ) ;
#4323=ORIENTED_EDGE ( 'NONE', *, *, #12648, .T. ) ;
#4324=CARTESIAN_POINT ( 'NONE',  ( -4.820912286398000290, 1.283685947151999869E-14, 0.000000000000000000 ) ) ;
#4325=CARTESIAN_POINT ( 'NONE',  ( 11.99362658531000037, -8.009633343651000104, -6.163949985837000156 ) ) ;
#4326=CARTESIAN_POINT ( 'NONE',  ( -15.96940374187999900, -8.848765849800999561, 7.112061138617000289 ) ) ;
#4328=CARTESIAN_POINT ( 'NONE',  ( 16.47858580085999947, 8.864729889898001147, -7.134999139258999534 ) ) ;
#4329=DIRECTION ( 'NONE',  ( -1.000000000000000000, 0.000000000000000000, 0.000000000000000000 ) ) ;
#4331=CARTESIAN_POINT ( 'NONE',  ( 19.42786665163000137, 1.857528855125000211, 9.378182122424998823 ) ) ;
#4335=CARTESIAN_POINT ( 'NONE',  ( -23.74465998031000069, 7.716878364870000340, -11.63397459621999985 ) ) ;
#4337=CARTESIAN_POINT ( 'NONE',  ( 3.918384635635002500, 12.23938247889000763, 2.649806649680000348 ) ) ;
#4339=EDGE_CURVE ( 'NONE', #2252, #17770, #8435, .T. ) ;
#4340=CARTESIAN_POINT ( 'NONE',  ( -23.60650732633999738, 3.478347009544000112, 10.59213551982000112 ) ) ;
#4343=ORIENTED_EDGE ( 'NONE', *, *, #7592, .F. ) ;
#4346=DIRECTION ( 'NONE',  ( 0.000000000000000000, 1.000000000000000000, 0.000000000000000000 ) ) ;
#4347=CARTESIAN_POINT ( 'NONE',  ( -0.5078543351473996381, 12.73453039277000975, 6.462334485033003340 ) ) ;
#4349=CARTESIAN_POINT ( 'NONE',  ( 13.00725174931000083, 10.48226630763000067, 1.840397312871999924 ) ) ;
#4351=CARTESIAN_POINT ( 'NONE',  ( -17.05828119693000033, -8.427367219174998425, -6.829844779585000580 ) ) ;
#4352=AXIS2_PLACEMENT_3D ( 'NONE', #1945, #18762, #1826 ) ;
#4353=CARTESIAN_POINT ( 'NONE',  ( 15.01200125731000057, -8.889299820566000321, -2.243156938537000045 ) ) ;
#4358=CARTESIAN_POINT ( 'NONE',  ( 14.19128063372930093, -8.307842784655305124, -6.108522269369860425 ) ) ;
#4359=CARTESIAN_POINT ( 'NONE',  ( 4.859204854983003585, 14.34044420429000688, -3.623738212790001967 ) ) ;
#4360=CARTESIAN_POINT ( 'NONE',  ( -23.86847083086766474, 13.66493546065227349, -1.331637500005085073 ) ) ;
#4366=ADVANCED_FACE ( 'NONE', ( #13165 ), #22321, .F. ) ;
#4370=B_SPLINE_CURVE_WITH_KNOTS ( 'NONE', 3,
 ( #19770, #23509, #16352, #14423, #19999, #14535, #6793, #16239, #19882, #3421 ),
 .UNSPECIFIED., .F., .F.,
 ( 4, 2, 2, 2, 4 ),
 ( 0.000000000000000000, 0.2500000000000000555, 0.5000000000000001110, 0.7500000000000000000, 1.000000000000000000 ),
 .UNSPECIFIED. ) ;
#4372=CARTESIAN_POINT ( 'NONE',  ( 11.36448692219539680, -12.20430913922039906, 3.861467675482649131 ) ) ;
#4373=EDGE_LOOP ( 'NONE', ( #12942, #12279, #8611, #15844, #7582, #15139 ) ) ;
#4375=CARTESIAN_POINT ( 'NONE',  ( -5.759369968430410935, 16.25388642460873356, -2.084701305734063315 ) ) ;
#4376=CARTESIAN_POINT ( 'NONE',  ( -2.017784670879433140, 11.65584428263783145, 4.375368794292053387 ) ) ;
#4379=CARTESIAN_POINT ( 'NONE',  ( 14.05027129307999978, -10.57245532834000024, 3.048794078394999829 ) ) ;
#4385=CARTESIAN_POINT ( 'NONE',  ( -14.00000000000000000, 1.129711127297478246, -9.368077886284350342 ) ) ;
#4386=DIRECTION ( 'NONE',  ( 0.000000000000000000, -1.000000000000000000, 0.000000000000000000 ) ) ;
#4387=CARTESIAN_POINT ( 'NONE',  ( -14.39391696178579494, -8.762017990471466788, -9.823718642519271071 ) ) ;
#4390=AXIS2_PLACEMENT_3D ( 'NONE', #8983, #23856, #3758 ) ;
#4391=CARTESIAN_POINT ( 'NONE',  ( 0.000000000000000000, 22.00000000000000000, 0.000000000000000000 ) ) ;
#4392=CARTESIAN_POINT ( 'NONE',  ( 15.58582384231821294, -7.050459548571376800, 7.574867977535271635 ) ) ;
#4394=CARTESIAN_POINT ( 'NONE',  ( -15.30747280464999882, 1.690426505166000126, -10.89665494706000004 ) ) ;
#4396=CARTESIAN_POINT ( 'NONE',  ( -20.69019690006062717, 4.549517228506217315, -9.473981616376564219 ) ) ;
#4397=AXIS2_PLACEMENT_3D ( 'NONE', #20179, #167, #20413 ) ;
#4398=B_SPLINE_CURVE_WITH_KNOTS ( 'NONE', 3,
 ( #12831, #20225, #3981, #212, #9196, #9549, #1808, #16927, #7369, #9315, #14868, #14754, #7605, #22150, #14984, #22381 ),
 .UNSPECIFIED., .F., .F.,
 ( 4, 2, 2, 1, 1, 2, 2, 2, 4 ),
 ( 0.000000000000000000, 0.1249999999999998057, 0.2499999999999996114, 0.3749999999999994449, 0.4374999999999993339, 0.4687499999999993339, 0.4999999999999993339, 0.7499999999999995559, 1.000000000000000000 ),
 .UNSPECIFIED. ) ;
#4399=CARTESIAN_POINT ( 'NONE',  ( -12.61636557635000067, 8.538192823868000048, -4.467067395255999607 ) ) ;
#4401=EDGE_LOOP ( 'NONE', ( #3077, #14503, #23367, #14633 ) ) ;
#4402=CARTESIAN_POINT ( 'NONE',  ( -18.36980313993808522, 8.462731522496705239, 6.141897997985012125 ) ) ;
#4404=CARTESIAN_POINT ( 'NONE',  ( 5.512521265958003625, 13.91027821615000093, -3.003820387280002446 ) ) ;
#4405=CARTESIAN_POINT ( 'NONE',  ( -12.50000000000000000, 6.965460728298000781, -5.686777139159000072 ) ) ;
#4407=CARTESIAN_POINT ( 'NONE',  ( 17.91675158530999923, 7.007286630565999985, -7.497846106583000214 ) ) ;
#4409=CARTESIAN_POINT ( 'NONE',  ( 18.28712270046333899, -3.700215461176396659, 8.424836998218975026 ) ) ;
#4415=B_SPLINE_CURVE_WITH_KNOTS ( 'NONE', 3,
 ( #22622, #2652, #13298, #20939 ),
 .UNSPECIFIED., .F., .F.,
 ( 4, 4 ),
 ( 0.000000000000000000, 1.000000000000000000 ),
 .UNSPECIFIED. ) ;
#4419=DIRECTION ( 'NONE',  ( -0.9996708941621513800, -0.02565352539212875996, 2.352933579521886060E-14 ) ) ;
#4420=CARTESIAN_POINT ( 'NONE',  ( 17.66271362385008104, -10.35725960301209092, -0.9534308961195087084 ) ) ;
#4421=DIRECTION ( 'NONE',  ( -1.000000000000000000, 0.000000000000000000, 0.000000000000000000 ) ) ;
#4422=CYLINDRICAL_SURFACE ( 'NONE', #13383, 10.59999999999999964 ) ;
#4423=CARTESIAN_POINT ( 'NONE',  ( 19.86738723104999949, 5.001395480264999804, -10.00765157440999964 ) ) ;
#4426=CARTESIAN_POINT ( 'NONE',  ( -4.750000000000000000, 22.00000000000000000, 0.000000000000000000 ) ) ;
#4429=CARTESIAN_POINT ( 'NONE',  ( -16.71228743917333759, -7.277179538279706428, 5.592378764700831617 ) ) ;
#4430=CARTESIAN_POINT ( 'NONE',  ( 19.64727180480999991, 9.968845625174999725, -2.620031903844999732 ) ) ;
#4431=CARTESIAN_POINT ( 'NONE',  ( 1.073567819982733207, 12.84232628255067965, -6.588562543359082646 ) ) ;
#4435=CARTESIAN_POINT ( 'NONE',  ( -4.900699999999999612, 1.284663064832999817E-14, 0.000000000000000000 ) ) ;
#4437=CARTESIAN_POINT ( 'NONE',  ( -18.38214185013208990, 10.40616288478918250, -1.044753050767677438 ) ) ;
#4442=ORIENTED_EDGE ( 'NONE', *, *, #8066, .F. ) ;
#4443=VERTEX_POINT ( 'NONE', #4569 ) ;
#4444=DIRECTION ( 'NONE',  ( -1.000000000000000000, 0.000000000000000000, 0.000000000000000000 ) ) ;
#4445=VECTOR ( 'NONE', #12429, 1000.000000000000114 ) ;
#4446=CARTESIAN_POINT ( 'NONE',  ( 14.32350174931000097, 0.2192049860668999761, -10.67495121044000150 ) ) ;
#4447=CARTESIAN_POINT ( 'NONE',  ( -14.50244144996998408, -6.856859659331884238, -5.968632047789297346 ) ) ;
#4448=EDGE_CURVE ( 'NONE', #22775, #23793, #15120, .T. ) ;
#4449=CARTESIAN_POINT ( 'NONE',  ( -18.61009826548999868, 10.52931532496999978, -4.437563658045000636 ) ) ;
#4450=LINE ( 'NONE', #438, #19299 ) ;
#4451=CARTESIAN_POINT ( 'NONE',  ( 17.29249951746000136, 7.620899816286000217, -6.134110199842999656 ) ) ;
#4452=FACE_OUTER_BOUND ( 'NONE', #4992, .T. ) ;
#4453=DIRECTION ( 'NONE',  ( -1.000000000000000000, 0.000000000000000000, 0.000000000000000000 ) ) ;
#4454=CARTESIAN_POINT ( 'NONE',  ( 22.70900596046000075, 7.018910044166999818, -6.751668252317999830 ) ) ;
#4457=CARTESIAN_POINT ( 'NONE',  ( 1.719681894094051477, 13.83405848052206544, 5.882549610230969783 ) ) ;
#4460=CARTESIAN_POINT ( 'NONE',  ( -4.368769711663002653, 12.39958269994001405, 1.811125832054002460 ) ) ;
#4463=CARTESIAN_POINT ( 'NONE',  ( -19.44985663072000293, -9.321637154864999886, 5.906755658224999372 ) ) ;
#4465=ORIENTED_EDGE ( 'NONE', *, *, #3936, .T. ) ;
#4466=CARTESIAN_POINT ( 'NONE',  ( 12.00000000000000000, -9.392874664203999302, -3.575135015595999999 ) ) ;
#4467=CARTESIAN_POINT ( 'NONE',  ( -4.623015465243438982, 12.49838439281774605, 1.255993161249728152 ) ) ;
#4468=CARTESIAN_POINT ( 'NONE',  ( -3.119235558199998870, 14.27943171969000424, 5.298223175322998024 ) ) ;
#4470=DIRECTION ( 'NONE',  ( 1.000000000000000000, 0.000000000000000000, 0.000000000000000000 ) ) ;
#4471=CARTESIAN_POINT ( 'NONE',  ( -15.43323841317000067, -10.79835415318000003, -0.2870680789784999520 ) ) ;
#4473=CARTESIAN_POINT ( 'NONE',  ( 11.50200125730999900, -7.192471199227000511, -5.535041905695000430 ) ) ;
#4474=CARTESIAN_POINT ( 'NONE',  ( 18.93770726999534304, 2.186149537270711818, 10.20320327474726518 ) ) ;
#4475=EDGE_CURVE ( 'NONE', #17483, #12075, #18852, .T. ) ;
#4476=VERTEX_POINT ( 'NONE', #13755 ) ;
#4477=CARTESIAN_POINT ( 'NONE',  ( 21.15333103379665758, 7.368134783748077510, -5.662595685174294680 ) ) ;
#4480=CARTESIAN_POINT ( 'NONE',  ( 1.677186332128803858, 13.82756761789674016, -5.893844231589445037 ) ) ;
#4481=ORIENTED_EDGE ( 'NONE', *, *, #4685, .F. ) ;
#4482=CARTESIAN_POINT ( 'NONE',  ( -3.762852402474997859, 13.17351449657999751, -6.004728637638001132 ) ) ;
#4483=CARTESIAN_POINT ( 'NONE',  ( -24.33938584177417397, 12.23286334202277814, -3.811912743503483636 ) ) ;
#4485=CARTESIAN_POINT ( 'NONE',  ( 11.92450592358672345, -4.711271677206839037, 12.50004466715123819 ) ) ;
#4486=CARTESIAN_POINT ( 'NONE',  ( 18.57372678207664407, 7.390588772882653146, 7.422355515149504868 ) ) ;
#4487=CARTESIAN_POINT ( 'NONE',  ( -4.473272619823412732, 13.51709772982548863, 5.071849929001408519 ) ) ;
#4490=ORIENTED_EDGE ( 'NONE', *, *, #3324, .F. ) ;
#4491=CARTESIAN_POINT ( 'NONE',  ( 19.07919363423065207, -2.897106654752859889, 10.08163500782726452 ) ) ;
#4492=AXIS2_PLACEMENT_3D ( 'NONE', #20335, #3521, #16450 ) ;
#4493=CARTESIAN_POINT ( 'NONE',  ( 11.39490977864459254, -9.382231423108610358, 8.749413452969770688 ) ) ;
#4494=ORIENTED_EDGE ( 'NONE', *, *, #16073, .T. ) ;
#4496=CARTESIAN_POINT ( 'NONE',  ( -0.9083185118202660169, 12.83142204585589141, 6.609727340865822143 ) ) ;
#4497=B_SPLINE_CURVE_WITH_KNOTS ( 'NONE', 3,
 ( #18899, #18772, #6178, #9576, #2308, #21074, #16961, #4486, #17077, #6296, #474, #15245, #2542, #22637, #6049, #4253, #11876, #19010, #11757, #2423, #9812, #17197, #592, #22415, #7995, #22759, #13678, #13565, #9932, #19129, #17318, #7642, #721, #10063, #15494, #239, #13205, #15015, #8490, #15610, #3044, #13800, #19387, #8244, #12370, #15856, #21199, #12124, #23363, #841, #6781, #10181, #12247, #10302, #14052, #6905, #14173, #4983, #5103, #12003, #10550, #23245, #10431, #964, #17821, #8731, #6658, #13928, #17571, #19758, #21323, #1092, #1216, #8607, #3167, #21572, #15731, #16092, #8363, #14298, #4614, #17693, #19869, #4738, #2921, #21445, #2799, #23118, #22998, #17934, #23493, #21691, #6544, #19511, #4859, #12484, #3285, #17448, #5447, #3628, #9314, #23839, #1585, #18288, #22255, #1688, #16688, #14410, #7133, #18516, #21802 ),
 .UNSPECIFIED., .F., .F.,
 ( 4, 2, 2, 2, 1, 2, 2, 2, 2, 2, 2, 2, 2, 2, 2, 2, 2, 2, 2, 2, 2, 2, 2, 2, 2, 2, 1, 2, 2, 2, 2, 2, 2, 2, 2, 2, 2, 2, 2, 2, 2, 2, 2, 2, 2, 2, 2, 2, 2, 2, 1, 2, 2, 2, 2, 2, 4 ),
 ( 0.000000000000000000, 0.01562500000000002429, 0.03125000000000004857, 0.04687500000000006939, 0.06250000000000009714, 0.07812500000000012490, 0.09375000000000012490, 0.1093750000000001388, 0.1250000000000001388, 0.1406250000000001665, 0.1562500000000001943, 0.1718750000000001943, 0.1875000000000001665, 0.2187500000000001665, 0.2500000000000001665, 0.2812500000000001665, 0.3125000000000001665, 0.3281250000000001665, 0.3437500000000001665, 0.3593750000000001110, 0.3750000000000000555, 0.3906250000000000555, 0.4062500000000000000, 0.4218750000000000000, 0.4374999999999999445, 0.4531249999999999445, 0.4687499999999998890, 0.4843749999999998890, 0.4999999999999998335, 0.5156249999999997780, 0.5312499999999997780, 0.5468749999999998890, 0.5624999999999998890, 0.5781249999999998890, 0.5937499999999998890, 0.6093750000000000000, 0.6250000000000000000, 0.6562499999999998890, 0.6874999999999998890, 0.7187499999999997780, 0.7499999999999996669, 0.7656249999999997780, 0.7812499999999997780, 0.7968749999999997780, 0.8124999999999997780, 0.8281249999999998890, 0.8437499999999998890, 0.8593749999999998890, 0.8749999999999998890, 0.8906249999999998890, 0.9062500000000000000, 0.9218750000000000000, 0.9375000000000000000, 0.9531250000000000000, 0.9687500000000001110, 0.9843750000000001110, 1.000000000000000000 ),
 .UNSPECIFIED. ) ;
#4498=DIRECTION ( 'NONE',  ( 0.000000000000000000, 0.000000000000000000, -1.000000000000000000 ) ) ;
#4499=CARTESIAN_POINT ( 'NONE',  ( -21.02465558280167102, 9.210815812710263728, 1.074409851512047709 ) ) ;
#4500=EDGE_CURVE ( 'NONE', #18008, #2459, #16907, .T. ) ;
#4504=CARTESIAN_POINT ( 'NONE',  ( -14.00000000000000178, 6.538808555185156024, -6.342236805579152481 ) ) ;
#4506=PLANE ( 'NONE',  #9800 ) ;
#4507=EDGE_CURVE ( 'NONE', #3740, #11779, #23881, .T. ) ;
#4513=CARTESIAN_POINT ( 'NONE',  ( 15.67109199796810870, -8.941468266330055314, 5.214144890658016784 ) ) ;
#4515=CARTESIAN_POINT ( 'NONE',  ( -14.73144114140000127, 5.129804779319999675, 9.743316905584000764 ) ) ;
#4517=CARTESIAN_POINT ( 'NONE',  ( -20.66446177431374664, 5.378666414508218807, -9.027109991765231101 ) ) ;
#4524=CARTESIAN_POINT ( 'NONE',  ( -15.90997336282494068, -10.10479736080180935, 2.829305410829486167 ) ) ;
#4527=CARTESIAN_POINT ( 'NONE',  ( 6.081233116141000927, 14.07697478751998865, -0.1743049402906998169 ) ) ;
#4528=CARTESIAN_POINT ( 'NONE',  ( 12.00000000000000000, -8.391897884961000642, -3.194141202603999918 ) ) ;
#4530=CARTESIAN_POINT ( 'NONE',  ( -24.50000000000000000, 2.477372277342497320, -10.08213454178133262 ) ) ;
#4531=CARTESIAN_POINT ( 'NONE',  ( 18.68456408531000079, -2.737678269967000144, 9.911560247287001246 ) ) ;
#4533=CARTESIAN_POINT ( 'NONE',  ( -20.25016455292000117, -8.657612072530000091, 3.085311466348000131 ) ) ;
#4536=VERTEX_POINT ( 'NONE', #10137 ) ;
#4538=CARTESIAN_POINT ( 'NONE',  ( 21.88941666666665853, -8.992648239743624927, 2.416837407849719899 ) ) ;
#4541=CARTESIAN_POINT ( 'NONE',  ( 18.24479701682594524, 5.317422275654474007, -8.971661253277336101 ) ) ;
#4542=AXIS2_PLACEMENT_3D ( 'NONE', #3723, #23945, #14963 ) ;
#4543=CARTESIAN_POINT ( 'NONE',  ( -19.24432910583999856, 9.165129126472001175, 0.000000000000000000 ) ) ;
#4544=CARTESIAN_POINT ( 'NONE',  ( -14.47793699669620082, -9.918738539658672693, 7.820229401576953343 ) ) ;
#4545=CARTESIAN_POINT ( 'NONE',  ( 21.00559437492999848, -10.99239965671000085, -2.243720458468000167 ) ) ;
#4548=CARTESIAN_POINT ( 'NONE',  ( -3.814110361793421777, 14.06619296737819091, -4.853167711928797701 ) ) ;
#4550=AXIS2_PLACEMENT_3D ( 'NONE', #6128, #432, #20917 ) ;
#4553=ORIENTED_EDGE ( 'NONE', *, *, #8381, .F. ) ;
#4554=CARTESIAN_POINT ( 'NONE',  ( 23.11666699040146256, 6.120247413312933205, 6.979269264195818501 ) ) ;
#4555=CARTESIAN_POINT ( 'NONE',  ( 20.27958633591999771, 5.102243454006000434, 9.587269077152999586 ) ) ;
#4556=CARTESIAN_POINT ( 'NONE',  ( 0.4857502373169989007, 12.81005527578991021, -6.651029881555492018 ) ) ;
#4558=CARTESIAN_POINT ( 'NONE',  ( -20.02841779011528445, 9.302829480802380147, 4.853780416162542188 ) ) ;
#4559=CARTESIAN_POINT ( 'NONE',  ( -24.49594166687721497, -11.08137607233546262, -5.806427241621102020 ) ) ;
#4562=CARTESIAN_POINT ( 'NONE',  ( -2.200752960429002592, 11.65894100333001049, -4.414476351808999333 ) ) ;
#4568=ORIENTED_EDGE ( 'NONE', *, *, #20286, .F. ) ;
#4569=CARTESIAN_POINT ( 'NONE',  ( -12.25000000000000000, 15.43375672974000068, 0.000000000000000000 ) ) ;
#4570=CARTESIAN_POINT ( 'NONE',  ( 19.04006424931000296, -6.376715009848999749, 8.397789983599000863 ) ) ;
#4571=CARTESIAN_POINT ( 'NONE',  ( -20.52603093369999954, 8.128879616565001243, -7.602789782659999496 ) ) ;
#4572=CARTESIAN_POINT ( 'NONE',  ( -16.03545417928000205, -10.81513078882999856, -0.2875120158770000378 ) ) ;
#4574=CARTESIAN_POINT ( 'NONE',  ( 15.46437451745999958, 7.273707250726999973, -6.465632430407000086 ) ) ;
#4580=CARTESIAN_POINT ( 'NONE',  ( 5.972633094028000578, 13.70648281483999931, -2.690721685423999698 ) ) ;
#4581=ORIENTED_EDGE ( 'NONE', *, *, #42, .F. ) ;
#4582=CARTESIAN_POINT ( 'NONE',  ( -2.122717293740024047, 13.91157511087565801, 5.745406846198405582 ) ) ;
#4584=CARTESIAN_POINT ( 'NONE',  ( 1.622513874808999113, 11.61236050540001408, 4.518257084142999425 ) ) ;
#4586=CIRCLE ( 'NONE', #13453, 15.43375672974000068 ) ;
#4588=CARTESIAN_POINT ( 'NONE',  ( -22.91770619432000089, -5.961201402843000707, -9.398931195371998726 ) ) ;
#4592=ADVANCED_FACE ( 'NONE', ( #6503 ), #4699, .F. ) ;
#4593=CARTESIAN_POINT ( 'NONE',  ( -24.27585716845587172, 3.329860787255026988, -12.49993117326402725 ) ) ;
#4595=CARTESIAN_POINT ( 'NONE',  ( 2.226738457365001533, 12.92672802123999354, 6.099565130748998421 ) ) ;
#4600=CARTESIAN_POINT ( 'NONE',  ( -18.31782136596999777, 10.89202446812999980, 3.425794516969999925 ) ) ;
#4601=CARTESIAN_POINT ( 'NONE',  ( 12.37950125730999851, 7.739157895793999487, 4.784640364371000487 ) ) ;
#4605=CARTESIAN_POINT ( 'NONE',  ( -22.60725550533547334, 5.683890395623710567, 7.397078122659952903 ) ) ;
#4608=CARTESIAN_POINT ( 'NONE',  ( 1.115062346912461422, 13.75187981430681994, -6.022941901177309099 ) ) ;
#4610=CARTESIAN_POINT ( 'NONE',  ( 3.471681479329000730, 13.09611127607998604, -6.183014710993997021 ) ) ;
#4612=CARTESIAN_POINT ( 'NONE',  ( -6.250000000000000000, 1.301187224093999891E-14, 0.000000000000000000 ) ) ;
#4613=DIRECTION ( 'NONE',  ( 0.000000000000000000, -1.000000000000000000, 0.000000000000000000 ) ) ;
#4614=CARTESIAN_POINT ( 'NONE',  ( 14.78242786698757527, 10.12212803168152320, 2.276770427703745714 ) ) ;
#4615=CARTESIAN_POINT ( 'NONE',  ( -9.042815982636001948, 20.50000000000000000, 1.000000000000000000 ) ) ;
#4616=CARTESIAN_POINT ( 'NONE',  ( -6.250000000003000267, 15.09565008225999883, -3.212814891752000079 ) ) ;
#4617=CARTESIAN_POINT ( 'NONE',  ( -24.50000000000293454, -10.69708164072830847, 6.472111105557278421 ) ) ;
#4618=ORIENTED_EDGE ( 'NONE', *, *, #2464, .T. ) ;
#4619=CARTESIAN_POINT ( 'NONE',  ( -24.49999999999999645, -9.591485339921462128, -4.011769179669027352 ) ) ;
#4620=CARTESIAN_POINT ( 'NONE',  ( -1.256379856539187267, 11.63154580748610911, -4.622687534862957470 ) ) ;
#4621=VERTEX_POINT ( 'NONE', #7957 ) ;
#4623=EDGE_CURVE ( 'NONE', #16623, #2832, #21501, .T. ) ;
#4626=CARTESIAN_POINT ( 'NONE',  ( -4.254430764150507471, 13.40513193608355103, 5.356630145924516917 ) ) ;
#4628=CARTESIAN_POINT ( 'NONE',  ( 16.75703476075999987, 10.47950889854999801, -3.590276921464000015 ) ) ;
#4629=CARTESIAN_POINT ( 'NONE',  ( -5.330032540885996539, 15.50909013537999037, -2.864334533482998602 ) ) ;
#4630=AXIS2_PLACEMENT_3D ( 'NONE', #8606, #8730, #4613 ) ;
#4634=CARTESIAN_POINT ( 'NONE',  ( -14.00000000000000355, -9.419675942593046969, -3.728492687917730031 ) ) ;
#4636=FACE_OUTER_BOUND ( 'NONE', #16977, .T. ) ;
#4637=ORIENTED_EDGE ( 'NONE', *, *, #16712, .F. ) ;
#4641=CARTESIAN_POINT ( 'NONE',  ( 15.15874227237765659, 6.918783474670889611, 7.681163286608844842 ) ) ;
#4642=CARTESIAN_POINT ( 'NONE',  ( -16.39145269483999812, 4.899706566793000206, 9.911772188210001389 ) ) ;
#4645=CARTESIAN_POINT ( 'NONE',  ( -20.02108363062186669, 3.882350337173073207, 9.834850751737567620 ) ) ;
#4646=CARTESIAN_POINT ( 'NONE',  ( 4.736747859573000596, 12.61325828439998986, 0.1514365790727000005 ) ) ;
#4647=CARTESIAN_POINT ( 'NONE',  ( -16.28651788626999775, 5.579994563924000062, 9.896790535726999849 ) ) ;
#4648=EDGE_CURVE ( 'NONE', #19046, #11301, #372, .T. ) ;
#4652=CARTESIAN_POINT ( 'NONE',  ( -16.02573005821852092, -8.129144771390043545, 6.492559992316535578 ) ) ;
#4654=VERTEX_POINT ( 'NONE', #12202 ) ;
#4656=CARTESIAN_POINT ( 'NONE',  ( 5.190852480600997687, 14.34138478008000206, -3.176459389033000846 ) ) ;
#4657=CARTESIAN_POINT ( 'NONE',  ( 12.00000000000000000, -6.617649098573062716, -6.069521219509731225 ) ) ;
#4658=CARTESIAN_POINT ( 'NONE',  ( 17.46779166666665617, 9.119539674411541341, 1.193618004230074803 ) ) ;
#4659=B_SPLINE_CURVE_WITH_KNOTS ( 'NONE', 3,
 ( #11216, #9036, #7558, #18245, #16530, #18354, #18704, #14712, #10969, #2112, #22104, #7205, #12892, #9503, #14936, #16647, #11333, #22332, #5747, #16877, #284, #9385, #13010, #5406, #3819, #14483, #5628, #20292, #16406 ),
 .UNSPECIFIED., .F., .F.,
 ( 4, 2, 1, 1, 1, 2, 2, 2, 1, 1, 1, 2, 2, 2, 1, 2, 2, 4 ),
 ( 0.000000000000000000, 0.1249999999999825695, 0.1874999999999737987, 0.2187499999999698852, 0.2343749999999678313, 0.2421874999999675537, 0.2499999999999673039, 0.3749999999999690803, 0.4374999999999704126, 0.4687499999999713562, 0.4843749999999720779, 0.4921874999999727440, 0.4999999999999733546, 0.6249999999999801270, 0.6874999999999827915, 0.7187499999999846789, 0.7499999999999865663, 1.000000000000000000 ),
 .UNSPECIFIED. ) ;
#4660=CARTESIAN_POINT ( 'NONE',  ( 13.50281392131000047, -8.671483154093998280, -4.205333541112000084 ) ) ;
#4662=B_SPLINE_CURVE_WITH_KNOTS ( 'NONE', 3,
 ( #8245, #11878, #17449, #15734, #19130 ),
 .UNSPECIFIED., .F., .F.,
 ( 4, 1, 4 ),
 ( 0.000000000000000000, 0.5000000000000000000, 1.000000000000000000 ),
 .UNSPECIFIED. ) ;
#4663=CARTESIAN_POINT ( 'NONE',  ( -11.94558899291999943, 2.716703440716999651, -13.81957412132000051 ) ) ;
#4667=EDGE_CURVE ( 'NONE', #1513, #1991, #3243, .T. ) ;
#4669=CARTESIAN_POINT ( 'NONE',  ( 12.40357033521693175, 7.855338663088507367, 11.39415432486939572 ) ) ;
#4671=CARTESIAN_POINT ( 'NONE',  ( -14.00000000000000000, -4.764382124690100362, 8.836888828107323235 ) ) ;
#4672=CARTESIAN_POINT ( 'NONE',  ( 17.46750683744905785, -8.705786543820593693, 5.763209729995592667 ) ) ;
#4673=FACE_OUTER_BOUND ( 'NONE', #19178, .T. ) ;
#4674=CARTESIAN_POINT ( 'NONE',  ( -14.44600769525627726, 12.24671445775786971, -3.788037462221122809 ) ) ;
#4675=CARTESIAN_POINT ( 'NONE',  ( 21.37268830086000193, -1.097984307014999938, -11.17531938858999929 ) ) ;
#4678=CARTESIAN_POINT ( 'NONE',  ( 12.50897833293000083, 7.466860214713999966, -11.77832264250999827 ) ) ;
#4680=ORIENTED_EDGE ( 'NONE', *, *, #21353, .F. ) ;
#4681=CARTESIAN_POINT ( 'NONE',  ( 22.90890952007856995, 9.256333691698992894, 1.211909054350287507 ) ) ;
#4682=CARTESIAN_POINT ( 'NONE',  ( 24.72435780780000059, -7.322751853928000543, -7.090892171531000265 ) ) ;
#4685=EDGE_CURVE ( 'NONE', #4621, #19823, #3000, .T. ) ;
#4687=CARTESIAN_POINT ( 'NONE',  ( 4.843572631659477601, 14.61404048541572820, 3.775228271240138156 ) ) ;
#4689=CARTESIAN_POINT ( 'NONE',  ( -2.202567442112000062, 11.73255007762998581, -4.445896772107005290 ) ) ;
#4691=CARTESIAN_POINT ( 'NONE',  ( -14.69785853588606450, 10.31120977210299117, 0.9820122563291259210 ) ) ;
#4694=CONICAL_SURFACE ( 'NONE', #3906, 9.161549281532000322, 0.02565634000431304615 ) ;
#4699=PLANE ( 'NONE',  #15749 ) ;
#4700=EDGE_CURVE ( 'NONE', #44, #11336, #12559, .T. ) ;
#4701=CARTESIAN_POINT ( 'NONE',  ( -12.47890960666999938, 9.613013645102999050, -12.04164784824000023 ) ) ;
#4702=CARTESIAN_POINT ( 'NONE',  ( -23.36459867855000283, -10.41392035115000070, 2.403458430719999761 ) ) ;
#4703=CARTESIAN_POINT ( 'NONE',  ( -14.07020113697999975, -0.8985174727690999896, -10.18952336305999928 ) ) ;
#4704=CARTESIAN_POINT ( 'NONE',  ( -6.222637507652000188, 15.85814527750000913, 1.061553398158999517 ) ) ;
#4705=CARTESIAN_POINT ( 'NONE',  ( 19.12062451746000136, 7.953000653253999630, -5.784009966395999847 ) ) ;
#4707=B_SPLINE_CURVE_WITH_KNOTS ( 'NONE', 3,
 ( #11297, #22771, #13450, #11531 ),
 .UNSPECIFIED., .F., .F.,
 ( 4, 4 ),
 ( 0.6207796204815331231, 1.000000000000000000 ),
 .UNSPECIFIED. ) ;
#4711=CARTESIAN_POINT ( 'NONE',  ( 0.6113494706473727724, 13.70697912404423491, 6.098629219130683232 ) ) ;
#4714=CARTESIAN_POINT ( 'NONE',  ( -20.07726891605999953, 1.668335638170999946, 10.92619773972000097 ) ) ;
#4717=CARTESIAN_POINT ( 'NONE',  ( -23.74465998031000069, -13.93375672974000068, 0.8660254037843999608 ) ) ;
#4718=CARTESIAN_POINT ( 'NONE',  ( 4.262829215123017157, 12.23638733703982773, -2.301400808804427101 ) ) ;
#4719=CARTESIAN_POINT ( 'NONE',  ( -3.887848091610002221, 14.54074437727999225, 4.743303306622997262 ) ) ;
#4721=CARTESIAN_POINT ( 'NONE',  ( 0.000000000000000000, 22.00000000000000000, 0.000000000000000000 ) ) ;
#4723=CARTESIAN_POINT ( 'NONE',  ( -19.46889333780000086, -9.261490887677000572, 5.613638565637999456 ) ) ;
#4724=CARTESIAN_POINT ( 'NONE',  ( 13.36668875730999950, -6.148145076040000490, -6.742444596879999530 ) ) ;
#4725=CARTESIAN_POINT ( 'NONE',  ( 18.96142490315194706, 1.354195692915298732, 10.35531029028993011 ) ) ;
#4726=CONICAL_SURFACE ( 'NONE', #5867, 14.37500000000000000, 0.7853981633972997312 ) ;
#4728=CARTESIAN_POINT ( 'NONE',  ( -6.042815982636000172, 21.50000000000000000, 1.000000000000000000 ) ) ;
#4730=B_SPLINE_CURVE_WITH_KNOTS ( 'NONE', 3,
 ( #14940, #7333, #2116, #5751, #22336, #20534, #290, #22109, #15065, #5519 ),
 .UNSPECIFIED., .F., .F.,
 ( 4, 2, 2, 2, 4 ),
 ( 0.5908772401967050669, 0.6931579301475288002, 0.7954386200983525335, 0.8977193100491762667, 1.000000000000000000 ),
 .UNSPECIFIED. ) ;
#4732=CARTESIAN_POINT ( 'NONE',  ( 1.048474406570862216, 13.74492151073522805, -6.034635998210232444 ) ) ;
#4734=DIRECTION ( 'NONE',  ( 1.000000000000000000, 0.000000000000000000, 0.000000000000000000 ) ) ;
#4737=LINE ( 'NONE', #3043, #15047 ) ;
#4738=CARTESIAN_POINT ( 'NONE',  ( 14.64304187746229502, 10.02171780537468138, -2.677710796655983660 ) ) ;
#4742=CARTESIAN_POINT ( 'NONE',  ( -24.50000000000000000, -10.82531754731000007, 6.250000000000000000 ) ) ;
#4743=ORIENTED_EDGE ( 'NONE', *, *, #22654, .F. ) ;
#4745=CARTESIAN_POINT ( 'NONE',  ( 11.48478210366629426, -9.189386602278768024, 9.083340531715208499 ) ) ;
#4746=ORIENTED_EDGE ( 'NONE', *, *, #1055, .F. ) ;
#4749=CARTESIAN_POINT ( 'NONE',  ( 2.656543060185477145, 13.04243739147230841, 6.182893541209614874 ) ) ;
#4751=CARTESIAN_POINT ( 'NONE',  ( 6.156715153800679907, 14.09036096121806736, -0.3579005024942175650 ) ) ;
#4752=CARTESIAN_POINT ( 'NONE',  ( -20.72159387545667286, 3.650365305096916924, 8.516053178569631399 ) ) ;
#4755=CARTESIAN_POINT ( 'NONE',  ( -4.900699999999999612, 1.284663064832999817E-14, 0.000000000000000000 ) ) ;
#4759=CARTESIAN_POINT ( 'NONE',  ( -20.60455590132000125, -6.094466645755999501, -8.781673769740001134 ) ) ;
#4760=CARTESIAN_POINT ( 'NONE',  ( 25.72500000000000142, 0.000000000000000000, 0.000000000000000000 ) ) ;
#4762=CARTESIAN_POINT ( 'NONE',  ( 14.97329753049621637, 10.12988386828463483, 2.035425917223504744 ) ) ;
#4763=CARTESIAN_POINT ( 'NONE',  ( -14.06900898629000096, -10.21389801573999989, -2.520607692115000020 ) ) ;
#4765=CARTESIAN_POINT ( 'NONE',  ( 18.75008227645999881, 0.000000000000000000, 0.000000000000000000 ) ) ;
#4766=CARTESIAN_POINT ( 'NONE',  ( 13.52097745565073694, 5.132826260074074831, -7.447908584389146824 ) ) ;
#4767=CARTESIAN_POINT ( 'NONE',  ( -4.776902322660998124, 12.47834578811000483, 0.1510698533714998903 ) ) ;
#4768=VECTOR ( 'NONE', #10319, 1000.000000000000000 ) ;
#4769=CARTESIAN_POINT ( 'NONE',  ( -14.00000000000000000, -10.27687089286999900, -0.6428416445564000270 ) ) ;
#4771=ORIENTED_EDGE ( 'NONE', *, *, #10719, .F. ) ;
#4773=CARTESIAN_POINT ( 'NONE',  ( -14.46301467040578892, -0.3024465970358821698, 10.35139680070230916 ) ) ;
#4775=CARTESIAN_POINT ( 'NONE',  ( -23.74465998031000069, 6.216878364870000340, -12.50000000000000000 ) ) ;
#4776=CARTESIAN_POINT ( 'NONE',  ( 4.909136497312005076, 14.89158879234001986, -3.677509687533000893 ) ) ;
#4777=EDGE_CURVE ( 'NONE', #16006, #4621, #4160, .T. ) ;
#4778=CARTESIAN_POINT ( 'NONE',  ( 12.00000000000000000, -5.414213694566718083, -7.209897367101869570 ) ) ;
#4779=B_SPLINE_CURVE_WITH_KNOTS ( 'NONE', 3,
 ( #12019, #19400, #6062, #8380, #2322, #2814, #17586, #15748, #6559, #13943, #4268, #22773 ),
 .UNSPECIFIED., .F., .F.,
 ( 4, 1, 1, 1, 1, 2, 2, 4 ),
 ( 0.000000000000000000, 0.2499999999999981681, 0.3749999999999972244, 0.4374999999999967804, 0.4687499999999966138, 0.4843749999999967248, 0.4999999999999967804, 1.000000000000000000 ),
 .UNSPECIFIED. ) ;
#4780=CARTESIAN_POINT ( 'NONE',  ( -20.37217920454666498, -8.954726317883316966, -2.406646174506601898 ) ) ;
#4781=CARTESIAN_POINT ( 'NONE',  ( 14.29706408530999973, 7.153286345558000470, -7.225396115407999531 ) ) ;
#4782=VERTEX_POINT ( 'NONE', #18708 ) ;
#4784=CARTESIAN_POINT ( 'NONE',  ( -8.789091492920999116, 10.90342355828000009, -9.585088201729998758 ) ) ;
#4787=CARTESIAN_POINT ( 'NONE',  ( 11.40904387244028939, 12.29944272054195942, 3.696645716850592400 ) ) ;
#4789=CARTESIAN_POINT ( 'NONE',  ( -4.841618408765723913, 13.27908324391153627, -5.800473559599023332 ) ) ;
#4790=CARTESIAN_POINT ( 'NONE',  ( 16.27408216237130389, -0.09528988118115871986, -10.36544040251896526 ) ) ;
#4792=DIRECTION ( 'NONE',  ( 0.000000000000000000, 0.000000000000000000, -1.000000000000000000 ) ) ;
#4793=ADVANCED_FACE ( 'NONE', ( #16652 ), #9278, .T. ) ;
#4794=CARTESIAN_POINT ( 'NONE',  ( -14.49863740493600339, -11.08451042427809519, 5.800992024733008456 ) ) ;
#4795=CARTESIAN_POINT ( 'NONE',  ( -3.915804718101239423, 13.94229419359897015, -4.846387647554452727 ) ) ;
#4796=CARTESIAN_POINT ( 'NONE',  ( -24.50000000000000000, 10.82531754731000007, -6.250000000000000000 ) ) ;
#4798=VERTEX_POINT ( 'NONE', #11092 ) ;
#4799=CARTESIAN_POINT ( 'NONE',  ( -24.50000000000452971, -0.5124611670954127840, 12.50000000000233946 ) ) ;
#4800=CARTESIAN_POINT ( 'NONE',  ( 24.14460500711999913, -3.573525003673000189, 10.36867931893000083 ) ) ;
#4801=CARTESIAN_POINT ( 'NONE',  ( 23.50544148562050140, -1.024754352332091445, -10.55397606538692479 ) ) ;
#4803=ORIENTED_EDGE ( 'NONE', *, *, #5527, .T. ) ;
#4805=FACE_OUTER_BOUND ( 'NONE', #7299, .T. ) ;
#4807=CARTESIAN_POINT ( 'NONE',  ( 4.644870904606005269, 12.40269947270000372, -1.737130352826000257 ) ) ;
#4808=ORIENTED_EDGE ( 'NONE', *, *, #11921, .T. ) ;
#4809=CARTESIAN_POINT ( 'NONE',  ( -16.56791143023856350, 10.36026656484473563, -1.037743970940367966 ) ) ;
#4813=CARTESIAN_POINT ( 'NONE',  ( -14.41332695378262585, -3.614289100528644383, -12.49991738135552488 ) ) ;
#4815=CARTESIAN_POINT ( 'NONE',  ( -18.96831264622833757, -3.696727937718024659, 8.446581985469661547 ) ) ;
#4816=CARTESIAN_POINT ( 'NONE',  ( -4.001664678273323617, 14.92001132474814895, -4.637136486520930134 ) ) ;
#4817=CARTESIAN_POINT ( 'NONE',  ( -14.32510917350998803, -2.162566426017664689, -8.825035394896943330 ) ) ;
#4819=CARTESIAN_POINT ( 'NONE',  ( -20.16411157606999893, -6.838742577979000536, 6.702193969124000006 ) ) ;
#4820=CARTESIAN_POINT ( 'NONE',  ( 22.38070833333331677, -1.210375094748616709, -9.245614798928990297 ) ) ;
#4821=EDGE_CURVE ( 'NONE', #12346, #9620, #14766, .T. ) ;
#4822=CARTESIAN_POINT ( 'NONE',  ( 14.38056994526000132, -9.435743274165000471, 3.981841483676999527 ) ) ;
#4823=CARTESIAN_POINT ( 'NONE',  ( -11.75044449363000076, 1.368548241523999952E-14, 0.000000000000000000 ) ) ;
#4824=CARTESIAN_POINT ( 'NONE',  ( 19.75818759120999957, -0.05617709961787999834, 9.259200605838000087 ) ) ;
#4825=CARTESIAN_POINT ( 'NONE',  ( 15.54041666666666011, 8.833960962437073405, -2.374191386965657458 ) ) ;
#4826=ORIENTED_EDGE ( 'NONE', *, *, #16612, .F. ) ;
#4830=CARTESIAN_POINT ( 'NONE',  ( -20.00016243917331593, -8.025264609412063876, -4.625618550852887978 ) ) ;
#4831=CARTESIAN_POINT ( 'NONE',  ( -23.08479074010000076, -10.13546262256000219, -4.609682220154000198 ) ) ;
#4832=EDGE_CURVE ( 'NONE', #17213, #9887, #6170, .T. ) ;
#4833=EDGE_CURVE ( 'NONE', #12220, #6975, #4730, .T. ) ;
#4834=FACE_OUTER_BOUND ( 'NONE', #14080, .T. ) ;
#4836=CARTESIAN_POINT ( 'NONE',  ( 0.7413504348446855463, 11.50606621628979376, 4.755316385197891904 ) ) ;
#4839=CARTESIAN_POINT ( 'NONE',  ( -24.17970357213072319, -4.108081272002119810, -12.49999456974979850 ) ) ;
#4842=CARTESIAN_POINT ( 'NONE',  ( 11.64693288521071146, -5.045341008171505770, -7.448699753728570627 ) ) ;
#4843=CARTESIAN_POINT ( 'NONE',  ( -3.000000000000000000, 20.00000000000000000, 0.000000000000000000 ) ) ;
#4845=CARTESIAN_POINT ( 'NONE',  ( -16.89590893017999562, 5.628454363070000355, -9.888856528401998247 ) ) ;
#4846=CARTESIAN_POINT ( 'NONE',  ( 12.84468892131000040, 2.447276857699999919, 9.303608529293999396 ) ) ;
#4847=CARTESIAN_POINT ( 'NONE',  ( 18.88799200410561596, 3.848042924961065925, 9.710018918712066238 ) ) ;
#4849=CARTESIAN_POINT ( 'NONE',  ( 5.202457668997545248, 13.92662484198413786, 4.051450832662363055 ) ) ;
#4852=DIRECTION ( 'NONE',  ( 0.000000000000000000, 0.8660254037844288266, -0.5000000000000169864 ) ) ;
#4857=CARTESIAN_POINT ( 'NONE',  ( 12.52688711657000020, 7.716878364870000340, -11.63397459621999985 ) ) ;
#4859=CARTESIAN_POINT ( 'NONE',  ( 14.19700671098188494, -2.419028854851438481, -10.07012218490691602 ) ) ;
#4861=CARTESIAN_POINT ( 'NONE',  ( -21.36066243917331420, 4.643201456420162465, -8.055771210932663351 ) ) ;
#4864=EDGE_CURVE ( 'NONE', #13328, #15471, #23201, .T. ) ;
#4866=CARTESIAN_POINT ( 'NONE',  ( 11.06626444616127181, -10.69977336182518890, 6.467440677471968158 ) ) ;
#4869=CARTESIAN_POINT ( 'NONE',  ( 18.85240113949000218, -1.886779804701000041, 10.26112574610000117 ) ) ;
#4870=CARTESIAN_POINT ( 'NONE',  ( 4.108814524948330771, 13.36799685942058424, 5.443337052582164937 ) ) ;
#4871=TOROIDAL_SURFACE ( 'NONE', #16066, 4.649999999999999467, 0.1000000000000000056 ) ;
#4872=CARTESIAN_POINT ( 'NONE',  ( 12.52688711657000020, 13.93375672974000068, 0.8660254037843999608 ) ) ;
#4875=VERTEX_POINT ( 'NONE', #2726 ) ;
#4877=DIRECTION ( 'NONE',  ( -1.000000000000000000, 0.000000000000000000, 0.000000000000000000 ) ) ;
#4879=ORIENTED_EDGE ( 'NONE', *, *, #13460, .T. ) ;
#4880=CARTESIAN_POINT ( 'NONE',  ( -18.81836685165999867, -9.538331588883998791, -0.2187837708677999871 ) ) ;
#4882=CARTESIAN_POINT ( 'NONE',  ( 14.93427632872033151, 10.32886035222818144, 0.5993738056831997563 ) ) ;
#4883=CARTESIAN_POINT ( 'NONE',  ( 24.39431354042982747, 9.829649394705615606, 2.587219325858395311E-05 ) ) ;
#4886=CARTESIAN_POINT ( 'NONE',  ( 13.54033214797704510, 5.602808354962728110, -7.083871603166172370 ) ) ;
#4887=CARTESIAN_POINT ( 'NONE',  ( -3.534157655880000082, 12.11469834677999735, -3.146902133593000528 ) ) ;
#4889=CIRCLE ( 'NONE', #19972, 13.77250448649000525 ) ;
#4890=CARTESIAN_POINT ( 'NONE',  ( -13.03643231875999930, 10.05168146521000061, -2.584826834016999531 ) ) ;
#4893=CARTESIAN_POINT ( 'NONE',  ( -5.833999999999999631, 1.296092693409999996E-14, 0.000000000000000000 ) ) ;
#4894=CARTESIAN_POINT ( 'NONE',  ( -17.24117535985082839, -1.801531964190819846, -10.27922315481419879 ) ) ;
#4896=CARTESIAN_POINT ( 'NONE',  ( 5.087085786689997668, 13.95627596892002309, -4.275520105690998385 ) ) ;
#4898=CARTESIAN_POINT ( 'NONE',  ( 18.92995383753999761, -3.765411593996000228, 9.972057857162001326 ) ) ;
#4899=EDGE_CURVE ( 'NONE', #17895, #744, #5045, .T. ) ;
#4900=CARTESIAN_POINT ( 'NONE',  ( 16.81987658530999852, -0.9597138970337001362, 10.18860816546999892 ) ) ;
#4904=CARTESIAN_POINT ( 'NONE',  ( -9.807316492921000162, 3.926761037699000312, 13.97645183750999998 ) ) ;
#4906=CARTESIAN_POINT ( 'NONE',  ( 0.000000000000000000, 20.00000000000000000, 0.000000000000000000 ) ) ;
#4907=ORIENTED_EDGE ( 'NONE', *, *, #10862, .F. ) ;
#4908=DIRECTION ( 'NONE',  ( 0.000000000000000000, 1.000000000000000000, 0.000000000000000000 ) ) ;
#4909=CARTESIAN_POINT ( 'NONE',  ( 24.50000000000000000, -8.246372141814999779, 6.625187740483999832 ) ) ;
#4910=CARTESIAN_POINT ( 'NONE',  ( 16.37938660649435008, 3.607586543031612081, -9.735980039821285459 ) ) ;
#4911=CARTESIAN_POINT ( 'NONE',  ( -5.212518166047371615, 14.09657958914241327, 5.244949423492627716 ) ) ;
#4913=CARTESIAN_POINT ( 'NONE',  ( -14.49863740493600339, 11.08451042427808630, -5.800992024733025332 ) ) ;
#4915=CARTESIAN_POINT ( 'NONE',  ( -3.973605493815425049, 13.87927994308086177, -4.849889199551084218 ) ) ;
#4916=DIRECTION ( 'NONE',  ( 1.000000000000000000, 0.000000000000000000, 0.000000000000000000 ) ) ;
#4919=CARTESIAN_POINT ( 'NONE',  ( -24.50000000000000000, 2.324045842668999493E-14, 12.50000000000000000 ) ) ;
#4920=CARTESIAN_POINT ( 'NONE',  ( 20.85933913659999916, -10.86187836322000067, 0.5627353714132999896 ) ) ;
#4921=CARTESIAN_POINT ( 'NONE',  ( 21.96499999999999986, -9.234946903777000671, 0.000000000000000000 ) ) ;
#4924=ORIENTED_EDGE ( 'NONE', *, *, #19914, .T. ) ;
#4926=CARTESIAN_POINT ( 'NONE',  ( 4.850875767706668285, 14.57047331221209241, 3.780275422591365508 ) ) ;
#4927=CARTESIAN_POINT ( 'NONE',  ( 4.324670136826001432, 12.22299900889000313, -2.374696254288002795 ) ) ;
#4930=CARTESIAN_POINT ( 'NONE',  ( -14.94905967094816290, 7.407576688393448627, -7.256950101879053427 ) ) ;
#4931=CARTESIAN_POINT ( 'NONE',  ( 12.52688711657000020, -7.716878364870000340, -11.63397459621999985 ) ) ;
#4933=AXIS2_PLACEMENT_3D ( 'NONE', #2288, #574, #18757 ) ;
#4937=EDGE_LOOP ( 'NONE', ( #23334, #671, #16910 ) ) ;
#4939=VECTOR ( 'NONE', #10225, 1000.000000000000000 ) ;
#4940=CARTESIAN_POINT ( 'NONE',  ( -3.644450799678000230, 14.33206891749000000, -4.922778709793999674 ) ) ;
#4941=CARTESIAN_POINT ( 'NONE',  ( -19.40192413892000189, -10.54206147813000172, 0.0004700072724199000481 ) ) ;
#4942=ADVANCED_FACE ( 'NONE', ( #19061 ), #4726, .T. ) ;
#4943=CARTESIAN_POINT ( 'NONE',  ( -15.69524392073999941, 5.514258150326999619, -8.668746646227001307 ) ) ;
#4944=CARTESIAN_POINT ( 'NONE',  ( -5.955309883888003419, 16.41439389789001524, 1.007156795900999935 ) ) ;
#4946=CARTESIAN_POINT ( 'NONE',  ( 15.59931994526000132, 7.986743723743999546, 6.465068481474999906 ) ) ;
#4948=CARTESIAN_POINT ( 'NONE',  ( -11.25088898725999975, -14.74911101273999847, 0.000000000000000000 ) ) ;
#4949=CARTESIAN_POINT ( 'NONE',  ( 14.97354166666666231, -5.565137440292659221, -7.241319157828933761 ) ) ;
#4951=CARTESIAN_POINT ( 'NONE',  ( -17.53780420454667777, 7.293940459210209504, 5.605577091469953643 ) ) ;
#4957=CARTESIAN_POINT ( 'NONE',  ( -24.20553229332079326, 1.579827530622199605, -10.48222709070751080 ) ) ;
#4958=CARTESIAN_POINT ( 'NONE',  ( -24.92272074369000023, -9.957998588256000261, -3.566033666137000235 ) ) ;
#4959=CARTESIAN_POINT ( 'NONE',  ( -4.850000000102999920, 12.44999864901999942, -1.732907964652000048E-09 ) ) ;
#4961=CARTESIAN_POINT ( 'NONE',  ( -3.644446339697000159, 14.33206891720999998, 4.922772686299000000 ) ) ;
#4963=CARTESIAN_POINT ( 'NONE',  ( 4.737384275571143277, 12.40724550023213979, -1.031760218791433648 ) ) ;
#4964=CARTESIAN_POINT ( 'NONE',  ( -10.24501790109506771, 15.78861284533561360, 1.147143686903685289 ) ) ;
#4968=CARTESIAN_POINT ( 'NONE',  ( -16.48964823424000059, 10.66299948276999920, 3.938515806081000825 ) ) ;
#4970=CARTESIAN_POINT ( 'NONE',  ( 14.05125142131000082, 6.790538403688000102, -6.859017754185999571 ) ) ;
#4971=CARTESIAN_POINT ( 'NONE',  ( 18.97467215409325547, 0.8747362461518826127, 10.41931741152851565 ) ) ;
#4972=ORIENTED_EDGE ( 'NONE', *, *, #20921, .T. ) ;
#4973=EDGE_CURVE ( 'NONE', #11532, #15235, #8982, .T. ) ;
#4974=CARTESIAN_POINT ( 'NONE',  ( -14.25243324638999809, 6.216878364870000340, 12.50000000000000000 ) ) ;
#4976=CARTESIAN_POINT ( 'NONE',  ( -14.70932910584000020, -9.048752088456000209, 0.000000000000000000 ) ) ;
#4977=CARTESIAN_POINT ( 'NONE',  ( 3.665360768552284654, 14.33851491488757190, -4.911089631563983815 ) ) ;
#4978=VERTEX_POINT ( 'NONE', #19316 ) ;
#4981=CARTESIAN_POINT ( 'NONE',  ( 16.37183333333332058, -7.943906292456897944, 4.578726549357134523 ) ) ;
#4983=CARTESIAN_POINT ( 'NONE',  ( 16.06477897062039162, -0.5085830284804089274, -10.39831413926051340 ) ) ;
#4984=CARTESIAN_POINT ( 'NONE',  ( -3.997397281504051492, 13.85564045854561144, 4.853569219738316676 ) ) ;
#4986=CARTESIAN_POINT ( 'NONE',  ( 4.944937400867998711, 12.51442848420999177, -0.02374814528528999477 ) ) ;
#4987=CARTESIAN_POINT ( 'NONE',  ( 20.43528936713000377, -9.195691514035999603, 0.000000000000000000 ) ) ;
#4992=EDGE_LOOP ( 'NONE', ( #18013, #7675, #19460, #14610 ) ) ;
#4996=CARTESIAN_POINT ( 'NONE',  ( -12.06624327026013077, 1.367011989547999955E-14, 0.000000000000000000 ) ) ;
#4998=B_SPLINE_CURVE_WITH_KNOTS ( 'NONE', 3,
 ( #2347, #12578, #9737, #22328, #17122, #7920, #19965, #10767, #22209, #14933, #18161, #1563, #8948, #5624, #21363, #10350, #4658, #19306 ),
 .UNSPECIFIED., .F., .F.,
 ( 4, 2, 2, 2, 2, 2, 2, 2, 4 ),
 ( 0.000000000000000000, 0.1250000000000000000, 0.2500000000000000000, 0.3750000000000000000, 0.4999999999999999445, 0.6250000000000000000, 0.7500000000000000000, 0.8750000000000000000, 1.000000000000000000 ),
 .UNSPECIFIED. ) ;
#4999=CARTESIAN_POINT ( 'NONE',  ( 6.237174757059936070, 13.69932272150512986, -1.574127311046002564 ) ) ;
#5000=LINE ( 'NONE', #12260, #10615 ) ;
#5001=CARTESIAN_POINT ( 'NONE',  ( 5.699442596042000098, 1.405570106087591467E-14, 14.15464499511999996 ) ) ;
#5006=DIRECTION ( 'NONE',  ( 0.000000000000000000, -0.8660254037844288266, -0.5000000000000169864 ) ) ;
#5008=EDGE_CURVE ( 'NONE', #7629, #16706, #7929, .T. ) ;
#5009=CARTESIAN_POINT ( 'NONE',  ( -19.50383379408999929, 7.131897092901000157, 7.202928260512999614 ) ) ;
#5011=CARTESIAN_POINT ( 'NONE',  ( 14.88774677762132548, 10.27520863958742225, -1.073445734337063362 ) ) ;
#5013=DIRECTION ( 'NONE',  ( -1.000000000000000000, 0.000000000000000000, 0.000000000000000000 ) ) ;
#5015=CARTESIAN_POINT ( 'NONE',  ( -23.16929462096833703, 9.265295224643226746, 1.607743681355135241E-05 ) ) ;
#5016=CARTESIAN_POINT ( 'NONE',  ( -2.674561911689002702, 11.95584864995998942, -3.929436066563998686 ) ) ;
#5023=CARTESIAN_POINT ( 'NONE',  ( -14.37619714886207589, -3.353739287365657074, 9.799118382956658380 ) ) ;
#5024=AXIS2_PLACEMENT_3D ( 'NONE', #13684, #8497, #19264 ) ;
#5028=CARTESIAN_POINT ( 'NONE',  ( 12.00000000000000000, -0.4784485517439919233, -8.984160855930003464 ) ) ;
#5029=CARTESIAN_POINT ( 'NONE',  ( 17.03897356148999975, -6.252405066107000309, 9.153620030820999176 ) ) ;
#5030=CARTESIAN_POINT ( 'NONE',  ( 12.98081408531000136, 6.028018288394999757, 8.144720004203000130 ) ) ;
#5032=CARTESIAN_POINT ( 'NONE',  ( -10.21460649291999978, 13.31930243424999993, -5.775538145385999300 ) ) ;
#5033=DIRECTION ( 'NONE',  ( 0.000000000000000000, 0.000000000000000000, 1.000000000000000000 ) ) ;
#5039=CARTESIAN_POINT ( 'NONE',  ( 23.14703506890763762, -6.420007756874271720, -8.432966434426246494 ) ) ;
#5040=CARTESIAN_POINT ( 'NONE',  ( -5.771212219718563574, 15.14896488348015602, 2.962084404041542829 ) ) ;
#5042=CARTESIAN_POINT ( 'NONE',  ( 16.27412392735353563, -0.09384471782549831664, -10.36545610267682349 ) ) ;
#5043=CYLINDRICAL_SURFACE ( 'NONE', #6756, 11.50000000000000000 ) ;
#5045=B_SPLINE_CURVE_WITH_KNOTS ( 'NONE', 3,
 ( #4297, #9626, #4538, #5982, #13490, #2233, #20891, #23048, #13365, #891, #409, #13854, #9864, #17010, #21005, #17373, #21127, #11931 ),
 .UNSPECIFIED., .F., .F.,
 ( 4, 2, 2, 2, 2, 2, 2, 2, 4 ),
 ( 0.000000000000000000, 0.1250000000000000555, 0.2500000000000001110, 0.3750000000000001665, 0.5000000000000001110, 0.6250000000000001110, 0.7500000000000001110, 0.8750000000000000000, 1.000000000000000000 ),
 .UNSPECIFIED. ) ;
#5046=LINE ( 'NONE', #3226, #4445 ) ;
#5047=EDGE_CURVE ( 'NONE', #4023, #837, #13364, .T. ) ;
#5049=ORIENTED_EDGE ( 'NONE', *, *, #3881, .T. ) ;
#5050=CARTESIAN_POINT ( 'NONE',  ( 18.78614059787999935, 2.403158705886000224, 10.26025450743999912 ) ) ;
#5051=CARTESIAN_POINT ( 'NONE',  ( 23.27845441632221579, -8.182943452958516772, -6.730593103882281270 ) ) ;
#5054=CARTESIAN_POINT ( 'NONE',  ( -12.50000000000000000, 7.500000000000000000, 0.000000000000000000 ) ) ;
#5055=CARTESIAN_POINT ( 'NONE',  ( 5.155702020191999857, 13.97328941143999970, -4.008166040501000893 ) ) ;
#5056=CYLINDRICAL_SURFACE ( 'NONE', #10838, 13.93375672974000068 ) ;
#5057=ORIENTED_EDGE ( 'NONE', *, *, #602, .T. ) ;
#5058=CARTESIAN_POINT ( 'NONE',  ( 16.76700125730999957, -9.205641116351999997, -0.3944625347444000174 ) ) ;
#5061=DIRECTION ( 'NONE',  ( -1.000000000000000000, 0.000000000000000000, 0.000000000000000000 ) ) ;
#5064=CARTESIAN_POINT ( 'NONE',  ( -10.04351714999000045, 16.35737901934999883, -1.000000000000000000 ) ) ;
#5065=CARTESIAN_POINT ( 'NONE',  ( 12.12975174931000133, -10.21766741648000121, -2.893652579598999797 ) ) ;
#5066=CARTESIAN_POINT ( 'NONE',  ( -19.72463381927000015, -10.05713679925000115, 1.864893016109999913 ) ) ;
#5067=CARTESIAN_POINT ( 'NONE',  ( -17.72654740043000032, -1.911761373924000029, -10.15213107020000116 ) ) ;
#5069=DIRECTION ( 'NONE',  ( 0.000000000000000000, 1.000000000000000000, 0.000000000000000000 ) ) ;
#5071=DIRECTION ( 'NONE',  ( -1.000000000000000000, 0.000000000000000000, 0.000000000000000000 ) ) ;
#5072=ADVANCED_FACE ( 'NONE', ( #16019 ), #10229, .F. ) ;
#5073=CARTESIAN_POINT ( 'NONE',  ( 15.57820833333332899, 9.071049241905111415, -1.187524516768772909 ) ) ;
#5074=ORIENTED_EDGE ( 'NONE', *, *, #23157, .F. ) ;
#5075=CARTESIAN_POINT ( 'NONE',  ( 23.61487358290123950, -0.1110235858477790771, 9.341576594489977126 ) ) ;
#5080=CARTESIAN_POINT ( 'NONE',  ( -4.745427439048141238, 12.41027624259845474, 0.9937658293378628382 ) ) ;
#5082=DIRECTION ( 'NONE',  ( 0.000000000000000000, -1.000000000000000000, 0.000000000000000000 ) ) ;
#5083=CARTESIAN_POINT ( 'NONE',  ( 3.041824996438589057, 11.87257502931641184, -3.747603760614300672 ) ) ;
#5084=ADVANCED_FACE ( 'NONE', ( #19805 ), #22491, .F. ) ;
#5085=CARTESIAN_POINT ( 'NONE',  ( -10.32545159102639687, 15.68979046979564629, 1.216685051509786897 ) ) ;
#5089=DIRECTION ( 'NONE',  ( -1.000000000000000000, 0.000000000000000000, 0.000000000000000000 ) ) ;
#5090=CARTESIAN_POINT ( 'NONE',  ( 13.61250142131000196, -6.495520710102000272, -7.123429297049000297 ) ) ;
#5091=CARTESIAN_POINT ( 'NONE',  ( 18.58801564342164880, 10.31582294119393062, 1.512955792960317458 ) ) ;
#5092=ORIENTED_EDGE ( 'NONE', *, *, #20156, .F. ) ;
#5096=CARTESIAN_POINT ( 'NONE',  ( -4.850000000102999920, 12.44999864901999942, -1.732907964652000048E-09 ) ) ;
#5097=ORIENTED_EDGE ( 'NONE', *, *, #8627, .T. ) ;
#5099=CARTESIAN_POINT ( 'NONE',  ( -24.50000000000000000, 10.82531754731000007, -6.250000000000000000 ) ) ;
#5101=DIRECTION ( 'NONE',  ( 0.000000000000000000, -1.000000000000000000, 0.000000000000000000 ) ) ;
#5102=CARTESIAN_POINT ( 'NONE',  ( -23.74802958432387001, -8.939121534312308270, 3.416678463770061125 ) ) ;
#5103=CARTESIAN_POINT ( 'NONE',  ( 16.03690177271507977, -1.513574074359952393, -10.29584712833434956 ) ) ;
#5104=CARTESIAN_POINT ( 'NONE',  ( -4.122522811283552358, 13.74083509578544593, 4.883161027967257262 ) ) ;
#5105=CARTESIAN_POINT ( 'NONE',  ( -0.1177307150814000253, 11.52529143281000756, 4.975641586845003239 ) ) ;
#5107=ORIENTED_EDGE ( 'NONE', *, *, #346, .T. ) ;
#5112=CARTESIAN_POINT ( 'NONE',  ( 6.081503308973005950, 14.07691240018000123, -0.05979963850814000448 ) ) ;
#5114=CARTESIAN_POINT ( 'NONE',  ( -19.35893705290999733, -9.828989445528000246, 3.502754984265999738 ) ) ;
#5116=CARTESIAN_POINT ( 'NONE',  ( -5.339884851010002542, 16.17859235010000418, -3.014934905543001697 ) ) ;
#5122=ORIENTED_EDGE ( 'NONE', *, *, #1441, .F. ) ;
#5123=CARTESIAN_POINT ( 'NONE',  ( -20.26182243010999784, 5.856841114788999825, -8.930757166044001494 ) ) ;
#5124=CARTESIAN_POINT ( 'NONE',  ( 23.99062354302999722, 7.716878364870000340, -11.63397459621999985 ) ) ;
#5125=CARTESIAN_POINT ( 'NONE',  ( 15.09446924968909265, 8.461638818015519092, 5.944720952507684508 ) ) ;
#5127=CARTESIAN_POINT ( 'NONE',  ( 24.12589274536999895, -0.1537909274696999951, 11.30391051099999977 ) ) ;
#5130=CARTESIAN_POINT ( 'NONE',  ( 13.60025666663938182, 6.914934984708120957, -5.791751039375853338 ) ) ;
#5132=CARTESIAN_POINT ( 'NONE',  ( -2.096968522445999739, 11.83164223350000022, -4.269451356421001265 ) ) ;
#5135=ORIENTED_EDGE ( 'NONE', *, *, #21380, .T. ) ;
#5139=ORIENTED_EDGE ( 'NONE', *, *, #6801, .F. ) ;
#5143=CARTESIAN_POINT ( 'NONE',  ( -11.00000000000000000, 1.359357947053999856E-14, 0.000000000000000000 ) ) ;
#5145=CARTESIAN_POINT ( 'NONE',  ( 15.41491548087999774, -10.50213854228000088, 3.406209761678000270 ) ) ;
#5147=CARTESIAN_POINT ( 'NONE',  ( -11.74194399291999957, 12.57219865750999865, -7.259580034594999454 ) ) ;
#5148=CARTESIAN_POINT ( 'NONE',  ( 13.50000000000000000, 8.460810473535371301, 5.109280266387623115 ) ) ;
#5149=CARTESIAN_POINT ( 'NONE',  ( -14.49999963946489423, -11.08494587600286607, -5.800314632280170635 ) ) ;
#5151=CARTESIAN_POINT ( 'NONE',  ( 11.48478210365700214, 12.46109695280949481, 3.416571976947520017 ) ) ;
#5152=CARTESIAN_POINT ( 'NONE',  ( 20.85269734244679540, -7.751883840963948558, 7.131172731233752948 ) ) ;
#5154=CARTESIAN_POINT ( 'NONE',  ( -14.00000000000000000, 6.194304242614928846, 6.983547833180894671 ) ) ;
#5155=CARTESIAN_POINT ( 'NONE',  ( 17.63245649294800188, -10.44981949161595480, 0.1351922335406884057 ) ) ;
#5156=CARTESIAN_POINT ( 'NONE',  ( -18.44683259648000018, 8.205914313535998872, -7.494097690689000224 ) ) ;
#5158=CARTESIAN_POINT ( 'NONE',  ( -17.17989538244000158, -1.375580078895000113, 9.682594755839000200 ) ) ;
#5161=CARTESIAN_POINT ( 'NONE',  ( -23.97728971654375840, -5.151501961001863528, 12.49974207333311682 ) ) ;
#5162=CARTESIAN_POINT ( 'NONE',  ( 19.36589339856000080, -11.12755619508000038, -2.338388569975000220 ) ) ;
#5164=DIRECTION ( 'NONE',  ( 1.000000000000000000, 0.000000000000000000, 0.000000000000000000 ) ) ;
#5165=ORIENTED_EDGE ( 'NONE', *, *, #20801, .F. ) ;
#5169=CARTESIAN_POINT ( 'NONE',  ( -2.759390417760998471, 11.76777182245000297, -3.989101613333998930 ) ) ;
#5171=DIRECTION ( 'NONE',  ( -1.000000000000000000, 0.000000000000000000, 0.000000000000000000 ) ) ;
#5173=DIRECTION ( 'NONE',  ( 0.000000000000000000, 1.000000000000000000, 0.000000000000000000 ) ) ;
#5177=ORIENTED_EDGE ( 'NONE', *, *, #18729, .F. ) ;
#5178=CARTESIAN_POINT ( 'NONE',  ( -15.00576253787999903, -9.056359154562001024, 0.000000000000000000 ) ) ;
#5179=CARTESIAN_POINT ( 'NONE',  ( -4.826881622125675619, 15.75359399380821657, -3.770934508614922187 ) ) ;
#5180=CARTESIAN_POINT ( 'NONE',  ( -20.47403834912999798, 9.927636560707998825, 3.742326232843000255 ) ) ;
#5181=CARTESIAN_POINT ( 'NONE',  ( -16.98007644595000087, -1.848015147739999975, 9.597958940837999720 ) ) ;
#5182=CARTESIAN_POINT ( 'NONE',  ( -5.909536333224996163, 14.79956399133001810, -4.310204494228000449 ) ) ;
#5183=CARTESIAN_POINT ( 'NONE',  ( -23.31517972632249780, -7.442898316286663096, 7.519379713872949011 ) ) ;
#5187=ORIENTED_EDGE ( 'NONE', *, *, #1258, .F. ) ;
#5188=CYLINDRICAL_SURFACE ( 'NONE', #11480, 1.000000000000000222 ) ;
#5189=FACE_OUTER_BOUND ( 'NONE', #16421, .T. ) ;
#5192=CARTESIAN_POINT ( 'NONE',  ( -24.44651966850621250, -6.713893699755834277, -8.217035123213300096 ) ) ;
#5194=CARTESIAN_POINT ( 'NONE',  ( -3.108885457403288921, 11.88968526009767501, 3.692999778167153746 ) ) ;
#5195=ORIENTED_EDGE ( 'NONE', *, *, #17181, .T. ) ;
#5196=CARTESIAN_POINT ( 'NONE',  ( -23.99212502906157951, -5.142273543674428460, -12.50000000000263434 ) ) ;
#5197=CARTESIAN_POINT ( 'NONE',  ( -10.43398789387893011, 15.58306147486352877, 1.312348021278911148 ) ) ;
#5204=B_SPLINE_CURVE_WITH_KNOTS ( 'NONE', 3,
 ( #1122, #22907, #17600, #994 ),
 .UNSPECIFIED., .F., .F.,
 ( 4, 4 ),
 ( 0.000000000000000000, 1.000000000000000000 ),
 .UNSPECIFIED. ) ;
#5205=CARTESIAN_POINT ( 'NONE',  ( 12.29625142131000004, 8.002767958507000401, -5.312704480003000995 ) ) ;
#5206=CARTESIAN_POINT ( 'NONE',  ( 18.70341255878536657, 8.877609467350925598, 5.471030932658075052 ) ) ;
#5208=CARTESIAN_POINT ( 'NONE',  ( -24.41904027020412471, 2.048447027921860730, 12.49998758062118043 ) ) ;
#5209=CARTESIAN_POINT ( 'NONE',  ( 13.50000000000000000, -4.865356088987999428, 9.073685197596999430 ) ) ;
#5211=CARTESIAN_POINT ( 'NONE',  ( -12.48432065477999942, 7.040382122447000235, -5.593108346885999005 ) ) ;
#5212=CARTESIAN_POINT ( 'NONE',  ( 13.50000000000000178, -7.950673624646070969, 6.148396972236939817 ) ) ;
#5213=ORIENTED_EDGE ( 'NONE', *, *, #7355, .T. ) ;
#5216=EDGE_CURVE ( 'NONE', #8248, #7244, #14001, .T. ) ;
#5218=DIRECTION ( 'NONE',  ( -1.000000000000000000, 0.000000000000000000, 0.000000000000000000 ) ) ;
#5221=CARTESIAN_POINT ( 'NONE',  ( -21.80950322054000168, 10.92268532154000127, 1.975424663057999908 ) ) ;
#5222=VERTEX_POINT ( 'NONE', #22770 ) ;
#5228=CARTESIAN_POINT ( 'NONE',  ( 4.423870970800860114, 13.45434385453613935, 5.228893201776090294 ) ) ;
#5229=CARTESIAN_POINT ( 'NONE',  ( 6.211427289479426683, 13.82660551420464401, -1.072280536642061799 ) ) ;
#5237=EDGE_LOOP ( 'NONE', ( #20410, #13794, #1778 ) ) ;
#5238=CARTESIAN_POINT ( 'NONE',  ( -20.87476767895000052, -6.966064718177999993, 7.414690272311999841 ) ) ;
#5240=CARTESIAN_POINT ( 'NONE',  ( 14.45765107457843790, -0.1846454227282073313, -10.32464630637213610 ) ) ;
#5242=CARTESIAN_POINT ( 'NONE',  ( 22.06995078665000065, 10.92978255278999811, 2.657704805107000023 ) ) ;
#5245=CARTESIAN_POINT ( 'NONE',  ( -22.67826950129917307, -1.210252803577252623, 9.252159271244858374 ) ) ;
#5246=CARTESIAN_POINT ( 'NONE',  ( -6.528459799380125439, 15.44739108384869652, -1.496013491918405824 ) ) ;
#5250=CIRCLE ( 'NONE', #9113, 7.000000000000000000 ) ;
#5252=ADVANCED_FACE ( 'NONE', ( #12494 ), #12382, .T. ) ;
#5254=CARTESIAN_POINT ( 'NONE',  ( 16.93870833333332016, -1.192094632364749440, -9.105962353309886126 ) ) ;
#5256=CARTESIAN_POINT ( 'NONE',  ( 18.08784964760000236, 6.116917080091000436, -9.279135471629999188 ) ) ;
#5259=VERTEX_POINT ( 'NONE', #4869 ) ;
#5260=CARTESIAN_POINT ( 'NONE',  ( -11.93084113877000085, 14.40041274848999997, 4.922277236253999710 ) ) ;
#5261=DIRECTION ( 'NONE',  ( 1.000000000000000000, 0.000000000000000000, 0.000000000000000000 ) ) ;
#5262=AXIS2_PLACEMENT_3D ( 'NONE', #12055, #2850, #15424 ) ;
#5264=CARTESIAN_POINT ( 'NONE',  ( 23.50001010374794319, 5.742227407948574225, -8.919603998024165037 ) ) ;
#5265=CARTESIAN_POINT ( 'NONE',  ( -14.00000000000000355, 7.385559139612836610, 5.491114351475929745 ) ) ;
#5266=CARTESIAN_POINT ( 'NONE',  ( 16.18747732770967929, -3.153525216371673157, -9.872168078842983974 ) ) ;
#5267=CARTESIAN_POINT ( 'NONE',  ( -16.45953613113000102, 10.95060232793000132, -1.541397029415000119 ) ) ;
#5270=CARTESIAN_POINT ( 'NONE',  ( -18.03317485555000133, 9.527592921995999831, -4.015252424095000272 ) ) ;
#5272=ORIENTED_EDGE ( 'NONE', *, *, #1441, .T. ) ;
#5273=CARTESIAN_POINT ( 'NONE',  ( 23.77835672501372599, -9.281039036324623126, -1.918975276430111748E-05 ) ) ;
#5274=CARTESIAN_POINT ( 'NONE',  ( 19.36292747085767374, -10.00180209951941990, 3.178979607523860995 ) ) ;
#5275=DIRECTION ( 'NONE',  ( -1.000000000000000000, 0.000000000000000000, 0.000000000000000000 ) ) ;
#5277=CARTESIAN_POINT ( 'NONE',  ( 24.36414987671882315, -9.252522660948818256, -8.974160653052738468 ) ) ;
#5280=CARTESIAN_POINT ( 'NONE',  ( 3.165694020515001039, 11.93377496087999035, -3.621555223535997126 ) ) ;
#5283=CARTESIAN_POINT ( 'NONE',  ( 15.77981375731000036, 8.935760978467000015, -2.138706884349000248 ) ) ;
#5288=CARTESIAN_POINT ( 'NONE',  ( -15.27030420454666881, -5.569817527973411231, 7.247409029951263015 ) ) ;
#5289=CARTESIAN_POINT ( 'NONE',  ( -21.38556587436000100, -2.927468598044000281, -9.682091324420001754 ) ) ;
#5290=CARTESIAN_POINT ( 'NONE',  ( -14.74564261827999978, -9.684186272450000743, -0.7343631782695000387 ) ) ;
#5291=FACE_OUTER_BOUND ( 'NONE', #21435, .T. ) ;
#5293=ADVANCED_FACE ( 'NONE', ( #1594 ), #4694, .F. ) ;
#5294=CARTESIAN_POINT ( 'NONE',  ( -23.75267686402872513, 7.098219836623489876, 7.857347574748650310 ) ) ;
#5298=CARTESIAN_POINT ( 'NONE',  ( 14.70899999999999963, -9.048743642952000954, 0.000000000000000000 ) ) ;
#5300=CARTESIAN_POINT ( 'NONE',  ( 23.82624429608483752, -6.322309633054134181, 6.887171283258536114 ) ) ;
#5301=PLANE ( 'NONE',  #12715 ) ;
#5302=CARTESIAN_POINT ( 'NONE',  ( 13.90456468140257762, 7.335179754185822354, -5.351963236174892558 ) ) ;
#5303=CARTESIAN_POINT ( 'NONE',  ( 6.124991240379277890, 14.37502773510814258, -0.3470611857344685913 ) ) ;
#5305=AXIS2_PLACEMENT_3D ( 'NONE', #15801, #12071, #12434 ) ;
#5307=ORIENTED_EDGE ( 'NONE', *, *, #4070, .F. ) ;
#5308=AXIS2_PLACEMENT_3D ( 'NONE', #3879, #2290, #11272 ) ;
#5309=CARTESIAN_POINT ( 'NONE',  ( -0.5142367539521975894, 11.49354789453873771, -4.785507151825866501 ) ) ;
#5310=CARTESIAN_POINT ( 'NONE',  ( -10.08844022186643308, 16.08101672535666538, 1.020213274384780711 ) ) ;
#5312=CARTESIAN_POINT ( 'NONE',  ( -20.93905420454666810, 1.205278475426004414, 9.208619112632755233 ) ) ;
#5315=CARTESIAN_POINT ( 'NONE',  ( -15.91276253787999728, 9.079634562165001199, 0.000000000000000000 ) ) ;
#5316=CARTESIAN_POINT ( 'NONE',  ( 18.43875142131000189, -2.600393254974000090, 9.414598814742999977 ) ) ;
#5317=CARTESIAN_POINT ( 'NONE',  ( 18.45153449517520272, 9.899776480682962898, -3.255785108000626593 ) ) ;
#5322=CARTESIAN_POINT ( 'NONE',  ( 13.50000000000000355, -9.639306618178025587, 1.525625742284485220 ) ) ;
#5326=CARTESIAN_POINT ( 'NONE',  ( 21.71804314170000083, 2.151407657623999992, -11.09278661996000004 ) ) ;
#5329=AXIS2_PLACEMENT_3D ( 'NONE', #15452, #17648, #13635 ) ;
#5330=FACE_OUTER_BOUND ( 'NONE', #11801, .T. ) ;
#5331=CARTESIAN_POINT ( 'NONE',  ( -3.844548120735902685, 14.02704052081174169, 4.849063890147514044 ) ) ;
#5332=CARTESIAN_POINT ( 'NONE',  ( 4.345815406654997659, 12.29811303589001170, 2.369899738314000359 ) ) ;
#5333=ADVANCED_FACE ( 'NONE', ( #23255 ), #12641, .F. ) ;
#5339=CARTESIAN_POINT ( 'NONE',  ( 6.042541019908000521, 14.08632821477999642, 0.7169115693609001694 ) ) ;
#5340=CARTESIAN_POINT ( 'NONE',  ( 11.48478210364558372, -3.271710350470782735, -12.49991250862539438 ) ) ;
#5342=DIRECTION ( 'NONE',  ( 1.000000000000000000, 0.000000000000000000, 0.000000000000000000 ) ) ;
#5344=CARTESIAN_POINT ( 'NONE',  ( -17.58615607838000372, 9.339993809354998788, 2.937842867551999859 ) ) ;
#5345=B_SPLINE_CURVE_WITH_KNOTS ( 'NONE', 3,
 ( #791, #17764, #4559, #13996, #19580, #2746, #16040, #1167, #23064, #23196 ),
 .UNSPECIFIED., .F., .F.,
 ( 4, 2, 2, 2, 4 ),
 ( 0.000000000000000000, 0.1250000000000000000, 0.2500000000000000000, 0.5000000000000000000, 1.000000000000000000 ),
 .UNSPECIFIED. ) ;
#5349=CARTESIAN_POINT ( 'NONE',  ( -22.21937821538000080, 9.009440378489999901, -6.747651641374000420 ) ) ;
#5351=CARTESIAN_POINT ( 'NONE',  ( 14.77023523311244801, 9.038162366719310725, -4.996207612869733694 ) ) ;
#5352=CARTESIAN_POINT ( 'NONE',  ( -10.04281598263999875, 21.50000000000000000, -1.000000000000000000 ) ) ;
#5353=CARTESIAN_POINT ( 'NONE',  ( 22.76721327243999937, -6.127619913867999202, 9.455514623800999274 ) ) ;
#5355=CARTESIAN_POINT ( 'NONE',  ( 13.67356850472780749, 8.184989867075946890, -3.810691912912268275 ) ) ;
#5356=CARTESIAN_POINT ( 'NONE',  ( -3.905562087987998421, 12.31943552251999208, -2.827962661607000605 ) ) ;
#5357=AXIS2_PLACEMENT_3D ( 'NONE', #20341, #3749, #18523 ) ;
#5358=CARTESIAN_POINT ( 'NONE',  ( -6.249999999202001000, 16.31160201366999729, 0.9999995866763998764 ) ) ;
#5362=CARTESIAN_POINT ( 'NONE',  ( -14.98299556802001042, -9.055909390997985753, -0.7059549453755520343 ) ) ;
#5363=CARTESIAN_POINT ( 'NONE',  ( 24.50000000000000711, -10.20789478510817183, 0.08277775137279635986 ) ) ;
#5364=VERTEX_POINT ( 'NONE', #9558 ) ;
#5366=CARTESIAN_POINT ( 'NONE',  ( -15.88087077250664336, 5.579446455848312780, -7.259938483122335029 ) ) ;
#5369=VECTOR ( 'NONE', #22617, 1000.000000000000000 ) ;
#5371=CARTESIAN_POINT ( 'NONE',  ( 15.59536637872000142, -10.51441018936999861, -3.384303748290000247 ) ) ;
#5372=CARTESIAN_POINT ( 'NONE',  ( -15.56310688998895309, -10.21939891028472225, -2.520456394419640311 ) ) ;
#5375=CARTESIAN_POINT ( 'NONE',  ( -10.70897113876999995, 10.20678111663000109, -11.28814482413000064 ) ) ;
#5377=CARTESIAN_POINT ( 'NONE',  ( 13.49999999999999645, 8.617162124728089623, -3.694302656813622576 ) ) ;
#5378=CARTESIAN_POINT ( 'NONE',  ( -14.44633158889241287, -12.24656508597831994, -3.788310138431896235 ) ) ;
#5380=CARTESIAN_POINT ( 'NONE',  ( 22.08810996438781871, 9.926075803855315627, 4.086635304993818885 ) ) ;
#5381=CARTESIAN_POINT ( 'NONE',  ( 0.000000000000000000, -1.100000000000000089, 0.000000000000000000 ) ) ;
#5382=CARTESIAN_POINT ( 'NONE',  ( 16.19333199072176299, -2.944109594543157460, -9.936999019503081954 ) ) ;
#5383=EDGE_CURVE ( 'NONE', #6063, #4443, #7978, .T. ) ;
#5385=VECTOR ( 'NONE', #10293, 1000.000000000000000 ) ;
#5388=CARTESIAN_POINT ( 'NONE',  ( -14.33607051085999906, 5.206569482801000071, -8.184903637703000001 ) ) ;
#5393=CARTESIAN_POINT ( 'NONE',  ( 20.04388867876481939, 4.856218826689362444, -9.325685060479351307 ) ) ;
#5398=CARTESIAN_POINT ( 'NONE',  ( -6.180868275463003769, 14.99143150885001674, 3.733093067224003025 ) ) ;
#5399=CARTESIAN_POINT ( 'NONE',  ( -4.762191296987998257, 12.38133858908998342, -1.240028857443999710 ) ) ;
#5400=ORIENTED_EDGE ( 'NONE', *, *, #20478, .F. ) ;
#5401=AXIS2_PLACEMENT_3D ( 'NONE', #7461, #3500, #10879 ) ;
#5402=EDGE_CURVE ( 'NONE', #21964, #3898, #4415, .T. ) ;
#5404=ORIENTED_EDGE ( 'NONE', *, *, #13392, .T. ) ;
#5406=CARTESIAN_POINT ( 'NONE',  ( -4.183874459663874390, 15.15165427196963321, 4.473433887328480907 ) ) ;
#5408=CARTESIAN_POINT ( 'NONE',  ( -14.46758738532133748, -2.198682497502864042, -12.49996900093299779 ) ) ;
#5409=VERTEX_POINT ( 'NONE', #17547 ) ;
#5410=CARTESIAN_POINT ( 'NONE',  ( 23.08070603379666252, 9.022423395855687644, -2.424839258728616276 ) ) ;
#5411=CARTESIAN_POINT ( 'NONE',  ( -20.26145907959000070, -4.462377008713000137, 9.043718231252999118 ) ) ;
#5413=CARTESIAN_POINT ( 'NONE',  ( -4.977206276429998688, 14.08710956103999123, -4.416616116876000753 ) ) ;
#5414=CARTESIAN_POINT ( 'NONE',  ( -22.54312595389323093, 3.311030361751837070, -10.15954820832290828 ) ) ;
#5421=CARTESIAN_POINT ( 'NONE',  ( -17.31105420454667154, 1.193091500503425273, 9.115517482220022671 ) ) ;
#5422=CARTESIAN_POINT ( 'NONE',  ( 3.938926221699930785, 14.43711117119245912, 4.690475690813843634 ) ) ;
#5423=CARTESIAN_POINT ( 'NONE',  ( 14.55789964817296678, -0.5615422284792254137, 9.079793271584962966 ) ) ;
#5424=CARTESIAN_POINT ( 'NONE',  ( -14.25243324638999809, 13.93375672974000068, -0.8660254037843999608 ) ) ;
#5427=CARTESIAN_POINT ( 'NONE',  ( 3.109386963286208783, 11.88982568152370511, 3.692506106354862538 ) ) ;
#5429=CARTESIAN_POINT ( 'NONE',  ( -4.216012483316842641, 12.22071140417023827, -2.378417243159645533 ) ) ;
#5430=EDGE_CURVE ( 'NONE', #17203, #5222, #18580, .T. ) ;
#5436=CARTESIAN_POINT ( 'NONE',  ( -16.74417920454665420, -8.864047873708042147, -2.382277019715667521 ) ) ;
#5437=CARTESIAN_POINT ( 'NONE',  ( 17.91675158530999923, 7.007286630565999985, -7.497846106583000214 ) ) ;
#5438=CARTESIAN_POINT ( 'NONE',  ( 18.74522683489179897, 8.029184222409153193, 6.664625274391158705 ) ) ;
#5442=CARTESIAN_POINT ( 'NONE',  ( 13.50000000000000533, -9.258200915230130335, -2.291781170659658251 ) ) ;
#5445=CARTESIAN_POINT ( 'NONE',  ( 22.42623955032000183, 5.397027846906000015, 9.949281446147001162 ) ) ;
#5446=CARTESIAN_POINT ( 'NONE',  ( -24.22578504060297533, 9.828293348740496427, 2.165122153287891926 ) ) ;
#5447=CARTESIAN_POINT ( 'NONE',  ( 14.00186632564677858, -8.256169930635699927, -6.399381488568168130 ) ) ;
#5451=CARTESIAN_POINT ( 'NONE',  ( -22.47784140366999850, -5.954807860543000153, -9.388852349241998851 ) ) ;
#5452=ORIENTED_EDGE ( 'NONE', *, *, #2886, .T. ) ;
#5456=CARTESIAN_POINT ( 'NONE',  ( 5.925473642861002865, 13.78915593935999517, 2.071179814652999163 ) ) ;
#5457=CARTESIAN_POINT ( 'NONE',  ( 11.70388046502803192, 4.051054454412691186, -12.49994163047266760 ) ) ;
#5458=FACE_OUTER_BOUND ( 'NONE', #17558, .T. ) ;
#5459=CARTESIAN_POINT ( 'NONE',  ( 6.141065375610000210, 14.19649368052000149, -1.893142280157000292E-06 ) ) ;
#5460=CARTESIAN_POINT ( 'NONE',  ( 19.00350174931000069, -5.312632942934000013, 9.204603991398000673 ) ) ;
#5461=SHAPE_REPRESENTATION_RELATIONSHIP ( 'NONE' , 'NONE' ,  #22521, #3328 ) ;
#5462=ORIENTED_EDGE ( 'NONE', *, *, #7923, .F. ) ;
#5463=CARTESIAN_POINT ( 'NONE',  ( -14.53920085882999835, -1.325901587985999885, -9.615240848067001522 ) ) ;
#5467=CARTESIAN_POINT ( 'NONE',  ( -20.50571085929999882, 6.147220618581999751, -9.373623392419000666 ) ) ;
#5469=CARTESIAN_POINT ( 'NONE',  ( 14.64207395721290084, 6.016812397516473787, -8.392094434179488971 ) ) ;
#5471=CARTESIAN_POINT ( 'NONE',  ( 22.95076023539999710, -10.54968755136000169, 3.971415078648000474 ) ) ;
#5473=CARTESIAN_POINT ( 'NONE',  ( 14.10175746976851130, 4.515222539071673147, 7.822146031336756344 ) ) ;
#5474=CARTESIAN_POINT ( 'NONE',  ( -4.816593466898998699, 12.64429630393999027, -0.01116993232460000360 ) ) ;
#5475=CARTESIAN_POINT ( 'NONE',  ( 12.00000000000000000, 5.273090321616999532, -7.267806174758000282 ) ) ;
#5477=CARTESIAN_POINT ( 'NONE',  ( -14.56584880966472717, -0.3730513441123999296, -9.047783283317706093 ) ) ;
#5478=CARTESIAN_POINT ( 'NONE',  ( -14.05786623653591505, -10.40599112028010964, 1.415392338571896280 ) ) ;
#5479=ORIENTED_EDGE ( 'NONE', *, *, #499, .F. ) ;
#5482=CARTESIAN_POINT ( 'NONE',  ( 12.00000000000000711, 4.679724461038802907, -7.698317349844846724 ) ) ;
#5484=CARTESIAN_POINT ( 'NONE',  ( 19.22319703131000068, -3.768127178825000367, 9.979248983095997616 ) ) ;
#5485=CARTESIAN_POINT ( 'NONE',  ( -14.27918997744984608, 0.2643314657130956813, 10.34628390161341116 ) ) ;
#5488=CARTESIAN_POINT ( 'NONE',  ( -9.690746138770000684, -14.59218309192000085, -4.320739656328999700 ) ) ;
#5489=CARTESIAN_POINT ( 'NONE',  ( 13.50000000000000178, 7.080145657724991715, 7.062653394649239580 ) ) ;
#5490=CARTESIAN_POINT ( 'NONE',  ( -14.25243324638999809, -7.716878364870000340, 11.63397459621999985 ) ) ;
#5492=ORIENTED_EDGE ( 'NONE', *, *, #14088, .T. ) ;
#5493=CARTESIAN_POINT ( 'NONE',  ( 23.58825386245753819, 8.156183226283769017, -6.776067362772733027 ) ) ;
#5495=CARTESIAN_POINT ( 'NONE',  ( 16.00713081564376594, -8.311260887379887663, -6.185970973389042449 ) ) ;
#5496=CARTESIAN_POINT ( 'NONE',  ( -15.37555624093999995, -9.817107509510000440, -5.025949249001999242 ) ) ;
#5499=CARTESIAN_POINT ( 'NONE',  ( -17.62691415960999919, 5.507581498160999622, 8.736692431694999428 ) ) ;
#5502=VERTEX_POINT ( 'NONE', #13658 ) ;
#5504=CARTESIAN_POINT ( 'NONE',  ( 21.15045064161181898, -9.711026941284815805, 4.098456068966175536 ) ) ;
#5505=DIRECTION ( 'NONE',  ( 0.000000000000000000, 0.000000000000000000, -1.000000000000000000 ) ) ;
#5508=CARTESIAN_POINT ( 'NONE',  ( 0.000000000000000000, 20.00000000000000000, 0.000000000000000000 ) ) ;
#5510=CARTESIAN_POINT ( 'NONE',  ( 4.726723308362996256, 12.38017690019999861, -1.078906772315999296 ) ) ;
#5512=CARTESIAN_POINT ( 'NONE',  ( 13.14731375731000007, -9.095564035174998452, -0.6525005121013000009 ) ) ;
#5519=CARTESIAN_POINT ( 'NONE',  ( -23.50032910583999879, -5.270462733209999584, -7.631233524726999562 ) ) ;
#5520=CARTESIAN_POINT ( 'NONE',  ( 12.00000000000000000, -3.609001420916660319, -8.868091556110934803 ) ) ;
#5521=CARTESIAN_POINT ( 'NONE',  ( 11.70388046502923096, -8.799739770593536292, -9.758286884884382673 ) ) ;
#5522=CARTESIAN_POINT ( 'NONE',  ( 18.71491666666665310, -2.395514397407730200, -8.913304601090439760 ) ) ;
#5523=CARTESIAN_POINT ( 'NONE',  ( -23.52106073230301320, -0.7157372019101019278, 10.55885782059828593 ) ) ;
#5525=DIRECTION ( 'NONE',  ( 0.000000000000000000, 0.000000000000000000, -1.000000000000000000 ) ) ;
#5526=CARTESIAN_POINT ( 'NONE',  ( -5.934366589030004135, 15.81056974690001837, 1.225118323253999275 ) ) ;
#5527=EDGE_CURVE ( 'NONE', #8899, #2037, #10878, .T. ) ;
#5531=CARTESIAN_POINT ( 'NONE',  ( 13.50000000000000000, -4.002954420673999536, -8.080569262580000967 ) ) ;
#5532=AXIS2_PLACEMENT_3D ( 'NONE', #1598, #17836, #23742 ) ;
#5533=CARTESIAN_POINT ( 'NONE',  ( -20.99236729085494702, -10.09761506543422804, -2.944074382273693224 ) ) ;
#5535=CARTESIAN_POINT ( 'NONE',  ( -14.00000000000000000, 1.396097351027999937E-14, 0.000000000000000000 ) ) ;
#5538=CARTESIAN_POINT ( 'NONE',  ( -4.585468453814590006, 12.35085399519005911, -1.572948697367331006 ) ) ;
#5540=CARTESIAN_POINT ( 'NONE',  ( -19.10482910584000038, 1.458613477275000161E-14, 0.000000000000000000 ) ) ;
#5542=EDGE_CURVE ( 'NONE', #12558, #22774, #74, .T. ) ;
#5544=CARTESIAN_POINT ( 'NONE',  ( -23.75390978279000009, 13.93375672974000068, 0.5776826028407999747 ) ) ;
#5546=CARTESIAN_POINT ( 'NONE',  ( 16.16175158531000022, 8.345400111538999965, -5.893156809269999741 ) ) ;
#5547=CARTESIAN_POINT ( 'NONE',  ( 18.05781943074418550, -1.146451644013575244, -10.34773016139448032 ) ) ;
#5548=CARTESIAN_POINT ( 'NONE',  ( -24.17970357213072319, 4.108081272002125139, 12.49999456974980561 ) ) ;
#5550=DIRECTION ( 'NONE',  ( 0.000000000000000000, -0.9761919106981273853, 0.2169086293524060682 ) ) ;
#5551=CARTESIAN_POINT ( 'NONE',  ( 13.50000000000000000, -9.000981082165885994, 4.172073181103733930 ) ) ;
#5552=ORIENTED_EDGE ( 'NONE', *, *, #2376, .F. ) ;
#5555=CARTESIAN_POINT ( 'NONE',  ( 19.41640481369000071, -11.20635663128000203, -0.8231659222257999842 ) ) ;
#5556=EDGE_CURVE ( 'NONE', #18434, #629, #20091, .T. ) ;
#5558=ORIENTED_EDGE ( 'NONE', *, *, #22567, .T. ) ;
#5560=CARTESIAN_POINT ( 'NONE',  ( 24.50000000000000355, -5.730830435609104434, 8.891180258077504561 ) ) ;
#5562=CARTESIAN_POINT ( 'NONE',  ( -4.283717669607001177, 12.21694329250999367, 2.261528323867997958 ) ) ;
#5564=CARTESIAN_POINT ( 'NONE',  ( -20.13865776273999941, 10.50400506863999972, -3.445110567144999525 ) ) ;
#5567=ORIENTED_EDGE ( 'NONE', *, *, #14863, .F. ) ;
#5568=CIRCLE ( 'NONE', #8285, 12.44999999999999929 ) ;
#5570=CARTESIAN_POINT ( 'NONE',  ( 6.232327572681000127, 13.71183716028998845, 0.7484834382456998503 ) ) ;
#5571=CARTESIAN_POINT ( 'NONE',  ( -19.55887123173999953, -9.833822427806001798, 3.504477313184999776 ) ) ;
#5573=CARTESIAN_POINT ( 'NONE',  ( 23.99062354302999722, -13.93375672974000068, 0.8660254037843999608 ) ) ;
#5574=CARTESIAN_POINT ( 'NONE',  ( 17.72381424930999927, -7.480404092888999656, -7.743571870822999692 ) ) ;
#5577=CARTESIAN_POINT ( 'NONE',  ( -16.36737399056000086, -1.805578197078999914, -9.588658350757999216 ) ) ;
#5579=ORIENTED_EDGE ( 'NONE', *, *, #16595, .T. ) ;
#5580=CARTESIAN_POINT ( 'NONE',  ( -10.29403125534151009, 15.72585302211925296, -1.189404080594516078 ) ) ;
#5582=CARTESIAN_POINT ( 'NONE',  ( 14.40569269110591577, -1.986665269285088797, -10.12885916003707898 ) ) ;
#5584=CARTESIAN_POINT ( 'NONE',  ( 23.46447575822000076, -6.913963705398000315, -8.920945031365000943 ) ) ;
#5587=CARTESIAN_POINT ( 'NONE',  ( 13.70021229750822123, 8.494204404046966417, -3.039004686995299132 ) ) ;
#5588=DIRECTION ( 'NONE',  ( -1.000000000000000000, 0.000000000000000000, 0.000000000000000000 ) ) ;
#5589=CARTESIAN_POINT ( 'NONE',  ( -6.737757365823932254, 15.34323595062688206, 1.749766658884769344 ) ) ;
#5590=CARTESIAN_POINT ( 'NONE',  ( 21.68490460127999953, 4.300247781276000048, -10.59540847689999943 ) ) ;
#5592=CARTESIAN_POINT ( 'NONE',  ( -14.62564808937985994, -2.249539402723780945, -8.791895681600211176 ) ) ;
#5593=CARTESIAN_POINT ( 'NONE',  ( 12.12543434882657323, -13.45291906885515409, 1.698934468806285514 ) ) ;
#5596=CARTESIAN_POINT ( 'NONE',  ( 23.99062354302999722, 7.716878364870000340, 11.63397459621999985 ) ) ;
#5597=CARTESIAN_POINT ( 'NONE',  ( 21.41787270046332026, 8.980959603804187452, 2.413435494101626499 ) ) ;
#5598=CIRCLE ( 'NONE', #14107, 10.30000000000000071 ) ;
#5599=CARTESIAN_POINT ( 'NONE',  ( 18.92244553490999692, 7.034701712467999357, 8.633984044295999638 ) ) ;
#5600=CARTESIAN_POINT ( 'NONE',  ( -6.225913922104028053, 15.76757470349466139, 1.159797651207155944 ) ) ;
#5604=CARTESIAN_POINT ( 'NONE',  ( -11.83639256584999977, 14.79789546886000018, -1.442137029629999789 ) ) ;
#5606=CARTESIAN_POINT ( 'NONE',  ( -14.49863740983932558, -10.56606202787202164, -6.698971014606366126 ) ) ;
#5608=CARTESIAN_POINT ( 'NONE',  ( -24.36724102300186701, 9.545677019765191673, 8.466242377950417008 ) ) ;
#5609=CARTESIAN_POINT ( 'NONE',  ( 18.91133465082729614, -3.947989545138891998, 9.718486893964049855 ) ) ;
#5610=CARTESIAN_POINT ( 'NONE',  ( 23.99062354302999722, 13.93375672974000068, 0.8660254037843999608 ) ) ;
#5611=CARTESIAN_POINT ( 'NONE',  ( 15.92946909780416220, -9.691739620817704903, -3.655258532792393211 ) ) ;
#5612=CARTESIAN_POINT ( 'NONE',  ( -18.92073910527999914, 2.264199207268999814, -10.89315635654000047 ) ) ;
#5615=CARTESIAN_POINT ( 'NONE',  ( -16.20500172382000059, 9.665285290698001575, -3.525418390172999850 ) ) ;
#5617=EDGE_LOOP ( 'NONE', ( #8988, #22154, #1245, #14646, #3239, #12009, #16635, #21819 ) ) ;
#5619=CARTESIAN_POINT ( 'NONE',  ( 20.95183695597172147, -4.891656435019153371, 9.332274347635205913 ) ) ;
#5620=LINE ( 'NONE', #21751, #6451 ) ;
#5621=ORIENTED_EDGE ( 'NONE', *, *, #20208, .T. ) ;
#5622=EDGE_CURVE ( 'NONE', #20307, #8984, #7633, .T. ) ;
#5624=CARTESIAN_POINT ( 'NONE',  ( 17.61895833333332462, 7.295785356393542642, 5.606677399942485707 ) ) ;
#5625=CARTESIAN_POINT ( 'NONE',  ( 12.70856375730999943, -1.114725866925000197, 9.038927914362998806 ) ) ;
#5626=ORIENTED_EDGE ( 'NONE', *, *, #10251, .F. ) ;
#5627=AXIS2_PLACEMENT_3D ( 'NONE', #1685, #9073, #16446 ) ;
#5628=CARTESIAN_POINT ( 'NONE',  ( -3.931174283351645204, 14.83584528699218552, 4.702583796344565137 ) ) ;
#5629=CARTESIAN_POINT ( 'NONE',  ( -14.48875654244861089, 1.295999377426451771, -12.49999522859631185 ) ) ;
#5630=VERTEX_POINT ( 'NONE', #14684 ) ;
#5631=CARTESIAN_POINT ( 'NONE',  ( 22.28708103379667804, -9.243212137893149105, -1.209806691843604343 ) ) ;
#5632=CARTESIAN_POINT ( 'NONE',  ( 2.259444391955999443, 11.86379749507999648, 4.184941550337999416 ) ) ;
#5633=CARTESIAN_POINT ( 'NONE',  ( -22.13650671462999853, -8.888489588850999823, 3.669257322618999950 ) ) ;
#5634=CARTESIAN_POINT ( 'NONE',  ( -13.73165055702999915, 8.564239710418998897, -4.480696141197999971 ) ) ;
#5635=CARTESIAN_POINT ( 'NONE',  ( -21.38504529524956510, -9.746759242728279204, 3.986291022453713584 ) ) ;
#5637=CARTESIAN_POINT ( 'NONE',  ( 16.25845833333332990, -5.585221661844576246, 7.267866498838181144 ) ) ;
#5640=ORIENTED_EDGE ( 'NONE', *, *, #20635, .F. ) ;
#5641=CARTESIAN_POINT ( 'NONE',  ( -17.69487077250666829, 5.608054106645548487, -7.297163626529473035 ) ) ;
#5644=VECTOR ( 'NONE', #20196, 1000.000000000000000 ) ;
#5645=EDGE_CURVE ( 'NONE', #12531, #7629, #17520, .T. ) ;
#5646=CARTESIAN_POINT ( 'NONE',  ( -24.07165041821819784, 6.096641539000005494, -8.671681623059738442 ) ) ;
#5649=CARTESIAN_POINT ( 'NONE',  ( 3.083557478243028172, 11.88318476793270584, 3.713866788134294605 ) ) ;
#5651=CARTESIAN_POINT ( 'NONE',  ( 0.4544561634010835793, 11.49156783371328849, -4.790238354834232659 ) ) ;
#5652=CARTESIAN_POINT ( 'NONE',  ( 24.00034722001000276, -6.716786535997999685, -12.21137788282999992 ) ) ;
#5654=ORIENTED_EDGE ( 'NONE', *, *, #2299, .F. ) ;
#5655=ADVANCED_FACE ( 'NONE', ( #14000 ), #14006, .F. ) ;
#5659=CARTESIAN_POINT ( 'NONE',  ( 14.29706408530999973, 7.153286345558000470, -7.225396115407999531 ) ) ;
#5660=CARTESIAN_POINT ( 'NONE',  ( 18.33301707778365497, 7.724375581193626772, -6.994159490549959557 ) ) ;
#5664=CARTESIAN_POINT ( 'NONE',  ( 13.50000000000000178, -8.365255057625532231, -4.267281750524336559 ) ) ;
#5666=EDGE_CURVE ( 'NONE', #21240, #14252, #22461, .T. ) ;
#5668=CARTESIAN_POINT ( 'NONE',  ( 21.45820040743999968, -10.73102562442999819, 0.8320772051962000981 ) ) ;
#5669=DIRECTION ( 'NONE',  ( 0.1671082301074949539, 0.9859385576344705804, 0.000000000000000000 ) ) ;
#5671=CARTESIAN_POINT ( 'NONE',  ( 24.50000000000000000, -5.821110578647480160, 8.832467286812930141 ) ) ;
#5673=CARTESIAN_POINT ( 'NONE',  ( 1.648798782356001080, 11.55618995303000496, 4.569391161061998829 ) ) ;
#5674=AXIS2_PLACEMENT_3D ( 'NONE', #22834, #20915, #675 ) ;
#5676=EDGE_CURVE ( 'NONE', #1912, #5222, #9307, .T. ) ;
#5677=CARTESIAN_POINT ( 'NONE',  ( -12.24999999999999822, 10.00898580939830218, -10.96118423669926756 ) ) ;
#5679=FACE_BOUND ( 'NONE', #20973, .T. ) ;
#5680=EDGE_LOOP ( 'NONE', ( #23833, #1710, #1579, #18476, #13818, #22129 ) ) ;
#5682=CARTESIAN_POINT ( 'NONE',  ( 5.373436897387995792, 13.85347760506000192, 3.916935352515997781 ) ) ;
#5684=CARTESIAN_POINT ( 'NONE',  ( 15.97587270046332542, 8.844941937541273447, 2.376881761915226488 ) ) ;
#5686=CARTESIAN_POINT ( 'NONE',  ( 24.00034722001000276, -13.93375672974000068, -0.2887811715185000239 ) ) ;
#5688=( LENGTH_UNIT ( ) NAMED_UNIT ( * ) SI_UNIT ( .MILLI., .METRE. ) );
#5690=CARTESIAN_POINT ( 'NONE',  ( -18.39867747026000089, -7.918532069388001027, -5.797808426274999150 ) ) ;
#5693=CARTESIAN_POINT ( 'NONE',  ( -14.29262089130507363, 5.684429818794539457, 12.49999999999983658 ) ) ;
#5695=CARTESIAN_POINT ( 'NONE',  ( -23.07621189342000179, -10.06116254826999956, 5.098950990742999956 ) ) ;
#5697=CARTESIAN_POINT ( 'NONE',  ( 14.55979580643064963, 3.396064661906295523, -9.748015653831131999 ) ) ;
#5698=CARTESIAN_POINT ( 'NONE',  ( -17.87792920454667467, 7.977774763500829813, -4.597956546261363187 ) ) ;
#5699=CARTESIAN_POINT ( 'NONE',  ( 19.68384026807999732, -1.917285116153000013, -11.01718559352000071 ) ) ;
#5700=CIRCLE ( 'NONE', #19238, 12.44999999999999929 ) ;
#5702=CARTESIAN_POINT ( 'NONE',  ( 13.69887155650829058, 8.480249914508103615, -3.077469453800580013 ) ) ;
#5703=CARTESIAN_POINT ( 'NONE',  ( 2.352846606927001538, 11.89851893293999652, -4.242708344949997823 ) ) ;
#5704=CARTESIAN_POINT ( 'NONE',  ( -6.216900810347000039, 16.31160418525000111, 0.9999988273041999776 ) ) ;
#5706=CARTESIAN_POINT ( 'NONE',  ( 11.32654380052400178, 9.540497826158469863, -8.475313523008512817 ) ) ;
#5711=MECHANICAL_DESIGN_GEOMETRIC_PRESENTATION_REPRESENTATION('',(#16148),#16920);
#5716=CARTESIAN_POINT ( 'NONE',  ( 14.26455149188999982, -6.229792639309999380, -9.077012475588000839 ) ) ;
#5719=EDGE_CURVE ( 'NONE', #1386, #23264, #20163, .T. ) ;
#5723=CARTESIAN_POINT ( 'NONE',  ( -10.91261613876999981, -1.790000681266999960, -15.11279232617999924 ) ) ;
#5724=CARTESIAN_POINT ( 'NONE',  ( 4.835177208035999818, -12.44999999999999929, 0.000000000000000000 ) ) ;
#5725=CARTESIAN_POINT ( 'NONE',  ( -24.41513307467231186, -9.801374016731797312, -8.023466425255969980 ) ) ;
#5727=CARTESIAN_POINT ( 'NONE',  ( -24.50000000000294165, 10.56908696370082446, 6.693804389267354438 ) ) ;
#5728=CARTESIAN_POINT ( 'NONE',  ( 19.32313885814015819, -10.19623967642864670, -2.501916320087661738 ) ) ;
#5730=CARTESIAN_POINT ( 'NONE',  ( 16.15164999724400730, -4.403807630409194651, -9.396662404489285692 ) ) ;
#5732=CARTESIAN_POINT ( 'NONE',  ( -19.28206573533999801, -9.640750581229999838, -5.573920775363999880 ) ) ;
#5734=CARTESIAN_POINT ( 'NONE',  ( -12.99567423753000028, 6.199143636224999199, -8.762012042742998830 ) ) ;
#5739=CARTESIAN_POINT ( 'NONE',  ( 22.31375937178523117, 9.342772961303669632, 4.957017412827640079 ) ) ;
#5740=DIRECTION ( 'NONE',  ( 0.000000000000000000, -0.9761919106981273853, 0.2169086293524060682 ) ) ;
#5742=ORIENTED_EDGE ( 'NONE', *, *, #9402, .T. ) ;
#5743=CARTESIAN_POINT ( 'NONE',  ( -5.366767308139002601, 16.51611458662000942, 3.205250738674000566 ) ) ;
#5745=CARTESIAN_POINT ( 'NONE',  ( 11.83106375730999993, 2.025755645688000151, -8.855592440447001223 ) ) ;
#5746=VERTEX_POINT ( 'NONE', #16681 ) ;
#5747=CARTESIAN_POINT ( 'NONE',  ( -4.619909110842619349, 15.59001540809187780, 4.021459351379646385 ) ) ;
#5748=CARTESIAN_POINT ( 'NONE',  ( -14.47158022755351325, 2.069973096334361884, -12.49996948346235470 ) ) ;
#5749=AXIS2_PLACEMENT_3D ( 'NONE', #11404, #4123, #8129 ) ;
#5751=CARTESIAN_POINT ( 'NONE',  ( -23.08127083529245027, 7.060724976932586827, -6.230165419677522465 ) ) ;
#5752=CARTESIAN_POINT ( 'NONE',  ( -4.622166446016002794, 12.56867761721000676, 1.067424028279999826 ) ) ;
#5756=CARTESIAN_POINT ( 'NONE',  ( 12.00000000000000000, 1.135109584198050303, -9.208780385958741377 ) ) ;
#5758=LINE ( 'NONE', #13496, #17267 ) ;
#5760=CARTESIAN_POINT ( 'NONE',  ( -5.155920576390994547, 15.83913996291999204, -2.700030400707001288 ) ) ;
#5763=CARTESIAN_POINT ( 'NONE',  ( 5.299443700753212028, 13.76429532417504831, -4.351754427252301660 ) ) ;
#5768=CARTESIAN_POINT ( 'NONE',  ( 14.86901153711125012, -8.273827554593831124, 3.800866100364200584 ) ) ;
#5769=CARTESIAN_POINT ( 'NONE',  ( -23.57552075937401526, -7.930447722602094629, -5.012726446680143333 ) ) ;
#5771=CARTESIAN_POINT ( 'NONE',  ( -23.24158279258278625, -3.596034818408476053, 9.948339823417249761 ) ) ;
#5775=VERTEX_POINT ( 'NONE', #16214 ) ;
#5776=CARTESIAN_POINT ( 'NONE',  ( -2.752375951156815326, 11.80288882812367390, -3.961635973783927511 ) ) ;
#5777=CARTESIAN_POINT ( 'NONE',  ( 23.99062354302999722, -13.93375672974000068, -0.8660254037843999608 ) ) ;
#5779=CARTESIAN_POINT ( 'NONE',  ( -21.35476253787999923, 9.219287007783998789, 0.000000000000000000 ) ) ;
#5782=CARTESIAN_POINT ( 'NONE',  ( 14.95518908531000157, 0.8306535110907999897, 10.15076156001000207 ) ) ;
#5784=CARTESIAN_POINT ( 'NONE',  ( -19.82722067471999949, -8.836429628019001115, 5.355976217871000422 ) ) ;
#5786=CARTESIAN_POINT ( 'NONE',  ( 17.76551537305999773, -10.38510595533999847, 3.229171968965000250 ) ) ;
#5788=VERTEX_POINT ( 'NONE', #7241 ) ;
#5790=CARTESIAN_POINT ( 'NONE',  ( 21.28115130527999810, -8.293037263826001038, 6.853370783829999091 ) ) ;
#5791=LINE ( 'NONE', #17165, #23922 ) ;
#5793=CARTESIAN_POINT ( 'NONE',  ( 11.38563810340999893, -8.030754667131001057, -4.228659338699999104 ) ) ;
#5796=CARTESIAN_POINT ( 'NONE',  ( 4.835175158044003219, 12.42241705055999823, 0.2482835134780999597 ) ) ;
#5799=CARTESIAN_POINT ( 'NONE',  ( -19.19184533664999748, -10.45696971737000069, 1.867641980438999871 ) ) ;
#5800=ORIENTED_EDGE ( 'NONE', *, *, #6277, .T. ) ;
#5801=PLANE ( 'NONE',  #9978 ) ;
#5802=ORIENTED_EDGE ( 'NONE', *, *, #16764, .F. ) ;
#5806=CARTESIAN_POINT ( 'NONE',  ( 6.243179582884000212, 1.578914512950999657E-14, -13.77250448649344250 ) ) ;
#5807=CARTESIAN_POINT ( 'NONE',  ( -12.50000000000000000, 1.557342902441000195E-14, 1.045589212608000028E-14 ) ) ;
#5809=CARTESIAN_POINT ( 'NONE',  ( 14.98162674931000105, 7.974294229383000143, 7.126218918095000632 ) ) ;
#5810=CARTESIAN_POINT ( 'NONE',  ( -14.21445632535000136, 4.821896674351999756, 9.628268207709998805 ) ) ;
#5812=CARTESIAN_POINT ( 'NONE',  ( -14.49863740500227038, -0.5184489068381992194, 12.49996363569670521 ) ) ;
#5813=ADVANCED_FACE ( 'NONE', ( #3399 ), #8893, .F. ) ;
#5814=ORIENTED_EDGE ( 'NONE', *, *, #13218, .T. ) ;
#5815=CARTESIAN_POINT ( 'NONE',  ( -10.62523811313343991, 15.45380396666532263, -1.485942923904584489 ) ) ;
#5817=CARTESIAN_POINT ( 'NONE',  ( 13.84556716760639006, -8.683927038290656597, 5.545870859834080235 ) ) ;
#5818=DIRECTION ( 'NONE',  ( 0.000000000000000000, 1.000000000000000000, 0.000000000000000000 ) ) ;
#5819=CARTESIAN_POINT ( 'NONE',  ( 19.83046186496999752, -1.917974774180999820, -11.02115077512000063 ) ) ;
#5821=CARTESIAN_POINT ( 'NONE',  ( 13.76087388038597936, 8.957244340564407992, -1.248995784414053345 ) ) ;
#5822=LINE ( 'NONE', #20597, #14636 ) ;
#5824=ADVANCED_FACE ( 'NONE', ( #14746 ), #2796, .F. ) ;
#5825=CARTESIAN_POINT ( 'NONE',  ( 11.90008533511768896, 13.14613689767754146, -2.230302227733069298 ) ) ;
#5826=VERTEX_POINT ( 'NONE', #14258 ) ;
#5827=CARTESIAN_POINT ( 'NONE',  ( 24.25008227645999881, 0.000000000000000000, 0.000000000000000000 ) ) ;
#5832=CARTESIAN_POINT ( 'NONE',  ( 13.36229700266000187, 5.683036826372999784, 8.581013501291998580 ) ) ;
#5834=CARTESIAN_POINT ( 'NONE',  ( -12.41173981160000039, 6.613190111079999767, -13.46349570337000046 ) ) ;
#5837=ORIENTED_EDGE ( 'NONE', *, *, #9282, .F. ) ;
#5838=CARTESIAN_POINT ( 'NONE',  ( -14.00000000000000178, -9.062199998400112477, -4.448848724211252659 ) ) ;
#5839=CARTESIAN_POINT ( 'NONE',  ( -11.92346721169000112, 5.896127864781000483, 14.40918513707999971 ) ) ;
#5841=CARTESIAN_POINT ( 'NONE',  ( -24.27585716846449060, -9.160327548061168557, -9.133709619347802899 ) ) ;
#5842=EDGE_CURVE ( 'NONE', #13740, #6468, #1655, .T. ) ;
#5844=EDGE_CURVE ( 'NONE', #16663, #13012, #23573, .T. ) ;
#5845=CARTESIAN_POINT ( 'NONE',  ( 20.08416666666666828, -9.000201972419345609, 2.126478957478491694 ) ) ;
#5846=CARTESIAN_POINT ( 'NONE',  ( 19.52904096179855031, -6.069165301658948408, -8.568664490119912713 ) ) ;
#5848=CARTESIAN_POINT ( 'NONE',  ( 15.56286596738189942, -6.410929410329065270, 8.147947015818964189 ) ) ;
#5849=CARTESIAN_POINT ( 'NONE',  ( -14.98018789272999918, 7.746190468795000506, -7.835402896861000777 ) ) ;
#5851=CARTESIAN_POINT ( 'NONE',  ( -14.62071702128999995, 10.29594144910999809, -3.192455093500000007 ) ) ;
#5853=EDGE_CURVE ( 'NONE', #1942, #21964, #15730, .T. ) ;
#5854=ORIENTED_EDGE ( 'NONE', *, *, #23442, .F. ) ;
#5856=EDGE_CURVE ( 'NONE', #8899, #2380, #13900, .T. ) ;
#5857=CARTESIAN_POINT ( 'NONE',  ( -4.820914651057999656, 13.20110358116999905, -5.836454220812999694 ) ) ;
#5858=CARTESIAN_POINT ( 'NONE',  ( 4.821047785747002656, 14.92830715209997905, -3.789723698138999897 ) ) ;
#5861=CARTESIAN_POINT ( 'NONE',  ( -4.419368126936999097, 15.75034981608000351, 4.320386041415997802 ) ) ;
#5862=CARTESIAN_POINT ( 'NONE',  ( -6.250000000000000000, -15.43375672974000068, 0.000000000000000000 ) ) ;
#5863=CARTESIAN_POINT ( 'NONE',  ( 12.05043875730999936, 7.573215573255999367, -5.027566056405999184 ) ) ;
#5865=CARTESIAN_POINT ( 'NONE',  ( -6.316928638995997325, 15.85590696878002603, -1.061654000538000409 ) ) ;
#5867=AXIS2_PLACEMENT_3D ( 'NONE', #9745, #6098, #2354 ) ;
#5870=CARTESIAN_POINT ( 'NONE',  ( -18.99854661335000117, 6.966878364870000340, -12.06698729810999993 ) ) ;
#5871=CARTESIAN_POINT ( 'NONE',  ( -4.522737060985000390, 12.53062717673999593, 1.434513612155000395 ) ) ;
#5872=CARTESIAN_POINT ( 'NONE',  ( -22.93944013947999849, 9.633115978054998862, -0.2991401492583000143 ) ) ;
#5873=CARTESIAN_POINT ( 'NONE',  ( 19.22595603379665619, 4.615378250370806512, -8.008001678105078014 ) ) ;
#5874=CARTESIAN_POINT ( 'NONE',  ( -5.340888267555999214, 16.50102740467002249, -3.245487968687000624 ) ) ;
#5875=CARTESIAN_POINT ( 'NONE',  ( 6.243179582884000212, -13.77250448648999814, 0.000000000000000000 ) ) ;
#5881=CARTESIAN_POINT ( 'NONE',  ( 24.16831550194999778, -8.024295071342999464, -4.916962988213999353 ) ) ;
#5882=CARTESIAN_POINT ( 'NONE',  ( 4.312196806323354004, 13.42372324865281641, -5.304433147621987921 ) ) ;
#5884=CARTESIAN_POINT ( 'NONE',  ( -24.15197954327974372, 3.481455606802188019, -10.01183836013010442 ) ) ;
#5886=CARTESIAN_POINT ( 'NONE',  ( 12.00000000000000000, 0.000000000000000000, 0.000000000000000000 ) ) ;
#5887=ORIENTED_EDGE ( 'NONE', *, *, #7018, .F. ) ;
#5891=DIRECTION ( 'NONE',  ( 0.000000000000000000, -1.000000000000000000, 0.000000000000000000 ) ) ;
#5893=CARTESIAN_POINT ( 'NONE',  ( 15.72300158530999958, -5.453124986814999353, -8.625711720232999369 ) ) ;
#5894=CARTESIAN_POINT ( 'NONE',  ( -19.62575000533999869, -7.533253386014000519, 7.382837537152000529 ) ) ;
#5895=CARTESIAN_POINT ( 'NONE',  ( -10.04281598261999875, 16.38798294975000047, 0.9999999999983999466 ) ) ;
#5896=CARTESIAN_POINT ( 'NONE',  ( 18.37489037306000128, 2.572692777010999965, -10.58437343029000033 ) ) ;
#5899=FACE_OUTER_BOUND ( 'NONE', #17336, .T. ) ;
#5900=CARTESIAN_POINT ( 'NONE',  ( 19.78196485594000009, -8.739116552734000010, 5.237636975568999986 ) ) ;
#5903=CARTESIAN_POINT ( 'NONE',  ( 12.10937109324999916, -8.506090310477000926, -2.885017716830000190 ) ) ;
#5904=CARTESIAN_POINT ( 'NONE',  ( 6.243179582884000212, 1.148189900220999940E-14, 0.000000000000000000 ) ) ;
#5905=CARTESIAN_POINT ( 'NONE',  ( 4.599771440748003037, 12.33202429268000166, 1.513355409791999229 ) ) ;
#5907=CARTESIAN_POINT ( 'NONE',  ( -23.77359187212000080, 8.708980288023001393, 6.967567546233000009 ) ) ;
#5908=ORIENTED_EDGE ( 'NONE', *, *, #15329, .T. ) ;
#5909=B_SPLINE_CURVE_WITH_KNOTS ( 'NONE', 3,
 ( #8489, #23491, #15855, #5102, #12483, #19868, #7022, #12002, #10666, #18054, #1460, #14409, #8362, #23837, #96, #22147, #18395, #3864, #2040, #22037, #14523, #3627, #5446, #16572, #23962, #16686, #18514, #20110, #20451, #21914, #7481, #20332 ),
 .UNSPECIFIED., .F., .F.,
 ( 4, 2, 2, 2, 2, 2, 2, 2, 2, 2, 2, 2, 1, 2, 1, 2, 4 ),
 ( 0.000000000000000000, 0.06250000000000006939, 0.1250000000000001388, 0.1875000000000002220, 0.2500000000000002776, 0.3125000000000002776, 0.3750000000000002776, 0.4375000000000003331, 0.5000000000000003331, 0.5625000000000003331, 0.6250000000000002220, 0.6875000000000002220, 0.7500000000000001110, 0.8125000000000001110, 0.8750000000000001110, 0.9375000000000000000, 1.000000000000000000 ),
 .UNSPECIFIED. ) ;
#5910=CARTESIAN_POINT ( 'NONE',  ( 24.24531177150999994, 0.000000000000000000, 0.000000000000000000 ) ) ;
#5913=CARTESIAN_POINT ( 'NONE',  ( 15.63574770046331430, 5.575401216236696378, -7.255087836980721683 ) ) ;
#5918=CARTESIAN_POINT ( 'NONE',  ( 16.84631424931000154, 6.637278256850999369, 8.448060240267999177 ) ) ;
#5920=CARTESIAN_POINT ( 'NONE',  ( -17.42378381163999990, -1.451785825221999948, 10.21952336923999916 ) ) ;
#5923=DIRECTION ( 'NONE',  ( 0.000000000000000000, 1.000000000000000000, 0.000000000000000000 ) ) ;
#5925=EDGE_CURVE ( 'NONE', #10616, #16623, #16889, .T. ) ;
#5927=CARTESIAN_POINT ( 'NONE',  ( 13.63524120837945830, -2.821342633397881272, 9.926079101813042982 ) ) ;
#5928=CARTESIAN_POINT ( 'NONE',  ( 2.917722632763000146, 13.60402666298999996, -5.360392733824004274 ) ) ;
#5929=CARTESIAN_POINT ( 'NONE',  ( 21.07836523965000097, -5.385920316227999827, 9.843973735277000259 ) ) ;
#5931=CARTESIAN_POINT ( 'NONE',  ( 11.09594815121216271, -0.9954690943958549587, 12.49999871278813046 ) ) ;
#5932=CARTESIAN_POINT ( 'NONE',  ( -6.722873803920665026, 15.34560435500414144, -1.730847659303734298 ) ) ;
#5933=CARTESIAN_POINT ( 'NONE',  ( -6.313954834032534436, 15.63752586476230633, 1.252296258704070464 ) ) ;
#5937=ORIENTED_EDGE ( 'NONE', *, *, #18467, .F. ) ;
#5940=CARTESIAN_POINT ( 'NONE',  ( 24.36165043081784276, 9.237917109185875830, 8.999458210778742639 ) ) ;
#5942=ORIENTED_EDGE ( 'NONE', *, *, #1664, .F. ) ;
#5943=CARTESIAN_POINT ( 'NONE',  ( 14.08410059404000059, -10.35854663702999900, -3.714083093220999832 ) ) ;
#5947=ORIENTED_EDGE ( 'NONE', *, *, #18378, .F. ) ;
#5948=CARTESIAN_POINT ( 'NONE',  ( -24.46742986864730796, 10.18447769906778788, -7.359979596042377281 ) ) ;
#5952=CARTESIAN_POINT ( 'NONE',  ( 17.88295603379667043, 7.701996700470298940, 5.081089778053197392 ) ) ;
#5953=EDGE_LOOP ( 'NONE', ( #16932, #17799, #2200, #8525, #7704 ) ) ;
#5954=EDGE_CURVE ( 'NONE', #11139, #12251, #17793, .T. ) ;
#5955=CARTESIAN_POINT ( 'NONE',  ( -19.60267883610000084, 8.869063186870999260, -3.716108411551000579 ) ) ;
#5956=CARTESIAN_POINT ( 'NONE',  ( -14.41332674684316828, 12.63239273138172436, 3.119888754832823796 ) ) ;
#5957=CARTESIAN_POINT ( 'NONE',  ( 6.225676751962361699, 13.76137232892522633, 1.306414714001897126 ) ) ;
#5958=CARTESIAN_POINT ( 'NONE',  ( 15.73262886950022654, -9.839481850775154470, 3.264375423814056987 ) ) ;
#5959=CARTESIAN_POINT ( 'NONE',  ( -15.19489292590999874, -5.010861156605001199, -9.819261828225998912 ) ) ;
#5962=CARTESIAN_POINT ( 'NONE',  ( -17.91156067002999919, -1.604197317876000062, 11.29338059605000133 ) ) ;
#5963=ADVANCED_FACE ( 'NONE', ( #10334 ), #22402, .F. ) ;
#5967=AXIS2_PLACEMENT_3D ( 'NONE', #17722, #14328, #1120 ) ;
#5968=CARTESIAN_POINT ( 'NONE',  ( -18.57237735687682445, 10.43290785388021291, -0.7825199175144633701 ) ) ;
#5969=ORIENTED_EDGE ( 'NONE', *, *, #10158, .F. ) ;
#5971=CARTESIAN_POINT ( 'NONE',  ( -4.858535779299999469, 13.29855084970999890, 5.919202098683998159 ) ) ;
#5972=EDGE_CURVE ( 'NONE', #4443, #10646, #10448, .T. ) ;
#5974=CARTESIAN_POINT ( 'NONE',  ( -14.00000000000000178, -10.31294900121941005, -0.06607431037178398969 ) ) ;
#5975=CARTESIAN_POINT ( 'NONE',  ( 18.51187642130999933, -4.805399430337999434, 8.325799818148999165 ) ) ;
#5976=ORIENTED_EDGE ( 'NONE', *, *, #8212, .F. ) ;
#5978=DIRECTION ( 'NONE',  ( -0.7071067811865969777, -0.7071067811864980568, -2.474840881013989736E-09 ) ) ;
#5981=CARTESIAN_POINT ( 'NONE',  ( -16.55522087121331865, -5.589901749525623131, -7.273956370960904749 ) ) ;
#5982=CARTESIAN_POINT ( 'NONE',  ( 21.81383333333333141, -8.065932698539254986, 4.649058171626129443 ) ) ;
#5983=CARTESIAN_POINT ( 'NONE',  ( 4.414629580919998020, 12.49396588617999271, 1.935277879409999624 ) ) ;
#5986=CARTESIAN_POINT ( 'NONE',  ( -21.97592002967000013, -9.481613672941000104, -1.576156473507000166 ) ) ;
#5988=CARTESIAN_POINT ( 'NONE',  ( -11.99999999434999864, -6.999999994347000154, -4.083277946868999946E-09 ) ) ;
#5989=CARTESIAN_POINT ( 'NONE',  ( -12.50000000000000000, 6.992973968623999781, -5.709239639804999378 ) ) ;
#5990=CARTESIAN_POINT ( 'NONE',  ( 5.562517841236772398, 14.53154872498324579, 2.570889057986909698 ) ) ;
#5994=CARTESIAN_POINT ( 'NONE',  ( 22.68672501132000008, 1.244886420992999954, -9.776971065933000915 ) ) ;
#5995=CARTESIAN_POINT ( 'NONE',  ( -2.218324364786688818, 12.96888396011062738, -6.336184367259724226 ) ) ;
#5997=EDGE_CURVE ( 'NONE', #13163, #20695, #13126, .T. ) ;
#5998=CARTESIAN_POINT ( 'NONE',  ( -21.01914366587545402, -10.32835885544590582, -1.990128420184432700 ) ) ;
#6000=ADVANCED_FACE ( 'NONE', ( #12151 ), #12754, .F. ) ;
#6005=LINE ( 'NONE', #5777, #15745 ) ;
#6007=APPLICATION_CONTEXT ( 'automotive_design' ) ;
#6010=EDGE_CURVE ( 'NONE', #2558, #15509, #19214, .T. ) ;
#6012=CARTESIAN_POINT ( 'NONE',  ( 13.99443924931000005, -9.599271117524001085, -4.655318192544999789 ) ) ;
#6014=CARTESIAN_POINT ( 'NONE',  ( -14.75062165406000148, 10.41229764572999983, 4.438028563735000098 ) ) ;
#6016=CARTESIAN_POINT ( 'NONE',  ( 15.32801537305999950, 8.400340696411999986, 6.799953174600000594 ) ) ;
#6019=CARTESIAN_POINT ( 'NONE',  ( 23.77130057337999958, -9.515117350267999541, 2.208807626390000056 ) ) ;
#6020=DIRECTION ( 'NONE',  ( -0.9996708941621511579, -0.02565352539213875543, -5.387480945348741403E-14 ) ) ;
#6021=VERTEX_POINT ( 'NONE', #13677 ) ;
#6022=CARTESIAN_POINT ( 'NONE',  ( 11.99054877623999893, -6.470940098446000377, -6.715655461047000507 ) ) ;
#6024=CARTESIAN_POINT ( 'NONE',  ( -0.1178155359250000339, 11.45056912575998886, 4.946867145734003657 ) ) ;
#6025=CARTESIAN_POINT ( 'NONE',  ( 24.50000000000000000, -9.344098705406999272, -3.489386534399999906 ) ) ;
#6026=CARTESIAN_POINT ( 'NONE',  ( -23.79405482100999691, 11.10233715562999990, 1.069494977660000012 ) ) ;
#6027=ORIENTED_EDGE ( 'NONE', *, *, #23448, .T. ) ;
#6030=CARTESIAN_POINT ( 'NONE',  ( 3.792292039899240574, 12.19805237062407954, 2.925708645425909804 ) ) ;
#6032=CARTESIAN_POINT ( 'NONE',  ( -4.752065375082999310, 13.48440873408998364, 5.196329956053004295 ) ) ;
#6034=VECTOR ( 'NONE', #6323, 1000.000000000000114 ) ;
#6036=CARTESIAN_POINT ( 'NONE',  ( 16.07850174930999998, -1.960161522604999762, -10.54265994730999978 ) ) ;
#6037=CARTESIAN_POINT ( 'NONE',  ( -16.85515084895999749, -2.006433207287000364, -10.65451757797000099 ) ) ;
#6038=CARTESIAN_POINT ( 'NONE',  ( 14.35387625730999872, 4.075369344914999914, 8.193037116081999471 ) ) ;
#6039=CARTESIAN_POINT ( 'NONE',  ( 24.34804274388857337, 12.49056186101158872, -3.365712241645715253 ) ) ;
#6040=ORIENTED_EDGE ( 'NONE', *, *, #5997, .T. ) ;
#6043=CARTESIAN_POINT ( 'NONE',  ( 13.65222839007885192, -3.408405854262552381, 9.739428946578977175 ) ) ;
#6044=FACE_OUTER_BOUND ( 'NONE', #3941, .T. ) ;
#6045=CARTESIAN_POINT ( 'NONE',  ( 19.97708346185000039, -1.918664432208000203, -11.02511595671000144 ) ) ;
#6046=EDGE_CURVE ( 'NONE', #22071, #9831, #119, .T. ) ;
#6048=CARTESIAN_POINT ( 'NONE',  ( 14.46013925473697981, -5.946942342394209824, 6.857621950180825543 ) ) ;
#6049=CARTESIAN_POINT ( 'NONE',  ( 18.23920040721611358, 9.753634886311211005, -3.797171640280522897 ) ) ;
#6051=LINE ( 'NONE', #3777, #9856 ) ;
#6052=CARTESIAN_POINT ( 'NONE',  ( 24.37713355803437665, -12.31988888405492411, -3.661326509212557756 ) ) ;
#6056=CARTESIAN_POINT ( 'NONE',  ( -5.778907386873838092, 16.26325521095871451, -2.029774016053516927 ) ) ;
#6060=CARTESIAN_POINT ( 'NONE',  ( 6.164405146010373038, 14.04569583898674523, -0.4648891801310362504 ) ) ;
#6061=CARTESIAN_POINT ( 'NONE',  ( -23.74465998031000069, -6.216878364870000340, 12.50000000000000000 ) ) ;
#6062=CARTESIAN_POINT ( 'NONE',  ( 24.48327518124253288, -1.286795374954470939, -12.49999999999999822 ) ) ;
#6063=VERTEX_POINT ( 'NONE', #2541 ) ;
#6064=VERTEX_POINT ( 'NONE', #10430 ) ;
#6065=AXIS2_PLACEMENT_3D ( 'NONE', #5827, #16372, #7165 ) ;
#6066=CARTESIAN_POINT ( 'NONE',  ( -14.00000000000000355, -9.276317213022405639, -4.032382767787531463 ) ) ;
#6067=CARTESIAN_POINT ( 'NONE',  ( -9.887017211694999475, -14.92817890949999970, -4.420227885350999308 ) ) ;
#6070=ORIENTED_EDGE ( 'NONE', *, *, #15908, .T. ) ;
#6071=CARTESIAN_POINT ( 'NONE',  ( -22.17317987022000025, -9.611087939101999211, -1.202903246196999953 ) ) ;
#6072=CARTESIAN_POINT ( 'NONE',  ( -14.47125382252185766, 11.86037473473944992, 4.457180938888235744 ) ) ;
#6074=CARTESIAN_POINT ( 'NONE',  ( 15.58068586916286158, -6.908712814867072893, 7.703922221359164269 ) ) ;
#6076=EDGE_CURVE ( 'NONE', #19490, #9820, #7375, .T. ) ;
#6078=CARTESIAN_POINT ( 'NONE',  ( -19.55887123173999953, -9.833822427806001798, 3.504477313184999776 ) ) ;
#6079=CARTESIAN_POINT ( 'NONE',  ( -19.53660345378999708, -7.531619525312000185, 7.381236299612999652 ) ) ;
#6086=CARTESIAN_POINT ( 'NONE',  ( -3.341782429828001888, 13.63576718287998268, 5.133260327393998068 ) ) ;
#6088=B_SPLINE_CURVE_WITH_KNOTS ( 'NONE', 3,
 ( #8924, #3475, #23317, #23569, #4931 ),
 .UNSPECIFIED., .F., .F.,
 ( 4, 1, 4 ),
 ( 0.000000000000000000, 0.5000000000000000000, 1.000000000000000000 ),
 .UNSPECIFIED. ) ;
#6089=CARTESIAN_POINT ( 'NONE',  ( -24.50000000000000000, 3.293267271483000247, -9.759323269498999309 ) ) ;
#6090=CARTESIAN_POINT ( 'NONE',  ( 18.13612658530999866, 10.25022803218000078, -0.6090841227779000278 ) ) ;
#6095=B_SPLINE_SURFACE_WITH_KNOTS ( 'NONE', 3, 3, ( 
 ( #23859, #14769, #16357, #5690, #22054, #10919, #21932, #5344, #22165, #12618, #12733, #20474, #20127, #5577, #3535, #12955, #11274, #16590, #1600, #20003, #7502, #8985, #5463, #16703, #9212, #12845, #20241, #20354, #3645, #2, #3760, #11149, #1943, #9330, #113 ),
 ( #14884, #3883, #18651, #2058, #16243, #7043, #23635, #7625, #9683, #5920, #6280, #7748, #2407, #11861, #7864, #705, #4238, #11628, #18998, #20584, #15002, #7984, #13665, #15232, #577, #9798, #17184, #8115, #11509, #15114, #16822, #16945, #13549, #347, #11390 ),
 ( #21058, #17305, #15481, #11742, #18885, #20702, #15356, #20825, #9919, #22746, #6163, #20945, #4351, #6037, #19115, #227, #2528, #22399, #17063, #13305, #4471, #22511, #22867, #19243, #22626, #9448, #5810, #13193, #3995, #18760, #2172, #9563, #4111, #13425, #2293 ),
 ( #461, #4723, #8348, #10050, #10169, #6767, #17554, #4600, #17434, #14159, #8230, #21677, #17677, #828, #4845, #1202, #4968, #12354, #15841, #10287, #12231, #11989, #12469, #1326, #12110, #19743, #3153, #1074, #10415, #13784, #21310, #19497, #10536, #17921, #14282 ) ),
 .UNSPECIFIED., .F., .F., .F.,
 ( 4, 4 ),
 ( 4, 1, 1, 1, 1, 1, 1, 1, 1, 1, 1, 1, 1, 1, 1, 1, 1, 1, 1, 1, 1, 1, 1, 1, 1, 1, 1, 1, 1, 1, 1, 1, 4 ),
 ( -0.08408083179840999954, 1.084080831798000188 ),
 ( -0.02000000000000000042, 0.01250000000000000069, 0.04499999999999999833, 0.07749999999999999944, 0.1100000000000000006, 0.1424999999999999878, 0.1749999999999999889, 0.2074999999999999900, 0.2399999999999999911, 0.2725000000000000200, 0.3049999999999999933, 0.3375000000000000222, 0.3699999999999999956, 0.4025000000000000244, 0.4349999999999999978, 0.4675000000000000266, 0.5000000000000000000, 0.5324999999999999734, 0.5649999999999999467, 0.5975000000000000311, 0.6300000000000000044, 0.6624999999999999778, 0.6949999999999999512, 0.7275000000000000355, 0.7600000000000000089, 0.7924999999999999822, 0.8249999999999999556, 0.8575000000000000400, 0.8900000000000000133, 0.9224999999999999867, 0.9549999999999999600, 0.9875000000000000444, 1.020000000000000018 ),
 .UNSPECIFIED. ) ;
#6096=ORIENTED_EDGE ( 'NONE', *, *, #2904, .F. ) ;
#6098=DIRECTION ( 'NONE',  ( 1.000000000000000000, 0.000000000000000000, 0.000000000000000000 ) ) ;
#6099=CARTESIAN_POINT ( 'NONE',  ( 4.740896961984002012, 12.61498246287000669, -0.02295444947824999346 ) ) ;
#6101=CARTESIAN_POINT ( 'NONE',  ( 17.89236288313008316, -6.599759852709097707, -8.116454319322453870 ) ) ;
#6102=AXIS2_PLACEMENT_3D ( 'NONE', #16253, #17848, #14201 ) ;
#6103=CARTESIAN_POINT ( 'NONE',  ( -23.75392437285000113, 6.466984436016000259, 12.35560119250000000 ) ) ;
#6107=DIRECTION ( 'NONE',  ( 0.000000000000000000, -0.7746237854577067150, 0.6324223201336057754 ) ) ;
#6108=CARTESIAN_POINT ( 'NONE',  ( 4.835177208035999818, -12.44999999999999929, 0.000000000000000000 ) ) ;
#6109=CARTESIAN_POINT ( 'NONE',  ( 14.70899999999999963, -9.048743642952000954, 0.000000000000000000 ) ) ;
#6111=ORIENTED_EDGE ( 'NONE', *, *, #10839, .T. ) ;
#6112=CARTESIAN_POINT ( 'NONE',  ( -16.59891243917333270, -8.860514229207437253, 2.381066699024747546 ) ) ;
#6113=CARTESIAN_POINT ( 'NONE',  ( 20.75421567572999848, -2.745092682207000312, -9.410255969462001602 ) ) ;
#6114=CARTESIAN_POINT ( 'NONE',  ( -0.8045575664689312845, 12.82434487819426572, -6.623413967079410547 ) ) ;
#6117=CARTESIAN_POINT ( 'NONE',  ( -19.89453591501058582, 6.153835458516363488, 8.498639860652758671 ) ) ;
#6119=EDGE_CURVE ( 'NONE', #17324, #12095, #4737, .T. ) ;
#6123=CARTESIAN_POINT ( 'NONE',  ( -17.57271597048792700, -9.444424520270592538, 4.430025553576289354 ) ) ;
#6128=CARTESIAN_POINT ( 'NONE',  ( -12.25000000000000000, 1.374666032043000015E-14, 0.000000000000000000 ) ) ;
#6130=CARTESIAN_POINT ( 'NONE',  ( 16.99624770046333921, -7.283006694536083181, -5.596856954334615608 ) ) ;
#6131=VECTOR ( 'NONE', #19108, 1000.000000000000227 ) ;
#6132=CARTESIAN_POINT ( 'NONE',  ( 17.17537674931000069, -4.906342569036000079, 9.567493125660998743 ) ) ;
#6134=CARTESIAN_POINT ( 'NONE',  ( -19.21948930940000011, -9.233400656586999489, -6.760258690304999263 ) ) ;
#6137=CARTESIAN_POINT ( 'NONE',  ( 15.86921080085999769, -10.66112877511999990, -3.930111991920000047 ) ) ;
#6138=CARTESIAN_POINT ( 'NONE',  ( 13.50000000000000000, -8.269916559704732606, -4.425252021080920528 ) ) ;
#6139=CARTESIAN_POINT ( 'NONE',  ( 0.000000000000000000, 20.10000000000000142, 0.000000000000000000 ) ) ;
#6140=CARTESIAN_POINT ( 'NONE',  ( 25.09343792058000133, -5.309646865108000213, 8.124620694544001154 ) ) ;
#6144=CARTESIAN_POINT ( 'NONE',  ( 12.61436189658999929, 4.419636859381000704, -7.963858022973001383 ) ) ;
#6147=CARTESIAN_POINT ( 'NONE',  ( 4.392057029119999179, 12.33170126310999670, 1.899976486714999746 ) ) ;
#6149=CARTESIAN_POINT ( 'NONE',  ( -19.78402572227999912, 1.667133957923000009, 10.91833191109000012 ) ) ;
#6150=ORIENTED_EDGE ( 'NONE', *, *, #7770, .T. ) ;
#6152=EDGE_CURVE ( 'NONE', #12183, #20328, #16031, .T. ) ;
#6156=CARTESIAN_POINT ( 'NONE',  ( -24.50000000000000000, 0.000000000000000000, -12.50000000000000000 ) ) ;
#6157=CARTESIAN_POINT ( 'NONE',  ( -2.921311158041803413, 11.94552971169360589, 3.795700454126800238 ) ) ;
#6159=CARTESIAN_POINT ( 'NONE',  ( 4.918565628415999313, 13.52958698473998567, 5.101225743681996327 ) ) ;
#6161=CARTESIAN_POINT ( 'NONE',  ( 13.55568924931000119, -5.133899498893999436, 9.338903284905999413 ) ) ;
#6162=VECTOR ( 'NONE', #20377, 1000.000000000000000 ) ;
#6163=CARTESIAN_POINT ( 'NONE',  ( -17.46454189286000158, -8.119858849493999386, 7.209780893148999503 ) ) ;
#6165=CARTESIAN_POINT ( 'NONE',  ( 12.16012625731000085, 8.900490462747001175, -1.861105101465000189 ) ) ;
#6167=CARTESIAN_POINT ( 'NONE',  ( 24.45564077607145492, 11.85537957198067005, -4.465880238315118156 ) ) ;
#6168=ORIENTED_EDGE ( 'NONE', *, *, #50, .F. ) ;
#6170=B_SPLINE_CURVE_WITH_KNOTS ( 'NONE', 3,
 ( #16410, #5631, #1888, #7209, #13014, #3823, #16534, #2005, #23921, #9389, #16761, #21995, #11338, #12793, #170, #5410, #7561, #13255 ),
 .UNSPECIFIED., .F., .F.,
 ( 4, 2, 2, 2, 2, 2, 2, 2, 4 ),
 ( 0.000000000000000000, 0.1250000000000000000, 0.2500000000000000000, 0.3750000000000000000, 0.5000000000000000000, 0.6250000000000000000, 0.7500000000000000000, 0.8750000000000000000, 1.000000000000000000 ),
 .UNSPECIFIED. ) ;
#6172=CARTESIAN_POINT ( 'NONE',  ( 14.02876822787055033, -10.30979721075241073, -0.6943530198432756873 ) ) ;
#6174=CARTESIAN_POINT ( 'NONE',  ( -2.256930243168998818, 12.92976665894000732, -6.094107447253994891 ) ) ;
#6177=CARTESIAN_POINT ( 'NONE',  ( 11.48478210364236674, 3.271710350470132589, 12.49991250862224490 ) ) ;
#6178=CARTESIAN_POINT ( 'NONE',  ( 18.79674436531792736, 0.1206336078962078756, 10.48047579883863989 ) ) ;
#6180=CARTESIAN_POINT ( 'NONE',  ( -21.24728743917332352, 7.370242396797828555, -5.663897891694076314 ) ) ;
#6181=CARTESIAN_POINT ( 'NONE',  ( 23.99999963380687618, 13.93375672974000246, -1.355252715606880543E-17 ) ) ;
#6182=ORIENTED_EDGE ( 'NONE', *, *, #23738, .T. ) ;
#6183=CARTESIAN_POINT ( 'NONE',  ( 11.72559253312535432, -8.766982473567979994, 9.815058145095289177 ) ) ;
#6184=EDGE_LOOP ( 'NONE', ( #15415, #17829, #15750, #610, #5579, #20497, #14952, #1323 ) ) ;
#6186=CARTESIAN_POINT ( 'NONE',  ( -4.772412363876479269, 12.42044774334072166, 0.8590728381116085055 ) ) ;
#6188=CARTESIAN_POINT ( 'NONE',  ( -23.76320767108999732, -6.966447585166999801, -12.06723600888999925 ) ) ;
#6189=CARTESIAN_POINT ( 'NONE',  ( 15.31342757799999887, 6.394788428435000505, 8.996804509239000325 ) ) ;
#6190=CARTESIAN_POINT ( 'NONE',  ( -7.088468813309002137, 15.38200575439001128, -1.346721112802998332 ) ) ;
#6195=CARTESIAN_POINT ( 'NONE',  ( -24.17970357207700260, 8.771272208504171886, -9.807700027458217562 ) ) ;
#6197=CARTESIAN_POINT ( 'NONE',  ( -14.45960647534970178, -9.597314625688284195, -8.376896358978855872 ) ) ;
#6200=CARTESIAN_POINT ( 'NONE',  ( 6.220388596125608238, 13.78688666331658830, 1.207122575335724424 ) ) ;
#6201=CARTESIAN_POINT ( 'NONE',  ( 15.25236472003948940, 4.074645878791661069, 9.504836835712692888 ) ) ;
#6202=CARTESIAN_POINT ( 'NONE',  ( -19.60935064726000121, -11.08680168281000000, 1.130667934175000111 ) ) ;
#6204=CARTESIAN_POINT ( 'NONE',  ( -20.84460765454501185, -0.9149537475125872898, -10.47345582031393896 ) ) ;
#6205=CARTESIAN_POINT ( 'NONE',  ( -15.43323841317000067, -10.79835415318000003, -0.2870680789784999520 ) ) ;
#6211=ORIENTED_EDGE ( 'NONE', *, *, #22377, .F. ) ;
#6212=CARTESIAN_POINT ( 'NONE',  ( -23.74465998031000069, 7.716878364870000340, -11.63397459621999985 ) ) ;
#6213=CARTESIAN_POINT ( 'NONE',  ( 5.899122318018997113, 14.55469254769999488, -1.683791433005999760 ) ) ;
#6215=B_SPLINE_CURVE_WITH_KNOTS ( 'NONE', 3,
 ( #19772, #15870, #3060, #18197, #3182 ),
 .UNSPECIFIED., .F., .F.,
 ( 4, 1, 4 ),
 ( 0.000000000000000000, 0.5000000000000000000, 1.000000000000000000 ),
 .UNSPECIFIED. ) ;
#6216=CARTESIAN_POINT ( 'NONE',  ( -24.50000000000000000, -1.873582633960999999, -10.39897383761999983 ) ) ;
#6218=CARTESIAN_POINT ( 'NONE',  ( 18.24581408530999838, 9.747919580236001025, 3.236577786812999680 ) ) ;
#6220=CARTESIAN_POINT ( 'NONE',  ( -6.250000000000000000, 1.301187224093999891E-14, 0.000000000000000000 ) ) ;
#6222=CYLINDRICAL_SURFACE ( 'NONE', #19982, 15.43375672974000068 ) ;
#6224=CARTESIAN_POINT ( 'NONE',  ( -12.50000000000000000, 6.965460728298000781, -5.686777139159000072 ) ) ;
#6226=CARTESIAN_POINT ( 'NONE',  ( -23.39099967059616958, 6.713552081593185505, -6.458098826819107963 ) ) ;
#6227=CARTESIAN_POINT ( 'NONE',  ( -12.50000000000000000, 1.377727649040999975E-14, 0.000000000000000000 ) ) ;
#6228=CARTESIAN_POINT ( 'NONE',  ( 18.40433895126197683, 9.206357412411914964, -4.883359051719883936 ) ) ;
#6229=CARTESIAN_POINT ( 'NONE',  ( 0.000000000000000000, 17.00000000000000000, 0.000000000000000000 ) ) ;
#6230=ADVANCED_FACE ( 'NONE', ( #1340 ), #23182, .F. ) ;
#6231=CARTESIAN_POINT ( 'NONE',  ( -14.40719418339326729, 8.953944931993316203, -9.491079701373065447 ) ) ;
#6232=CARTESIAN_POINT ( 'NONE',  ( -5.090709799003004576, 16.33848066163001889, -3.590694264005000136 ) ) ;
#6233=DIRECTION ( 'NONE',  ( -0.7071067811865975328, -0.7071067811864976127, -1.204881101557994910E-09 ) ) ;
#6238=CARTESIAN_POINT ( 'NONE',  ( 19.31333166812999735, -6.932005976255000590, -8.325654194909999362 ) ) ;
#6239=CARTESIAN_POINT ( 'NONE',  ( -4.227279577313947101, 13.39853892358859433, -5.369578654743469848 ) ) ;
#6241=CARTESIAN_POINT ( 'NONE',  ( -19.97486504007325436, 8.250260110346381737, 6.482288355094454779 ) ) ;
#6245=EDGE_CURVE ( 'NONE', #1842, #8248, #5909, .T. ) ;
#6246=CARTESIAN_POINT ( 'NONE',  ( -17.07031370036265017, -2.772578259958148550, -10.04572367896972906 ) ) ;
#6252=CARTESIAN_POINT ( 'NONE',  ( 11.88393908531000065, -9.721606288483000569, -2.753149205743999683 ) ) ;
#6253=CARTESIAN_POINT ( 'NONE',  ( -22.77424452324999748, -7.081648116287999173, -8.665291262669999384 ) ) ;
#6254=EDGE_CURVE ( 'NONE', #2037, #9910, #7601, .T. ) ;
#6255=CARTESIAN_POINT ( 'NONE',  ( -13.12557887030999915, 10.05389705766999953, -2.585396581761999713 ) ) ;
#6257=CARTESIAN_POINT ( 'NONE',  ( 14.04108580085999947, -10.79197239458999924, -3.388753120225000082 ) ) ;
#6259=DIRECTION ( 'NONE',  ( 0.9989428060277519839, 0.000000000000000000, -0.04597031961386779941 ) ) ;
#6260=CARTESIAN_POINT ( 'NONE',  ( 25.36474249277999959, -5.041558719633999708, 7.714402359875999871 ) ) ;
#6261=B_SPLINE_CURVE_WITH_KNOTS ( 'NONE', 3,
 ( #13082, #4246, #19004, #3890, #586, #10058, #836, #21562, #10176, #14167, #10543, #13672, #15963, #8601, #4977, #2665, #19381, #11869, #17928, #1335, #2792, #21317, #23357, #13793, #8722, #10423, #8238, #17441, #12118, #21066, #19253, #10296, #23237, #17563, #21194, #4480, #15606, #11996, #4608, #4732, #22991, #958, #19504, #6774, #16086, #17685, #8356, #12362, #15722, #6410, #19750, #17814, #1084, #6651, #2913, #23113, #6537, #3161 ),
 .UNSPECIFIED., .F., .F.,
 ( 4, 2, 2, 2, 1, 1, 2, 2, 2, 2, 1, 1, 1, 2, 2, 2, 2, 1, 1, 2, 2, 2, 1, 1, 2, 2, 2, 2, 2, 1, 1, 1, 2, 2, 4 ),
 ( 0.000000000000000000, 0.06249999999999863998, 0.09374999999999787670, 0.1093749999999975575, 0.1171874999999975020, 0.1210937499999974604, 0.1230468749999975020, 0.1249999999999975298, 0.1874999999999997502, 0.2187500000000008882, 0.2343750000000013323, 0.2421875000000015543, 0.2460937500000017486, 0.2480468750000016931, 0.2500000000000016098, 0.3125000000000025535, 0.3437500000000031086, 0.3593750000000033862, 0.3671875000000035527, 0.3710937500000035527, 0.3750000000000034972, 0.4375000000000021649, 0.4687500000000014988, 0.4843750000000012212, 0.4921875000000011102, 0.5000000000000009992, 0.7499999999999970024, 0.8124999999999960032, 0.8437499999999955591, 0.8593749999999952260, 0.8671874999999951150, 0.8710937499999951150, 0.8730468749999953371, 0.8749999999999954481, 1.000000000000000000 ),
 .UNSPECIFIED. ) ;
#6264=CARTESIAN_POINT ( 'NONE',  ( -12.00000000000000000, 1.554281285376986145E-14, -7.000000000000000000 ) ) ;
#6267=CARTESIAN_POINT ( 'NONE',  ( -1.925363223002000357, 11.65848132151000094, 4.402296118137997816 ) ) ;
#6270=CARTESIAN_POINT ( 'NONE',  ( -21.26732368540999829, -11.05878950324999899, 0.7642943787211000650 ) ) ;
#6276=CARTESIAN_POINT ( 'NONE',  ( 5.267359632244998480, 13.90542513608999897, 3.709429151287999105 ) ) ;
#6277=EDGE_CURVE ( 'NONE', #17401, #23059, #12829, .T. ) ;
#6280=CARTESIAN_POINT ( 'NONE',  ( -17.22065346366999705, -7.714380452752999773, 6.849660182178999968 ) ) ;
#6282=CARTESIAN_POINT ( 'NONE',  ( 12.26981375731000057, 8.958847990383999260, 1.572873132563999965 ) ) ;
#6283=CARTESIAN_POINT ( 'NONE',  ( 24.37713355803437665, 2.989142673506741232, 12.50000000000000355 ) ) ;
#6286=CARTESIAN_POINT ( 'NONE',  ( 20.32323479018660706, 8.891074209933115924, 5.624032425053880679 ) ) ;
#6287=CARTESIAN_POINT ( 'NONE',  ( 12.52688711657000020, -13.93375672974000068, -0.8660254037843999608 ) ) ;
#6291=ORIENTED_EDGE ( 'NONE', *, *, #11500, .F. ) ;
#6292=CARTESIAN_POINT ( 'NONE',  ( -3.963089716433997101, 14.56865066125998709, -4.679596269295001498 ) ) ;
#6295=CARTESIAN_POINT ( 'NONE',  ( 12.52688711657000020, -6.216878364870000340, 12.50000000000000000 ) ) ;
#6296=CARTESIAN_POINT ( 'NONE',  ( 18.46221799045618184, 9.641442781986372168, 4.082290055557257880 ) ) ;
#6297=DIRECTION ( 'NONE',  ( -1.000000000000000000, 0.000000000000000000, 0.000000000000000000 ) ) ;
#6299=ORIENTED_EDGE ( 'NONE', *, *, #7750, .F. ) ;
#6301=CARTESIAN_POINT ( 'NONE',  ( 4.623021688823209630, 12.49842695769186740, -1.256073083333553830 ) ) ;
#6303=B_SPLINE_SURFACE_WITH_KNOTS ( 'NONE', 3, 3, ( 
 ( #13153, #5881, #11233, #11700, #539, #11584, #2016, #20545, #22229, #5994, #15193, #18611, #7944, #18959, #16774, #15309, #13379, #422, #4309, #6113, #2488, #4187, #9877, #11348, #20781, #4071, #17263, #7454, #14837, #2367, #18841, #11463, #183, #7573, #14953 ),
 ( #22349, #18720, #2130, #9519, #16896, #299, #15075, #13266, #20660, #2245, #9639, #17023, #8306, #10369, #15555, #8432, #21018, #2979, #1162, #2860, #13870, #22942, #15671, #12306, #23060, #23305, #4430, #21140, #8556, #11820, #2742, #10122, #21273, #2612, #13620 ),
 ( #4682, #6488, #10243, #10001, #4800, #10496, #12069, #1030, #17759, #19452, #15799, #19198, #19331, #17511, #15914, #6722, #19696, #905, #23191, #17392, #11946, #4920, #22824, #14113, #4555, #787, #19574, #17633, #6359, #6238, #6608, #8187, #21508, #13991, #13741 ),
 ( #21385, #3112, #662, #8068, #15437, #12185, #18666, #21749, #14236, #18120, #12432, #9463, #20492, #16839, #8915, #1958, #2073, #10612, #5590, #14782, #3778, #12544, #16156, #8794, #16717, #243, #10728, #1282, #1526, #9344, #5162, #128, #13208, #18553, #5050 ) ),
 .UNSPECIFIED., .F., .F., .F.,
 ( 4, 4 ),
 ( 4, 1, 1, 1, 1, 1, 1, 1, 1, 1, 1, 1, 1, 1, 1, 1, 1, 1, 1, 1, 1, 1, 1, 1, 1, 1, 1, 1, 1, 1, 1, 1, 4 ),
 ( -0.08331297109794999489, 1.083312971098000066 ),
 ( 0.1014657448152999908, 0.1300955127501000064, 0.1587252806848999942, 0.1873550486197999854, 0.2159848165546000009, 0.2446145844893999888, 0.2732443524242000321, 0.3018741203590000199, 0.3305038882938000078, 0.3591336562285999956, 0.3877634241634000389, 0.4163931920982000268, 0.4450229600330000146, 0.4736527279678000024, 0.5022824959025999902, 0.5309122638374000891, 0.5595420317721999659, 0.5881717997070000647, 0.6168015676417999416, 0.6454313355766000404, 0.6740611035114000282, 0.7026908714463000472, 0.7313206393811000350, 0.7599504073159000228, 0.7885801752507000106, 0.8172099431854999985, 0.8458397111202999863, 0.8744694790551000851, 0.9030992469899000730, 0.9317290149246999498, 0.9603587828595000486, 0.9889885507942999254, 1.017618318728999993 ),
 .UNSPECIFIED. ) ;
#6304=CARTESIAN_POINT ( 'NONE',  ( -5.769429997167383029, 16.25870916169602509, -2.056550855362532015 ) ) ;
#6305=CARTESIAN_POINT ( 'NONE',  ( 0.5498409912916205622, 11.49495375948718490, 4.782145214771198027 ) ) ;
#6307=CARTESIAN_POINT ( 'NONE',  ( -2.056952183161803394, 12.94126637194106877, 6.392751251890534725 ) ) ;
#6309=CARTESIAN_POINT ( 'NONE',  ( -20.62057330634167940, 0.5096360985298603596, 9.248796765395695729 ) ) ;
#6313=CARTESIAN_POINT ( 'NONE',  ( -13.99999999999999822, -7.572152359989809511, -6.464702211010298072 ) ) ;
#6316=EDGE_LOOP ( 'NONE', ( #17035, #1899, #16159, #16856, #9023 ) ) ;
#6318=CARTESIAN_POINT ( 'NONE',  ( -23.95936891989000017, -4.964537398340999275, -8.976378852492999272 ) ) ;
#6320=CARTESIAN_POINT ( 'NONE',  ( 6.190667799111778891, 13.91886042571875670, 0.7936539895852133819 ) ) ;
#6321=CARTESIAN_POINT ( 'NONE',  ( 15.61445477932001502, -7.782978770127811252, 6.824697942149217766 ) ) ;
#6322=CARTESIAN_POINT ( 'NONE',  ( -17.11410595495999942, 1.976719737850999969, -10.89867228117000053 ) ) ;
#6323=DIRECTION ( 'NONE',  ( -0.9999999999999998890, 9.268912834351999024E-09, -3.975900789814998879E-09 ) ) ;
#6324=CARTESIAN_POINT ( 'NONE',  ( -21.30783991800640464, -10.44792467106556977, 1.268519232389238693 ) ) ;
#6325=B_SPLINE_CURVE_WITH_KNOTS ( 'NONE', 3,
 ( #17127, #8046, #523, #7926, #15293, #4294 ),
 .UNSPECIFIED., .F., .F.,
 ( 4, 1, 1, 4 ),
 ( 0.000000000000000000, 0.3333333333333000081, 0.6666666666667000474, 1.000000000000000000 ),
 .UNSPECIFIED. ) ;
#6327=CARTESIAN_POINT ( 'NONE',  ( -24.05763402810364937, -5.201095832796127638, -8.431872254508961717 ) ) ;
#6332=CARTESIAN_POINT ( 'NONE',  ( -16.48875683979265361, 6.849824468384817067, 8.049161493870508721 ) ) ;
#6333=ORIENTED_EDGE ( 'NONE', *, *, #21116, .F. ) ;
#6335=CARTESIAN_POINT ( 'NONE',  ( 6.081505281638999172, 14.07690835503000493, 0.05978829213082002131 ) ) ;
#6336=CARTESIAN_POINT ( 'NONE',  ( 12.00000000000000178, -1.529947326563451560, -8.848046545010550545 ) ) ;
#6338=VECTOR ( 'NONE', #6233, 1000.000000000000114 ) ;
#6339=CARTESIAN_POINT ( 'NONE',  ( 17.25862658530999738, -10.23584709072999921, -0.4386478486912999686 ) ) ;
#6341=CARTESIAN_POINT ( 'NONE',  ( -6.297602208228999743, 15.63806030118000656, -1.260321238843998604 ) ) ;
#6345=DIRECTION ( 'NONE',  ( 0.000000000000000000, -1.000000000000000000, 6.254561278617999028E-11 ) ) ;
#6346=CARTESIAN_POINT ( 'NONE',  ( 11.70388046502542245, 8.799739770623126844, 9.758286884852591214 ) ) ;
#6349=CARTESIAN_POINT ( 'NONE',  ( -7.034000000000000696, -11.50000000000000000, -2.869685045148000171E-11 ) ) ;
#6350=CARTESIAN_POINT ( 'NONE',  ( 18.40159154013413811, 9.157578505391652968, -4.974487616550520741 ) ) ;
#6351=DIRECTION ( 'NONE',  ( 0.000000000000000000, 1.000000000000000000, 0.000000000000000000 ) ) ;
#6352=CARTESIAN_POINT ( 'NONE',  ( -14.25243324638999809, 13.93375672974000068, -0.8660254037843999608 ) ) ;
#6353=CARTESIAN_POINT ( 'NONE',  ( 23.39170489349999826, 6.484734603292000799, -9.235218885525998900 ) ) ;
#6354=CARTESIAN_POINT ( 'NONE',  ( 0.000000000000000000, 20.00000000000000000, 0.000000000000000000 ) ) ;
#6355=CARTESIAN_POINT ( 'NONE',  ( -4.029105800529611869, 13.82458363547321589, -4.859102542853258377 ) ) ;
#6359=CARTESIAN_POINT ( 'NONE',  ( 19.50658260167999813, -0.2703046275102000129, -10.83567124763000145 ) ) ;
#6360=CARTESIAN_POINT ( 'NONE',  ( 0.7331010873566492503, 12.82195173545669320, -6.628039790227788330 ) ) ;
#6362=CARTESIAN_POINT ( 'NONE',  ( -19.38578478962144302, -9.503017921997821915, 4.413944164837940498 ) ) ;
#6363=CARTESIAN_POINT ( 'NONE',  ( 4.914858397426013603, 14.34199478478198841, 3.826882337439999393 ) ) ;
#6364=CARTESIAN_POINT ( 'NONE',  ( -1.474515923050999655, 11.54597486106999504, -4.712210093417001922 ) ) ;
#6365=ORIENTED_EDGE ( 'NONE', *, *, #20189, .F. ) ;
#6366=CARTESIAN_POINT ( 'NONE',  ( -16.79120132807066312, 6.696678809309016600, -7.978545510531970919 ) ) ;
#6367=DIRECTION ( 'NONE',  ( 0.000000000000000000, 1.000000000000000000, 0.000000000000000000 ) ) ;
#6368=AXIS2_PLACEMENT_3D ( 'NONE', #22933, #777, #6351 ) ;
#6375=CARTESIAN_POINT ( 'NONE',  ( 13.11693924931000055, 9.054732109491999026, 5.598051111924999823 ) ) ;
#6376=CARTESIAN_POINT ( 'NONE',  ( -21.32896435853999861, -10.30805567071999995, 4.255407315586999140 ) ) ;
#6377=CARTESIAN_POINT ( 'NONE',  ( -6.294047091888000267, 15.63810218524001172, 1.260373451110999188 ) ) ;
#6378=CARTESIAN_POINT ( 'NONE',  ( 15.66749951745999958, 9.735035431332001110, -0.2247563725877999852 ) ) ;
#6380=DIRECTION ( 'NONE',  ( 0.000000000000000000, -0.8660254037844288266, 0.5000000000000169864 ) ) ;
#6381=CARTESIAN_POINT ( 'NONE',  ( 24.65654608415999860, 9.344931615893999677, -2.926056642454999857 ) ) ;
#6383=CARTESIAN_POINT ( 'NONE',  ( 23.99062354302999722, -7.716878364870000340, 11.63397459621999985 ) ) ;
#6385=CARTESIAN_POINT ( 'NONE',  ( 0.000000000000000000, 17.00000000000000000, 0.000000000000000000 ) ) ;
#6388=CARTESIAN_POINT ( 'NONE',  ( -0.1122646929101999980, 11.54752496335999012, 4.753533889266998713 ) ) ;
#6390=CARTESIAN_POINT ( 'NONE',  ( -20.91269164496000244, 1.066062916854000120, -11.02412034271000074 ) ) ;
#6392=EDGE_LOOP ( 'NONE', ( #5272, #19451, #4680, #16371 ) ) ;
#6393=CARTESIAN_POINT ( 'NONE',  ( -24.11803009776757634, 4.367939700858217478, -12.49970390892939243 ) ) ;
#6394=CARTESIAN_POINT ( 'NONE',  ( -1.254111594709508504, 11.63130255791515033, 4.623328579164538432 ) ) ;
#6395=EDGE_CURVE ( 'NONE', #2137, #14425, #1687, .T. ) ;
#6396=CARTESIAN_POINT ( 'NONE',  ( -3.693067381368000834, 13.86499636515999967, 4.815635213893004973 ) ) ;
#6397=B_SPLINE_CURVE_WITH_KNOTS ( 'NONE', 3,
 ( #18163, #3387, #5310, #21549, #16431, #4964, #7004, #3265, #3610, #5085, #23709, #9176, #5197, #22017, #1565, #8951, #7115, #17917, #12349, #12699, #10993, #18379, #3150, #9060 ),
 .UNSPECIFIED., .F., .F.,
 ( 4, 2, 2, 2, 2, 2, 2, 2, 1, 1, 2, 2, 4 ),
 ( 0.000000000000000000, 0.2500000000000229816, 0.3750000000000345834, 0.4375000000000403011, 0.4687500000000402456, 0.5000000000000401901, 0.6250000000000424105, 0.6875000000000435207, 0.7187500000000440759, 0.7343750000000448530, 0.7421875000000460743, 0.7500000000000471845, 1.000000000000000000 ),
 .UNSPECIFIED. ) ;
#6400=CARTESIAN_POINT ( 'NONE',  ( -6.159325028044951189, 15.88311956943892689, -1.090658714736985280 ) ) ;
#6403=CARTESIAN_POINT ( 'NONE',  ( 15.23137625731000000, -4.902144360783999844, -7.754105707547999771 ) ) ;
#6405=CARTESIAN_POINT ( 'NONE',  ( 24.36881528991199986, 3.090117214402293477, 12.50000000000000178 ) ) ;
#6406=ORIENTED_EDGE ( 'NONE', *, *, #23877, .F. ) ;
#6407=CARTESIAN_POINT ( 'NONE',  ( 20.62424770046331091, -7.357456981350354752, -5.654072255929076363 ) ) ;
#6410=CARTESIAN_POINT ( 'NONE',  ( -2.357926041848682708, 13.96279335765504648, -5.653421260559023942 ) ) ;
#6411=VERTEX_POINT ( 'NONE', #20685 ) ;
#6416=CARTESIAN_POINT ( 'NONE',  ( 12.04708237236142487, -5.050716351111039337, 12.50004921246056355 ) ) ;
#6417=CARTESIAN_POINT ( 'NONE',  ( -4.333208638113355882, 13.59008039607882345, 4.978090617012794539 ) ) ;
#6418=CARTESIAN_POINT ( 'NONE',  ( -21.70078743917332886, -5.671049804393380356, -7.379548682649590852 ) ) ;
#6419=CARTESIAN_POINT ( 'NONE',  ( 24.48327518124254354, -11.46871523476161059, -5.135602515852324856 ) ) ;
#6423=CARTESIAN_POINT ( 'NONE',  ( -4.749997084077000054, 12.55000000011000161, -4.491085162427999259E-09 ) ) ;
#6425=DIRECTION ( 'NONE',  ( -1.000000000000000000, 0.000000000000000000, 0.000000000000000000 ) ) ;
#6428=CARTESIAN_POINT ( 'NONE',  ( 4.058888790243617706, 13.35463775849163426, 5.476079634781732430 ) ) ;
#6429=CARTESIAN_POINT ( 'NONE',  ( 6.148088670540117207, 14.14458356372224834, -0.2229764228181548014 ) ) ;
#6430=CARTESIAN_POINT ( 'NONE',  ( -6.418772728474004374, 15.32337082171999931, -1.206311712873000097 ) ) ;
#6434=ORIENTED_EDGE ( 'NONE', *, *, #15129, .T. ) ;
#6435=DIRECTION ( 'NONE',  ( -1.000000000000000000, 0.000000000000000000, 0.000000000000000000 ) ) ;
#6437=CARTESIAN_POINT ( 'NONE',  ( -20.18427425486666849, -9.189249971530744077, 1.048513845136502587 ) ) ;
#6438=ORIENTED_EDGE ( 'NONE', *, *, #20801, .T. ) ;
#6440=CONICAL_SURFACE ( 'NONE', #9536, 13.23032192316000000, 1.093540295016705466 ) ;
#6441=CARTESIAN_POINT ( 'NONE',  ( 6.141065375610000210, 14.19649368052000149, -1.893142280157000292E-06 ) ) ;
#6442=CARTESIAN_POINT ( 'NONE',  ( 15.22242881478463694, 5.018927266204900484, 9.044725437050461281 ) ) ;
#6443=CARTESIAN_POINT ( 'NONE',  ( -17.29476926998999886, -4.783536645008999777, -9.995794592903001430 ) ) ;
#6445=CARTESIAN_POINT ( 'NONE',  ( 12.00000000000000000, -9.392874664203999302, -3.575135015595999999 ) ) ;
#6446=CARTESIAN_POINT ( 'NONE',  ( -21.82254243295554375, 3.501655625743340661, 10.07467862742537967 ) ) ;
#6451=VECTOR ( 'NONE', #5275, 1000.000000000000000 ) ;
#6453=CARTESIAN_POINT ( 'NONE',  ( -15.41800740740231213, -1.436686530438418430, -10.28770811664919727 ) ) ;
#6454=CIRCLE ( 'NONE', #3744, 10.65000000000000036 ) ;
#6456=CARTESIAN_POINT ( 'NONE',  ( -24.50000000000000000, 1.524685264937999788E-14, 0.000000000000000000 ) ) ;
#6457=CARTESIAN_POINT ( 'NONE',  ( 6.085566944076997942, 14.50612891015002326, -0.7765878609773998464 ) ) ;
#6458=EDGE_CURVE ( 'NONE', #21807, #2989, #5791, .T. ) ;
#6459=CARTESIAN_POINT ( 'NONE',  ( -4.820913734138907003, 13.23370548858168227, -5.762714020006541205 ) ) ;
#6462=CARTESIAN_POINT ( 'NONE',  ( -20.18322087121332586, -5.647117051120087439, -7.348406657775178985 ) ) ;
#6463=CARTESIAN_POINT ( 'NONE',  ( 14.49000142131000146, 7.205444258087999820, 6.439089808501999634 ) ) ;
#6464=VERTEX_POINT ( 'NONE', #15338 ) ;
#6466=DIRECTION ( 'NONE',  ( 1.000000000000000000, 0.000000000000000000, 0.000000000000000000 ) ) ;
#6468=VERTEX_POINT ( 'NONE', #13174 ) ;
#6471=CARTESIAN_POINT ( 'NONE',  ( 4.811405344589000599, 12.64229255396000617, -0.1541548637438999170 ) ) ;
#6472=CARTESIAN_POINT ( 'NONE',  ( -13.99999999999999822, -3.511891994211063572, 9.329532952517192612 ) ) ;
#6473=CARTESIAN_POINT ( 'NONE',  ( 16.85684936900776876, 9.467955822817058831, 4.441589298551446241 ) ) ;
#6476=B_SPLINE_CURVE_WITH_KNOTS ( 'NONE', 3,
 ( #6287, #22751, #353, #11395, #13670 ),
 .UNSPECIFIED., .F., .F.,
 ( 4, 1, 4 ),
 ( 0.000000000000000000, 0.5000000000000000000, 1.000000000000000000 ),
 .UNSPECIFIED. ) ;
#6477=CARTESIAN_POINT ( 'NONE',  ( -14.49999965082560038, -10.56569440617049693, 6.699684590240001292 ) ) ;
#6478=CARTESIAN_POINT ( 'NONE',  ( 22.98768560147999906, -10.84767042793000158, -3.069029816253999954 ) ) ;
#6481=CARTESIAN_POINT ( 'NONE',  ( -4.396880683728629613, 13.55034449960124476, -5.013219078665608563 ) ) ;
#6483=DIRECTION ( 'NONE',  ( 0.000000000000000000, -0.9925668416490733836, 0.1217007183987965646 ) ) ;
#6484=CIRCLE ( 'NONE', #4550, 15.45000000000000107 ) ;
#6486=ORIENTED_EDGE ( 'NONE', *, *, #11940, .F. ) ;
#6487=CARTESIAN_POINT ( 'NONE',  ( -17.16578743917332872, 5.599530677400165857, 7.286485824131497147 ) ) ;
#6488=CARTESIAN_POINT ( 'NONE',  ( 24.65994082994999914, -8.903700310608000379, -5.455873167974000459 ) ) ;
#6489=CARTESIAN_POINT ( 'NONE',  ( 23.02309396335594371, -10.39063195256835392, 2.065499158806352042 ) ) ;
#6491=CARTESIAN_POINT ( 'NONE',  ( -20.34973429036302761, 8.472421900539268691, -6.203803128982323223 ) ) ;
#6495=CARTESIAN_POINT ( 'NONE',  ( -3.292290159323002285, 11.90693939058999717, -3.664509819767999499 ) ) ;
#6496=EDGE_LOOP ( 'NONE', ( #6701, #1599, #1659, #538, #12935 ) ) ;
#6497=CARTESIAN_POINT ( 'NONE',  ( -15.39563946661559335, -7.162326101167759695, -7.704075600233069920 ) ) ;
#6498=CARTESIAN_POINT ( 'NONE',  ( -24.12232999016000079, 1.520060141252000183E-14, 0.000000000000000000 ) ) ;
#6502=EDGE_LOOP ( 'NONE', ( #16852, #11827, #14915, #2493, #3081 ) ) ;
#6503=FACE_OUTER_BOUND ( 'NONE', #3322, .T. ) ;
#6504=CARTESIAN_POINT ( 'NONE',  ( -12.13322999603999897, 6.430159825535999296, -13.55186498671000095 ) ) ;
#6505=CARTESIAN_POINT ( 'NONE',  ( -20.68661761865999793, 2.890438285933000451, -10.75281663302000013 ) ) ;
#6506=CARTESIAN_POINT ( 'NONE',  ( 13.83937451745999958, 9.661954171790000601, -0.6968930456070000501 ) ) ;
#6507=CARTESIAN_POINT ( 'NONE',  ( -12.50000000000000000, 1.377727649040999975E-14, 0.000000000000000000 ) ) ;
#6509=DIRECTION ( 'NONE',  ( 1.000000000000000000, 0.000000000000000000, 0.000000000000000000 ) ) ;
#6511=ORIENTED_EDGE ( 'NONE', *, *, #3738, .F. ) ;
#6512=CARTESIAN_POINT ( 'NONE',  ( -2.591910195247867588, 14.01870539676982652, 5.551144025186765418 ) ) ;
#6514=CARTESIAN_POINT ( 'NONE',  ( -1.894626972038001789, 11.71448426407998689, 4.353454451108000889 ) ) ;
#6515=CARTESIAN_POINT ( 'NONE',  ( -19.84899577250665104, -4.623430325997634149, -8.021972148549920689 ) ) ;
#6517=CARTESIAN_POINT ( 'NONE',  ( -24.86702589508999850, -9.268724920833001590, -5.486562022343000500 ) ) ;
#6518=DIRECTION ( 'NONE',  ( 4.064457104213683579E-11, -1.000000000000000000, 0.000000000000000000 ) ) ;
#6521=CARTESIAN_POINT ( 'NONE',  ( 4.715134770518538687, 12.39891044673686871, -1.126757662178899722 ) ) ;
#6522=DIRECTION ( 'NONE',  ( 0.000000000000000000, 0.9995435980848492719, 0.03020919607658151262 ) ) ;
#6530=CARTESIAN_POINT ( 'NONE',  ( 16.87668875730999929, -8.405545991651999671, -3.781450583054000170 ) ) ;
#6531=CARTESIAN_POINT ( 'NONE',  ( 18.93569518786017625, 2.254188637666244333, 10.18821787601618389 ) ) ;
#6534=CARTESIAN_POINT ( 'NONE',  ( 5.254686582598590228, 13.86014107681422658, 4.146971818284736599 ) ) ;
#6536=CARTESIAN_POINT ( 'NONE',  ( -15.54074577250666955, 8.833969188127328565, 2.374193597558468927 ) ) ;
#6537=CARTESIAN_POINT ( 'NONE',  ( -3.244655456173217711, 14.19450280349881588, -5.218741847022917213 ) ) ;
#6540=CARTESIAN_POINT ( 'NONE',  ( -23.97728971655646291, -13.40084515672999999, 1.788539470836744583 ) ) ;
#6541=FACE_OUTER_BOUND ( 'NONE', #14528, .T. ) ;
#6544=CARTESIAN_POINT ( 'NONE',  ( 14.28063830469686479, 0.5579475798881706750, -10.34970908510135068 ) ) ;
#6547=CARTESIAN_POINT ( 'NONE',  ( 19.79283103379665931, 5.641139947076246663, 7.340215926192572127 ) ) ;
#6548=ORIENTED_EDGE ( 'NONE', *, *, #4899, .F. ) ;
#6549=CARTESIAN_POINT ( 'NONE',  ( -24.50000000000000355, -8.564163989839817859, -6.165454747490947796 ) ) ;
#6550=CARTESIAN_POINT ( 'NONE',  ( 11.10357421855443860, -10.32596577201156585, 7.114843450789537727 ) ) ;
#6552=CONICAL_SURFACE ( 'NONE', #19334, 7.249999994833000727, 0.7853981633972997312 ) ;
#6556=CARTESIAN_POINT ( 'NONE',  ( 6.155602479547902739, 14.09697471573797323, -0.3418480430767212863 ) ) ;
#6559=CARTESIAN_POINT ( 'NONE',  ( 24.36881528991200341, -3.090117214402293921, -12.50000000000000178 ) ) ;
#6560=B_SPLINE_CURVE_WITH_KNOTS ( 'NONE', 3,
 ( #14642, #3409, #16094, #1464, #8859, #3630 ),
 .UNSPECIFIED., .F., .F.,
 ( 4, 2, 4 ),
 ( 0.000000000000000000, 0.5000000000000000000, 1.000000000000000000 ),
 .UNSPECIFIED. ) ;
#6561=VERTEX_POINT ( 'NONE', #18743 ) ;
#6564=CARTESIAN_POINT ( 'NONE',  ( 24.50000000000000000, 0.000000000000000000, 12.50000000000000000 ) ) ;
#6566=CARTESIAN_POINT ( 'NONE',  ( -24.54599082030000190, -10.10573440607999984, 1.235225690210000060 ) ) ;
#6567=FACE_OUTER_BOUND ( 'NONE', #587, .T. ) ;
#6568=CARTESIAN_POINT ( 'NONE',  ( 20.41554166666666248, -5.650960392684353906, -7.352994588050344227 ) ) ;
#6569=CARTESIAN_POINT ( 'NONE',  ( 15.23327592022675248, 4.680385583748051914, 9.218627023934693909 ) ) ;
#6570=CARTESIAN_POINT ( 'NONE',  ( -14.37011451133999884, -7.634104718556999458, 7.921771262350999265 ) ) ;
#6573=CARTESIAN_POINT ( 'NONE',  ( -22.26176253788000281, -9.242562415387000740, 0.000000000000000000 ) ) ;
#6574=CARTESIAN_POINT ( 'NONE',  ( 4.741968828122999469, 12.61531461105000140, -0.1095802255754999566 ) ) ;
#6577=EDGE_LOOP ( 'NONE', ( #17366, #10756, #20977 ) ) ;
#6578=CARTESIAN_POINT ( 'NONE',  ( -6.042815635770000249, 16.39253429789999927, 0.9999999720525000191 ) ) ;
#6579=CARTESIAN_POINT ( 'NONE',  ( -14.69452806119251953, 7.308005346171998262, 7.484391584288502486 ) ) ;
#6580=AXIS2_PLACEMENT_3D ( 'NONE', #6507, #6628, #810 ) ;
#6581=EDGE_CURVE ( 'NONE', #7389, #1524, #17025, .T. ) ;
#6583=DIRECTION ( 'NONE',  ( -1.000000000000000000, 0.000000000000000000, 0.000000000000000000 ) ) ;
#6584=CARTESIAN_POINT ( 'NONE',  ( 5.996003309297000428, 13.65988289665999567, -2.867731330265999912 ) ) ;
#6585=CARTESIAN_POINT ( 'NONE',  ( 12.00000000000000000, -7.193466889194404246, -5.390184783310134620 ) ) ;
#6586=CARTESIAN_POINT ( 'NONE',  ( -12.25000000000000000, -13.75000000000000000, 0.000000000000000000 ) ) ;
#6587=EDGE_CURVE ( 'NONE', #19976, #7164, #19039, .T. ) ;
#6588=CARTESIAN_POINT ( 'NONE',  ( 18.75768908530999823, -5.059016186635999723, 8.765201904772998986 ) ) ;
#6593=PRESENTATION_STYLE_ASSIGNMENT (( #23172 ) ) ;
#6595=CARTESIAN_POINT ( 'NONE',  ( 11.09594815121266009, 10.32758188523873422, 7.112100880971675920 ) ) ;
#6598=CARTESIAN_POINT ( 'NONE',  ( 16.97422162585966632, 6.903272406789144000, 7.796750432489865545 ) ) ;
#6599=CARTESIAN_POINT ( 'NONE',  ( -24.00016455340000121, 1.715543117993999783E-14, 0.000000000000000000 ) ) ;
#6600=CARTESIAN_POINT ( 'NONE',  ( -14.44097954155595431, 12.31212079859723296, -3.674767524707307054 ) ) ;
#6601=EDGE_CURVE ( 'NONE', #17, #4069, #23370, .T. ) ;
#6602=EDGE_CURVE ( 'NONE', #18727, #14183, #1720, .T. ) ;
#6603=CARTESIAN_POINT ( 'NONE',  ( 6.243179582884000212, 13.63341776306000064, 1.952383140737000033 ) ) ;
#6604=CARTESIAN_POINT ( 'NONE',  ( -23.74465998031000069, 7.716878364870000340, -11.63397459621999985 ) ) ;
#6608=CARTESIAN_POINT ( 'NONE',  ( 19.12008073456999924, -10.59683341338999973, -2.226802362819999548 ) ) ;
#6609=CARTESIAN_POINT ( 'NONE',  ( 23.36357456730870297, -5.878505771248656586, -8.824699706630454443 ) ) ;
#6610=CARTESIAN_POINT ( 'NONE',  ( -6.250000000134000366, 16.31160393816000109, 2.000000000000000000 ) ) ;
#6612=CARTESIAN_POINT ( 'NONE',  ( 4.830312662056223338, 14.72996090241747069, 3.766125697359624880 ) ) ;
#6613=FACE_OUTER_BOUND ( 'NONE', #15740, .T. ) ;
#6615=CARTESIAN_POINT ( 'NONE',  ( -16.20506534625953776, 4.177158590315693587, 9.526121724279519754 ) ) ;
#6618=VECTOR ( 'NONE', #20265, 1000.000000000000114 ) ;
#6620=CARTESIAN_POINT ( 'NONE',  ( -14.40719416829300670, -3.742543968318162051, -12.49988362782814022 ) ) ;
#6623=CARTESIAN_POINT ( 'NONE',  ( -4.069982105474159617, 15.01090283079260956, -4.577251214387113798 ) ) ;
#6624=CARTESIAN_POINT ( 'NONE',  ( -20.04427087878999814, 6.764050733548000238, 8.822657572077998722 ) ) ;
#6625=CARTESIAN_POINT ( 'NONE',  ( -18.26988800695000137, -1.530349862213000067, 10.77306797024999874 ) ) ;
#6626=CARTESIAN_POINT ( 'NONE',  ( -5.982938424327000071, 16.41764137798000434, 1.007171089178999113 ) ) ;
#6627=CARTESIAN_POINT ( 'NONE',  ( 15.05812451745999958, -5.188080995363999470, -8.220389579339999031 ) ) ;
#6628=DIRECTION ( 'NONE',  ( -1.000000000000000000, 0.000000000000000000, 0.000000000000000000 ) ) ;
#6629=CARTESIAN_POINT ( 'NONE',  ( -14.25622743459000041, 13.93375672974000068, 0.4334889134416999856 ) ) ;
#6630=CARTESIAN_POINT ( 'NONE',  ( 24.15736593521593178, -8.253730364077119575, 10.70411965744399119 ) ) ;
#6632=CARTESIAN_POINT ( 'NONE',  ( 2.724105571843130402, 14.05267863184722721, 5.486037458710886661 ) ) ;
#6634=CARTESIAN_POINT ( 'NONE',  ( -20.15132910583999859, -9.188404534074999574, 1.125025998286999896E-14 ) ) ;
#6635=CARTESIAN_POINT ( 'NONE',  ( -21.07977619073999875, -5.139443787745999970, -9.816022020342002108 ) ) ;
#6637=DIRECTION ( 'NONE',  ( 0.000000000000000000, -1.000000000000000000, 0.000000000000000000 ) ) ;
#6638=CARTESIAN_POINT ( 'NONE',  ( -23.74465998031000069, -6.216878364870000340, -12.50000000000000000 ) ) ;
#6639=CARTESIAN_POINT ( 'NONE',  ( 0.7390662495429000112, 13.81263551691999503, 6.128930807943001824 ) ) ;
#6641=DIRECTION ( 'NONE',  ( -1.000000000000000000, 0.000000000000000000, 0.000000000000000000 ) ) ;
#6643=CARTESIAN_POINT ( 'NONE',  ( 11.64686211521070724, -8.383335983967715066, -3.190882296136046570 ) ) ;
#6644=CARTESIAN_POINT ( 'NONE',  ( 15.14812642130999976, -9.595485766438999420, 1.281252696419999948 ) ) ;
#6645=CARTESIAN_POINT ( 'NONE',  ( 18.90322913654150483, 3.341522535781485281, 9.898536439817744892 ) ) ;
#6646=AXIS2_PLACEMENT_3D ( 'NONE', #21257, #8050, #17131 ) ;
#6651=CARTESIAN_POINT ( 'NONE',  ( -2.523824298054621718, 14.00207580638300264, -5.580858811804300323 ) ) ;
#6654=CARTESIAN_POINT ( 'NONE',  ( -24.41513307469962513, -11.84921275889466763, 4.476505678113710474 ) ) ;
#6655=B_SPLINE_SURFACE_WITH_KNOTS ( 'NONE', 3, 3, ( 
 ( #10847, #23783, #14354, #21745, #6962, #18457, #18340, #1750, #12540, #5158, #7189, #9137, #21973, #19928, #14806, #16151, #23670, #14698, #1867, #3346, #20046, #8789, #3463, #5388, #41, #10723, #21859, #9257, #18116, #1632, #9021, #12774, #1521, #8911, #16277 ),
 ( #20164, #7079, #16632, #16512, #14466, #7309, #5270, #22090, #5499, #12878, #3803, #12656, #20279, #7424, #22201, #5615, #12996, #11198, #1397, #18932, #15161, #626, #13347, #2099, #11433, #18806, #13590, #11670, #20747, #15401, #2454, #19044, #20987, #4399, #16993 ),
 ( #9488, #7911, #18581, #9845, #17227, #9606, #22557, #7545, #9727, #3924, #4154, #11550, #16864, #4282, #1984, #8028, #22791, #11316, #393, #16742, #6205, #20874, #20518, #2339, #5851, #14923, #15048, #9369, #17112, #153, #509, #22317, #5734, #13123, #18691 ),
 ( #6079, #267, #7672, #7791, #22441, #4038, #13236, #20627, #2215, #5962, #15277, #22669, #13470, #11911, #8637, #15521, #15999, #4647, #10465, #871, #15638, #14081, #17476, #21235, #22910, #23394, #23154, #15885, #2706, #19417, #21475, #10090, #19543, #8156, #4890 ) ),
 .UNSPECIFIED., .F., .F., .F.,
 ( 4, 4 ),
 ( 4, 1, 1, 1, 1, 1, 1, 1, 1, 1, 1, 1, 1, 1, 1, 1, 1, 1, 1, 1, 1, 1, 1, 1, 1, 1, 1, 1, 1, 1, 1, 1, 4 ),
 ( -0.08408083179840999954, 1.084080831798000188 ),
 ( -0.02000000000000000042, 0.01250000000000000069, 0.04499999999999999833, 0.07749999999999999944, 0.1100000000000000006, 0.1424999999999999878, 0.1749999999999999889, 0.2074999999999999900, 0.2399999999999999911, 0.2725000000000000200, 0.3049999999999999933, 0.3375000000000000222, 0.3699999999999999956, 0.4025000000000000244, 0.4349999999999999978, 0.4675000000000000266, 0.5000000000000000000, 0.5324999999999999734, 0.5649999999999999467, 0.5975000000000000311, 0.6300000000000000044, 0.6624999999999999778, 0.6949999999999999512, 0.7275000000000000355, 0.7600000000000000089, 0.7924999999999999822, 0.8249999999999999556, 0.8575000000000000400, 0.8900000000000000133, 0.9224999999999999867, 0.9549999999999999600, 0.9875000000000000444, 1.020000000000000018 ),
 .UNSPECIFIED. ) ;
#6657=CARTESIAN_POINT ( 'NONE',  ( -5.911109520797385386, 16.32704292856097439, 1.639614246112896856 ) ) ;
#6658=CARTESIAN_POINT ( 'NONE',  ( 15.70237539785324365, -10.03438503088997891, -2.734757645857814889 ) ) ;
#6659=CARTESIAN_POINT ( 'NONE',  ( -3.920367541008654477, 13.93676790526789411, 4.846056852944322202 ) ) ;
#6662=CARTESIAN_POINT ( 'NONE',  ( 19.67945603379666153, 8.018170545278437089, 4.621239218893133049 ) ) ;
#6663=VERTEX_POINT ( 'NONE', #15696 ) ;
#6665=CARTESIAN_POINT ( 'NONE',  ( 11.12576011241401197, -10.20205618040264994, 7.329535452952375962 ) ) ;
#6666=ORIENTED_EDGE ( 'NONE', *, *, #6010, .F. ) ;
#6668=CARTESIAN_POINT ( 'NONE',  ( 5.929709434395003420, 14.11474726611999664, 1.364385784323000506 ) ) ;
#6672=CARTESIAN_POINT ( 'NONE',  ( -20.38485864507334000, -6.393576149522361085, 6.693947997704227326 ) ) ;
#6676=FACE_BOUND ( 'NONE', #10185, .T. ) ;
#6678=CARTESIAN_POINT ( 'NONE',  ( -14.00000000000000000, 10.59999999999999964, 0.000000000000000000 ) ) ;
#6680=CARTESIAN_POINT ( 'NONE',  ( -22.31822325740000323, -2.751304892524999879, -10.37736970521999957 ) ) ;
#6682=CARTESIAN_POINT ( 'NONE',  ( 14.98414533422809036, 10.04427201105623446, 2.428330160207583965 ) ) ;
#6683=CARTESIAN_POINT ( 'NONE',  ( 11.50000000000000000, 0.000000000000000000, 0.000000000000000000 ) ) ;
#6685=CARTESIAN_POINT ( 'NONE',  ( -22.41358485479884877, -8.081562438851669583, 4.657891738322038400 ) ) ;
#6686=CARTESIAN_POINT ( 'NONE',  ( 0.3636138132592998673, 11.55177073541999277, -4.743661845547999079 ) ) ;
#6688=VECTOR ( 'NONE', #1354, 1000.000000000000000 ) ;
#6693=CARTESIAN_POINT ( 'NONE',  ( -14.75240640888930521, 8.576432255687270967, 5.819130627761911256 ) ) ;
#6696=CARTESIAN_POINT ( 'NONE',  ( 4.981589731873999227, 14.41790566382999650, -3.496892685228000008 ) ) ;
#6697=CARTESIAN_POINT ( 'NONE',  ( 12.00000000000000000, -2.135184344106596299, -8.725065291608126827 ) ) ;
#6698=CARTESIAN_POINT ( 'NONE',  ( 17.36604605622000008, -10.43477088592999813, 3.767700144398000273 ) ) ;
#6700=CARTESIAN_POINT ( 'NONE',  ( 13.52925158531000172, -9.668754250937999117, 3.079128054934999525 ) ) ;
#6701=ORIENTED_EDGE ( 'NONE', *, *, #20189, .T. ) ;
#6702=DIRECTION ( 'NONE',  ( -1.000000000000000000, 0.000000000000000000, 0.000000000000000000 ) ) ;
#6707=CARTESIAN_POINT ( 'NONE',  ( 11.45478115325815160, 9.254429737878785645, 8.970723317470367775 ) ) ;
#6709=CARTESIAN_POINT ( 'NONE',  ( -6.044090623820190800, 14.96394378892167509, -3.756777771135694000 ) ) ;
#6710=CARTESIAN_POINT ( 'NONE',  ( 17.24009154054752457, -2.043749485021590928, 10.22276658632487667 ) ) ;
#6711=AXIS2_PLACEMENT_3D ( 'NONE', #11063, #9247, #19918 ) ;
#6713=CARTESIAN_POINT ( 'NONE',  ( -18.63966243917333898, -4.608035645285467830, 7.994758007891237028 ) ) ;
#6714=CARTESIAN_POINT ( 'NONE',  ( -14.45960639177118701, 12.05326364612464829, -4.123067891182894407 ) ) ;
#6717=EDGE_CURVE ( 'NONE', #2989, #15509, #2884, .T. ) ;
#6719=VERTEX_POINT ( 'NONE', #18485 ) ;
#6722=CARTESIAN_POINT ( 'NONE',  ( 22.01884473796000208, 7.419280916948000737, 7.996861738661001695 ) ) ;
#6723=CARTESIAN_POINT ( 'NONE',  ( 22.90960042870581148, -8.796780507069112076, 5.889649883977557288 ) ) ;
#6728=CARTESIAN_POINT ( 'NONE',  ( 3.268619611001000624, 11.96755932734001782, -3.750657828938995575 ) ) ;
#6730=CARTESIAN_POINT ( 'NONE',  ( -15.11652709432294905, 2.218820346475768090, -10.13318491115196984 ) ) ;
#6731=ADVANCED_FACE ( 'NONE', ( #21887 ), #3064, .T. ) ;
#6738=CARTESIAN_POINT ( 'NONE',  ( -12.15500686398999797, 12.23011958036999935, -9.372058967585999767 ) ) ;
#6739=CARTESIAN_POINT ( 'NONE',  ( -23.41659126313000172, -2.571795304491000245, 10.90924587281000058 ) ) ;
#6740=CARTESIAN_POINT ( 'NONE',  ( -19.14845983621999892, 9.556232533099999316, -4.027326457250000047 ) ) ;
#6741=CARTESIAN_POINT ( 'NONE',  ( -6.019884510648998877, 15.84348053695000580, 1.061877742816000225 ) ) ;
#6742=CARTESIAN_POINT ( 'NONE',  ( 15.19306994526000132, 7.671504830348000681, -6.819139572487000756 ) ) ;
#6744=CARTESIAN_POINT ( 'NONE',  ( 20.05326942813999835, -8.291560945558000384, 4.969461368340999385 ) ) ;
#6746=CARTESIAN_POINT ( 'NONE',  ( 24.40278699097224546, -9.495349905928280876, 8.553571527287482823 ) ) ;
#6750=CARTESIAN_POINT ( 'NONE',  ( -17.57559587121334488, 7.970898357189208028, 4.594283802594034682 ) ) ;
#6751=CARTESIAN_POINT ( 'NONE',  ( -3.644446339697000159, 14.33206891720999998, 4.922772686299000000 ) ) ;
#6753=B_SPLINE_CURVE_WITH_KNOTS ( 'NONE', 3,
 ( #11883, #20963, #6301, #2926, #847, #3052, #17323, #10438, #19136, #8613, #4620, #9937, #970, #10309, #1098, #8498, #12011, #6423 ),
 .UNSPECIFIED., .F., .F.,
 ( 4, 2, 2, 2, 2, 2, 2, 2, 4 ),
 ( 0.000000000000000000, 0.1250000000000000000, 0.2500000000000000000, 0.3750000000000000000, 0.5000000000000000000, 0.6250000000000000000, 0.7500000000000000000, 0.8750000000000000000, 1.000000000000000000 ),
 .UNSPECIFIED. ) ;
#6754=CARTESIAN_POINT ( 'NONE',  ( -19.43328743917331636, 7.333017253390695878, -5.635290240896845937 ) ) ;
#6755=CARTESIAN_POINT ( 'NONE',  ( -23.92021346900000012, 8.712087150140002123, 6.970052773374000310 ) ) ;
#6756=AXIS2_PLACEMENT_3D ( 'NONE', #14462, #1273, #19809 ) ;
#6757=CARTESIAN_POINT ( 'NONE',  ( -3.058559774358916350, 11.87684768202457342, 3.734032921821529794 ) ) ;
#6760=CARTESIAN_POINT ( 'NONE',  ( 4.713500436508303970, 12.39829890550265290, -1.133475946671276491 ) ) ;
#6761=EDGE_CURVE ( 'NONE', #23793, #20574, #8102, .T. ) ;
#6762=CARTESIAN_POINT ( 'NONE',  ( 24.01519597621253510, -6.071732368389049839, -7.117487303104867102 ) ) ;
#6765=CARTESIAN_POINT ( 'NONE',  ( -20.82567920454666677, -2.409692318855363169, 8.966061123404951871 ) ) ;
#6767=CARTESIAN_POINT ( 'NONE',  ( -18.72408206190999991, 5.159378177076999528, -10.19862909758999869 ) ) ;
#6768=CARTESIAN_POINT ( 'NONE',  ( 15.91593892131000132, 7.924234377949000319, -5.595770532261999719 ) ) ;
#6769=CARTESIAN_POINT ( 'NONE',  ( 24.38510397947347741, 2.890284505278650773, 12.50000000000000000 ) ) ;
#6771=CARTESIAN_POINT ( 'NONE',  ( -22.38043928506862557, -1.210159647712697240, 9.247744296678623854 ) ) ;
#6773=CARTESIAN_POINT ( 'NONE',  ( -14.78491243917333442, -8.815175007119801620, 2.368882121629280579 ) ) ;
#6774=CARTESIAN_POINT ( 'NONE',  ( -0.5814258234044360485, 13.67896451797541779, -6.147206943646843946 ) ) ;
#6778=CARTESIAN_POINT ( 'NONE',  ( -24.36724102302310158, 12.10481948367283422, -4.033677606666548066 ) ) ;
#6779=CARTESIAN_POINT ( 'NONE',  ( 6.038532390086429835, 14.39630362418530751, 1.042615058007298812 ) ) ;
#6781=CARTESIAN_POINT ( 'NONE',  ( 16.39930534548422614, 9.330189097337756365, -4.632983890435689034 ) ) ;
#6783=CARTESIAN_POINT ( 'NONE',  ( -4.371713857110997026, 12.30683965646000999, 2.325230957305000068 ) ) ;
#6784=CARTESIAN_POINT ( 'NONE',  ( 20.13295603379664911, -4.627100187415565280, 8.028339412451956036 ) ) ;
#6793=CARTESIAN_POINT ( 'NONE',  ( 19.41266666666667007, 7.735111250169313557, 5.102936606934582286 ) ) ;
#6795=FACE_OUTER_BOUND ( 'NONE', #15404, .T. ) ;
#6796=ORIENTED_EDGE ( 'NONE', *, *, #6601, .F. ) ;
#6799=DIRECTION ( 'NONE',  ( 1.000000000000000000, 0.000000000000000000, 0.000000000000000000 ) ) ;
#6801=EDGE_CURVE ( 'NONE', #22764, #12346, #13537, .T. ) ;
#6802=EDGE_LOOP ( 'NONE', ( #14759, #4803, #13221, #16409, #7587, #6365 ) ) ;
#6803=CARTESIAN_POINT ( 'NONE',  ( -23.41894536462999810, 0.9629491129631000401, 11.24764485372000067 ) ) ;
#6804=DIRECTION ( 'NONE',  ( 6.552635476078902493E-07, -0.9999999999997853939, -1.009232707941984266E-09 ) ) ;
#6805=CARTESIAN_POINT ( 'NONE',  ( 15.00664151501544374, 9.822743592524254552, 3.215862093219099105 ) ) ;
#6809=CARTESIAN_POINT ( 'NONE',  ( -18.69965283593333538, -8.970713245661908530, 2.088197045339661884 ) ) ;
#6810=CARTESIAN_POINT ( 'NONE',  ( 4.614156076205000012, 12.49299253157998635, -1.062903411340000437 ) ) ;
#6815=ORIENTED_EDGE ( 'NONE', *, *, #17844, .T. ) ;
#6817=CARTESIAN_POINT ( 'NONE',  ( -14.83922393043447308, 9.919015930220274058, 3.020892133029422943 ) ) ;
#6820=CARTESIAN_POINT ( 'NONE',  ( 11.36701043059983718, -12.20499207204286840, -3.860262462454134624 ) ) ;
#6821=CARTESIAN_POINT ( 'NONE',  ( 12.00000000000000000, -1.827539693554861788, -8.792163972483878709 ) ) ;
#6822=CARTESIAN_POINT ( 'NONE',  ( 18.84348253994000189, -5.598984228891000114, 8.803251650347998947 ) ) ;
#6823=CARTESIAN_POINT ( 'NONE',  ( 13.85831408531000086, -6.842896344163999167, -7.504413997217999288 ) ) ;
#6825=CARTESIAN_POINT ( 'NONE',  ( -10.82554149291999934, -14.29998144107999991, -2.504234213954000143 ) ) ;
#6828=( NAMED_UNIT ( * ) PLANE_ANGLE_UNIT ( ) SI_UNIT ( $, .RADIAN. ) );
#6829=EDGE_CURVE ( 'NONE', #5826, #4476, #579, .T. ) ;
#6832=CARTESIAN_POINT ( 'NONE',  ( 11.10357421856110705, 11.32461805837391822, 5.385126951717674082 ) ) ;
#6833=CARTESIAN_POINT ( 'NONE',  ( 21.55864741212693758, 1.361786730296197678, -10.62933302226472065 ) ) ;
#6834=CARTESIAN_POINT ( 'NONE',  ( -14.00000000000000178, 8.277532166501742950, 3.835819509332607513 ) ) ;
#6835=CARTESIAN_POINT ( 'NONE',  ( 16.20461591949403513, -2.540617249209156103, -10.04820973369444914 ) ) ;
#6836=CARTESIAN_POINT ( 'NONE',  ( -6.249999999916000526, 15.09564573669999987, 3.212813967733000098 ) ) ;
#6837=DIRECTION ( 'NONE',  ( 0.000000000000000000, 1.000000000000000000, 0.000000000000000000 ) ) ;
#6842=CARTESIAN_POINT ( 'NONE',  ( 11.18529249866647213, 11.69879683432484541, -4.737131156255078857 ) ) ;
#6844=CONICAL_SURFACE ( 'NONE', #1442, 13.23032192316000000, 1.235249617460683957 ) ;
#6847=CARTESIAN_POINT ( 'NONE',  ( 24.28455689590255773, -8.829963675777257492, -9.706054284564595847 ) ) ;
#6848=CARTESIAN_POINT ( 'NONE',  ( 4.861474503319399787, 14.51472929299590753, 3.787796979831960176 ) ) ;
#6849=CARTESIAN_POINT ( 'NONE',  ( -18.63376253787999914, -9.149460784975000038, 0.000000000000000000 ) ) ;
#6851=CARTESIAN_POINT ( 'NONE',  ( 18.26606375730999687, -4.551782674040000032, 7.886397731525000232 ) ) ;
#6854=CARTESIAN_POINT ( 'NONE',  ( 8.124934037954998800, 0.000000000000000000, 0.000000000000000000 ) ) ;
#6857=EDGE_CURVE ( 'NONE', #15294, #12632, #18244, .T. ) ;
#6858=ORIENTED_EDGE ( 'NONE', *, *, #4623, .T. ) ;
#6859=VECTOR ( 'NONE', #16434, 1000.000000000000000 ) ;
#6860=CARTESIAN_POINT ( 'NONE',  ( -18.86729207711333345, -6.366495818929248429, 6.665594812321431917 ) ) ;
#6861=CARTESIAN_POINT ( 'NONE',  ( -12.36677000395999926, 13.67685060524999940, -6.159850446377999056 ) ) ;
#6862=CARTESIAN_POINT ( 'NONE',  ( -22.07990519880999969, 5.007857226526000183, 9.402496424037000367 ) ) ;
#6864=CARTESIAN_POINT ( 'NONE',  ( -17.11715635651999889, 9.674678649335000102, 3.573597797309999713 ) ) ;
#6866=CARTESIAN_POINT ( 'NONE',  ( 17.69874951746000136, 7.302264014228000200, 6.527174038894000496 ) ) ;
#6868=CARTESIAN_POINT ( 'NONE',  ( 12.00000000000000000, 0.000000000000000000, 0.000000000000000000 ) ) ;
#6872=CARTESIAN_POINT ( 'NONE',  ( 23.29781751312559379, 8.206174485158717502, 4.349602372406548234 ) ) ;
#6873=CARTESIAN_POINT ( 'NONE',  ( 1.483509881833009691, 13.79912375866350338, 5.942645371621392947 ) ) ;
#6876=CARTESIAN_POINT ( 'NONE',  ( -24.75563619790999681, -6.749210113364999764, -8.912303601106998485 ) ) ;
#6878=CARTESIAN_POINT ( 'NONE',  ( -1.495637945045119599, 11.56875457997782775, 4.606283421593187377 ) ) ;
#6879=ORIENTED_EDGE ( 'NONE', *, *, #22555, .F. ) ;
#6880=CARTESIAN_POINT ( 'NONE',  ( 22.24928936712999672, -9.242242329243000043, 0.000000000000000000 ) ) ;
#6881=CARTESIAN_POINT ( 'NONE',  ( 3.757891690360106285, 12.07210435675419369, -3.048890984311763308 ) ) ;
#6882=DIRECTION ( 'NONE',  ( 0.9996708941621509359, -0.02565352539214875091, -2.545944944692875236E-14 ) ) ;
#6883=CARTESIAN_POINT ( 'NONE',  ( -20.44776253787999920, -9.196011600180998613, 0.000000000000000000 ) ) ;
#6887=LINE ( 'NONE', #23604, #6859 ) ;
#6888=CARTESIAN_POINT ( 'NONE',  ( -6.082217688135330924, 16.10188874983086649, -1.020520473285583485 ) ) ;
#6890=CARTESIAN_POINT ( 'NONE',  ( 13.50281392131000047, -8.671483154093998280, -4.205333541112000084 ) ) ;
#6891=CARTESIAN_POINT ( 'NONE',  ( 18.76830727444978208, 7.489704376429600963, 7.283379905210109584 ) ) ;
#6892=ORIENTED_EDGE ( 'NONE', *, *, #2453, .F. ) ;
#6893=CARTESIAN_POINT ( 'NONE',  ( 5.155714003469999973, 13.97328511022999997, 4.008150528822999270 ) ) ;
#6895=PLANE ( 'NONE',  #14932 ) ;
#6896=CARTESIAN_POINT ( 'NONE',  ( 13.49999999999999645, -7.667152171304032038, 6.546859119036191998 ) ) ;
#6900=CARTESIAN_POINT ( 'NONE',  ( -24.43506354683005100, -11.72249354572810986, 4.696109227415885989 ) ) ;
#6903=CARTESIAN_POINT ( 'NONE',  ( -5.554207712812456954, 16.15574578901152947, 2.609433215957428942 ) ) ;
#6905=CARTESIAN_POINT ( 'NONE',  ( 16.14841056433666822, 2.481077197559224512, -10.10691008888976938 ) ) ;
#6908=CARTESIAN_POINT ( 'NONE',  ( 4.540657248691003289, 12.36579710560998002, 1.969985720665999640 ) ) ;
#6909=CARTESIAN_POINT ( 'NONE',  ( 20.24633103379666821, -7.349522212044369951, 5.648291859775539159 ) ) ;
#6910=ORIENTED_EDGE ( 'NONE', *, *, #8942, .T. ) ;
#6914=ORIENTED_EDGE ( 'NONE', *, *, #15154, .F. ) ;
#6916=CARTESIAN_POINT ( 'NONE',  ( 5.994133932293998157, 14.09831428825999744, 1.046105555905998408 ) ) ;
#6917=CARTESIAN_POINT ( 'NONE',  ( 12.04708237234661183, 5.050716351078905042, -12.50004921245747802 ) ) ;
#6918=CARTESIAN_POINT ( 'NONE',  ( 6.187913781813814573, 13.93138848470324831, -0.7590350555155512824 ) ) ;
#6919=CARTESIAN_POINT ( 'NONE',  ( 13.49999999999999822, -2.699842513522783261, 10.00691734096826480 ) ) ;
#6920=AXIS2_PLACEMENT_3D ( 'NONE', #13317, #22881, #360 ) ;
#6923=CARTESIAN_POINT ( 'NONE',  ( 0.000000000000000000, 22.00000000000000000, 0.000000000000000000 ) ) ;
#6925=PLANE ( 'NONE',  #16719 ) ;
#6928=CARTESIAN_POINT ( 'NONE',  ( -23.86052387786999773, 6.793182627230999415, -8.367515183292999481 ) ) ;
#6930=CARTESIAN_POINT ( 'NONE',  ( 14.89101776721218684, 10.28666262955564825, -0.9606185904953363774 ) ) ;
#6933=CARTESIAN_POINT ( 'NONE',  ( 20.60157508292000017, 1.509805238461999988, 11.10580479464999826 ) ) ;
#6935=CARTESIAN_POINT ( 'NONE',  ( 13.59973893363859609, 6.904209829052242675, -5.804544132843785675 ) ) ;
#6936=CARTESIAN_POINT ( 'NONE',  ( -4.447662105364998730, 12.42909450830998352, -1.606648311090999481 ) ) ;
#6938=CARTESIAN_POINT ( 'NONE',  ( -21.84605420454664326, -1.208325219156637376, -9.231894520236238577 ) ) ;
#6942=CARTESIAN_POINT ( 'NONE',  ( 19.75000000000000000, -1.659811535170000019, 9.026773995975998943 ) ) ;
#6943=AXIS2_PLACEMENT_3D ( 'NONE', #13240, #17453, #9610 ) ;
#6945=ORIENTED_EDGE ( 'NONE', *, *, #20286, .T. ) ;
#6947=CARTESIAN_POINT ( 'NONE',  ( 11.22285964979241690, -9.825076113722889914, -7.982449282815227143 ) ) ;
#6948=CARTESIAN_POINT ( 'NONE',  ( 24.50000000000000000, 0.000000000000000000, 0.000000000000000000 ) ) ;
#6949=AXIS2_PLACEMENT_3D ( 'NONE', #22446, #17116, #22562 ) ;
#6950=CARTESIAN_POINT ( 'NONE',  ( 17.58032625501999746, -6.868895417556999838, -8.719434656480000712 ) ) ;
#6952=CARTESIAN_POINT ( 'NONE',  ( -11.23283149291999905, -0.5530958232186000689, 14.50705838281999860 ) ) ;
#6953=CARTESIAN_POINT ( 'NONE',  ( 13.50000000000000000, 6.526939024554766711, 7.647570657964006813 ) ) ;
#6955=ORIENTED_EDGE ( 'NONE', *, *, #15839, .F. ) ;
#6956=CARTESIAN_POINT ( 'NONE',  ( 11.06619116163223282, 10.57612823871844654, 6.681605107870990601 ) ) ;
#6957=CARTESIAN_POINT ( 'NONE',  ( 21.08801403234133787, -10.51584647305647735, -0.7453109682132889047 ) ) ;
#6959=CARTESIAN_POINT ( 'NONE',  ( 16.27412929406614950, -0.09366976407831074936, -10.36545759699181168 ) ) ;
#6960=CARTESIAN_POINT ( 'NONE',  ( -18.86641243917333099, 2.396297420769109454, 8.917188256816995562 ) ) ;
#6962=CARTESIAN_POINT ( 'NONE',  ( -18.19554712229000160, -2.285746783449999597, -9.537972663088998715 ) ) ;
#6964=ORIENTED_EDGE ( 'NONE', *, *, #19487, .T. ) ;
#6965=CARTESIAN_POINT ( 'NONE',  ( 23.34331150348194228, -0.6078572885738241505, 9.272076336171188871 ) ) ;
#6966=CARTESIAN_POINT ( 'NONE',  ( 11.10357421854642013, 10.32596577204267518, -7.114843450730285568 ) ) ;
#6967=CARTESIAN_POINT ( 'NONE',  ( 22.82448027771794585, -6.707976417501984479, 8.192708876736357837 ) ) ;
#6969=B_SPLINE_CURVE_WITH_KNOTS ( 'NONE', 3,
 ( #13390, #7352, #11357, #20791, #80, #11241, #14848, #3846, #16906, #310, #9885, #12079 ),
 .UNSPECIFIED., .F., .F.,
 ( 4, 1, 1, 1, 1, 2, 2, 4 ),
 ( 0.000000000000000000, 0.2500000000000006106, 0.3750000000000012768, 0.4375000000000013323, 0.4687500000000012768, 0.4843750000000014433, 0.5000000000000016653, 1.000000000000000000 ),
 .UNSPECIFIED. ) ;
#6974=CARTESIAN_POINT ( 'NONE',  ( -4.009361469255999566, 12.11895015699999689, -2.855765722793998762 ) ) ;
#6975=VERTEX_POINT ( 'NONE', #19318 ) ;
#6976=DIRECTION ( 'NONE',  ( 1.000000000000000000, 0.000000000000000000, 0.000000000000000000 ) ) ;
#6979=SHAPE_DEFINITION_REPRESENTATION ( #8253, #22521 ) ;
#6981=EDGE_CURVE ( 'NONE', #10557, #20353, #775, .T. ) ;
#6982=ORIENTED_EDGE ( 'NONE', *, *, #21465, .F. ) ;
#6983=CARTESIAN_POINT ( 'NONE',  ( -19.17035378445833871, 2.613855109476041161, 8.847292803866498190 ) ) ;
#6984=CARTESIAN_POINT ( 'NONE',  ( -4.690941914108488930, 15.65021434981036741, -3.939840772426298265 ) ) ;
#6985=CARTESIAN_POINT ( 'NONE',  ( -25.02553073364999747, -3.263946373367999865, -9.309921254180999028 ) ) ;
#6986=CARTESIAN_POINT ( 'NONE',  ( -18.19885853377000373, -7.619903537905999613, -6.175610338995999982 ) ) ;
#6988=CARTESIAN_POINT ( 'NONE',  ( -23.90708761851598751, 10.11530264397083556, 3.143216488129493058 ) ) ;
#6990=LINE ( 'NONE', #12209, #3101 ) ;
#6992=ORIENTED_EDGE ( 'NONE', *, *, #5925, .F. ) ;
#6994=B_SPLINE_CURVE_WITH_KNOTS ( 'NONE', 3,
 ( #10193, #22651, #13693, #21087, #11653, #15746, #17584, #17459, #853, #23012, #6429, #13814, #19524, #21213, #6556, #13941, #21335, #4751, #9708, #6060, #19024, #17947, #3179, #10317, #6918, #21457, #12729, #18067, #10681, #14063, #5229, #3057, #12259, #23631, #23740, #21585, #12614, #18195, #17708, #1105, #19647, #17833, #14314, #4999, #7036, #1475, #8869 ),
 .UNSPECIFIED., .F., .F.,
 ( 4, 2, 1, 1, 2, 2, 2, 1, 1, 1, 2, 2, 2, 2, 1, 1, 2, 2, 2, 1, 1, 1, 1, 2, 2, 2, 2, 2, 4 ),
 ( 0.000000000000000000, 0.06249999999999583666, 0.09374999999999411582, 0.1093749999999932415, 0.1171874999999927419, 0.1249999999999922562, 0.1874999999999966138, 0.2187499999999982236, 0.2343749999999995837, 0.2421875000000003331, 0.2460937500000001665, 0.2500000000000000000, 0.3750000000000012768, 0.4375000000000019429, 0.4687500000000022760, 0.4843750000000019984, 0.4921875000000016098, 0.5000000000000013323, 0.6249999999999892308, 0.6874999999999834577, 0.7187499999999802380, 0.7343749999999787947, 0.7421874999999783507, 0.7460937499999782396, 0.7499999999999782396, 0.8124999999999840128, 0.8437499999999866773, 0.8749999999999892308, 1.000000000000000000 ),
 .UNSPECIFIED. ) ;
#6996=EDGE_CURVE ( 'NONE', #14445, #709, #12718, .T. ) ;
#6997=CARTESIAN_POINT ( 'NONE',  ( 5.575791046645279359, 14.52390015031493320, -2.648501204029414247 ) ) ;
#7000=CARTESIAN_POINT ( 'NONE',  ( -3.280903357640863049, 11.93481450532642540, 3.545272627676774313 ) ) ;
#7003=CARTESIAN_POINT ( 'NONE',  ( 4.559109341211414979, 12.34130269922110834, -1.643108070882763450 ) ) ;
#7004=CARTESIAN_POINT ( 'NONE',  ( -10.26377187911747768, 15.76328787329322623, 1.163182374018775889 ) ) ;
#7005=CARTESIAN_POINT ( 'NONE',  ( 11.47028936713000036, -8.379193606113998882, -3.189305674207999708 ) ) ;
#7010=CARTESIAN_POINT ( 'NONE',  ( 13.39312642131000075, -9.609817522467999140, -0.6894128909195000876 ) ) ;
#7011=CARTESIAN_POINT ( 'NONE',  ( 18.46047941552955862, 9.997012766731819156, -2.944153169368156409 ) ) ;
#7012=VERTEX_POINT ( 'NONE', #17012 ) ;
#7016=CARTESIAN_POINT ( 'NONE',  ( 13.50000000000000178, -5.635803601607234370, 8.567832869351823533 ) ) ;
#7018=EDGE_CURVE ( 'NONE', #15471, #20328, #11033, .T. ) ;
#7021=DIRECTION ( 'NONE',  ( 0.000000000000000000, 1.000000000000000000, 0.000000000000000000 ) ) ;
#7022=CARTESIAN_POINT ( 'NONE',  ( -23.81628036379132141, -7.177005027323463793, 6.439087892836417026 ) ) ;
#7024=DIRECTION ( 'NONE',  ( 0.000000000000000000, 1.000000000000000000, 0.000000000000000000 ) ) ;
#7025=CARTESIAN_POINT ( 'NONE',  ( -4.940775639143002884, 12.51284741021001246, -0.1550196392192998707 ) ) ;
#7028=EDGE_LOOP ( 'NONE', ( #21028, #20962 ) ) ;
#7029=DIRECTION ( 'NONE',  ( 0.000000000000000000, -1.000000000000000000, 0.000000000000000000 ) ) ;
#7030=ADVANCED_FACE ( 'NONE', ( #8052 ), #23809, .F. ) ;
#7034=CARTESIAN_POINT ( 'NONE',  ( 6.081738458038996598, 14.07685609792998527, -0.03589047288854997630 ) ) ;
#7035=CARTESIAN_POINT ( 'NONE',  ( 11.40904387244272655, -2.948332260696405971, -12.49995270680654613 ) ) ;
#7036=CARTESIAN_POINT ( 'NONE',  ( 6.242375959467782565, 13.66332201415649372, -1.753597398281198094 ) ) ;
#7038=B_SPLINE_CURVE_WITH_KNOTS ( 'NONE', 3,
 ( #18738, #17283, #7725, #7839, #20800, #4210, #10144, #13760, #8574, #4820, #17900, #1181, #23328, #1051, #3133, #19595, #21162, #8207 ),
 .UNSPECIFIED., .F., .F.,
 ( 4, 2, 2, 2, 2, 2, 2, 2, 4 ),
 ( 0.000000000000000000, 0.1249999999999999445, 0.2499999999999998890, 0.3749999999999999445, 0.5000000000000000000, 0.6250000000000000000, 0.7500000000000001110, 0.8750000000000000000, 1.000000000000000000 ),
 .UNSPECIFIED. ) ;
#7040=CARTESIAN_POINT ( 'NONE',  ( -12.24999999459000044, 1.554281285377000029E-14, -7.249999994590990759 ) ) ;
#7041=EDGE_CURVE ( 'NONE', #379, #3901, #411, .T. ) ;
#7042=EDGE_LOOP ( 'NONE', ( #18790, #5621, #785, #14124, #12737, #1816, #3476 ) ) ;
#7043=CARTESIAN_POINT ( 'NONE',  ( -18.23630520352000062, 4.669879042777999700, -9.230749285618999878 ) ) ;
#7044=DIRECTION ( 'NONE',  ( 0.000000000000000000, 0.000000000000000000, -1.000000000000000000 ) ) ;
#7046=EDGE_LOOP ( 'NONE', ( #5057, #8725, #19166, #4771 ) ) ;
#7047=CARTESIAN_POINT ( 'NONE',  ( -22.14685652178999931, 3.522049787583000136, -10.13679110321000110 ) ) ;
#7049=CARTESIAN_POINT ( 'NONE',  ( 14.77010906259511458, 9.035887590412290393, -5.000320054086365040 ) ) ;
#7052=CARTESIAN_POINT ( 'NONE',  ( 22.65751704163000113, -10.54215396955000017, 3.968579886229999687 ) ) ;
#7054=CARTESIAN_POINT ( 'NONE',  ( 13.60043579687980220, 6.918659888968194949, -5.787303501411981799 ) ) ;
#7055=CARTESIAN_POINT ( 'NONE',  ( -6.483873887681529169, 15.48026478585757459, -1.444101027390730208 ) ) ;
#7056=CARTESIAN_POINT ( 'NONE',  ( -21.65709587121331836, 4.647032519295968278, -8.062418161751203627 ) ) ;
#7061=B_SPLINE_CURVE_WITH_KNOTS ( 'NONE', 3,
 ( #6181, #13568, #20961, #21576, #3288 ),
 .UNSPECIFIED., .F., .F.,
 ( 4, 1, 4 ),
 ( 0.4999999999411116058, 0.6666666666667000474, 1.000000000000000000 ),
 .UNSPECIFIED. ) ;
#7062=VERTEX_POINT ( 'NONE', #20893 ) ;
#7063=CARTESIAN_POINT ( 'NONE',  ( 17.16545833333331217, 5.599525487243289135, -7.286479070541918901 ) ) ;
#7064=CARTESIAN_POINT ( 'NONE',  ( 21.60683103379665226, 5.669747597873476153, 7.377441069599709245 ) ) ;
#7065=CARTESIAN_POINT ( 'NONE',  ( 18.62920234113000006, 7.029629189252000643, 8.627757148559000555 ) ) ;
#7066=EDGE_CURVE ( 'NONE', #8104, #20493, #4177, .T. ) ;
#7068=EDGE_CURVE ( 'NONE', #10512, #5826, #11064, .T. ) ;
#7069=CARTESIAN_POINT ( 'NONE',  ( -9.189007565846001313, -0.05028646118644999885, -14.86791649126999992 ) ) ;
#7070=CARTESIAN_POINT ( 'NONE',  ( 13.50000000000000000, 9.554725887819582653, 1.841566180535791020 ) ) ;
#7074=CARTESIAN_POINT ( 'NONE',  ( 21.79396410202163992, 8.711539071920352484, -6.251501696449420997 ) ) ;
#7076=CARTESIAN_POINT ( 'NONE',  ( 16.01296168114131646, -8.180747814225620473, -6.354282860866971028 ) ) ;
#7077=CARTESIAN_POINT ( 'NONE',  ( -19.16874577250666789, 8.924647632302601608, 2.398562752349402416 ) ) ;
#7079=CARTESIAN_POINT ( 'NONE',  ( -18.98111647941000157, -8.384220026111998791, 5.081857170174999716 ) ) ;
#7081=ORIENTED_EDGE ( 'NONE', *, *, #8381, .T. ) ;
#7082=CARTESIAN_POINT ( 'NONE',  ( 23.41885967450824069, -2.987232380683592758, 8.797512113848760862 ) ) ;
#7083=CARTESIAN_POINT ( 'NONE',  ( 20.29924913173047329, 10.29758103606868858, -2.152088117745763363 ) ) ;
#7086=CARTESIAN_POINT ( 'NONE',  ( 24.32802197706127245, -9.050607035110887821, -9.323888775846091548 ) ) ;
#7087=CARTESIAN_POINT ( 'NONE',  ( 4.934031413263280541, 14.29560215800634992, -3.841103650033387495 ) ) ;
#7088=( GEOMETRIC_REPRESENTATION_CONTEXT ( 3 ) GLOBAL_UNCERTAINTY_ASSIGNED_CONTEXT ( ( #18171 ) ) GLOBAL_UNIT_ASSIGNED_CONTEXT ( ( #5688, #2171, #20583 ) ) REPRESENTATION_CONTEXT ( 'NONE', 'WORKASPACE' ) );
#7089=CARTESIAN_POINT ( 'NONE',  ( 4.202976386093998151, 12.26255958046999694, -2.314965097242001502 ) ) ;
#7090=VERTEX_POINT ( 'NONE', #7811 ) ;
#7091=CARTESIAN_POINT ( 'NONE',  ( 15.88950125731000007, 9.094565878156000593, 1.328064802524999921 ) ) ;
#7092=ORIENTED_EDGE ( 'NONE', *, *, #6254, .T. ) ;
#7095=ORIENTED_EDGE ( 'NONE', *, *, #13069, .F. ) ;
#7096=CARTESIAN_POINT ( 'NONE',  ( -15.08134587121334391, -8.822584081656442478, 2.370873255088651099 ) ) ;
#7097=CARTESIAN_POINT ( 'NONE',  ( -22.56166525371000375, 8.878912038559001019, -5.909991768459000205 ) ) ;
#7099=CARTESIAN_POINT ( 'NONE',  ( -19.01137992565000445, 5.242525404089000141, 8.316352798856000206 ) ) ;
#7100=CARTESIAN_POINT ( 'NONE',  ( 18.82829166666665799, 1.198188119826057330, -9.154452785816511451 ) ) ;
#7101=CARTESIAN_POINT ( 'NONE',  ( -23.28944460057455501, -8.084059691274644521, 6.822389599746202293 ) ) ;
#7103=FACE_OUTER_BOUND ( 'NONE', #1355, .T. ) ;
#7107=DIRECTION ( 'NONE',  ( 1.000000000000000000, 0.000000000000000000, 0.000000000000000000 ) ) ;
#7111=B_SPLINE_CURVE_WITH_KNOTS ( 'NONE', 3,
 ( #4959, #21668, #10405, #10529, #6186, #14029, #21420, #3260, #5080, #19609, #17205, #17798, #14151, #2551, #12345, #10645, #8585, #12461, #3018, #604, #1193, #18032, #19735, #15948, #8834, #21545, #9941, #12219, #23340, #14388, #16196, #17913, #7000, #21781, #5194, #19021, #2432, #6757, #9822, #22889, #15380, #8005, #22769, #20966, #1316, #8705, #4376, #16069, #19139, #23468, #6878, #17327, #731, #14272, #15502, #6305, #4836, #10990, #10765, #16782, #14844, #20432, #188, #22014, #1561, #21895, #18493, #18375, #11110, #18616, #16428, #9296, #20199, #7581, #14502, #76, #14960, #1666, #3606, #5649, #5427, #22356, #9410, #22234, #16669, #23941, #9173, #1906, #3383, #13035, #18159, #12810, #12576, #9056, #1785, #16550, #8946, #16313, #23704, #3843, #14732, #7112 ),
 .UNSPECIFIED., .F., .F.,
 ( 4, 1, 1, 1, 1, 1, 2, 2, 2, 1, 1, 1, 1, 2, 2, 2, 1, 1, 1, 2, 2, 2, 1, 1, 1, 1, 2, 2, 2, 2, 1, 1, 1, 2, 2, 2, 2, 2, 1, 1, 1, 2, 2, 2, 2, 1, 1, 1, 2, 2, 2, 1, 1, 1, 2, 2, 2, 1, 1, 1, 2, 2, 2, 1, 2, 2, 4 ),
 ( 0.000000000000000000, 0.06249999999999630851, 0.09374999999999449052, 0.1093749999999935330, 0.1171874999999930889, 0.1210937499999928946, 0.1230468749999928113, 0.1249999999999927558, 0.1874999999999895361, 0.2187499999999878708, 0.2343749999999870381, 0.2421874999999866218, 0.2460937499999863998, 0.2480468749999863165, 0.2499999999999862332, 0.2812499999999854561, 0.2968749999999850675, 0.3046874999999850120, 0.3085937499999849565, 0.3105468749999849010, 0.3124999999999847899, 0.3437499999999842903, 0.3593749999999841238, 0.3671874999999840128, 0.3710937499999839573, 0.3730468749999839018, 0.3740234374999838463, 0.3749999999999837907, 0.4062499999999852895, 0.4218749999999860112, 0.4296874999999864553, 0.4335937499999866773, 0.4355468749999868439, 0.4365234374999868994, 0.4374999999999868994, 0.4999999999999902300, 0.5312499999999917843, 0.5468749999999926725, 0.5546874999999931166, 0.5585937499999933387, 0.5605468749999934497, 0.5615234374999934497, 0.5624999999999935607, 0.5937499999999940048, 0.6093749999999942268, 0.6171874999999943379, 0.6210937499999943379, 0.6230468749999943379, 0.6240234374999942268, 0.6249999999999941158, 0.6562499999999938938, 0.6718749999999937828, 0.6796874999999935607, 0.6835937499999934497, 0.6855468749999934497, 0.6874999999999934497, 0.7187499999999924505, 0.7343749999999917843, 0.7421874999999915623, 0.7460937499999914513, 0.7480468749999914513, 0.7499999999999914513, 0.8124999999999935607, 0.8437499999999946709, 0.8593749999999952260, 0.8749999999999956701, 1.000000000000000000 ),
 .UNSPECIFIED. ) ;
#7112=CARTESIAN_POINT ( 'NONE',  ( 4.835083642289389694, 12.44448910615697912, 0.3758261001295359338 ) ) ;
#7114=CARTESIAN_POINT ( 'NONE',  ( -1.916536428469591602, 11.63903121779952166, -4.419911752329476862 ) ) ;
#7115=CARTESIAN_POINT ( 'NONE',  ( -10.60253945176744850, 15.46640669614848029, 1.465117989003546839 ) ) ;
#7117=AXIS2_PLACEMENT_3D ( 'NONE', #10447, #5342, #12386 ) ;
#7118=ORIENTED_EDGE ( 'NONE', *, *, #20674, .T. ) ;
#7121=CARTESIAN_POINT ( 'NONE',  ( 16.57406392130999961, -0.9113449805282999305, 9.675305505412000073 ) ) ;
#7122=CARTESIAN_POINT ( 'NONE',  ( 18.70295191285947212, 8.885977204415825170, 5.457387397214819025 ) ) ;
#7123=ADVANCED_FACE ( 'NONE', ( #9988 ), #18775, .F. ) ;
#7127=CARTESIAN_POINT ( 'NONE',  ( 17.90046080085999947, -5.121794679728999711, -10.20598855136000083 ) ) ;
#7128=CARTESIAN_POINT ( 'NONE',  ( 13.50000000000000000, -9.665509359224504493, 1.178091801883024647 ) ) ;
#7131=CARTESIAN_POINT ( 'NONE',  ( 21.54099403953999925, -4.622832731814000340, -10.30527021446000013 ) ) ;
#7133=CARTESIAN_POINT ( 'NONE',  ( 13.55583115916570591, -6.549353884295403105, 8.008559588132170504 ) ) ;
#7134=CARTESIAN_POINT ( 'NONE',  ( -3.950971430524645722, 13.90373848699781156, 4.848256008918679250 ) ) ;
#7136=CARTESIAN_POINT ( 'NONE',  ( -12.25000000000000000, 13.93375672974001311, 0.000000000000000000 ) ) ;
#7137=EDGE_CURVE ( 'NONE', #8984, #23190, #1210, .T. ) ;
#7138=CARTESIAN_POINT ( 'NONE',  ( 12.50000000000000000, 13.93375672974000068, -0.1443254485109999874 ) ) ;
#7140=CARTESIAN_POINT ( 'NONE',  ( -14.70932910584000020, -9.048752088456000209, 0.000000000000000000 ) ) ;
#7144=FACE_OUTER_BOUND ( 'NONE', #8446, .T. ) ;
#7148=CARTESIAN_POINT ( 'NONE',  ( 0.6124999999999999334, 1.217145837503000065E-14, 0.000000000000000000 ) ) ;
#7149=AXIS2_PLACEMENT_3D ( 'NONE', #18423, #7509, #5818 ) ;
#7150=DIRECTION ( 'NONE',  ( 0.000000000000000000, 1.000000000000000000, 0.000000000000000000 ) ) ;
#7154=CARTESIAN_POINT ( 'NONE',  ( -10.30434581488849766, 15.71366939120218831, -1.198334145822568253 ) ) ;
#7156=CARTESIAN_POINT ( 'NONE',  ( 14.42245774912164258, -1.407376103902506781, -10.22147709090256740 ) ) ;
#7157=DIRECTION ( 'NONE',  ( 0.000000000000000000, 1.000000000000000000, 0.000000000000000000 ) ) ;
#7158=CARTESIAN_POINT ( 'NONE',  ( 20.23448115697999938, 11.04732755767000008, 1.830078991042999759 ) ) ;
#7160=CARTESIAN_POINT ( 'NONE',  ( 13.63441501275057455, 7.583512906543072418, -4.912741062689508276 ) ) ;
#7163=EDGE_CURVE ( 'NONE', #18008, #9228, #9377, .T. ) ;
#7164=VERTEX_POINT ( 'NONE', #21497 ) ;
#7165=DIRECTION ( 'NONE',  ( 0.000000000000000000, -1.000000000000000000, 0.000000000000000000 ) ) ;
#7166=AXIS2_PLACEMENT_3D ( 'NONE', #10551, #17935, #7024 ) ;
#7167=FACE_BOUND ( 'NONE', #3428, .T. ) ;
#7170=CARTESIAN_POINT ( 'NONE',  ( 11.40904387244264839, -12.29944272054649090, -3.696645716843500296 ) ) ;
#7171=DIRECTION ( 'NONE',  ( -1.000000000000000000, 0.000000000000000000, 0.000000000000000000 ) ) ;
#7172=CARTESIAN_POINT ( 'NONE',  ( 16.28334066915000022, 6.390059127348000523, -9.032722790995999063 ) ) ;
#7173=CARTESIAN_POINT ( 'NONE',  ( -14.44665740082351313, 5.895018559233071720, 8.513858593212594528 ) ) ;
#7175=CARTESIAN_POINT ( 'NONE',  ( -11.63274756584999992, 10.81900388182999961, 10.19838060593999884 ) ) ;
#7176=CARTESIAN_POINT ( 'NONE',  ( 13.50000000000000000, 3.113621395416312776, 9.816120523786178609 ) ) ;
#7178=EDGE_CURVE ( 'NONE', #8876, #9820, #17885, .T. ) ;
#7181=EDGE_CURVE ( 'NONE', #14234, #16706, #8345, .T. ) ;
#7182=B_SPLINE_CURVE_WITH_KNOTS ( 'NONE', 3,
 ( #8445, #19828, #1415, #10742, #18135 ),
 .UNSPECIFIED., .F., .F.,
 ( 4, 1, 4 ),
 ( 0.4999999972379591262, 0.6666666666667000474, 1.000000000000000000 ),
 .UNSPECIFIED. ) ;
#7183=CARTESIAN_POINT ( 'NONE',  ( 20.76445358373760897, -5.248161719249965884, 9.136987755281875678 ) ) ;
#7184=AXIS2_PLACEMENT_3D ( 'NONE', #19424, #10216, #17359 ) ;
#7185=DIRECTION ( 'NONE',  ( 0.000000000000000000, 1.000000000000000000, 0.000000000000000000 ) ) ;
#7186=CARTESIAN_POINT ( 'NONE',  ( 16.10220164495252604, -5.930837905678782107, -8.497072249795241561 ) ) ;
#7187=CARTESIAN_POINT ( 'NONE',  ( -18.80815922653999905, -4.543843182026999550, -10.15237538699000019 ) ) ;
#7189=CARTESIAN_POINT ( 'NONE',  ( -16.97676503447000229, -7.308902056012999360, 6.489539471208999544 ) ) ;
#7193=CARTESIAN_POINT ( 'NONE',  ( 23.68327827309638423, -8.806622002366150781, 2.989114013944147885 ) ) ;
#7195=CARTESIAN_POINT ( 'NONE',  ( 20.52623620103448232, 8.810251038339160345, 5.766288655265187302 ) ) ;
#7197=EDGE_LOOP ( 'NONE', ( #21888, #814, #17084, #22887 ) ) ;
#7201=CARTESIAN_POINT ( 'NONE',  ( 4.778349813156999915, 12.47891620327999718, 0.1052890627751000563 ) ) ;
#7202=EDGE_LOOP ( 'NONE', ( #13058, #5479, #14168, #6291 ) ) ;
#7205=CARTESIAN_POINT ( 'NONE',  ( -4.901008216611518975, 15.80730880277564410, 3.675502705389401825 ) ) ;
#7207=ORIENTED_EDGE ( 'NONE', *, *, #15591, .F. ) ;
#7209=CARTESIAN_POINT ( 'NONE',  ( 22.40045603379666161, -8.079183748319792358, -4.656405030027713110 ) ) ;
#7210=B_SPLINE_CURVE_WITH_KNOTS ( 'NONE', 3,
 ( #13891, #19722, #15576, #12091, #927 ),
 .UNSPECIFIED., .F., .F.,
 ( 4, 1, 4 ),
 ( 0.000000000000000000, 0.5000000000000000000, 1.000000000000000000 ),
 .UNSPECIFIED. ) ;
#7211=CARTESIAN_POINT ( 'NONE',  ( -20.63462503408999993, 10.41122961072999864, -2.064309927181999793 ) ) ;
#7212=CARTESIAN_POINT ( 'NONE',  ( -20.36558224544999973, -7.982288314729000689, 4.838215421970999408 ) ) ;
#7213=CARTESIAN_POINT ( 'NONE',  ( -4.783137886507999426, 13.34123574856998218, -4.957011659754998689 ) ) ;
#7214=CARTESIAN_POINT ( 'NONE',  ( -22.90341771435761942, -8.498744592154324096, -6.277662391787633744 ) ) ;
#7215=CARTESIAN_POINT ( 'NONE',  ( -7.034000000000000696, 1.310788454998999989E-14, 0.000000000000000000 ) ) ;
#7218=DIRECTION ( 'NONE',  ( 0.000000000000000000, 1.000000000000000000, 0.000000000000000000 ) ) ;
#7219=ORIENTED_EDGE ( 'NONE', *, *, #10262, .F. ) ;
#7221=CARTESIAN_POINT ( 'NONE',  ( -10.04281598263999875, 16.40330333354999937, -1.000000000000000000 ) ) ;
#7224=CIRCLE ( 'NONE', #20765, 0.9999999984430005817 ) ;
#7225=CARTESIAN_POINT ( 'NONE',  ( -24.50000000000000000, 10.82531754731000007, 6.250000000000000000 ) ) ;
#7227=CIRCLE ( 'NONE', #5308, 13.75000000000000000 ) ;
#7228=CARTESIAN_POINT ( 'NONE',  ( -0.8487876267396665675, 11.51352355685487794, -4.737227332089804399 ) ) ;
#7231=DIRECTION ( 'NONE',  ( 0.000000000000000000, 1.000000000000000000, 0.000000000000000000 ) ) ;
#7235=CARTESIAN_POINT ( 'NONE',  ( -16.32847087121332663, 1.190044756772780543, -9.090302457316877138 ) ) ;
#7236=CARTESIAN_POINT ( 'NONE',  ( 18.35550158530999809, 7.854726640733000309, 6.622681824707000509 ) ) ;
#7237=CARTESIAN_POINT ( 'NONE',  ( 18.68520931625605641, 9.205899787919600286, 4.917199649007022444 ) ) ;
#7238=UNCERTAINTY_MEASURE_WITH_UNIT (LENGTH_MEASURE( 1.000000000000000082E-05 ), #12292, 'distance_accuracy_value', 'NONE');
#7241=CARTESIAN_POINT ( 'NONE',  ( -14.25243324638999809, -7.716878364870000340, 11.63397459621999985 ) ) ;
#7242=CARTESIAN_POINT ( 'NONE',  ( 13.50000000000000000, -4.865356088987999428, 9.073685197596999430 ) ) ;
#7243=AXIS2_PLACEMENT_3D ( 'NONE', #701, #8111, #6522 ) ;
#7244=VERTEX_POINT ( 'NONE', #16386 ) ;
#7246=CARTESIAN_POINT ( 'NONE',  ( 20.47869942662000042, 9.225975305757000200, 6.464965578640000210 ) ) ;
#7248=CONICAL_SURFACE ( 'NONE', #7632, 13.23032192316000000, 1.093540295016705466 ) ;
#7251=CARTESIAN_POINT ( 'NONE',  ( -9.042815982636001948, 21.50000000000000000, 1.000000000000000000 ) ) ;
#7253=CARTESIAN_POINT ( 'NONE',  ( -12.25000000000000000, 12.83205029844341460, -7.862349573137913161 ) ) ;
#7256=ORIENTED_EDGE ( 'NONE', *, *, #14594, .T. ) ;
#7258=CARTESIAN_POINT ( 'NONE',  ( 6.274337143909004766, 13.70212203095000447, 0.1150566321023998723 ) ) ;
#7260=CIRCLE ( 'NONE', #21186, 3.850000000000000977 ) ;
#7261=CYLINDRICAL_SURFACE ( 'NONE', #18078, 12.44999999999999929 ) ;
#7262=CARTESIAN_POINT ( 'NONE',  ( 24.50000000000000000, 0.000000000000000000, 0.000000000000000000 ) ) ;
#7263=CARTESIAN_POINT ( 'NONE',  ( 18.49162674931000083, 10.23722398798000022, 3.399059637929999766 ) ) ;
#7265=FACE_OUTER_BOUND ( 'NONE', #1786, .T. ) ;
#7268=CARTESIAN_POINT ( 'NONE',  ( 23.99999963380687618, 13.93375672974000246, -1.355252715606880543E-17 ) ) ;
#7269=ORIENTED_EDGE ( 'NONE', *, *, #7285, .T. ) ;
#7270=ADVANCED_FACE ( 'NONE', ( #7667 ), #16627, .F. ) ;
#7271=FACE_OUTER_BOUND ( 'NONE', #2934, .T. ) ;
#7273=CARTESIAN_POINT ( 'NONE',  ( 14.88762324588007679, 10.27475985081747467, -1.077678046861461736 ) ) ;
#7274=DIRECTION ( 'NONE',  ( 0.000000000000000000, 1.000000000000000000, 0.000000000000000000 ) ) ;
#7275=CARTESIAN_POINT ( 'NONE',  ( 18.91272705013000177, 2.168976607551000413, 10.20678623380999994 ) ) ;
#7277=CARTESIAN_POINT ( 'NONE',  ( 13.69815667207068977, 8.472763392864036902, -3.097978430159455954 ) ) ;
#7278=CARTESIAN_POINT ( 'NONE',  ( 4.812800256644999664, 12.64283093136000424, 0.1074564704997999637 ) ) ;
#7279=AXIS2_PLACEMENT_3D ( 'NONE', #22419, #20602, #20846 ) ;
#7281=CARTESIAN_POINT ( 'NONE',  ( -14.73482540465084689, -5.357977798521391222, -7.317081367224309574 ) ) ;
#7282=B_SPLINE_CURVE_WITH_KNOTS ( 'NONE', 3,
 ( #4872, #15867, #1596, #10446, #1228 ),
 .UNSPECIFIED., .F., .F.,
 ( 4, 1, 4 ),
 ( 0.000000000000000000, 0.5000000000000000000, 1.000000000000000000 ),
 .UNSPECIFIED. ) ;
#7285=EDGE_CURVE ( 'NONE', #15508, #1857, #22313, .T. ) ;
#7291=CARTESIAN_POINT ( 'NONE',  ( 14.29838079285000063, 0.2591618801014000106, -11.00707472443999890 ) ) ;
#7292=CARTESIAN_POINT ( 'NONE',  ( -14.02798884238528565, -7.733277215070094357, 6.870939237852974557 ) ) ;
#7295=CARTESIAN_POINT ( 'NONE',  ( -9.181633638770000161, 11.42978193837999967, -10.04780447355000028 ) ) ;
#7297=CARTESIAN_POINT ( 'NONE',  ( 13.50000000000000000, 5.257133879617095218, 8.639483096027150921 ) ) ;
#7298=CARTESIAN_POINT ( 'NONE',  ( -14.32799102833200244, -13.40593186267523329, -1.779780195184996749 ) ) ;
#7299=EDGE_LOOP ( 'NONE', ( #12500, #10968, #8388, #7765, #13753 ) ) ;
#7300=ADVANCED_FACE ( 'NONE', ( #20514, #14574 ), #3919, .F. ) ;
#7301=CARTESIAN_POINT ( 'NONE',  ( 23.67649762116742096, 9.825750814993579496, -4.009899241536614589 ) ) ;
#7302=CARTESIAN_POINT ( 'NONE',  ( 24.50000000000000711, 10.56912816078165562, -6.693733033818888956 ) ) ;
#7303=CARTESIAN_POINT ( 'NONE',  ( 16.10209092903769701, -5.933957400870331078, -8.494887192401384013 ) ) ;
#7305=CARTESIAN_POINT ( 'NONE',  ( -16.24483109794999791, 4.897926442300000183, 9.908171963158000750 ) ) ;
#7309=CARTESIAN_POINT ( 'NONE',  ( -18.23630520352000062, 4.669879042777999700, -9.230749285618999878 ) ) ;
#7312=ORIENTED_EDGE ( 'NONE', *, *, #22377, .T. ) ;
#7314=CARTESIAN_POINT ( 'NONE',  ( 21.06533049062388230, -8.103789509103517474, 6.745704132337678516 ) ) ;
#7321=CARTESIAN_POINT ( 'NONE',  ( -3.947433534395999644, 12.10275648868998211, -2.807484267057001492 ) ) ;
#7324=CARTESIAN_POINT ( 'NONE',  ( 13.25700125730999979, -8.207589172378998654, -3.980341215395999832 ) ) ;
#7326=CIRCLE ( 'NONE', #6943, 15.43375672973999357 ) ;
#7329=CARTESIAN_POINT ( 'NONE',  ( -14.44600785535203791, 2.842816319751110044, -12.49998455205779102 ) ) ;
#7330=B_SPLINE_CURVE_WITH_KNOTS ( 'NONE', 3,
 ( #17016, #18832, #19067, #13371, #9632 ),
 .UNSPECIFIED., .F., .F.,
 ( 4, 1, 4 ),
 ( 0.000000000000000000, 0.5000000000000000000, 1.000000000000000000 ),
 .UNSPECIFIED. ) ;
#7333=CARTESIAN_POINT ( 'NONE',  ( -22.92422353055919970, 9.261441866921273913, -1.677491911259402002 ) ) ;
#7334=EDGE_CURVE ( 'NONE', #386, #3390, #11590, .T. ) ;
#7335=CARTESIAN_POINT ( 'NONE',  ( -20.58263244952000193, 6.141030327595999871, 8.010145565080000196 ) ) ;
#7336=CARTESIAN_POINT ( 'NONE',  ( 11.97297107871801458, -8.401874682647177295, -10.44762502816489480 ) ) ;
#7338=CARTESIAN_POINT ( 'NONE',  ( -23.70120661253317706, 5.594576894260432809, 8.987328952431388629 ) ) ;
#7340=DIRECTION ( 'NONE',  ( 1.000000000000000000, 0.000000000000000000, 0.000000000000000000 ) ) ;
#7343=FACE_OUTER_BOUND ( 'NONE', #20526, .T. ) ;
#7344=CARTESIAN_POINT ( 'NONE',  ( 13.74900873693342440, 3.555560787657467525, -8.351293932026473854 ) ) ;
#7345=CARTESIAN_POINT ( 'NONE',  ( -24.28586141838234269, -1.359960862156090800, -10.51926263243713144 ) ) ;
#7348=AXIS2_PLACEMENT_3D ( 'NONE', #4823, #9896, #13641 ) ;
#7351=CARTESIAN_POINT ( 'NONE',  ( 0.1315063851937676997, 11.48152553765250516, -4.814286258553329922 ) ) ;
#7352=CARTESIAN_POINT ( 'NONE',  ( 24.50000000000000711, 11.08150693382694030, 5.806266966183555311 ) ) ;
#7354=ORIENTED_EDGE ( 'NONE', *, *, #9343, .F. ) ;
#7355=EDGE_CURVE ( 'NONE', #10857, #3930, #16217, .T. ) ;
#7357=CARTESIAN_POINT ( 'NONE',  ( 18.68456408531000079, -2.737678269967000144, 9.911560247287001246 ) ) ;
#7358=CARTESIAN_POINT ( 'NONE',  ( 18.70488052352785147, 8.850818011485689141, 5.514450890227789337 ) ) ;
#7362=CARTESIAN_POINT ( 'NONE',  ( 13.50000000000000178, -5.180989882992017570, 8.880677523943516505 ) ) ;
#7363=ORIENTED_EDGE ( 'NONE', *, *, #15236, .T. ) ;
#7365=CARTESIAN_POINT ( 'NONE',  ( 22.69754412252000009, 5.148292089747000588, 9.490647990332998774 ) ) ;
#7368=CARTESIAN_POINT ( 'NONE',  ( 24.50000000000000355, -7.886533982023047784, 7.073078350185027396 ) ) ;
#7369=CARTESIAN_POINT ( 'NONE',  ( 24.50000000000000000, 3.215423653429137385, 9.789911160088649922 ) ) ;
#7370=VECTOR ( 'NONE', #11983, 1000.000000000000000 ) ;
#7371=CARTESIAN_POINT ( 'NONE',  ( -4.776913516551996253, 12.47840662102999509, -0.1494451571019999592 ) ) ;
#7373=CARTESIAN_POINT ( 'NONE',  ( -21.14116503741999864, -8.837159004920000172, 6.686531827553999996 ) ) ;
#7375=B_SPLINE_CURVE_WITH_KNOTS ( 'NONE', 3,
 ( #21444, #13927, #6657, #14172, #6903, #23243 ),
 .UNSPECIFIED., .F., .F.,
 ( 4, 2, 4 ),
 ( 0.000000000000000000, 0.5000000000000000000, 1.000000000000000000 ),
 .UNSPECIFIED. ) ;
#7376=CARTESIAN_POINT ( 'NONE',  ( -6.125000000000000000, 21.50000000000000000, 0.000000000000000000 ) ) ;
#7380=CARTESIAN_POINT ( 'NONE',  ( 12.28779254563088585, 5.665119685602451050, -12.50001287414461792 ) ) ;
#7383=CARTESIAN_POINT ( 'NONE',  ( 16.60050158530999909, 6.318772076511000257, 8.042630855556000213 ) ) ;
#7385=EDGE_LOOP ( 'NONE', ( #8383, #288, #20504, #524 ) ) ;
#7386=DIRECTION ( 'NONE',  ( -1.000000000000000000, 0.000000000000000000, 0.000000000000000000 ) ) ;
#7389=VERTEX_POINT ( 'NONE', #5610 ) ;
#7390=CARTESIAN_POINT ( 'NONE',  ( -10.83200247828752971, 15.36487885975186352, -1.677940321992645645 ) ) ;
#7392=CARTESIAN_POINT ( 'NONE',  ( 14.41647009244453947, -1.614193569338650880, -10.19093708827842271 ) ) ;
#7394=CARTESIAN_POINT ( 'NONE',  ( 19.27982097606999901, -9.756977011084000395, 5.441823009411000278 ) ) ;
#7395=EDGE_CURVE ( 'NONE', #2511, #3147, #7544, .T. ) ;
#7397=CARTESIAN_POINT ( 'NONE',  ( 14.10157458702998667, 4.520082339245768743, 7.819331374180982230 ) ) ;
#7398=CARTESIAN_POINT ( 'NONE',  ( -6.605774574140806266, 15.40025296468788341, -1.587926255657816643 ) ) ;
#7400=CARTESIAN_POINT ( 'NONE',  ( 12.04708237233490387, 13.35071834206844876, -1.875975938906002005 ) ) ;
#7403=CARTESIAN_POINT ( 'NONE',  ( -14.00000000000000000, -10.27687089286999900, -0.6428416445564000270 ) ) ;
#7408=CARTESIAN_POINT ( 'NONE',  ( 21.83358103379666204, -1.208283319978287418, 9.231574434091362136 ) ) ;
#7409=CARTESIAN_POINT ( 'NONE',  ( 18.20064194352000086, -0.4690725264157000751, -11.10709960042999889 ) ) ;
#7412=VERTEX_POINT ( 'NONE', #18925 ) ;
#7413=CARTESIAN_POINT ( 'NONE',  ( -10.71634506584999968, -1.748784590530000127, -14.76480909560000043 ) ) ;
#7415=CARTESIAN_POINT ( 'NONE',  ( -14.50000018026810089, -10.69550487835728347, -6.474840093751000225 ) ) ;
#7416=ORIENTED_EDGE ( 'NONE', *, *, #21412, .T. ) ;
#7417=CARTESIAN_POINT ( 'NONE',  ( -14.47793701804645217, 11.73188619686574263, 4.679765522763038810 ) ) ;
#7418=CARTESIAN_POINT ( 'NONE',  ( 20.29382020395017250, 9.419176356032403774, 4.682166151186863523 ) ) ;
#7420=CARTESIAN_POINT ( 'NONE',  ( 15.94258035992931966, -9.513174729914155137, -4.100360902401353869 ) ) ;
#7421=CARTESIAN_POINT ( 'NONE',  ( -16.60615772801000034, 10.95457934470999994, -1.541957209009000129 ) ) ;
#7424=CARTESIAN_POINT ( 'NONE',  ( -16.61126241975999918, -1.906005702182999917, -10.12158796435999975 ) ) ;
#7426=ORIENTED_EDGE ( 'NONE', *, *, #14380, .F. ) ;
#7428=CARTESIAN_POINT ( 'NONE',  ( 20.98021033963484427, -5.789786262372857983, 8.802753455338001132 ) ) ;
#7429=DIRECTION ( 'NONE',  ( 0.000000000000000000, 0.000000000000000000, -1.000000000000000000 ) ) ;
#7431=CARTESIAN_POINT ( 'NONE',  ( 24.45564077607145137, -2.060124049350608555, 12.50000000000000178 ) ) ;
#7432=CARTESIAN_POINT ( 'NONE',  ( -6.309599240701002643, 15.06635153518999104, 3.401153641079002199 ) ) ;
#7435=CARTESIAN_POINT ( 'NONE',  ( 13.69575125731000043, 3.560502093102000387, -8.410767149301999979 ) ) ;
#7438=CARTESIAN_POINT ( 'NONE',  ( -7.834000000000000519, -10.69999999999999929, 0.000000000000000000 ) ) ;
#7443=CARTESIAN_POINT ( 'NONE',  ( -4.811404347808999837, 12.64229228517000969, -0.1541852644638002090 ) ) ;
#7444=CARTESIAN_POINT ( 'NONE',  ( 11.99999999999999822, -2.116414852691937742, -9.237906777948852621 ) ) ;
#7446=CARTESIAN_POINT ( 'NONE',  ( 11.53663804754834743, -9.092401935506826405, -9.251313393160373266 ) ) ;
#7448=CARTESIAN_POINT ( 'NONE',  ( -19.89240800188232683, -0.7325527030282151797, 10.46337770069665396 ) ) ;
#7450=CARTESIAN_POINT ( 'NONE',  ( 15.76716666666666455, 7.930444964421201171, 4.570677355979499978 ) ) ;
#7451=CARTESIAN_POINT ( 'NONE',  ( -5.523874320477998978, 16.26076007236001431, 2.688832781278999828 ) ) ;
#7452=DIRECTION ( 'NONE',  ( -0.9996848865506517967, 0.000000000000000000, -0.02510234256419879503 ) ) ;
#7454=CARTESIAN_POINT ( 'NONE',  ( 19.20820820724999933, 5.862953550309000228, -7.802432380257999789 ) ) ;
#7455=CARTESIAN_POINT ( 'NONE',  ( 14.99328936713000004, -9.056039068417000237, 0.000000000000000000 ) ) ;
#7457=CARTESIAN_POINT ( 'NONE',  ( -22.46506791698822170, -1.100719659442045861, -10.63859953765026312 ) ) ;
#7459=EDGE_CURVE ( 'NONE', #13107, #15625, #9128, .T. ) ;
#7461=CARTESIAN_POINT ( 'NONE',  ( -11.04281598264000053, 1.359882291614000008E-14, 0.000000000000000000 ) ) ;
#7463=CARTESIAN_POINT ( 'NONE',  ( -4.671788442614717596, 12.38274754940156264, -1.292526076544993519 ) ) ;
#7467=CARTESIAN_POINT ( 'NONE',  ( -12.25000000000000000, 6.613190111079999767, -13.46349570337000046 ) ) ;
#7469=CARTESIAN_POINT ( 'NONE',  ( 15.61331408530999987, -8.260803322383997838, -5.986632065681000370 ) ) ;
#7470=CARTESIAN_POINT ( 'NONE',  ( 18.39251201459628859, 8.989286056864246532, -5.271706797561602542 ) ) ;
#7472=CARTESIAN_POINT ( 'NONE',  ( -23.74465998031000069, 6.216878364870000340, 12.50000000000000000 ) ) ;
#7475=DIRECTION ( 'NONE',  ( -7.335406816068161220E-08, -0.9999999999995213829, -9.756601275250212230E-07 ) ) ;
#7476=CIRCLE ( 'NONE', #21814, 6.125000000000000000 ) ;
#7478=ORIENTED_EDGE ( 'NONE', *, *, #11203, .F. ) ;
#7480=CARTESIAN_POINT ( 'NONE',  ( 22.16639681605000334, 7.771014960181000575, -7.474990234536999623 ) ) ;
#7481=CARTESIAN_POINT ( 'NONE',  ( -24.48172546360977009, 4.179826417290672502, -9.441142365384852297 ) ) ;
#7483=FACE_OUTER_BOUND ( 'NONE', #22096, .T. ) ;
#7485=CARTESIAN_POINT ( 'NONE',  ( 4.087091007756002092, 12.14415498498998680, 2.742727926892003509 ) ) ;
#7488=ORIENTED_EDGE ( 'NONE', *, *, #17020, .T. ) ;
#7492=ORIENTED_EDGE ( 'NONE', *, *, #19654, .F. ) ;
#7494=CARTESIAN_POINT ( 'NONE',  ( 4.918133982481998956, 14.11827433645001229, 3.900434897472001339 ) ) ;
#7495=CARTESIAN_POINT ( 'NONE',  ( 16.54274770046333742, -5.589705041635214755, 7.273700408684123708 ) ) ;
#7497=DIRECTION ( 'NONE',  ( 1.000000000000000000, 0.000000000000000000, 0.000000000000000000 ) ) ;
#7499=CARTESIAN_POINT ( 'NONE',  ( 12.02006424930999984, -10.30839584998999925, 1.075033486111000025 ) ) ;
#7502=CARTESIAN_POINT ( 'NONE',  ( -14.94546155477000049, -9.714114572133000891, -0.2583773470232999525 ) ) ;
#7506=CARTESIAN_POINT ( 'NONE',  ( -10.75755763812815680, 15.39137541006824250, -1.608313476896800154 ) ) ;
#7508=CARTESIAN_POINT ( 'NONE',  ( 14.57135008224444128, 3.797263269294576471, -9.601797994946904780 ) ) ;
#7509=DIRECTION ( 'NONE',  ( -1.000000000000000000, 0.000000000000000000, 0.000000000000000000 ) ) ;
#7510=CARTESIAN_POINT ( 'NONE',  ( 21.62900612854999949, -7.523913936368999522, -8.345185084459998848 ) ) ;
#7512=CARTESIAN_POINT ( 'NONE',  ( 13.80187520366866849, 9.025291185423055751, 0.006276713024069551644 ) ) ;
#7513=CARTESIAN_POINT ( 'NONE',  ( 4.816630038177000195, 12.64431341689999932, -0.1115539088738999873 ) ) ;
#7514=B_SPLINE_CURVE_WITH_KNOTS ( 'NONE', 3,
 ( #16613, #11173, #21, #22888 ),
 .UNSPECIFIED., .F., .F.,
 ( 4, 4 ),
 ( 0.000000000000000000, 1.000000000000000000 ),
 .UNSPECIFIED. ) ;
#7516=CARTESIAN_POINT ( 'NONE',  ( 11.12576011241902840, 10.20205618038153084, -7.329535452988973354 ) ) ;
#7517=ORIENTED_EDGE ( 'NONE', *, *, #21552, .T. ) ;
#7522=CARTESIAN_POINT ( 'NONE',  ( 24.50000000000000000, 10.31403833462485053, 7.135561573215231768 ) ) ;
#7525=CARTESIAN_POINT ( 'NONE',  ( 14.98635508327000032, 10.44157347027999982, 3.551293096755000267 ) ) ;
#7526=CARTESIAN_POINT ( 'NONE',  ( -6.171953915136863422, 15.86494870466900764, 1.104274664945693374 ) ) ;
#7530=ORIENTED_EDGE ( 'NONE', *, *, #22509, .F. ) ;
#7531=AXIS2_PLACEMENT_3D ( 'NONE', #15766, #1246, #21352 ) ;
#7532=CARTESIAN_POINT ( 'NONE',  ( -9.588923638769999869, -11.49744000511999964, -9.970428444189000317 ) ) ;
#7534=CARTESIAN_POINT ( 'NONE',  ( -14.25851235546000062, -6.966599976214999934, 12.06714802587000079 ) ) ;
#7536=CARTESIAN_POINT ( 'NONE',  ( -14.29262082160887637, 13.66753291840703710, 1.327138571200180861 ) ) ;
#7537=CARTESIAN_POINT ( 'NONE',  ( -21.96532910583999865, -9.234955349282000014, 0.000000000000000000 ) ) ;
#7538=B_SPLINE_CURVE_WITH_KNOTS ( 'NONE', 3,
 ( #6216, #13844, #17363, #1006, #4530, #6089 ),
 .UNSPECIFIED., .F., .F.,
 ( 4, 2, 4 ),
 ( 0.000000000000000000, 0.5000000000000000000, 1.000000000000000000 ),
 .UNSPECIFIED. ) ;
#7539=CARTESIAN_POINT ( 'NONE',  ( 24.48327518124252933, 10.18191985984368664, -7.364397484155817963 ) ) ;
#7540=CARTESIAN_POINT ( 'NONE',  ( 15.89621519439380570, -10.03933691619746682, -2.545899918998145939 ) ) ;
#7541=CARTESIAN_POINT ( 'NONE',  ( -18.41279087833000006, 11.03951774085000004, -1.267611736511999876 ) ) ;
#7544=B_SPLINE_CURVE_WITH_KNOTS ( 'NONE', 3,
 ( #12992, #20393, #18575, #3798, #11192, #9363, #16737, #14919, #8151, #2447, #22551, #865, #19037, #18801, #8269, #22904, #5957, #6200, #7904, #16988, #17105, #20623, #389, #15273, #6320, #11427, #19157, #4277, #15633, #13342, #15516, #23024, #9723, #11665, #13705, #22784, #15156, #4033, #20741, #11545, #7786, #17221, #2567, #2210, #21098, #9601, #20867, #6441 ),
 .UNSPECIFIED., .F., .F.,
 ( 4, 2, 2, 2, 2, 2, 1, 1, 2, 2, 2, 1, 1, 1, 2, 2, 2, 2, 1, 1, 1, 2, 2, 2, 1, 1, 2, 2, 4 ),
 ( 0.000000000000000000, 0.06250000000000340006, 0.09375000000000510703, 0.1250000000000068001, 0.1875000000000106859, 0.2187500000000128786, 0.2343750000000139333, 0.2421875000000143219, 0.2460937500000142386, 0.2500000000000142109, 0.3750000000000117684, 0.4375000000000104916, 0.4687500000000101585, 0.4843750000000100475, 0.4921875000000094924, 0.5000000000000089928, 0.6249999999999866773, 0.6874999999999755751, 0.7187499999999699130, 0.7343749999999678035, 0.7421874999999668043, 0.7460937499999671374, 0.7499999999999673594, 0.8124999999999765743, 0.8437499999999816813, 0.8593749999999849010, 0.8671874999999856781, 0.8749999999999864553, 1.000000000000000000 ),
 .UNSPECIFIED. ) ;
#7545=CARTESIAN_POINT ( 'NONE',  ( -18.07393293677000301, 10.37468091520999991, 3.263143967163999903 ) ) ;
#7549=CARTESIAN_POINT ( 'NONE',  ( 21.37743771091500378, -9.903291219543641333, -4.060970818798163684 ) ) ;
#7550=CARTESIAN_POINT ( 'NONE',  ( -22.87210175995843642, 9.258583067823760615, -6.329161777784410158E-06 ) ) ;
#7551=ORIENTED_EDGE ( 'NONE', *, *, #11360, .F. ) ;
#7555=CARTESIAN_POINT ( 'NONE',  ( 16.79343892131000260, -7.329510781495000238, 6.390029238976000059 ) ) ;
#7556=EDGE_LOOP ( 'NONE', ( #22967, #5937, #17008, #10196 ) ) ;
#7557=AXIS2_PLACEMENT_3D ( 'NONE', #9813, #6297, #21200 ) ;
#7558=CARTESIAN_POINT ( 'NONE',  ( -5.264900118121860650, 16.02290957484199652, 3.131682802096217966 ) ) ;
#7560=ORIENTED_EDGE ( 'NONE', *, *, #13086, .T. ) ;
#7561=CARTESIAN_POINT ( 'NONE',  ( 23.11849770046333674, 9.264547928196073201, -1.212853435574229310 ) ) ;
#7562=CARTESIAN_POINT ( 'NONE',  ( -4.814900992596998108, 12.64364337456001941, 0.1283334480982998294 ) ) ;
#7563=CARTESIAN_POINT ( 'NONE',  ( 11.99999999999999822, 0.7437781458199891338, -9.269733647780308061 ) ) ;
#7566=CARTESIAN_POINT ( 'NONE',  ( -4.263376217415998148, 14.54355705694000456, -4.183184883477999882 ) ) ;
#7567=CARTESIAN_POINT ( 'NONE',  ( -20.22696463660509636, 9.305942615553171038, 4.861376333746878053 ) ) ;
#7572=EDGE_LOOP ( 'NONE', ( #23487, #16760, #2724, #22101 ) ) ;
#7573=CARTESIAN_POINT ( 'NONE',  ( 18.11311958374000142, 0.09792845715294999642, 9.251054258097999750 ) ) ;
#7575=CONICAL_SURFACE ( 'NONE', #4492, 9.152445778720998959, 0.02565634000431304615 ) ;
#7576=B_SPLINE_CURVE_WITH_KNOTS ( 'NONE', 3,
 ( #8369, #21204, #15861, #4619, #12010, #15738, #6549, #13933 ),
 .UNSPECIFIED., .F., .F.,
 ( 4, 2, 2, 4 ),
 ( 0.000000000000000000, 0.2500000000000000555, 0.5000000000000003331, 1.000000000000000000 ),
 .UNSPECIFIED. ) ;
#7577=CARTESIAN_POINT ( 'NONE',  ( -23.50934654278774971, 5.808796177084403212, 8.845529366387745895 ) ) ;
#7581=CARTESIAN_POINT ( 'NONE',  ( 2.255701365037127815, 11.69874888801631307, 4.259317076402555635 ) ) ;
#7582=ORIENTED_EDGE ( 'NONE', *, *, #23836, .F. ) ;
#7583=EDGE_CURVE ( 'NONE', #3930, #5630, #8724, .T. ) ;
#7584=CARTESIAN_POINT ( 'NONE',  ( -4.534537486635951353, 12.33232649926562452, -1.710134897757592309 ) ) ;
#7587=ORIENTED_EDGE ( 'NONE', *, *, #21265, .F. ) ;
#7588=CARTESIAN_POINT ( 'NONE',  ( -23.74465998031000069, 13.93375672974000068, 0.8660254037843999608 ) ) ;
#7591=CARTESIAN_POINT ( 'NONE',  ( 18.13612658530999866, 10.25022803218000078, -0.6090841227779000278 ) ) ;
#7592=EDGE_CURVE ( 'NONE', #744, #16718, #22853, .T. ) ;
#7593=CARTESIAN_POINT ( 'NONE',  ( -19.69180044273999997, -10.89175753566999916, 0.7824706121295000871 ) ) ;
#7595=CARTESIAN_POINT ( 'NONE',  ( 19.18739037306000128, 0.9675627967257999229, 10.87120185456999977 ) ) ;
#7596=LINE ( 'NONE', #18740, #18950 ) ;
#7598=EDGE_LOOP ( 'NONE', ( #8019, #19277 ) ) ;
#7600=CARTESIAN_POINT ( 'NONE',  ( 20.30165032445999884, 11.26076864172999947, -0.02284890567960000049 ) ) ;
#7601=LINE ( 'NONE', #16448, #3103 ) ;
#7605=CARTESIAN_POINT ( 'NONE',  ( 24.49999999999999289, 5.386536742071421635, 8.691140576888541247 ) ) ;
#7606=B_SPLINE_CURVE_WITH_KNOTS ( 'NONE', 3,
 ( #19517, #18695, #16868, #4043, #15052, #17577, #11882, #22445, #11436 ),
 .UNSPECIFIED., .F., .F.,
 ( 4, 1, 2, 2, 4 ),
 ( 0.000000000000000000, 0.2499999999999995559, 0.3749999999999994449, 0.4999999999999993339, 1.000000000000000000 ),
 .UNSPECIFIED. ) ;
#7607=CARTESIAN_POINT ( 'NONE',  ( 3.728119965002001823, 12.03273885954999045, 3.094591559352003252 ) ) ;
#7608=AXIS2_PLACEMENT_3D ( 'NONE', #2056, #11027, #16701 ) ;
#7610=CARTESIAN_POINT ( 'NONE',  ( -21.30824958319999851, -3.742314851699000133, 10.43554850291999969 ) ) ;
#7616=EDGE_CURVE ( 'NONE', #8416, #17203, #1238, .T. ) ;
#7623=CARTESIAN_POINT ( 'NONE',  ( 17.28506424931000041, -8.106780832215999766, 7.067619055798999739 ) ) ;
#7625=CARTESIAN_POINT ( 'NONE',  ( -17.83004450757999848, 9.857337362280999216, 3.100493417357999881 ) ) ;
#7628=CARTESIAN_POINT ( 'NONE',  ( -14.50000017815840536, -0.2596243778326527973, 12.49999897408938487 ) ) ;
#7629=VERTEX_POINT ( 'NONE', #19780 ) ;
#7631=CARTESIAN_POINT ( 'NONE',  ( -19.30614371005000152, -10.53683211585999935, -0.2416866977026000118 ) ) ;
#7632=AXIS2_PLACEMENT_3D ( 'NONE', #10535, #18039, #19742 ) ;
#7633=B_SPLINE_CURVE_WITH_KNOTS ( 'NONE', 3,
 ( #17031, #7830, #11474, #546, #11955, #7952, #2622, #15201, #19341, #22597, #9884, #4197, #13274, #13388, #2749, #19081, #16905, #21025, #309, #7716, #8195, #21149, #20790, #4437, #15082, #11595, #22712, #10012, #18967, #2375, #17151, #22478, #672, #11828, #6123, #4317, #11709, #17272, #13515, #20913, #8077, #20669, #17402, #15447, #4079, #22832, #6246, #19207, #13629, #795, #15564, #22951, #6366, #13750, #1170, #1291, #1039, #4809, #19585, #913, #20150, #17768, #22077, #8563, #9122, #13879, #6615, #18329, #21281, #12195, #2990, #23316, #12076, #23067, #19461, #8314, #5372, #15922, #6497, #1734, #21517, #10378, #19707, #12761, #6730, #17889, #14122, #15680, #4930, #12316, #17641, #3120, #16495, #10505, #4691, #2868, #8678, #16043, #23437, #7173, #14564, #23885, #3557, #5485, #12865, #21959, #23199, #10942, #10130, #7292, #10252 ),
 .UNSPECIFIED., .F., .F.,
 ( 4, 2, 2, 2, 1, 2, 2, 2, 2, 2, 2, 2, 2, 2, 2, 2, 2, 2, 2, 2, 2, 2, 2, 2, 2, 2, 1, 2, 2, 2, 2, 2, 2, 2, 2, 2, 2, 2, 2, 2, 2, 2, 2, 2, 2, 2, 2, 2, 2, 2, 1, 2, 2, 2, 2, 2, 4 ),
 ( 0.000000000000000000, 0.01562500000000000000, 0.03125000000000000000, 0.04687500000000000000, 0.06250000000000000000, 0.07812500000000000000, 0.09375000000000000000, 0.1093750000000000000, 0.1250000000000000000, 0.1406250000000000000, 0.1562500000000000000, 0.1718750000000000000, 0.1875000000000000000, 0.2187500000000000000, 0.2500000000000000000, 0.2812500000000000000, 0.3125000000000000000, 0.3281250000000000000, 0.3437500000000000000, 0.3593750000000000000, 0.3750000000000000000, 0.3906250000000000000, 0.4062500000000000000, 0.4218750000000000000, 0.4375000000000000000, 0.4531250000000000000, 0.4687500000000000000, 0.4843750000000000000, 0.5000000000000000000, 0.5156250000000000000, 0.5312500000000000000, 0.5468750000000000000, 0.5625000000000000000, 0.5781250000000000000, 0.5937500000000000000, 0.6093750000000000000, 0.6250000000000000000, 0.6562500000000000000, 0.6875000000000000000, 0.7187500000000000000, 0.7500000000000000000, 0.7656250000000000000, 0.7812500000000000000, 0.7968750000000000000, 0.8125000000000000000, 0.8281250000000000000, 0.8437500000000000000, 0.8593750000000000000, 0.8750000000000000000, 0.8906250000000000000, 0.9062500000000000000, 0.9218750000000000000, 0.9375000000000000000, 0.9531250000000000000, 0.9687500000000000000, 0.9843750000000000000, 1.000000000000000000 ),
 .UNSPECIFIED. ) ;
#7636=CARTESIAN_POINT ( 'NONE',  ( 14.19161095287168273, -8.300789259405844334, -6.118116098091685551 ) ) ;
#7637=CARTESIAN_POINT ( 'NONE',  ( -18.33142920454666580, -4.603817514783774989, -7.987943630674345208 ) ) ;
#7638=CARTESIAN_POINT ( 'NONE',  ( 24.41913593913999847, -0.1539011931813000222, 11.31195935673000008 ) ) ;
#7641=CARTESIAN_POINT ( 'NONE',  ( 14.26651023885097302, -0.3455854243710511087, 9.058464311847558292 ) ) ;
#7642=CARTESIAN_POINT ( 'NONE',  ( 17.23562128263493776, -8.032680157772452034, 6.884423379150467426 ) ) ;
#7645=CARTESIAN_POINT ( 'NONE',  ( 12.28779254561780654, 13.65788853942738434, -1.343868873886438164 ) ) ;
#7653=CARTESIAN_POINT ( 'NONE',  ( 24.50000000000000000, 10.82531754731000007, 6.250000000000000000 ) ) ;
#7655=B_SPLINE_CURVE_WITH_KNOTS ( 'NONE', 3,
 ( #21631, #3897, #7645, #20370, #7400, #23558, #16281, #5825, #23674, #15018, #19816, #14358, #22417, #3230, #19931, #3349, #22178, #17996, #6842, #1401, #12970, #11167, #20599, #6966, #7516, #4009, #14900, #22291, #5706, #13093, #11288, #17880, #8667, #16033, #23425, #2426, #363, #725, #2310, #11406, #9698, #21078 ),
 .UNSPECIFIED., .F., .F.,
 ( 4, 2, 1, 2, 2, 2, 1, 2, 2, 2, 2, 2, 2, 2, 2, 1, 2, 2, 2, 1, 2, 2, 4 ),
 ( 0.000000000000000000, 0.06250000000000087430, 0.09375000000000137390, 0.1093750000000017208, 0.1250000000000020817, 0.1875000000000032196, 0.2187500000000036637, 0.2343750000000038025, 0.2500000000000039413, 0.3125000000000041633, 0.3750000000000043299, 0.5000000000000043299, 0.5625000000000044409, 0.6250000000000044409, 0.6875000000000043299, 0.7187500000000044409, 0.7343750000000045519, 0.7500000000000045519, 0.8125000000000032196, 0.8437500000000026645, 0.8593750000000024425, 0.8750000000000022204, 1.000000000000000000 ),
 .UNSPECIFIED. ) ;
#7656=CARTESIAN_POINT ( 'NONE',  ( 18.23447124448000167, 6.119127544384999950, -9.282487988299001458 ) ) ;
#7659=ORIENTED_EDGE ( 'NONE', *, *, #9399, .F. ) ;
#7663=CARTESIAN_POINT ( 'NONE',  ( 17.79862270046333350, 8.831439506605962109, 2.665405980357957727 ) ) ;
#7664=ORIENTED_EDGE ( 'NONE', *, *, #13868, .T. ) ;
#7665=CARTESIAN_POINT ( 'NONE',  ( -14.33281118273302290, 8.249344442837845293, 10.71171629587128926 ) ) ;
#7666=CARTESIAN_POINT ( 'NONE',  ( 19.44079720308818082, -8.366211633341873011, -6.347735393923803038 ) ) ;
#7667=FACE_OUTER_BOUND ( 'NONE', #1743, .T. ) ;
#7668=CARTESIAN_POINT ( 'NONE',  ( 15.58037287370735946, -6.899987183789440870, 7.711731525822442812 ) ) ;
#7669=CIRCLE ( 'NONE', #7279, 9.017718320138000010 ) ;
#7670=CARTESIAN_POINT ( 'NONE',  ( -15.73688287099999883, -7.860281848462999932, 7.750493481497999326 ) ) ;
#7672=CARTESIAN_POINT ( 'NONE',  ( -19.33347310582000134, -11.41588003357999881, 0.8201876405482001475 ) ) ;
#7675=ORIENTED_EDGE ( 'NONE', *, *, #6119, .T. ) ;
#7681=CARTESIAN_POINT ( 'NONE',  ( 24.35625626386766740, -3.237027092068850198, 12.50000000000000000 ) ) ;
#7682=B_SPLINE_CURVE_WITH_KNOTS ( 'NONE', 3,
 ( #14799, #7903, #22662, #20866, #2446, #9839, #12989, #22195, #5608, #20512, #9361, #22311, #5727, #16857 ),
 .UNSPECIFIED., .F., .F.,
 ( 4, 2, 2, 2, 2, 2, 4 ),
 ( 0.000000000000000000, 0.2500000000000001665, 0.3750000000000000555, 0.5000000000000000000, 0.6250000000000000000, 0.7499999999999998890, 1.000000000000000000 ),
 .UNSPECIFIED. ) ;
#7683=CARTESIAN_POINT ( 'NONE',  ( 13.50000000000000000, 2.048741218006000064, 10.08990150394999930 ) ) ;
#7684=CARTESIAN_POINT ( 'NONE',  ( 12.92793875730999886, -7.038709952280000515, 5.788476981990000603 ) ) ;
#7685=ORIENTED_EDGE ( 'NONE', *, *, #16471, .F. ) ;
#7686=CARTESIAN_POINT ( 'NONE',  ( -6.145346148252000873, 15.63690921201999018, -1.260321238843998604 ) ) ;
#7687=CARTESIAN_POINT ( 'NONE',  ( 24.28455689590275668, -12.82067141883539918, 2.793945715430803389 ) ) ;
#7690=DIRECTION ( 'NONE',  ( -0.8193292504149890521, 0.5733232765328929448, 2.256055603357969935E-11 ) ) ;
#7692=CARTESIAN_POINT ( 'NONE',  ( 4.720281943117000445, 12.53503215193000209, -0.1499393658648999206 ) ) ;
#7694=CARTESIAN_POINT ( 'NONE',  ( -20.37005317997999754, -8.126137106287000478, 5.051193361354000544 ) ) ;
#7695=CARTESIAN_POINT ( 'NONE',  ( -14.47125383376828367, 9.790219516183384485, -8.042794959416264433 ) ) ;
#7699=AXIS2_PLACEMENT_3D ( 'NONE', #23122, #10671, #19761 ) ;
#7704=ORIENTED_EDGE ( 'NONE', *, *, #21015, .T. ) ;
#7705=CARTESIAN_POINT ( 'NONE',  ( -17.61928743917333762, 7.295792109983556095, -5.606682590099613783 ) ) ;
#7707=CARTESIAN_POINT ( 'NONE',  ( -2.771665969827710185, 13.06403465582575052, -6.137156239621617715 ) ) ;
#7710=CARTESIAN_POINT ( 'NONE',  ( -23.72355754295171693, 10.26472423533547484, 2.601420961443067448 ) ) ;
#7712=CIRCLE ( 'NONE', #18930, 14.43375672973999890 ) ;
#7713=AXIS2_PLACEMENT_3D ( 'NONE', #14631, #18047, #18508 ) ;
#7716=CARTESIAN_POINT ( 'NONE',  ( -18.54960927350814970, 8.133714014779581447, -6.579685461590351281 ) ) ;
#7717=EDGE_CURVE ( 'NONE', #18727, #10512, #22990, .T. ) ;
#7718=CARTESIAN_POINT ( 'NONE',  ( 23.99062354302999722, -7.716878364870000340, -11.63397459621999985 ) ) ;
#7719=CARTESIAN_POINT ( 'NONE',  ( 4.834780805419000238, 12.45065217972999960, 0.000000000000000000 ) ) ;
#7720=VERTEX_POINT ( 'NONE', #10175 ) ;
#7722=CARTESIAN_POINT ( 'NONE',  ( 18.57487658530999752, 1.133029877492999882, 10.21722326572000128 ) ) ;
#7723=AXIS2_PLACEMENT_3D ( 'NONE', #4435, #13272, #11472 ) ;
#7724=CARTESIAN_POINT ( 'NONE',  ( -18.81322861345999797, 5.160499379352000204, -10.20084603521000055 ) ) ;
#7725=CARTESIAN_POINT ( 'NONE',  ( 22.79641666666664790, 9.015317850787624820, -2.422929696547522660 ) ) ;
#7726=CARTESIAN_POINT ( 'NONE',  ( 18.98426537306000128, 7.768735744027000401, 7.659878704847000286 ) ) ;
#7729=CARTESIAN_POINT ( 'NONE',  ( 20.13606306023999792, -7.887424479675998690, -6.464295009536999537 ) ) ;
#7732=ORIENTED_EDGE ( 'NONE', *, *, #15763, .T. ) ;
#7733=CARTESIAN_POINT ( 'NONE',  ( 11.73400169467000076, -6.466195830854000626, -6.710731160583000232 ) ) ;
#7735=CARTESIAN_POINT ( 'NONE',  ( -4.021760009708001959, 12.12704307397999770, 2.703375033665003091 ) ) ;
#7737=CARTESIAN_POINT ( 'NONE',  ( -24.72040429820999918, -9.265427320653000010, -5.484610141081000201 ) ) ;
#7740=ORIENTED_EDGE ( 'NONE', *, *, #12210, .T. ) ;
#7742=CARTESIAN_POINT ( 'NONE',  ( 4.811488400566996226, 14.48490630412999991, 3.723044770969999639 ) ) ;
#7746=CARTESIAN_POINT ( 'NONE',  ( -4.544340308300998998, 13.49051417780999884, -5.132142894851999593 ) ) ;
#7747=CARTESIAN_POINT ( 'NONE',  ( 14.54287674931000041, 7.516034287427999949, -7.591774476630000379 ) ) ;
#7748=CARTESIAN_POINT ( 'NONE',  ( -17.01752311569999776, -10.30819550402000040, 0.2320531645540999943 ) ) ;
#7750=EDGE_CURVE ( 'NONE', #2709, #3157, #12753, .T. ) ;
#7751=CARTESIAN_POINT ( 'NONE',  ( -11.00000000000000000, 1.359357947053999856E-14, 0.000000000000000000 ) ) ;
#7752=ORIENTED_EDGE ( 'NONE', *, *, #19016, .F. ) ;
#7755=CARTESIAN_POINT ( 'NONE',  ( 13.68447321782882220, -4.482739838237562502, 9.298704708330065571 ) ) ;
#7756=DIRECTION ( 'NONE',  ( -0.8193292504149890521, -0.5733232765328929448, -2.256442838868970230E-11 ) ) ;
#7760=CARTESIAN_POINT ( 'NONE',  ( 14.43361646158383849, -5.276216224350072537, 7.393200072960158131 ) ) ;
#7762=CARTESIAN_POINT ( 'NONE',  ( 24.50000000000000000, 10.82531754731000007, -6.250000000000000000 ) ) ;
#7765=ORIENTED_EDGE ( 'NONE', *, *, #16750, .F. ) ;
#7767=ORIENTED_EDGE ( 'NONE', *, *, #3900, .F. ) ;
#7769=CARTESIAN_POINT ( 'NONE',  ( 24.07420734439588372, 7.985988878874604069, 11.16786151310754960 ) ) ;
#7770=EDGE_CURVE ( 'NONE', #19823, #3092, #7803, .T. ) ;
#7773=CARTESIAN_POINT ( 'NONE',  ( 15.34725687895999791, -0.07841823125676000705, 11.03857397622999947 ) ) ;
#7777=ORIENTED_EDGE ( 'NONE', *, *, #17181, .F. ) ;
#7778=ORIENTED_EDGE ( 'NONE', *, *, #6046, .F. ) ;
#7779=CARTESIAN_POINT ( 'NONE',  ( -14.00000000000000178, 3.538282677300232937, -8.592818941365493401 ) ) ;
#7780=CARTESIAN_POINT ( 'NONE',  ( -11.10888721168999993, -1.831216772004999882, -15.46077555675999982 ) ) ;
#7782=CARTESIAN_POINT ( 'NONE',  ( -24.33938584176036102, -9.417644943810280722, -8.688014043590282398 ) ) ;
#7784=CARTESIAN_POINT ( 'NONE',  ( -20.11677904293000196, -5.490517660549000034, -7.911588380172000612 ) ) ;
#7785=CARTESIAN_POINT ( 'NONE',  ( -14.47826289458183702, 9.918718668892536172, 7.820280362110097805 ) ) ;
#7786=CARTESIAN_POINT ( 'NONE',  ( 6.147856022268394227, 14.14629814091362725, 0.2181625506079420684 ) ) ;
#7787=CARTESIAN_POINT ( 'NONE',  ( 15.84992198554521003, -10.31145118159957441, -0.9790302175844434185 ) ) ;
#7788=CARTESIAN_POINT ( 'NONE',  ( -17.69013761820000141, -8.094509216140998831, 7.584009060629000487 ) ) ;
#7791=CARTESIAN_POINT ( 'NONE',  ( -19.13034275784999849, -9.231395905450000328, -6.758791263612999423 ) ) ;
#7793=EDGE_LOOP ( 'NONE', ( #2888, #17047, #22717, #10824, #21960 ) ) ;
#7796=CARTESIAN_POINT ( 'NONE',  ( -19.44055257232857770, -10.47407731232025085, -0.6087492459073309270 ) ) ;
#7797=ORIENTED_EDGE ( 'NONE', *, *, #8518, .F. ) ;
#7798=CARTESIAN_POINT ( 'NONE',  ( -5.470390416431995639, 16.57655522344998644, 3.044249783594998426 ) ) ;
#7799=ADVANCED_FACE ( 'NONE', ( #19861 ), #6895, .T. ) ;
#7800=PLANE ( 'NONE',  #13381 ) ;
#7801=CARTESIAN_POINT ( 'NONE',  ( 16.90312642131000231, -9.179335210403001710, 3.217155551743000164 ) ) ;
#7803=B_SPLINE_CURVE_WITH_KNOTS ( 'NONE', 3,
 ( #14045, #1208, #6536, #12239, #13920, #8237, #21438, #19626, #21193, #17813, #8600, #21316, #15962, #1334, #23356, #6773, #14166, #4976 ),
 .UNSPECIFIED., .F., .F.,
 ( 4, 2, 2, 2, 2, 2, 2, 2, 4 ),
 ( 0.000000000000000000, 0.1250000000000000000, 0.2500000000000000000, 0.3750000000000000555, 0.5000000000000000000, 0.6250000000000000000, 0.7500000000000000000, 0.8750000000000000000, 1.000000000000000000 ),
 .UNSPECIFIED. ) ;
#7804=CARTESIAN_POINT ( 'NONE',  ( -6.100000173032002593, 16.42883599709998776, -1.007191989855000358 ) ) ;
#7806=AXIS2_PLACEMENT_3D ( 'NONE', #605, #8006, #15381 ) ;
#7808=FACE_OUTER_BOUND ( 'NONE', #15679, .T. ) ;
#7809=CARTESIAN_POINT ( 'NONE',  ( -12.48828895470000155, 6.965227931770999525, -5.686587078224999203 ) ) ;
#7810=CARTESIAN_POINT ( 'NONE',  ( -4.686906630868004520, 12.59381172247999636, 0.7274896323178006163 ) ) ;
#7811=CARTESIAN_POINT ( 'NONE',  ( 24.50000000000000000, 12.49999999999416822, 0.000000000000000000 ) ) ;
#7812=CARTESIAN_POINT ( 'NONE',  ( 11.99999999999999822, -4.176273271679210808, -8.652910017623161920 ) ) ;
#7814=FACE_BOUND ( 'NONE', #16123, .T. ) ;
#7819=( BOUNDED_SURFACE ( )  B_SPLINE_SURFACE ( 3, 3, ( 
 ( #21292, #6377, #13889, #10390, #17652, #2761 ),
 ( #19720, #10264, #4704, #12089, #8452, #6741 ),
 ( #23450, #15819, #19472, #15690, #8325, #14136 ),
 ( #23081, #19834, #23210, #21529, #6626, #4944 ) ),
 .UNSPECIFIED., .F., .F., .T. ) 
 B_SPLINE_SURFACE_WITH_KNOTS ( ( 4, 4 ),
 ( 4, 1, 1, 4 ),
 ( 0.000000000000000000, 1.000000000000000000 ),
 ( 0.01136608918049999972, 0.01481517776244999952, 0.02900961618256999927, 0.03401603006026000103 ),
 .UNSPECIFIED. ) 
 GEOMETRIC_REPRESENTATION_ITEM ( )  RATIONAL_B_SPLINE_SURFACE ( (
 ( 1.047527064320000090, 1.047527064320000090, 1.047527064320000090, 1.047527064320000090, 1.047527064320000090, 1.047527064320000090),
 ( 0.9841576452265000663, 0.9841576452265000663, 0.9841576452265000663, 0.9841576452265000663, 0.9841576452265000663, 0.9841576452265000663),
 ( 0.9841576452265000663, 0.9841576452265000663, 0.9841576452265000663, 0.9841576452265000663, 0.9841576452265000663, 0.9841576452265000663),
 ( 1.047527064320000090, 1.047527064320000090, 1.047527064320000090, 1.047527064320000090, 1.047527064320000090, 1.047527064320000090) ) ) 
 REPRESENTATION_ITEM ( '' )  SURFACE ( )  );
#7821=EDGE_LOOP ( 'NONE', ( #4138, #17335 ) ) ;
#7822=CARTESIAN_POINT ( 'NONE',  ( -18.29953743917332787, -9.140883910219043784, -1.196665853474646823 ) ) ;
#7823=CARTESIAN_POINT ( 'NONE',  ( 1.547176311163561024, 12.88373697569958232, -6.507343160275748772 ) ) ;
#7824=B_SPLINE_CURVE_WITH_KNOTS ( 'NONE', 3,
 ( #12861, #1964, #9468, #20261, #11410, #369, #16844, #9348, #11052, #18435, #15135, #247, #5366, #1846, #12756, #3783, #16722, #10938 ),
 .UNSPECIFIED., .F., .F.,
 ( 4, 2, 2, 2, 2, 2, 2, 2, 4 ),
 ( 0.000000000000000000, 0.1250000000000000555, 0.2500000000000000555, 0.3750000000000000555, 0.5000000000000000000, 0.6249999999999998890, 0.7500000000000000000, 0.8750000000000000000, 1.000000000000000000 ),
 .UNSPECIFIED. ) ;
#7825=CARTESIAN_POINT ( 'NONE',  ( -22.59894979209085619, -5.689294951490594165, -8.900361714202414731 ) ) ;
#7830=CARTESIAN_POINT ( 'NONE',  ( -19.33112391592212020, -10.16448900941933253, 2.551422195813828342 ) ) ;
#7831=LINE ( 'NONE', #18968, #9189 ) ;
#7834=EDGE_CURVE ( 'NONE', #6411, #14911, #14182, .T. ) ;
#7837=CARTESIAN_POINT ( 'NONE',  ( 14.65256424931000190, 9.798150841947000700, -4.264230833847999946 ) ) ;
#7839=CARTESIAN_POINT ( 'NONE',  ( 22.72083333333331367, 8.086270432886472292, -4.660780108671074728 ) ) ;
#7840=B_SPLINE_CURVE_WITH_KNOTS ( 'NONE', 3,
 ( #17613, #23167, #13971, #2959, #1733, #20149, #10706, #14341, #16010, #18099, #16134, #19912 ),
 .UNSPECIFIED., .F., .F.,
 ( 4, 1, 1, 1, 1, 2, 2, 4 ),
 ( 0.000000000000000000, 0.2500000000000007772, 0.3750000000000009437, 0.4375000000000009992, 0.4687500000000009437, 0.4843750000000008327, 0.5000000000000006661, 1.000000000000000000 ),
 .UNSPECIFIED. ) ;
#7841=CARTESIAN_POINT ( 'NONE',  ( 16.74989037305999773, 8.450119865360001370, -6.801369492786998983 ) ) ;
#7845=CARTESIAN_POINT ( 'NONE',  ( 24.12539877769000185, -5.296127428040000140, -8.219271541286000016 ) ) ;
#7846=B_SPLINE_SURFACE_WITH_KNOTS ( 'NONE', 3, 3, ( 
 ( #19324, #11814, #12510, #5127, #8180, #23645, #21134, #6353, #18082, #18208, #15664, #7052, #12627, #19191, #2601, #13736, #17382, #19895, #4675, #780, #4545, #3433, #12060, #14434, #23185, #15549, #9993, #21830, #22936, #21264, #17504, #1609, #2733, #14329, #3312 ),
 ( #10692, #11939, #10115, #10818, #898, #1488, #8300, #8882, #16365, #21717, #6478, #13861, #20012, #19446, #2854, #5242, #15793, #10236, #8995, #17628, #23754, #1022, #8425, #6933, #16252, #7158, #21011, #4423, #5699, #13085, #4003, #10928, #11400, #14668, #18769 ),
 ( #22062, #1835, #9221, #7638, #16478, #21943, #20485, #2179, #9572, #1953, #18660, #5471, #5353, #16958, #16601, #357, #18314, #16832, #22410, #16711, #3892, #12743, #1716, #14548, #11283, #20136, #9339, #3544, #5819, #9105, #11, #7394, #3771, #23868, #7275 ),
 ( #13201, #12966, #12853, #2066, #20249, #20594, #14777, #235, #3655, #5584, #22284, #11041, #22173, #20362, #18424, #11160, #18546, #123, #9458, #7510, #14893, #12000, #5929, #21195, #4249, #471, #2669, #11638, #6045, #13314, #17445, #19384, #20837, #11753, #7874 ) ),
 .UNSPECIFIED., .F., .F., .F.,
 ( 4, 4 ),
 ( 4, 1, 1, 1, 1, 1, 1, 1, 1, 1, 1, 1, 1, 1, 1, 1, 1, 1, 1, 1, 1, 1, 1, 1, 1, 1, 1, 1, 1, 1, 1, 1, 4 ),
 ( -0.6000240009599999702, 1.600024000959999970 ),
 ( 0.1465850610777999774, 0.1737772037394999802, 0.2009693464012999864, 0.2281614890629999892, 0.2553536317247000476, 0.2825457743865000260, 0.3097379170481999733, 0.3369300597100000072, 0.3641222023717000100, 0.3913143450334000129, 0.4185064876951999913, 0.4456986303568999941, 0.4728907730185999969, 0.5000829156803999753, 0.5272750583420999781, 0.5544672010039000121, 0.5816593436656000149, 0.6088514863273000177, 0.6360436289891000516, 0.6632357716507999434, 0.6904279143125000573, 0.7176200569742999802, 0.7448121996359999830, 0.7720043422976999858, 0.7991964849595000198, 0.8263886276212000226, 0.8535807702829999455, 0.8807729129446999483, 0.9079650556064000622, 0.9351571982681999851, 0.9623493409299000989, 0.9895414835915999907, 1.016733626253000011 ),
 .UNSPECIFIED. ) ;
#7848=ORIENTED_EDGE ( 'NONE', *, *, #15366, .F. ) ;
#7851=CARTESIAN_POINT ( 'NONE',  ( 0.8254538522422999458, 11.46557405689998710, 4.793380782510001659 ) ) ;
#7853=CARTESIAN_POINT ( 'NONE',  ( -19.95111026805999899, 7.370637296965999674, 8.231908711352000196 ) ) ;
#7858=CARTESIAN_POINT ( 'NONE',  ( -0.6273549637530023704, 11.57490430900510248, 4.750118582288012981 ) ) ;
#7860=CARTESIAN_POINT ( 'NONE',  ( -3.793527413694002703, 13.19029577252999097, 5.954828092150002306 ) ) ;
#7862=CARTESIAN_POINT ( 'NONE',  ( 16.95600174931000126, 3.031816831187000183, 10.30986099653000032 ) ) ;
#7863=EDGE_CURVE ( 'NONE', #3365, #14211, #5758, .T. ) ;
#7864=CARTESIAN_POINT ( 'NONE',  ( -16.40813207178999988, 5.092047131649000136, -8.946165747030999427 ) ) ;
#7865=CARTESIAN_POINT ( 'NONE',  ( 14.68293875730999964, -5.746474821545000111, 7.132383943660999925 ) ) ;
#7867=CARTESIAN_POINT ( 'NONE',  ( -14.47826287373907128, -1.813202974726752625, 12.50000251923937000 ) ) ;
#7868=EDGE_LOOP ( 'NONE', ( #12549, #8167 ) ) ;
#7871=CARTESIAN_POINT ( 'NONE',  ( 14.28671968858128771, -5.872878552574734456, -8.509277291877729965 ) ) ;
#7873=CARTESIAN_POINT ( 'NONE',  ( -4.752114190998003806, 13.48439568903999053, -5.196290741126996515 ) ) ;
#7874=CARTESIAN_POINT ( 'NONE',  ( 19.05934864702000198, 2.169758708643000134, 10.21046665093999906 ) ) ;
#7877=CARTESIAN_POINT ( 'NONE',  ( 11.85409292833783468, 4.507814091383394839, 12.50002426122780186 ) ) ;
#7880=CARTESIAN_POINT ( 'NONE',  ( -6.149942199219999850, 16.31029674404999952, 1.000000882129999935 ) ) ;
#7881=CARTESIAN_POINT ( 'NONE',  ( -5.625000000000000000, 22.00000000000000000, 0.000000000000000000 ) ) ;
#7882=ORIENTED_EDGE ( 'NONE', *, *, #2236, .T. ) ;
#7885=ORIENTED_EDGE ( 'NONE', *, *, #14408, .T. ) ;
#7890=VERTEX_POINT ( 'NONE', #16887 ) ;
#7891=CARTESIAN_POINT ( 'NONE',  ( 17.29838745430000202, 0.2858153280860000200, 11.08860699072000067 ) ) ;
#7892=CARTESIAN_POINT ( 'NONE',  ( -6.147641260848404343, 15.91672861095154801, 1.080128206638671928 ) ) ;
#7897=DIRECTION ( 'NONE',  ( -1.000000000000000000, 0.000000000000000000, 0.000000000000000000 ) ) ;
#7898=CARTESIAN_POINT ( 'NONE',  ( -12.30419030543999881, 4.907441476050999896, -14.08182655546000106 ) ) ;
#7902=CARTESIAN_POINT ( 'NONE',  ( -22.93116850624000236, 0.8725158193158999431, 10.19236064345000159 ) ) ;
#7903=CARTESIAN_POINT ( 'NONE',  ( -23.86847083084828114, 7.985699633921027107, 11.16836250006974396 ) ) ;
#7904=CARTESIAN_POINT ( 'NONE',  ( 6.214497071604325740, 13.81304699664710078, 1.115864161584470882 ) ) ;
#7905=CARTESIAN_POINT ( 'NONE',  ( 15.66809006278837835, -8.888817418492333644, 5.302822816444082932 ) ) ;
#7911=CARTESIAN_POINT ( 'NONE',  ( -19.22500490859999900, -8.822855456895000614, 5.347747867906999630 ) ) ;
#7919=CARTESIAN_POINT ( 'NONE',  ( -3.664365581929996285, 14.66068806201998420, 4.926677156548996628 ) ) ;
#7920=CARTESIAN_POINT ( 'NONE',  ( 18.07245833333331930, -5.613829312641806624, 7.305091642245316486 ) ) ;
#7922=CARTESIAN_POINT ( 'NONE',  ( 18.57487658530999752, 1.133029877492999882, 10.21722326572000128 ) ) ;
#7923=EDGE_CURVE ( 'NONE', #20918, #10557, #10986, .T. ) ;
#7924=ORIENTED_EDGE ( 'NONE', *, *, #12530, .T. ) ;
#7925=CARTESIAN_POINT ( 'NONE',  ( -5.985231639314995356, 16.12312885759999403, -0.9718497405647000820 ) ) ;
#7926=CARTESIAN_POINT ( 'NONE',  ( 24.00034722001000276, 7.216970193686000457, 11.92259671342000082 ) ) ;
#7927=ORIENTED_EDGE ( 'NONE', *, *, #7717, .F. ) ;
#7928=CARTESIAN_POINT ( 'NONE',  ( 0.000000000000000000, 20.10000000000000142, 0.000000000000000000 ) ) ;
#7929=LINE ( 'NONE', #11807, #1630 ) ;
#7930=CARTESIAN_POINT ( 'NONE',  ( 4.158710262565003646, 12.39730402461001013, 2.286416024636003019 ) ) ;
#7933=CARTESIAN_POINT ( 'NONE',  ( 18.05736718707166588, -1.162665227242019039, -10.34590908488389438 ) ) ;
#7934=CARTESIAN_POINT ( 'NONE',  ( 12.00000000000000000, 0.5465009267866380860, -9.295035738989342988 ) ) ;
#7936=CARTESIAN_POINT ( 'NONE',  ( -3.985645024478002174, 15.21034615980000737, -4.691483454359003602 ) ) ;
#7938=ADVANCED_FACE ( 'NONE', ( #4302 ), #9916, .F. ) ;
#7939=DIRECTION ( 'NONE',  ( -1.000000000000000000, 0.000000000000000000, 0.000000000000000000 ) ) ;
#7940=CARTESIAN_POINT ( 'NONE',  ( 5.155702020191999857, 13.97328941143999970, -4.008166040501000893 ) ) ;
#7944=CARTESIAN_POINT ( 'NONE',  ( 22.10697221064000217, -9.368869399783999796, 3.007899085511000159 ) ) ;
#7945=CARTESIAN_POINT ( 'NONE',  ( -0.5803961911334408752, 12.81517387975837785, -6.641171340469228745 ) ) ;
#7946=CARTESIAN_POINT ( 'NONE',  ( -23.53040576725368282, -6.468648380949139742, -6.731035015224344775 ) ) ;
#7947=CARTESIAN_POINT ( 'NONE',  ( -22.75960804221382716, -9.535639810683969486, -4.553883601656974811 ) ) ;
#7950=FACE_OUTER_BOUND ( 'NONE', #17124, .T. ) ;
#7952=CARTESIAN_POINT ( 'NONE',  ( -19.16365649254885994, -9.894903494359850171, -3.434324854208239852 ) ) ;
#7955=CARTESIAN_POINT ( 'NONE',  ( 11.50000000000000000, 0.000000000000000000, -7.000000000000000000 ) ) ;
#7956=ORIENTED_EDGE ( 'NONE', *, *, #4864, .T. ) ;
#7957=CARTESIAN_POINT ( 'NONE',  ( -15.91276253787999728, 9.079634562165001199, 0.000000000000000000 ) ) ;
#7958=CARTESIAN_POINT ( 'NONE',  ( 13.66537674931000090, -8.233391669162999804, 6.770876163316000174 ) ) ;
#7960=CARTESIAN_POINT ( 'NONE',  ( -14.95375200203000077, 10.81627527975999925, -3.353864774601000409 ) ) ;
#7962=CARTESIAN_POINT ( 'NONE',  ( 14.65046080086000124, 8.467099989590000320, -7.526153856646999429 ) ) ;
#7964=AXIS2_PLACEMENT_3D ( 'NONE', #13243, #20753, #18465 ) ;
#7966=CARTESIAN_POINT ( 'NONE',  ( 23.14589779687000259, -1.191954907644999784, 10.21085767065999939 ) ) ;
#7968=ORIENTED_EDGE ( 'NONE', *, *, #7178, .F. ) ;
#7971=CARTESIAN_POINT ( 'NONE',  ( -4.707944767739004277, 12.53013094992000021, 0.4102711938274001824 ) ) ;
#7973=CARTESIAN_POINT ( 'NONE',  ( -21.43440823118999816, -8.843504048032999165, 6.691333516387000913 ) ) ;
#7976=ORIENTED_EDGE ( 'NONE', *, *, #1724, .F. ) ;
#7978=LINE ( 'NONE', #17177, #7370 ) ;
#7983=CARTESIAN_POINT ( 'NONE',  ( 16.51725174930999884, 10.44001970777000032, -2.498676648948999990 ) ) ;
#7984=CARTESIAN_POINT ( 'NONE',  ( -14.98621963600000129, -7.639996621784999498, -6.839520901588999280 ) ) ;
#7985=CARTESIAN_POINT ( 'NONE',  ( 13.58606375731000071, 0.1873974521201000054, -9.128548663592997769 ) ) ;
#7986=CARTESIAN_POINT ( 'NONE',  ( -14.45529023502158417, -2.584742736866077806, 12.49997119546092428 ) ) ;
#7987=VERTEX_POINT ( 'NONE', #17135 ) ;
#7990=CARTESIAN_POINT ( 'NONE',  ( 14.24134250575724536, -7.125643292243364790, -7.467448625278665375 ) ) ;
#7991=CARTESIAN_POINT ( 'NONE',  ( 4.524261242948997896, 14.78625385561000982, -4.165603776964002414 ) ) ;
#7994=CARTESIAN_POINT ( 'NONE',  ( 11.36448692216853829, -2.758025466591909058, 12.49997558795521080 ) ) ;
#7995=CARTESIAN_POINT ( 'NONE',  ( 17.79316524073560046, -3.565549168114876100, -9.974336391710325600 ) ) ;
#7999=EDGE_CURVE ( 'NONE', #4782, #21708, #18781, .T. ) ;
#8001=ORIENTED_EDGE ( 'NONE', *, *, #2403, .F. ) ;
#8005=CARTESIAN_POINT ( 'NONE',  ( -2.443031855719502321, 11.73523197788490613, 4.158142541589644026 ) ) ;
#8006=DIRECTION ( 'NONE',  ( 1.000000000000000000, 0.000000000000000000, 0.000000000000000000 ) ) ;
#8009=CARTESIAN_POINT ( 'NONE',  ( 13.86982039523999966, -6.786930149467000462, 8.654887823694998872 ) ) ;
#8010=CARTESIAN_POINT ( 'NONE',  ( -20.68792035241834171, 2.624964421005299808, 8.884893743000107591 ) ) ;
#8016=CARTESIAN_POINT ( 'NONE',  ( -13.99999999999999822, 1.175534018597250263, -9.359874577866060363 ) ) ;
#8017=FACE_OUTER_BOUND ( 'NONE', #18150, .T. ) ;
#8018=CARTESIAN_POINT ( 'NONE',  ( -14.47826289458183524, -9.918718668888027779, -7.820280362116103667 ) ) ;
#8019=ORIENTED_EDGE ( 'NONE', *, *, #16502, .F. ) ;
#8020=CARTESIAN_POINT ( 'NONE',  ( -21.48771292778999964, 7.737897503461000248, -5.795162599746999987 ) ) ;
#8023=CARTESIAN_POINT ( 'NONE',  ( 15.36333275736410009, 0.2825445565885951749, 10.35592818220791145 ) ) ;
#8024=CARTESIAN_POINT ( 'NONE',  ( -18.16404412701000126, -2.121094635088999869, 10.90079736569000168 ) ) ;
#8025=DIRECTION ( 'NONE',  ( 1.000000000000000000, 0.000000000000000000, 0.000000000000000000 ) ) ;
#8026=CARTESIAN_POINT ( 'NONE',  ( -20.27843488810067285, 10.02134192589039330, 3.140444712618212009 ) ) ;
#8028=CARTESIAN_POINT ( 'NONE',  ( -16.44889015301999891, 10.17473773424000072, -3.711315847300999948 ) ) ;
#8031=ORIENTED_EDGE ( 'NONE', *, *, #2163, .T. ) ;
#8033=CARTESIAN_POINT ( 'NONE',  ( -18.39874231378647096, 9.042411196046327149, 5.258422072222084687 ) ) ;
#8035=ORIENTED_EDGE ( 'NONE', *, *, #21197, .F. ) ;
#8040=CARTESIAN_POINT ( 'NONE',  ( 15.58687642131000040, -1.771707419409999984, -9.528874100789000323 ) ) ;
#8041=B_SPLINE_CURVE_WITH_KNOTS ( 'NONE', 3,
 ( #286, #17369, #9504, #7687, #22685, #11683, #15177, #2230, #16878, #4054, #15538, #22805 ),
 .UNSPECIFIED., .F., .F.,
 ( 4, 1, 1, 1, 1, 2, 2, 4 ),
 ( 0.000000000000000000, 0.2499999999999964473, 0.3749999999999947820, 0.4374999999999936717, 0.4687499999999933387, 0.4843749999999933942, 0.4999999999999934497, 1.000000000000000000 ),
 .UNSPECIFIED. ) ;
#8045=DIRECTION ( 'NONE',  ( -0.1556330747009919968, -0.9878149351265710365, 5.988626934220810756E-08 ) ) ;
#8046=CARTESIAN_POINT ( 'NONE',  ( 23.99478584078000054, 6.383504859148000143, 12.40379814867000086 ) ) ;
#8050=DIRECTION ( 'NONE',  ( 0.000000000000000000, 1.000000000000000000, 0.000000000000000000 ) ) ;
#8051=CARTESIAN_POINT ( 'NONE',  ( 24.11771641471887406, 4.428067703116305154, 9.651354340895641926 ) ) ;
#8052=FACE_OUTER_BOUND ( 'NONE', #6392, .T. ) ;
#8053=CARTESIAN_POINT ( 'NONE',  ( 18.21437946870691960, 4.352035995711678318, -9.479931473404731079 ) ) ;
#8054=EDGE_CURVE ( 'NONE', #9910, #6464, #10712, .T. ) ;
#8055=CONICAL_SURFACE ( 'NONE', #3804, 12.68487026514999982, 0.6105562205522639951 ) ;
#8056=DIRECTION ( 'NONE',  ( 0.000000000000000000, -1.000000000000000000, 0.000000000000000000 ) ) ;
#8057=CARTESIAN_POINT ( 'NONE',  ( 19.45270603379666241, 8.931744951680411049, -2.400470103937684563 ) ) ;
#8058=CARTESIAN_POINT ( 'NONE',  ( -4.464533626733999228, 14.94938198047000455, -3.893093625067998165 ) ) ;
#8061=CARTESIAN_POINT ( 'NONE',  ( 5.415137083822752828, 14.57951453618345639, 2.868756701730457603 ) ) ;
#8063=ADVANCED_FACE ( 'NONE', ( #17381 ), #4422, .F. ) ;
#8066=EDGE_CURVE ( 'NONE', #5788, #15508, #16163, .T. ) ;
#8067=CARTESIAN_POINT ( 'NONE',  ( -16.82566243917332471, -4.584591771195801968, 7.954082539197118606 ) ) ;
#8068=CARTESIAN_POINT ( 'NONE',  ( 24.58366860467999970, -9.697657171452000568, 6.209474635623999816 ) ) ;
#8069=CARTESIAN_POINT ( 'NONE',  ( -3.174784089423522193, 13.14313549967478778, -5.966242404707048586 ) ) ;
#8072=CARTESIAN_POINT ( 'NONE',  ( -19.94808866505225708, 7.612438129746494475, 7.224177472218721974 ) ) ;
#8073=CARTESIAN_POINT ( 'NONE',  ( -3.644450799678000230, 14.33206891749000000, -4.922778709793999674 ) ) ;
#8077=CARTESIAN_POINT ( 'NONE',  ( -17.32151483542483561, -9.473612476238717051, -4.362928530524290416 ) ) ;
#8083=DIRECTION ( 'NONE',  ( 0.000000000000000000, 1.000000000000000000, 0.000000000000000000 ) ) ;
#8085=CARTESIAN_POINT ( 'NONE',  ( 17.71428936713000013, 9.125865291226999076, 0.000000000000000000 ) ) ;
#8086=VECTOR ( 'NONE', #9789, 1000.000000000000000 ) ;
#8087=CARTESIAN_POINT ( 'NONE',  ( 14.54287674931000041, 7.516034287427999949, -7.591774476630000379 ) ) ;
#8088=CARTESIAN_POINT ( 'NONE',  ( -22.61365783827999820, -1.438403498588999962, -11.09373300380999972 ) ) ;
#8089=CARTESIAN_POINT ( 'NONE',  ( -15.36001269797000113, -1.548705033035999934, -11.22934907313000075 ) ) ;
#8091=CARTESIAN_POINT ( 'NONE',  ( 19.05244494525999954, 10.34262564730999934, 0.7747601940386998898 ) ) ;
#8093=CARTESIAN_POINT ( 'NONE',  ( -24.50000000000000000, 7.216878364870000340, -12.50000000000000000 ) ) ;
#8094=CARTESIAN_POINT ( 'NONE',  ( 21.19835767317000119, 3.471603973022999945, 9.619727525801000212 ) ) ;
#8101=CARTESIAN_POINT ( 'NONE',  ( 4.204466630777001335, 12.26413482981000236, 2.286142766050001107 ) ) ;
#8102=LINE ( 'NONE', #15102, #15795 ) ;
#8103=CARTESIAN_POINT ( 'NONE',  ( -21.45487118009000227, -3.743657570342999730, 10.43929364024000073 ) ) ;
#8104=VERTEX_POINT ( 'NONE', #14077 ) ;
#8106=AXIS2_PLACEMENT_3D ( 'NONE', #14265, #23700, #3602 ) ;
#8107=ORIENTED_EDGE ( 'NONE', *, *, #1724, .T. ) ;
#8111=DIRECTION ( 'NONE',  ( 1.000000000000000000, 0.000000000000000000, 0.000000000000000000 ) ) ;
#8113=CARTESIAN_POINT ( 'NONE',  ( -14.25547362505000137, 7.466449067002999485, 11.77856001874999947 ) ) ;
#8114=AXIS2_PLACEMENT_3D ( 'NONE', #5886, #9882, #11592 ) ;
#8115=CARTESIAN_POINT ( 'NONE',  ( -13.76743754818000021, -2.422432655768999687, 9.928996171009998761 ) ) ;
#8117=CARTESIAN_POINT ( 'NONE',  ( 13.03762625731000036, -8.686210121801000383, 2.766264305181999728 ) ) ;
#8120=CARTESIAN_POINT ( 'NONE',  ( 18.99957840953792854, -6.685677144414598594, 8.077138694963919008 ) ) ;
#8121=CARTESIAN_POINT ( 'NONE',  ( -4.900699999999999612, 1.284663064832999817E-14, 0.000000000000000000 ) ) ;
#8123=CARTESIAN_POINT ( 'NONE',  ( 13.54165762163843212, 0.5435700620289271034, 10.30418047178718943 ) ) ;
#8125=CARTESIAN_POINT ( 'NONE',  ( 4.270538739245997029, 13.49097647299000791, -4.885090785149001746 ) ) ;
#8128=CARTESIAN_POINT ( 'NONE',  ( 11.78693030655488982, -4.312506568626711889, 12.49999836761128869 ) ) ;
#8129=DIRECTION ( 'NONE',  ( 0.000000000000000000, 1.000000000000000000, 0.000000000000000000 ) ) ;
#8130=DIRECTION ( 'NONE',  ( 0.000000000000000000, 1.000000000000000000, 0.000000000000000000 ) ) ;
#8131=CARTESIAN_POINT ( 'NONE',  ( -21.43624577250665197, 2.413793474093852698, -8.981321659912415711 ) ) ;
#8134=DIRECTION ( 'NONE',  ( -1.000000000000000000, 0.000000000000000000, 0.000000000000000000 ) ) ;
#8137=DIRECTION ( 'NONE',  ( -6.134662446597347369E-06, -0.9780939470516456513, 0.2081639514980881955 ) ) ;
#8139=DIRECTION ( 'NONE',  ( 0.000000000000000000, 1.000000000000000000, 0.000000000000000000 ) ) ;
#8140=CARTESIAN_POINT ( 'NONE',  ( -6.331662004670999266, 15.27947543293999821, -1.623597805356998602 ) ) ;
#8142=ORIENTED_EDGE ( 'NONE', *, *, #10113, .T. ) ;
#8143=ORIENTED_EDGE ( 'NONE', *, *, #1275, .F. ) ;
#8144=CARTESIAN_POINT ( 'NONE',  ( -14.00000000000000000, 1.110052840749007119, -9.371533619972057139 ) ) ;
#8146=CARTESIAN_POINT ( 'NONE',  ( -24.36724102300192740, -9.545677019768170624, -8.466242377946848308 ) ) ;
#8148=ORIENTED_EDGE ( 'NONE', *, *, #11874, .T. ) ;
#8149=CARTESIAN_POINT ( 'NONE',  ( -19.08857862928000060, 1.783951728274999926, 9.434913288203000903 ) ) ;
#8151=CARTESIAN_POINT ( 'NONE',  ( 6.233508746500216802, 13.72128517286145666, 1.472007961487105554 ) ) ;
#8152=CARTESIAN_POINT ( 'NONE',  ( 15.78996759782221737, -10.28928894160047314, 1.185823107492882666 ) ) ;
#8153=CARTESIAN_POINT ( 'NONE',  ( -16.71873760674999687, 9.784722624912999933, 5.167966991771000274 ) ) ;
#8155=CARTESIAN_POINT ( 'NONE',  ( -20.43284564258691560, 10.22652009526272110, -2.407089174038743451 ) ) ;
#8156=CARTESIAN_POINT ( 'NONE',  ( -13.10414243475000085, 9.447148007457000674, -4.942668164112999918 ) ) ;
#8160=CARTESIAN_POINT ( 'NONE',  ( -15.85209501512817987, -10.37091023683542801, 0.7487072676850166086 ) ) ;
#8163=CARTESIAN_POINT ( 'NONE',  ( 6.067719036437005720, 14.08021635583998155, -0.4562290550031999348 ) ) ;
#8166=CARTESIAN_POINT ( 'NONE',  ( 11.52843892131000025, -9.307182416847998851, 0.9706197651944000748 ) ) ;
#8167=ORIENTED_EDGE ( 'NONE', *, *, #14699, .F. ) ;
#8170=DIRECTION ( 'NONE',  ( 0.000000000000000000, 1.000000000000000000, 0.000000000000000000 ) ) ;
#8173=DIRECTION ( 'NONE',  ( -1.000000000000000000, 0.000000000000000000, 0.000000000000000000 ) ) ;
#8175=CARTESIAN_POINT ( 'NONE',  ( -23.19747332303477449, 9.265518480805006618, -0.8872243700272733902 ) ) ;
#8177=CARTESIAN_POINT ( 'NONE',  ( 18.32885411205448989, 7.626691132225033698, -7.100304570260450809 ) ) ;
#8178=CARTESIAN_POINT ( 'NONE',  ( 12.00000000000000178, -5.850718947441217566, -7.765274011324477144 ) ) ;
#8179=CARTESIAN_POINT ( 'NONE',  ( -14.49454883410026262, 11.27877807214811412, -5.464517788383438379 ) ) ;
#8180=CARTESIAN_POINT ( 'NONE',  ( 23.94234578240000033, 6.585182621219000332, 9.182389591044998411 ) ) ;
#8184=EDGE_CURVE ( 'NONE', #259, #14234, #11906, .T. ) ;
#8187=CARTESIAN_POINT ( 'NONE',  ( 18.92682980101000112, -9.687490077531000665, 4.826695779770999728 ) ) ;
#8188=CARTESIAN_POINT ( 'NONE',  ( 4.308859103450683570, 13.42278743254423468, -5.306801479098574248 ) ) ;
#8189=CARTESIAN_POINT ( 'NONE',  ( -23.66575074361468012, -9.444067616000523913, -0.7617870456259082657 ) ) ;
#8190=CARTESIAN_POINT ( 'NONE',  ( -20.05519416513632791, 9.717599291601674238, 3.967186786816359501 ) ) ;
#8191=CARTESIAN_POINT ( 'NONE',  ( 4.906142749732728348, 14.36517199318403648, 3.820454354895810312 ) ) ;
#8194=EDGE_CURVE ( 'NONE', #18434, #9620, #5204, .T. ) ;
#8195=CARTESIAN_POINT ( 'NONE',  ( -18.49378679904955902, 9.238542528155839761, -4.896975808983531131 ) ) ;
#8196=AXIS2_PLACEMENT_3D ( 'NONE', #1016, #14347, #17621 ) ;
#8197=CARTESIAN_POINT ( 'NONE',  ( -12.50000000000000000, 10.59999999999999964, 0.000000000000000000 ) ) ;
#8200=CARTESIAN_POINT ( 'NONE',  ( -14.06668704121266877, 9.028294978683996774, 1.058664089371861072 ) ) ;
#8204=CARTESIAN_POINT ( 'NONE',  ( 18.05287674931000197, 3.913226583351999910, -10.03953908883999979 ) ) ;
#8205=CARTESIAN_POINT ( 'NONE',  ( -22.29248446835000053, 9.305055704266001371, -6.193688370995000803 ) ) ;
#8206=CARTESIAN_POINT ( 'NONE',  ( -15.49211357277000012, 9.807665638945000097, -3.040989941390000340 ) ) ;
#8207=CARTESIAN_POINT ( 'NONE',  ( 21.96499999999999986, -9.234946903777000671, 0.000000000000000000 ) ) ;
#8208=CARTESIAN_POINT ( 'NONE',  ( 14.17744494526000132, -4.616554532313999815, 9.135639917857000469 ) ) ;
#8210=DIRECTION ( 'NONE',  ( 3.295974604355930324E-14, 1.000000000000000000, 0.000000000000000000 ) ) ;
#8211=CARTESIAN_POINT ( 'NONE',  ( 22.61475049040999963, 10.14616672796000074, -1.561894924173000243 ) ) ;
#8212=EDGE_CURVE ( 'NONE', #21190, #13265, #8522, .T. ) ;
#8213=CARTESIAN_POINT ( 'NONE',  ( 14.74679166666666674, -9.049713451602187320, -1.184477773038146831 ) ) ;
#8218=CARTESIAN_POINT ( 'NONE',  ( -4.509512206469002749, 12.45276351814001536, 1.421174038937999873 ) ) ;
#8223=CARTESIAN_POINT ( 'NONE',  ( -24.43506354683020731, 1.794296882888009259, -12.50003182001805868 ) ) ;
#8227=DIRECTION ( 'NONE',  ( 0.000000000000000000, 0.000000000000000000, 1.000000000000000000 ) ) ;
#8229=ADVANCED_FACE ( 'NONE', ( #19539 ), #19274, .F. ) ;
#8230=CARTESIAN_POINT ( 'NONE',  ( -17.70843032205999990, -8.525337246235000777, 7.569901604118999927 ) ) ;
#8232=CARTESIAN_POINT ( 'NONE',  ( 17.97356375731000000, 4.354347264933000616, 8.156255255558999551 ) ) ;
#8235=CARTESIAN_POINT ( 'NONE',  ( 18.97016382330117068, -5.824115247012692897, 8.721741054822143013 ) ) ;
#8236=DIRECTION ( 'NONE',  ( -1.000000000000000000, 0.000000000000000000, 0.000000000000000000 ) ) ;
#8237=CARTESIAN_POINT ( 'NONE',  ( -15.35178743917333577, 5.570923026602933703, 7.249260680724361805 ) ) ;
#8238=CARTESIAN_POINT ( 'NONE',  ( 2.459493327843513821, 13.98625086743180823, -5.610299872167907154 ) ) ;
#8240=CARTESIAN_POINT ( 'NONE',  ( 4.660957651440996052, 13.44002737945000625, -5.344716610742998419 ) ) ;
#8241=ADVANCED_FACE ( 'NONE', ( #14669 ), #18495, .T. ) ;
#8242=CARTESIAN_POINT ( 'NONE',  ( 11.18574820342087506, 1.750427062276028067, 12.50001947252512657 ) ) ;
#8244=CARTESIAN_POINT ( 'NONE',  ( 16.70595452243934886, 8.597629843446766174, 5.888985926558585327 ) ) ;
#8245=CARTESIAN_POINT ( 'NONE',  ( -14.25243324638999809, -13.93375672974000068, 0.8660254037843999608 ) ) ;
#8248=VERTEX_POINT ( 'NONE', #23869 ) ;
#8252=ORIENTED_EDGE ( 'NONE', *, *, #21817, .T. ) ;
#8253=PRODUCT_DEFINITION_SHAPE ( 'NONE', 'NONE',  #2198 ) ;
#8256=CARTESIAN_POINT ( 'NONE',  ( -3.967402132374007628, 13.32802061695993245, 5.543097348091962751 ) ) ;
#8257=CARTESIAN_POINT ( 'NONE',  ( 13.56906889882999856, 3.897513013205000210, 9.769895226178999081 ) ) ;
#8259=CARTESIAN_POINT ( 'NONE',  ( -6.518352534450451152, 15.19362126070188701, 2.752148752140309629 ) ) ;
#8260=ORIENTED_EDGE ( 'NONE', *, *, #19284, .T. ) ;
#8262=CARTESIAN_POINT ( 'NONE',  ( -13.99999999999999822, -1.124839544070808994, -9.501924303252614834 ) ) ;
#8266=ORIENTED_EDGE ( 'NONE', *, *, #13024, .T. ) ;
#8267=CARTESIAN_POINT ( 'NONE',  ( -22.51591334142999656, -4.717617794095999351, 8.470232659896000271 ) ) ;
#8269=CARTESIAN_POINT ( 'NONE',  ( 6.225893253368866453, 13.76032292270264357, 1.310517586579727389 ) ) ;
#8270=CARTESIAN_POINT ( 'NONE',  ( 15.10228429232423686, 8.300904500292098476, 6.166654416055827426 ) ) ;
#8271=CARTESIAN_POINT ( 'NONE',  ( -16.35741097668999799, -1.834076948381999861, 10.90256368047000102 ) ) ;
#8273=CARTESIAN_POINT ( 'NONE',  ( -20.58725639707271071, 7.574229625886635731, -7.286258484127539070 ) ) ;
#8274=CONICAL_SURFACE ( 'NONE', #11741, 9.152445778720998959, 0.02565634000431304615 ) ;
#8280=CARTESIAN_POINT ( 'NONE',  ( -17.15435783830565342, 1.323833875474687449, -10.33990276428391120 ) ) ;
#8281=EDGE_LOOP ( 'NONE', ( #21782, #16114, #12047 ) ) ;
#8282=CARTESIAN_POINT ( 'NONE',  ( 5.985422941791000540, 14.10050748988999558, -1.093390217131999353 ) ) ;
#8285=AXIS2_PLACEMENT_3D ( 'NONE', #10194, #23132, #11890 ) ;
#8286=CARTESIAN_POINT ( 'NONE',  ( 11.63812642131000175, -9.225545160481999574, -2.612645831888999570 ) ) ;
#8287=ORIENTED_EDGE ( 'NONE', *, *, #16205, .T. ) ;
#8288=CARTESIAN_POINT ( 'NONE',  ( -11.53829899291999794, 13.73725242156000093, 4.695599082074999764 ) ) ;
#8290=DIRECTION ( 'NONE',  ( 0.000000000000000000, 1.000000000000000000, 0.000000000000000000 ) ) ;
#8291=ORIENTED_EDGE ( 'NONE', *, *, #18417, .T. ) ;
#8292=DIRECTION ( 'NONE',  ( 0.000000000000000000, 1.000000000000000000, 0.000000000000000000 ) ) ;
#8293=CARTESIAN_POINT ( 'NONE',  ( 11.97297107869419897, 8.401874682668008631, 10.44762502811753180 ) ) ;
#8294=CIRCLE ( 'NONE', #21456, 10.59999999999999964 ) ;
#8297=CARTESIAN_POINT ( 'NONE',  ( 18.32220535724285426, 7.467675211945433489, -7.265422928116811896 ) ) ;
#8298=CARTESIAN_POINT ( 'NONE',  ( 12.00000000000000178, -4.492900714930693873, -8.522325693148694370 ) ) ;
#8299=CARTESIAN_POINT ( 'NONE',  ( -14.48875658296588753, -11.47331197282441195, 5.127631166282722752 ) ) ;
#8300=CARTESIAN_POINT ( 'NONE',  ( 23.72187345334999975, 10.71010072308000005, -3.583216764283999822 ) ) ;
#8302=CARTESIAN_POINT ( 'NONE',  ( -4.238876225541293508, 13.65117341093445447, -4.928522908460266194 ) ) ;
#8306=CARTESIAN_POINT ( 'NONE',  ( 22.35278487464000108, -9.885260220390001962, 3.173618722452000274 ) ) ;
#8307=CARTESIAN_POINT ( 'NONE',  ( 24.27152284451553044, 5.868235163808240173, 8.859447828480986331 ) ) ;
#8308=DIRECTION ( 'NONE',  ( 0.000000000000000000, 0.8660254037844288266, 0.5000000000000169864 ) ) ;
#8310=CARTESIAN_POINT ( 'NONE',  ( -20.26940516530154213, 9.853058826522531177, -3.638643124395733341 ) ) ;
#8312=CARTESIAN_POINT ( 'NONE',  ( 4.802957578314003051, 12.39660239800000241, -1.097938175032000307 ) ) ;
#8313=ORIENTED_EDGE ( 'NONE', *, *, #21412, .F. ) ;
#8314=CARTESIAN_POINT ( 'NONE',  ( -15.61892936444682434, -10.51941959121331038, -0.4572010232798279783 ) ) ;
#8318=CARTESIAN_POINT ( 'NONE',  ( -14.44633172592052439, -2.842506014212291987, -12.49999152948489822 ) ) ;
#8322=CARTESIAN_POINT ( 'NONE',  ( 12.32268908530999951, 2.255737295330999981, -9.860771559977997924 ) ) ;
#8323=CARTESIAN_POINT ( 'NONE',  ( -24.16753210339999924, 10.61389120149999954, 1.426895337364999961 ) ) ;
#8324=CARTESIAN_POINT ( 'NONE',  ( -19.35159018418999821, 4.683906058243999304, -9.258484707686999826 ) ) ;
#8325=CARTESIAN_POINT ( 'NONE',  ( -6.012804651762005292, 16.12591231748002585, 0.9718674177908998013 ) ) ;
#8326=CARTESIAN_POINT ( 'NONE',  ( 14.65187451745999958, -8.945410793015000195, 3.774998133422999835 ) ) ;
#8328=PLANE ( 'NONE',  #2294 ) ;
#8329=CARTESIAN_POINT ( 'NONE',  ( 24.38510397947347386, -9.380175294669545139, 8.753059805729597187 ) ) ;
#8331=CARTESIAN_POINT ( 'NONE',  ( 1.117133862669296374, 13.75138444617590494, 6.024180917838062754 ) ) ;
#8333=AXIS2_PLACEMENT_3D ( 'NONE', #4615, #19260, #8130 ) ;
#8334=CARTESIAN_POINT ( 'NONE',  ( 0.7982728184027000351, 11.57868860898998697, 4.682032524405000729 ) ) ;
#8336=ADVANCED_FACE ( 'NONE', ( #719 ), #8055, .F. ) ;
#8337=CARTESIAN_POINT ( 'NONE',  ( -24.58855165213000404, -0.7745665798849999950, -11.14856580036999922 ) ) ;
#8338=CARTESIAN_POINT ( 'NONE',  ( -6.838539683295000060, 15.31903503039000114, -1.878299264234999821 ) ) ;
#8341=CARTESIAN_POINT ( 'NONE',  ( 4.749997698793337442, 12.55003977317844566, 0.6286408267609251421 ) ) ;
#8342=CARTESIAN_POINT ( 'NONE',  ( -3.950437602410003191, 13.96089141542000966, 4.598127338115999940 ) ) ;
#8345=CIRCLE ( 'NONE', #3709, 7.000000000000000000 ) ;
#8348=CARTESIAN_POINT ( 'NONE',  ( -19.33347310582000134, -11.41588003357999881, 0.8201876405482001475 ) ) ;
#8349=AXIS2_PLACEMENT_3D ( 'NONE', #5508, #16523, #11439 ) ;
#8350=CARTESIAN_POINT ( 'NONE',  ( 13.14731375731000007, -9.095564035174998452, -0.6525005121013000009 ) ) ;
#8353=CARTESIAN_POINT ( 'NONE',  ( -22.73956496715868880, 8.318781100009532636, 4.101902574965182069 ) ) ;
#8356=CARTESIAN_POINT ( 'NONE',  ( -2.029239291679416635, 13.89258580265481235, -5.780038728331018838 ) ) ;
#8357=ORIENTED_EDGE ( 'NONE', *, *, #21465, .T. ) ;
#8361=CARTESIAN_POINT ( 'NONE',  ( -4.750000000000000000, 17.00000000000000000, 0.000000000000000000 ) ) ;
#8362=CARTESIAN_POINT ( 'NONE',  ( -23.96984461759712914, -0.1669632017148305891, 9.795628538752165326 ) ) ;
#8363=CARTESIAN_POINT ( 'NONE',  ( 14.89393665860769644, 8.649210458500339982, 5.983929458265615509 ) ) ;
#8364=CARTESIAN_POINT ( 'NONE',  ( -4.316401441148448370, 13.60025622239311183, 4.968485032647479649 ) ) ;
#8367=CARTESIAN_POINT ( 'NONE',  ( -24.49594166687720076, -10.56920153270462137, 6.693539566615260838 ) ) ;
#8369=CARTESIAN_POINT ( 'NONE',  ( -24.50000000000000000, -9.995791495354000133, -2.484784171996999635 ) ) ;
#8372=CARTESIAN_POINT ( 'NONE',  ( 11.32654380053060983, -9.540497826126133063, 8.475313523054548881 ) ) ;
#8377=CARTESIAN_POINT ( 'NONE',  ( -0.1474219169056815992, 12.80217572131716786, 6.666258639218459514 ) ) ;
#8378=DIRECTION ( 'NONE',  ( -1.000000000000000000, 0.000000000000000000, 0.000000000000000000 ) ) ;
#8379=CARTESIAN_POINT ( 'NONE',  ( -5.514248749579007125, 15.59707654392000009, -2.503767479304998211 ) ) ;
#8380=CARTESIAN_POINT ( 'NONE',  ( 24.43449445986660606, -2.200516184495610261, -12.50000000000000533 ) ) ;
#8381=EDGE_CURVE ( 'NONE', #8876, #23352, #4586, .T. ) ;
#8382=VECTOR ( 'NONE', #2902, 1000.000000000000114 ) ;
#8383=ORIENTED_EDGE ( 'NONE', *, *, #16502, .T. ) ;
#8387=LINE ( 'NONE', #1113, #10622 ) ;
#8388=ORIENTED_EDGE ( 'NONE', *, *, #14178, .F. ) ;
#8389=CARTESIAN_POINT ( 'NONE',  ( -19.33246705848000246, 1.882390077888999924, 9.955257576596000746 ) ) ;
#8393=CARTESIAN_POINT ( 'NONE',  ( 15.18172000152949863, 6.262995747030510429, 8.229460703160327739 ) ) ;
#8394=CARTESIAN_POINT ( 'NONE',  ( -16.53807429171999743, 4.901486691287000319, 9.915372413262000251 ) ) ;
#8395=DIRECTION ( 'NONE',  ( 0.000000000000000000, 0.9345904067404111615, 0.3557256971724040429 ) ) ;
#8396=CARTESIAN_POINT ( 'NONE',  ( -23.09420251723851436, 9.025778557754042808, 2.425918757917022717 ) ) ;
#8397=CARTESIAN_POINT ( 'NONE',  ( 3.119669807900996794, 11.98921412105999451, -3.586056005240998878 ) ) ;
#8398=CARTESIAN_POINT ( 'NONE',  ( -23.86804861157608570, -2.127868428593957528, -9.475271987823031594 ) ) ;
#8400=ORIENTED_EDGE ( 'NONE', *, *, #13967, .F. ) ;
#8403=CARTESIAN_POINT ( 'NONE',  ( -17.09647949060887839, 3.353307371398061676, -9.871714640295524035 ) ) ;
#8407=CARTESIAN_POINT ( 'NONE',  ( 5.267543338792999741, 14.75420436295999593, -3.146379728334001591 ) ) ;
#8411=CARTESIAN_POINT ( 'NONE',  ( 16.02562642131000104, 9.437180554902999674, -2.258696805882000280 ) ) ;
#8415=CARTESIAN_POINT ( 'NONE',  ( -5.194121241777001075, 0.000000000000000000, 0.000000000000000000 ) ) ;
#8416=VERTEX_POINT ( 'NONE', #8361 ) ;
#8418=CARTESIAN_POINT ( 'NONE',  ( 11.78924557932676009, 12.98180138941334505, 2.514846131752552338 ) ) ;
#8419=CARTESIAN_POINT ( 'NONE',  ( 24.50000000000000000, -10.82531754731000007, -6.250000000000000000 ) ) ;
#8421=CARTESIAN_POINT ( 'NONE',  ( 16.75103797537850525, 10.37411370639572006, 0.7522199250260709347 ) ) ;
#8422=TOROIDAL_SURFACE ( 'NONE', #23486, 14.44999999999999929, 3.850000000000000089 ) ;
#8424=CARTESIAN_POINT ( 'NONE',  ( -14.32799115970092885, -8.244301755411107990, 10.71998578050885342 ) ) ;
#8425=CARTESIAN_POINT ( 'NONE',  ( 20.78512204588000145, -5.382056054770000486, 9.836912527567999831 ) ) ;
#8431=CARTESIAN_POINT ( 'NONE',  ( -16.78787077250666471, -5.593750281246704148, 7.278551054825675770 ) ) ;
#8432=CARTESIAN_POINT ( 'NONE',  ( 21.77303207396000317, 7.050465134612999840, 7.599247105520000822 ) ) ;
#8435=B_SPLINE_CURVE_WITH_KNOTS ( 'NONE', 3,
 ( #7588, #5544, #1913, #9302, #11479 ),
 .UNSPECIFIED., .F., .F.,
 ( 4, 1, 4 ),
 ( 0.000000000000000000, 0.5000000000000000000, 1.000000000000000000 ),
 .UNSPECIFIED. ) ;
#8436=CARTESIAN_POINT ( 'NONE',  ( -20.83170904073196894, -7.016165085331945939, -7.830041573524264109 ) ) ;
#8437=CARTESIAN_POINT ( 'NONE',  ( 5.155714003469999973, 13.97328511022999997, 4.008150528822999270 ) ) ;
#8438=CONICAL_SURFACE ( 'NONE', #13444, 13.23032192316000000, 1.093540295016705466 ) ;
#8439=CARTESIAN_POINT ( 'NONE',  ( -4.939773666788001449, 12.51246242453999002, -0.3358430895244999825 ) ) ;
#8441=CARTESIAN_POINT ( 'NONE',  ( 11.99999999337999945, -7.499999993379000252, -2.839934906228000043E-09 ) ) ;
#8445=CARTESIAN_POINT ( 'NONE',  ( -23.75856372112281178, -13.93375672973999890, -3.388131789017201356E-17 ) ) ;
#8446=EDGE_LOOP ( 'NONE', ( #8400, #23749, #9086, #22443 ) ) ;
#8447=CARTESIAN_POINT ( 'NONE',  ( -18.90096560015167171, -5.540366411277957148, 7.367715573165199316 ) ) ;
#8448=CARTESIAN_POINT ( 'NONE',  ( 20.15099999999999980, -9.188396088570998543, 0.000000000000000000 ) ) ;
#8449=CARTESIAN_POINT ( 'NONE',  ( -19.88368419381999885, 1.085734961250999886, 11.05963058004999944 ) ) ;
#8450=ADVANCED_FACE ( 'NONE', ( #6541 ), #16552, .F. ) ;
#8451=CARTESIAN_POINT ( 'NONE',  ( -16.44171487522000064, -2.047536459366999573, 10.63496198587999864 ) ) ;
#8452=CARTESIAN_POINT ( 'NONE',  ( -6.041457567962996045, 15.84603627990999009, 1.061821870320000860 ) ) ;
#8453=CARTESIAN_POINT ( 'NONE',  ( 13.97431994526000132, 2.388644028223000149, 9.947419169996001287 ) ) ;
#8456=FACE_BOUND ( 'NONE', #10377, .T. ) ;
#8458=ORIENTED_EDGE ( 'NONE', *, *, #4339, .F. ) ;
#8459=CARTESIAN_POINT ( 'NONE',  ( 2.625751113930058001, 14.02718270572971093, 5.534244616725424670 ) ) ;
#8461=CARTESIAN_POINT ( 'NONE',  ( -19.73562077250665325, -1.201235969070628462, -9.177736638924091750 ) ) ;
#8464=CARTESIAN_POINT ( 'NONE',  ( -19.76356277338999945, -4.576085012665999763, 10.05190155114000028 ) ) ;
#8468=CARTESIAN_POINT ( 'NONE',  ( 15.82470603379664631, 8.841066507505132677, -2.376100949146749297 ) ) ;
#8469=CARTESIAN_POINT ( 'NONE',  ( 2.221750175568519836, 11.69191821601775771, -4.278409862297499089 ) ) ;
#8470=CARTESIAN_POINT ( 'NONE',  ( 0.8460338033015004644, 12.74950668468000714, 6.434662982751002680 ) ) ;
#8472=CARTESIAN_POINT ( 'NONE',  ( -14.25851234944000012, 6.966019679972999867, 12.06748306006000071 ) ) ;
#8473=CARTESIAN_POINT ( 'NONE',  ( -9.785194711695000436, -11.76217707223999831, -10.20000493973999944 ) ) ;
#8474=LINE ( 'NONE', #21555, #9237 ) ;
#8475=CARTESIAN_POINT ( 'NONE',  ( 16.24500142131000047, 8.402176888622001627, 4.865949138796000106 ) ) ;
#8478=ADVANCED_FACE ( 'NONE', ( #3042 ), #22734, .T. ) ;
#8479=VERTEX_POINT ( 'NONE', #21443 ) ;
#8480=CARTESIAN_POINT ( 'NONE',  ( -22.79626902222570095, 9.013103079406477036, 2.422627045988097194 ) ) ;
#8485=ORIENTED_EDGE ( 'NONE', *, *, #3025, .F. ) ;
#8489=CARTESIAN_POINT ( 'NONE',  ( -23.68078907432000335, -9.459496811531000304, -9.754788243598999975E-09 ) ) ;
#8490=CARTESIAN_POINT ( 'NONE',  ( 16.90109490777444279, 3.018130821474940273, 9.980111950484205963 ) ) ;
#8493=CARTESIAN_POINT ( 'NONE',  ( -21.88974577250666798, -8.992656465434315294, -2.416839618442697457 ) ) ;
#8497=DIRECTION ( 'NONE',  ( -1.000000000000000000, 0.000000000000000000, 0.000000000000000000 ) ) ;
#8498=CARTESIAN_POINT ( 'NONE',  ( -4.622974180749045203, 12.49837193735187668, -1.256033617784199530 ) ) ;
#8502=CARTESIAN_POINT ( 'NONE',  ( 5.574705741524002001, 14.65050554898000357, 2.561573290176999862 ) ) ;
#8503=CARTESIAN_POINT ( 'NONE',  ( -3.420654925002923896, 13.19662773910879139, 5.846983118698949156 ) ) ;
#8504=AXIS2_PLACEMENT_3D ( 'NONE', #10981, #23695, #9287 ) ;
#8505=CARTESIAN_POINT ( 'NONE',  ( 24.24531177150999994, 0.000000000000000000, 0.000000000000000000 ) ) ;
#8506=CARTESIAN_POINT ( 'NONE',  ( -20.99098205976333986, 9.020086631983017966, 2.148244413887738791 ) ) ;
#8508=ADVANCED_FACE ( 'NONE', ( #21689 ), #9214, .T. ) ;
#8512=DIRECTION ( 'NONE',  ( 0.000000000000000000, 0.8660254037844288266, 0.5000000000000169864 ) ) ;
#8513=APPLICATION_CONTEXT ( 'automotive_design' ) ;
#8517=CARTESIAN_POINT ( 'NONE',  ( -21.97548978617999893, 8.585592753479998507, -6.430155294164999980 ) ) ;
#8518=EDGE_CURVE ( 'NONE', #6561, #2989, #22249, .T. ) ;
#8520=CARTESIAN_POINT ( 'NONE',  ( 15.14773914344095296, 7.218886667550619585, 7.399516787738322776 ) ) ;
#8522=LINE ( 'NONE', #6445, #1087 ) ;
#8523=CARTESIAN_POINT ( 'NONE',  ( -12.00000000000000000, 1.371604415045000054E-14, 0.000000000000000000 ) ) ;
#8524=CARTESIAN_POINT ( 'NONE',  ( 2.325033434249998976, 11.79288290861998334, -4.153457988357001973 ) ) ;
#8525=ORIENTED_EDGE ( 'NONE', *, *, #11602, .T. ) ;
#8526=CARTESIAN_POINT ( 'NONE',  ( -23.99443888926111867, -4.202096428969419151, -8.897806421831953472 ) ) ;
#8531=CARTESIAN_POINT ( 'NONE',  ( -15.53376410279586928, -5.343199712982666938, -8.901057557536040221 ) ) ;
#8532=VECTOR ( 'NONE', #14517, 1000.000000000000227 ) ;
#8534=CARTESIAN_POINT ( 'NONE',  ( 4.820157802215999432, 14.15666734818999650, -4.018441328438997040 ) ) ;
#8535=CARTESIAN_POINT ( 'NONE',  ( 12.00000000000000355, -3.820038909443681074, -8.126794263889502545 ) ) ;
#8537=CARTESIAN_POINT ( 'NONE',  ( 18.71100174931000026, 5.082731606397000057, 9.520742961040999930 ) ) ;
#8539=FACE_OUTER_BOUND ( 'NONE', #6496, .T. ) ;
#8540=CARTESIAN_POINT ( 'NONE',  ( -24.50000000000000000, 1.524685264937999788E-14, 0.000000000000000000 ) ) ;
#8543=ORIENTED_EDGE ( 'NONE', *, *, #11697, .F. ) ;
#8545=CARTESIAN_POINT ( 'NONE',  ( 11.18529249867709474, 9.951874339556875171, 7.762889674103440996 ) ) ;
#8546=FACE_OUTER_BOUND ( 'NONE', #3019, .T. ) ;
#8548=CARTESIAN_POINT ( 'NONE',  ( 16.95399261017279713, 7.433768333657749139, 7.292702827057317982 ) ) ;
#8549=CARTESIAN_POINT ( 'NONE',  ( 11.99999999999999645, -5.748969532828861695, -7.831912490070881638 ) ) ;
#8551=CARTESIAN_POINT ( 'NONE',  ( -4.294719301634956743, 13.61382386032614100, -4.956612227401347326 ) ) ;
#8555=ORIENTED_EDGE ( 'NONE', *, *, #13218, .F. ) ;
#8556=CARTESIAN_POINT ( 'NONE',  ( 19.26076993769000367, -0.2568395230875999968, -10.29350776803000045 ) ) ;
#8557=CARTESIAN_POINT ( 'NONE',  ( 23.84592208957456805, 9.371304666163794650, -4.977627156037889300 ) ) ;
#8561=CARTESIAN_POINT ( 'NONE',  ( 0.000000000000000000, 22.00000000000000000, 0.000000000000000000 ) ) ;
#8563=CARTESIAN_POINT ( 'NONE',  ( -16.31671029517696780, 7.464073496724219048, 7.241521120158354030 ) ) ;
#8569=VERTEX_POINT ( 'NONE', #4857 ) ;
#8570=CARTESIAN_POINT ( 'NONE',  ( -15.91276253787999728, 9.079634562165001199, 0.000000000000000000 ) ) ;
#8572=CARTESIAN_POINT ( 'NONE',  ( -21.48955104351000145, -6.509886382642999791, 9.059949078605001205 ) ) ;
#8573=CARTESIAN_POINT ( 'NONE',  ( -13.39475965566999882, 9.583002289957001096, -2.464304261457999967 ) ) ;
#8574=CARTESIAN_POINT ( 'NONE',  ( 22.45629166666665455, 1.210375094748636471, -9.247554416229247565 ) ) ;
#8575=CARTESIAN_POINT ( 'NONE',  ( 14.44874951745999958, -4.376472204050999792, 8.660696927216999796 ) ) ;
#8577=CARTESIAN_POINT ( 'NONE',  ( 5.302302355349000074, 1.583778078195999810E-14, 0.000000000000000000 ) ) ;
#8578=CARTESIAN_POINT ( 'NONE',  ( 15.20029166666666320, 1.186001144903479299, -9.061351155403777113 ) ) ;
#8581=DIRECTION ( 'NONE',  ( 0.000000000000000000, -1.000000000000000000, 0.000000000000000000 ) ) ;
#8583=CARTESIAN_POINT ( 'NONE',  ( -19.28212077250665857, 9.166098935122516167, -1.199712597205310871 ) ) ;
#8585=CARTESIAN_POINT ( 'NONE',  ( -4.290394981784330319, 12.24616331916512024, 2.243719369978889322 ) ) ;
#8587=CARTESIAN_POINT ( 'NONE',  ( 15.86249770046331165, 9.078344667370600973, -1.188479485729073692 ) ) ;
#8588=CARTESIAN_POINT ( 'NONE',  ( -24.50000000000000000, 0.000000000000000000, -12.50000000000000000 ) ) ;
#8591=CARTESIAN_POINT ( 'NONE',  ( -14.25243324638999809, 6.216878364870000340, 12.50000000000000000 ) ) ;
#8593=CARTESIAN_POINT ( 'NONE',  ( -6.121054384213369559, 15.98142497799454809, -1.054679361892482570 ) ) ;
#8594=CARTESIAN_POINT ( 'NONE',  ( 16.90312642131000231, -9.179335210403001710, 3.217155551743000164 ) ) ;
#8596=AXIS2_PLACEMENT_3D ( 'NONE', #5870, #3591, #13141 ) ;
#8597=ORIENTED_EDGE ( 'NONE', *, *, #14380, .T. ) ;
#8598=LINE ( 'NONE', #4974, #5385 ) ;
#8600=CARTESIAN_POINT ( 'NONE',  ( -15.08724577250666776, -2.371147453209594413, 8.822634382605400560 ) ) ;
#8601=CARTESIAN_POINT ( 'NONE',  ( 3.839343825864000692, 14.39937964873592513, -4.778446983982809648 ) ) ;
#8605=CARTESIAN_POINT ( 'NONE',  ( 6.125000094578820331, 14.37502624149403552, 0.003861642916549869620 ) ) ;
#8606=CARTESIAN_POINT ( 'NONE',  ( 18.75008227645999881, 0.000000000000000000, 0.000000000000000000 ) ) ;
#8607=CARTESIAN_POINT ( 'NONE',  ( 15.28421742927796778, -4.014701272140648314, 9.733939712514935394 ) ) ;
#8608=CARTESIAN_POINT ( 'NONE',  ( -4.039176818549614190, 13.81482912323319390, 4.860923934985756034 ) ) ;
#8609=CARTESIAN_POINT ( 'NONE',  ( -4.695566743926001152, 12.35651713445999178, 1.468545715520999773 ) ) ;
#8611=ORIENTED_EDGE ( 'NONE', *, *, #10769, .F. ) ;
#8613=CARTESIAN_POINT ( 'NONE',  ( -0.6303327290807835270, 11.57525023284983234, -4.749574817190888254 ) ) ;
#8614=EDGE_LOOP ( 'NONE', ( #10136, #18868, #20205, #14687 ) ) ;
#8615=EDGE_CURVE ( 'NONE', #19206, #11018, #11229, .T. ) ;
#8617=CARTESIAN_POINT ( 'NONE',  ( 5.811180458947997174, 14.57924603701000521, 1.966607779951999202 ) ) ;
#8618=CARTESIAN_POINT ( 'NONE',  ( -0.4299899780664359628, 12.80997083806871828, 6.651184739924561384 ) ) ;
#8619=VECTOR ( 'NONE', #3426, 999.9999999999998863 ) ;
#8620=DIRECTION ( 'NONE',  ( -1.000000000000000000, 0.000000000000000000, 0.000000000000000000 ) ) ;
#8621=CARTESIAN_POINT ( 'NONE',  ( -5.398695926155999025, 16.20485681822998814, -2.910764035052000320 ) ) ;
#8627=EDGE_CURVE ( 'NONE', #12256, #4069, #283, .T. ) ;
#8628=CARTESIAN_POINT ( 'NONE',  ( -21.46138957935999869, 4.494222062375999194, 9.724264673970999695 ) ) ;
#8629=CARTESIAN_POINT ( 'NONE',  ( -4.750000000000000000, 17.00000000000000000, 0.000000000000000000 ) ) ;
#8630=CARTESIAN_POINT ( 'NONE',  ( 15.14749159410988888, 7.225522084805205303, 7.393037676230730604 ) ) ;
#8633=CARTESIAN_POINT ( 'NONE',  ( -12.24999999459000044, 1.554281285377000029E-14, 1.045589212608000028E-14 ) ) ;
#8634=CARTESIAN_POINT ( 'NONE',  ( 4.705295477336001397, 12.52895486067000164, -0.5082585761650004752 ) ) ;
#8636=VECTOR ( 'NONE', #12138, 1000.000000000000227 ) ;
#8637=CARTESIAN_POINT ( 'NONE',  ( -16.89590893017999562, 5.628454363070000355, -9.888856528401998247 ) ) ;
#8639=VERTEX_POINT ( 'NONE', #6108 ) ;
#8641=CARTESIAN_POINT ( 'NONE',  ( -14.92604145197964804, 10.36539917058194327, -0.05665573055404094643 ) ) ;
#8642=ORIENTED_EDGE ( 'NONE', *, *, #20575, .T. ) ;
#8645=CARTESIAN_POINT ( 'NONE',  ( 12.00000000000000178, 3.029763647141548777, -8.454266960972679712 ) ) ;
#8646=CARTESIAN_POINT ( 'NONE',  ( 13.79085740026999929, -10.35098683540000053, -3.711371709585999934 ) ) ;
#8648=CARTESIAN_POINT ( 'NONE',  ( 16.71018908530999880, 2.886377165994000293, 9.815223273854998709 ) ) ;
#8649=EDGE_LOOP ( 'NONE', ( #18958, #18609, #7777, #19839 ) ) ;
#8650=CARTESIAN_POINT ( 'NONE',  ( -10.72371899292000030, -11.98290193648999846, -8.195774483354998807 ) ) ;
#8651=CARTESIAN_POINT ( 'NONE',  ( 13.49999999999999645, 9.153938654719679491, -2.308705407138142540 ) ) ;
#8655=CARTESIAN_POINT ( 'NONE',  ( 12.06371966925979144, 13.38412994816690293, 1.818205397975688697 ) ) ;
#8656=CARTESIAN_POINT ( 'NONE',  ( 22.14693913686161864, 8.854242334004002402, 6.059094452743556403 ) ) ;
#8657=CARTESIAN_POINT ( 'NONE',  ( -14.00000000000000178, 7.941986550240724085, 4.595816627501706719 ) ) ;
#8658=CARTESIAN_POINT ( 'NONE',  ( 17.21630533617675596, -1.189482518535111666, 10.35523827938461494 ) ) ;
#8660=FACE_OUTER_BOUND ( 'NONE', #13852, .T. ) ;
#8663=CARTESIAN_POINT ( 'NONE',  ( -9.042815982636001948, 21.50000000000000000, 1.000000000000000000 ) ) ;
#8665=ORIENTED_EDGE ( 'NONE', *, *, #7018, .T. ) ;
#8667=CARTESIAN_POINT ( 'NONE',  ( 11.48478210364012675, 9.189386602319286723, -9.083340531634625847 ) ) ;
#8668=CARTESIAN_POINT ( 'NONE',  ( -4.544340308300998998, 13.49051417780999884, -5.132142894851999593 ) ) ;
#8671=VERTEX_POINT ( 'NONE', #6604 ) ;
#8672=EDGE_CURVE ( 'NONE', #11805, #3010, #21970, .T. ) ;
#8674=LINE ( 'NONE', #10374, #723 ) ;
#8677=ORIENTED_EDGE ( 'NONE', *, *, #13069, .T. ) ;
#8678=CARTESIAN_POINT ( 'NONE',  ( -14.61412482419791559, 9.602449638622033490, 3.892213435086770090 ) ) ;
#8680=VECTOR ( 'NONE', #14194, 1000.000000000000000 ) ;
#8683=CARTESIAN_POINT ( 'NONE',  ( -14.29262089130156532, -5.684429818840943227, -12.49999999999983658 ) ) ;
#8684=ORIENTED_EDGE ( 'NONE', *, *, #5853, .F. ) ;
#8687=EDGE_CURVE ( 'NONE', #20918, #20749, #5046, .T. ) ;
#8688=CARTESIAN_POINT ( 'NONE',  ( -4.096752709992895980, 15.04509484834502686, -4.553272908285909359 ) ) ;
#8690=CARTESIAN_POINT ( 'NONE',  ( -21.27697177397000061, -7.986013600915999433, -7.017649059653999544 ) ) ;
#8691=CARTESIAN_POINT ( 'NONE',  ( -14.00415069958000025, -7.656692200680000226, -7.563137310936999036 ) ) ;
#8693=CARTESIAN_POINT ( 'NONE',  ( 17.90187451746000136, 1.346331495725999972, 9.706975217397999955 ) ) ;
#8695=CARTESIAN_POINT ( 'NONE',  ( 19.69917122382999608, 1.762314512050999982, 8.897469563075999233 ) ) ;
#8698=CARTESIAN_POINT ( 'NONE',  ( 23.15628936713000030, 9.265517736846000219, 0.000000000000000000 ) ) ;
#8699=CARTESIAN_POINT ( 'NONE',  ( 0.9482458177890140671, 13.73472448189398953, 6.052214904559278352 ) ) ;
#8702=CARTESIAN_POINT ( 'NONE',  ( 24.50000000000000000, 10.82531754731000007, 6.250000000000000000 ) ) ;
#8703=CARTESIAN_POINT ( 'NONE',  ( -23.58604437744000037, -2.881458659258000043, 10.76926380789999982 ) ) ;
#8704=AXIS2_PLACEMENT_3D ( 'NONE', #6229, #21009, #4421 ) ;
#8705=CARTESIAN_POINT ( 'NONE',  ( -2.059536573449531005, 11.66298588225668809, 4.356317206734537706 ) ) ;
#8708=CARTESIAN_POINT ( 'NONE',  ( -24.46742986863962699, -1.281690452085482379, -12.50000620969121279 ) ) ;
#8709=CARTESIAN_POINT ( 'NONE',  ( 24.50000000000000000, 8.054858440593999802, 5.882793087032000656 ) ) ;
#8713=CARTESIAN_POINT ( 'NONE',  ( 13.50000000000000000, -10.65000000000000036, 0.000000000000000000 ) ) ;
#8714=B_SPLINE_CURVE_WITH_KNOTS ( 'NONE', 3,
 ( #19669, #3319, #16259, #23159, #6578 ),
 .UNSPECIFIED., .F., .F.,
 ( 4, 1, 4 ),
 ( 0.000000000000000000, 0.5000000000000000000, 1.000000000000000000 ),
 .UNSPECIFIED. ) ;
#8715=CARTESIAN_POINT ( 'NONE',  ( -6.102284808054873722, 16.03473069748903512, -1.037594296848572739 ) ) ;
#8716=CARTESIAN_POINT ( 'NONE',  ( 13.94156392131000111, 3.761510884484999817, -8.885545664707001023 ) ) ;
#8717=CARTESIAN_POINT ( 'NONE',  ( 18.52329378839496243, 10.39589489547862478, -0.7791414424835660935 ) ) ;
#8722=CARTESIAN_POINT ( 'NONE',  ( 2.893463358023975029, 14.09696930895991152, -5.402380196813071578 ) ) ;
#8724=B_SPLINE_CURVE_WITH_KNOTS ( 'NONE', 3,
 ( #5124, #14326, #13829, #12028, #12270, #2941 ),
 .UNSPECIFIED., .F., .F.,
 ( 4, 1, 1, 4 ),
 ( 0.000000000000000000, 0.3333333333333000081, 0.6666666666667000474, 1.000000000000000000 ),
 .UNSPECIFIED. ) ;
#8725=ORIENTED_EDGE ( 'NONE', *, *, #11360, .T. ) ;
#8729=CARTESIAN_POINT ( 'NONE',  ( 6.124999911758999716, 14.37502625872000195, -0.0001546258496581000123 ) ) ;
#8730=DIRECTION ( 'NONE',  ( 1.000000000000000000, 0.000000000000000000, 0.000000000000000000 ) ) ;
#8731=CARTESIAN_POINT ( 'NONE',  ( 15.73025259575829971, -9.722748992816393709, -3.694321794359110012 ) ) ;
#8733=CARTESIAN_POINT ( 'NONE',  ( 4.820392118736996245, 12.46745978434002033, 1.125972652643999261 ) ) ;
#8734=CARTESIAN_POINT ( 'NONE',  ( 19.60387270046332731, 8.935620381716546490, 2.401250916706160421 ) ) ;
#8735=ORIENTED_EDGE ( 'NONE', *, *, #20605, .T. ) ;
#8737=CARTESIAN_POINT ( 'NONE',  ( 23.99062354302999722, -6.216878364870000340, 12.50000000000000000 ) ) ;
#8738=VERTEX_POINT ( 'NONE', #19812 ) ;
#8740=CARTESIAN_POINT ( 'NONE',  ( 6.082313823887004922, 14.07671881673999970, 0.1102200398116000984 ) ) ;
#8741=CARTESIAN_POINT ( 'NONE',  ( 11.32654380052724719, -2.569587902914658439, -12.49997024370457588 ) ) ;
#8744=CARTESIAN_POINT ( 'NONE',  ( 13.50000000000000178, -1.374339424080784022, 10.20482255197515364 ) ) ;
#8746=CARTESIAN_POINT ( 'NONE',  ( -13.99999999999999822, -9.447486684801326362, -3.667138305862581493 ) ) ;
#8747=FACE_OUTER_BOUND ( 'NONE', #16728, .T. ) ;
#8748=CARTESIAN_POINT ( 'NONE',  ( -14.25243324638999809, 7.716878364870000340, 11.63397459621999985 ) ) ;
#8749=ORIENTED_EDGE ( 'NONE', *, *, #16073, .F. ) ;
#8750=CARTESIAN_POINT ( 'NONE',  ( -21.04613441456000089, -1.628084360272999964, 10.04728532985999934 ) ) ;
#8752=CARTESIAN_POINT ( 'NONE',  ( 14.89861762386097865, 10.30903294988296004, -0.6934164183026474415 ) ) ;
#8753=DIRECTION ( 'NONE',  ( 0.000000000000000000, 1.000000000000000000, 0.000000000000000000 ) ) ;
#8757=DIRECTION ( 'NONE',  ( 0.000000000000000000, 0.000000000000000000, -1.000000000000000000 ) ) ;
#8758=CARTESIAN_POINT ( 'NONE',  ( -4.297157081715999638, 12.44679617431000551, -2.013149773607997517 ) ) ;
#8759=ORIENTED_EDGE ( 'NONE', *, *, #13773, .T. ) ;
#8761=CARTESIAN_POINT ( 'NONE',  ( -21.43034587121331569, 8.981271358963487828, -2.413519275972843214 ) ) ;
#8763=EDGE_LOOP ( 'NONE', ( #23503, #17891, #15346, #11302 ) ) ;
#8766=ORIENTED_EDGE ( 'NONE', *, *, #6801, .T. ) ;
#8768=CARTESIAN_POINT ( 'NONE',  ( 17.39220833333331839, 9.117600057111475920, -1.193618004230062368 ) ) ;
#8770=CARTESIAN_POINT ( 'NONE',  ( 12.00000000000000355, -6.096004188759242659, -6.621033406203861382 ) ) ;
#8771=CARTESIAN_POINT ( 'NONE',  ( 18.12167894855999961, 10.39079625826000175, -3.946037309523999781 ) ) ;
#8773=ORIENTED_EDGE ( 'NONE', *, *, #7395, .T. ) ;
#8774=CIRCLE ( 'NONE', #22663, 13.77250448649000525 ) ;
#8775=CARTESIAN_POINT ( 'NONE',  ( -11.13100899292000001, -6.505098555691000151, 12.97861128357999938 ) ) ;
#8777=CARTESIAN_POINT ( 'NONE',  ( 13.49999999999999467, 9.320410925913344968, -1.763818356871138748 ) ) ;
#8781=CARTESIAN_POINT ( 'NONE',  ( 12.52688711657000020, 13.93375672974000068, 0.8660254037843999608 ) ) ;
#8782=CARTESIAN_POINT ( 'NONE',  ( 22.79406003406850445, -10.10745882294686560, 3.155071022957284477 ) ) ;
#8783=CARTESIAN_POINT ( 'NONE',  ( -14.00000000000000000, 6.631411874711850452, 6.523104844762785071 ) ) ;
#8784=CARTESIAN_POINT ( 'NONE',  ( 16.27407148470705067, -0.09565764253358223501, -10.36543647030853421 ) ) ;
#8785=CARTESIAN_POINT ( 'NONE',  ( -18.98882254156999849, -9.633796120427998488, -5.569900826749999645 ) ) ;
#8786=ADVANCED_FACE ( 'NONE', ( #18230 ), #6655, .F. ) ;
#8788=CONICAL_SURFACE ( 'NONE', #13391, 7.249999994833000727, 0.7853981633972997312 ) ;
#8789=CARTESIAN_POINT ( 'NONE',  ( -14.74233120679999942, -7.235896531433999357, -6.477854240395999774 ) ) ;
#8790=CONICAL_SURFACE ( 'NONE', #11871, 9.161549281532000322, 0.02565634000431304615 ) ;
#8793=CARTESIAN_POINT ( 'NONE',  ( 23.28665037521170333, 1.211924610667231450, 9.267172416750026898 ) ) ;
#8794=CARTESIAN_POINT ( 'NONE',  ( 20.71864993348000183, -2.045817035657000016, 11.22315166757000071 ) ) ;
#8795=CARTESIAN_POINT ( 'NONE',  ( 24.29989622817865325, 4.963438857751468092, 9.392559902825308171 ) ) ;
#8798=ORIENTED_EDGE ( 'NONE', *, *, #14150, .T. ) ;
#8800=CARTESIAN_POINT ( 'NONE',  ( 5.005054721376160032, 14.15887057945242411, -3.894303575199400846 ) ) ;
#8802=CARTESIAN_POINT ( 'NONE',  ( 2.434537302296001737, 11.69769071316999920, -4.313724188359998379 ) ) ;
#8804=CARTESIAN_POINT ( 'NONE',  ( 16.32825125730999716, -0.8629760640228999469, 9.162002845358001579 ) ) ;
#8806=CIRCLE ( 'NONE', #11888, 11.50000000000000000 ) ;
#8810=CARTESIAN_POINT ( 'NONE',  ( -12.25000000000000000, 1.374666032043000015E-14, 0.000000000000000000 ) ) ;
#8811=B_SPLINE_SURFACE_WITH_KNOTS ( 'NONE', 3, 3, ( 
 ( #13974, #21251, #4784, #23289, #14094, #21489, #3093, #10479, #19801, #21616, #12167, #23539, #4904, #3212, #23408, #12290, #5032, #10711, #16014, #17864, #19432, #8650, #6825, #17981, #1263, #8775, #6952, #14343, #885, #8288, #21734, #5147, #2842, #12527, #4663 ),
 ( #19916, #3561, #18221, #1622, #7069, #3450, #20153, #23890, #1740, #12868, #20268, #12984, #14794, #16381, #16730, #9010, #20387, #16620, #23773, #7413, #3913, #9244, #9125, #12644, #1853, #30, #22190, #10835, #7175, #9357, #5604, #14569, #21961, #20033, #16499 ),
 ( #12763, #3792, #7295, #22080, #14453, #14688, #7532, #5488, #3672, #18103, #21847, #10944, #11183, #8900, #18569, #11061, #22307, #5375, #1973, #5723, #18331, #18446, #140, #13109, #14912, #20506, #1508, #16267, #23659, #5260, #15712, #22658, #11988, #7898, #2204 ),
 ( #10286, #949, #13913, #16980, #20735, #22431, #8473, #6067, #23102, #9595, #4142, #14037, #2326, #9476, #12109, #18918, #9717, #383, #496, #7780, #17099, #23229, #15266, #17676, #15035, #15148, #19496, #5839, #13337, #11539, #13224, #2905, #2782, #21431, #2086 ) ),
 .UNSPECIFIED., .F., .F., .F.,
 ( 4, 4 ),
 ( 4, 1, 1, 1, 1, 1, 1, 1, 1, 1, 1, 1, 1, 1, 1, 1, 1, 1, 1, 1, 1, 1, 1, 1, 1, 1, 1, 1, 1, 1, 1, 1, 4 ),
 ( -0.1279891693871000047, 1.127989169386999890 ),
 ( -0.02000000000000000042, 0.01250000000000000069, 0.04499999999999999833, 0.07749999999999999944, 0.1100000000000000006, 0.1424999999999999878, 0.1749999999999999889, 0.2074999999999999900, 0.2399999999999999911, 0.2725000000000000200, 0.3049999999999999933, 0.3375000000000000222, 0.3699999999999999956, 0.4025000000000000244, 0.4349999999999999978, 0.4675000000000000266, 0.5000000000000000000, 0.5324999999999999734, 0.5649999999999999467, 0.5975000000000000311, 0.6300000000000000044, 0.6624999999999999778, 0.6949999999999999512, 0.7275000000000000355, 0.7600000000000000089, 0.7924999999999999822, 0.8249999999999999556, 0.8575000000000000400, 0.8900000000000000133, 0.9224999999999999867, 0.9549999999999999600, 0.9875000000000000444, 1.020000000000000018 ),
 .UNSPECIFIED. ) ;
#8816=CARTESIAN_POINT ( 'NONE',  ( -4.086025793108967186, 15.03144785070672995, -4.562901506959450515 ) ) ;
#8817=CARTESIAN_POINT ( 'NONE',  ( -23.15201940902000288, -1.306677278990999946, -10.07836265387000019 ) ) ;
#8819=CARTESIAN_POINT ( 'NONE',  ( -20.02703166550000091, -7.955150927529998306, -5.824612496301999620 ) ) ;
#8820=CARTESIAN_POINT ( 'NONE',  ( 18.94166666666666288, 4.611704135636504276, -8.001627034636081603 ) ) ;
#8821=EDGE_CURVE ( 'NONE', #2324, #2392, #3197, .T. ) ;
#8822=CARTESIAN_POINT ( 'NONE',  ( -23.59826610954376491, 2.101365615520589536, 10.37455059532381263 ) ) ;
#8824=CARTESIAN_POINT ( 'NONE',  ( -14.25699038479000080, 13.93375672974000068, 0.000000000000000000 ) ) ;
#8826=VERTEX_POINT ( 'NONE', #21107 ) ;
#8827=CARTESIAN_POINT ( 'NONE',  ( 12.00000000000000000, 0.000000000000000000, -7.500000000002917666 ) ) ;
#8830=VECTOR ( 'NONE', #1265, 1000.000000000000000 ) ;
#8831=CARTESIAN_POINT ( 'NONE',  ( 5.220711627940157307, 14.63818902522256771, -3.265501637091204223 ) ) ;
#8834=CARTESIAN_POINT ( 'NONE',  ( -3.861639638596443547, 12.10487486993750927, 2.911362801195074290 ) ) ;
#8835=ORIENTED_EDGE ( 'NONE', *, *, #20921, .F. ) ;
#8837=CARTESIAN_POINT ( 'NONE',  ( 4.718949164482028280, 12.40033812480790232, -1.110935410325604833 ) ) ;
#8838=DIRECTION ( 'NONE',  ( 0.000000000000000000, -1.000000000000000000, 0.000000000000000000 ) ) ;
#8843=CARTESIAN_POINT ( 'NONE',  ( 17.67093892131000032, 6.655236401869999874, -7.121176743063999837 ) ) ;
#8844=CARTESIAN_POINT ( 'NONE',  ( 18.70683015900163326, 8.814939528305005823, 5.571978707274588771 ) ) ;
#8848=CARTESIAN_POINT ( 'NONE',  ( -12.48665389351999977, 6.877253802972000507, -5.798544038930000255 ) ) ;
#8850=ORIENTED_EDGE ( 'NONE', *, *, #13375, .F. ) ;
#8851=CARTESIAN_POINT ( 'NONE',  ( -14.25699038479000080, -13.93375672974000068, 0.000000000000000000 ) ) ;
#8853=CARTESIAN_POINT ( 'NONE',  ( -24.33938584177814946, -12.23286334200125758, 3.811912743550009974 ) ) ;
#8856=PLANE ( 'NONE',  #16191 ) ;
#8857=CARTESIAN_POINT ( 'NONE',  ( -3.958969230662715333, 13.89523177694561973, 4.848950307086769662 ) ) ;
#8859=CARTESIAN_POINT ( 'NONE',  ( -12.25000000000000000, 8.148273666119854042, -12.70947166610607937 ) ) ;
#8860=CARTESIAN_POINT ( 'NONE',  ( 19.71724770046332154, 7.338844409646621436, 5.639768430530357257 ) ) ;
#8862=ADVANCED_FACE ( 'NONE', ( #17852 ), #23274, .F. ) ;
#8867=CARTESIAN_POINT ( 'NONE',  ( 5.983385025969996995, 14.53214776857002022, 1.355298851139999483 ) ) ;
#8868=CARTESIAN_POINT ( 'NONE',  ( 4.814391914611523937, 13.57103066341566766, 4.918137562955356756 ) ) ;
#8869=CARTESIAN_POINT ( 'NONE',  ( 6.243179582884000212, 13.63342035941999875, -1.952365010387999922 ) ) ;
#8871=VERTEX_POINT ( 'NONE', #4769 ) ;
#8874=LINE ( 'NONE', #10568, #8619 ) ;
#8876=VERTEX_POINT ( 'NONE', #2950 ) ;
#8877=CLOSED_SHELL ( 'NONE', ( #10670, #12078, #4942, #17211, #2113 ) ) ;
#8878=CARTESIAN_POINT ( 'NONE',  ( -21.29002284374999832, -1.712745750557999935, 10.57005027581000078 ) ) ;
#8880=CARTESIAN_POINT ( 'NONE',  ( 14.55000962749105931, 3.050471366525244310, -9.861052313355841648 ) ) ;
#8881=AXIS2_PLACEMENT_3D ( 'NONE', #14176, #23248, #10305 ) ;
#8882=CARTESIAN_POINT ( 'NONE',  ( 23.53832649037999758, 6.487047738608999303, -9.238512469485000267 ) ) ;
#8884=CARTESIAN_POINT ( 'NONE',  ( -24.00016455340000121, 1.715543117993999783E-14, 0.000000000000000000 ) ) ;
#8885=CARTESIAN_POINT ( 'NONE',  ( -3.150245644565998759, 12.00172895669998674, -3.533903776844997235 ) ) ;
#8887=CARTESIAN_POINT ( 'NONE',  ( -21.50592920454664636, 8.059125700889071098, -4.644844294440694021 ) ) ;
#8888=AXIS2_PLACEMENT_3D ( 'NONE', #19132, #11879, #23247 ) ;
#8891=CARTESIAN_POINT ( 'NONE',  ( 24.50000000000000000, -9.958777891625446799, 3.453140405739827390 ) ) ;
#8893=CONICAL_SURFACE ( 'NONE', #7713, 9.630770167580999797, 0.9419447502231289571 ) ;
#8894=ORIENTED_EDGE ( 'NONE', *, *, #3881, .F. ) ;
#8895=CARTESIAN_POINT ( 'NONE',  ( 17.42999999999999972, 9.118569865760999704, 0.000000000000000000 ) ) ;
#8896=FACE_OUTER_BOUND ( 'NONE', #23436, .T. ) ;
#8897=CARTESIAN_POINT ( 'NONE',  ( 13.24950470672999892, -0.4381588468272000214, 10.97213491105999950 ) ) ;
#8899=VERTEX_POINT ( 'NONE', #1127 ) ;
#8900=CARTESIAN_POINT ( 'NONE',  ( -10.30168113877000025, 9.808725055038999940, 11.63569968352999950 ) ) ;
#8901=CARTESIAN_POINT ( 'NONE',  ( 13.50000000000000000, 7.993555678485630089, -4.730236700590047860 ) ) ;
#8902=CARTESIAN_POINT ( 'NONE',  ( -14.29262082160975567, -13.66753291840124085, -1.327138571210202400 ) ) ;
#8905=CARTESIAN_POINT ( 'NONE',  ( 20.94094110115653962, -9.546404809872933939, 4.471938574268008892 ) ) ;
#8906=CARTESIAN_POINT ( 'NONE',  ( -14.00000000000000355, 2.181633025534562176, 9.406358577098494322 ) ) ;
#8907=CARTESIAN_POINT ( 'NONE',  ( 17.01556895440440798, 5.718620203982503369, 8.698992263909991252 ) ) ;
#8911=CARTESIAN_POINT ( 'NONE',  ( -12.37247714714999880, 8.083715232074000667, -4.229267010826999851 ) ) ;
#8913=ORIENTED_EDGE ( 'NONE', *, *, #16750, .T. ) ;
#8914=CARTESIAN_POINT ( 'NONE',  ( -24.27585716845300112, -3.329860787244067311, 12.49993117327242587 ) ) ;
#8915=CARTESIAN_POINT ( 'NONE',  ( 22.45790833551999910, 0.8992737871539999706, 11.42083163704999826 ) ) ;
#8916=CARTESIAN_POINT ( 'NONE',  ( 22.17189245347322313, 10.72406570084320698, -0.06313349674599283423 ) ) ;
#8919=LINE ( 'NONE', #1405, #14918 ) ;
#8921=CARTESIAN_POINT ( 'NONE',  ( 3.772394398227998380, 12.11624026657999131, -2.973371410456998376 ) ) ;
#8923=EDGE_CURVE ( 'NONE', #3365, #20695, #11843, .T. ) ;
#8924=CARTESIAN_POINT ( 'NONE',  ( 12.52688711657000020, -6.216878364870000340, -12.50000000000000000 ) ) ;
#8928=ORIENTED_EDGE ( 'NONE', *, *, #22063, .T. ) ;
#8930=CARTESIAN_POINT ( 'NONE',  ( -23.79436614888999912, -7.215319973546000298, 7.181436178667000902 ) ) ;
#8932=CARTESIAN_POINT ( 'NONE',  ( -15.55816401016000050, 8.955035067704001150, 3.817101925073999702 ) ) ;
#8933=CARTESIAN_POINT ( 'NONE',  ( 18.60154166666664821, -5.622352741887121752, -7.315769444643206221 ) ) ;
#8934=CARTESIAN_POINT ( 'NONE',  ( -24.16443887599344365, 8.804325591011858521, -5.901198901063593460 ) ) ;
#8936=CARTESIAN_POINT ( 'NONE',  ( -5.774423697881004180, 15.72625884058998302, 1.905284384892999228 ) ) ;
#8938=VERTEX_POINT ( 'NONE', #5475 ) ;
#8939=CARTESIAN_POINT ( 'NONE',  ( 23.19213215653367044, 9.263419914609070105, 1.127708713065163293 ) ) ;
#8942=EDGE_CURVE ( 'NONE', #1386, #4476, #18430, .T. ) ;
#8943=CARTESIAN_POINT ( 'NONE',  ( 5.925978167137946784, 14.42557216884380900, -1.550677319624406580 ) ) ;
#8946=CARTESIAN_POINT ( 'NONE',  ( 4.418282465362906919, 12.29075935838933020, 1.985689274626368572 ) ) ;
#8947=ORIENTED_EDGE ( 'NONE', *, *, #15869, .T. ) ;
#8948=CARTESIAN_POINT ( 'NONE',  ( 17.69454166666665529, 5.608048916488373337, 7.297156872939496886 ) ) ;
#8950=CARTESIAN_POINT ( 'NONE',  ( 4.761208897123116124, 12.41619411356198555, -0.9207184844910151211 ) ) ;
#8951=CARTESIAN_POINT ( 'NONE',  ( -10.58070998671075280, 15.47950041580538638, 1.445153319346881959 ) ) ;
#8955=CARTESIAN_POINT ( 'NONE',  ( -15.95055420454664841, 9.080604370815557047, -1.188521384907452294 ) ) ;
#8956=CARTESIAN_POINT ( 'NONE',  ( 18.00000142131000302, 9.258615172493000145, 3.074095935696000037 ) ) ;
#8957=CARTESIAN_POINT ( 'NONE',  ( 18.82474110796517053, 5.884666067428870662, 8.614044124011082104 ) ) ;
#8959=CARTESIAN_POINT ( 'NONE',  ( -24.50000000000000000, 2.324045842668999493E-14, 12.50000000000000000 ) ) ;
#8962=CARTESIAN_POINT ( 'NONE',  ( 13.50000000000000355, -8.015790134246481458, 6.051666939700164782 ) ) ;
#8965=CARTESIAN_POINT ( 'NONE',  ( 24.29098604190999922, 10.32447825566000077, 3.305036642305999806 ) ) ;
#8969=CARTESIAN_POINT ( 'NONE',  ( 3.419138964049998286, 12.01219122919000526, 3.585892243584002159 ) ) ;
#8970=CARTESIAN_POINT ( 'NONE',  ( -12.24999999999999822, 10.32537944888909642, -10.67953724782443814 ) ) ;
#8977=DIRECTION ( 'NONE',  ( 0.000000000000000000, 1.000000000000000000, 0.000000000000000000 ) ) ;
#8978=CARTESIAN_POINT ( 'NONE',  ( 11.18574820343433807, -1.750427062344837914, -12.50001947253043078 ) ) ;
#8981=CARTESIAN_POINT ( 'NONE',  ( -5.942997347608004688, 15.81517321836000178, -1.152667559718999923 ) ) ;
#8982=CIRCLE ( 'NONE', #6646, 5.625000000000000000 ) ;
#8983=CARTESIAN_POINT ( 'NONE',  ( 0.000000000000000000, 0.000000000000000000, 0.000000000000000000 ) ) ;
#8984=VERTEX_POINT ( 'NONE', #19901 ) ;
#8985=CARTESIAN_POINT ( 'NONE',  ( -14.74233120679999942, -7.235896531433999357, -6.477854240395999774 ) ) ;
#8988=ORIENTED_EDGE ( 'NONE', *, *, #17552, .T. ) ;
#8990=CARTESIAN_POINT ( 'NONE',  ( -10.82553598051486787, 15.36695194536291353, -1.671868630953385004 ) ) ;
#8992=CARTESIAN_POINT ( 'NONE',  ( 14.67988943935569957, 7.031391890844531645, -7.575081847691048864 ) ) ;
#8995=CARTESIAN_POINT ( 'NONE',  ( 21.51930989774999858, -1.098377462729000165, -11.17932485002999954 ) ) ;
#8997=CARTESIAN_POINT ( 'NONE',  ( 13.79014734960547450, 9.020246190001508069, -0.3553286354086955812 ) ) ;
#8998=CARTESIAN_POINT ( 'NONE',  ( -4.363055774502002215, 12.47547100499999395, -2.048634389234999631 ) ) ;
#9002=VECTOR ( 'NONE', #4877, 1000.000000000000000 ) ;
#9003=CARTESIAN_POINT ( 'NONE',  ( 24.50000000000000000, -8.246372141814999779, 6.625187740483999832 ) ) ;
#9006=CARTESIAN_POINT ( 'NONE',  ( 16.52299999999999969, -9.095294458157999529, 0.000000000000000000 ) ) ;
#9007=CARTESIAN_POINT ( 'NONE',  ( 18.75008227645999881, -9.152445778720998959, 0.000000000000000000 ) ) ;
#9008=CARTESIAN_POINT ( 'NONE',  ( 16.64424246484000136, 10.59610064161999965, 3.219381317545000343 ) ) ;
#9009=ORIENTED_EDGE ( 'NONE', *, *, #12093, .T. ) ;
#9010=CARTESIAN_POINT ( 'NONE',  ( -10.30905506584999998, 14.86577284560999956, 0.2581334465446999960 ) ) ;
#9011=CARTESIAN_POINT ( 'NONE',  ( 13.50000000000000000, 8.034926714834112360, -4.667990898080017992 ) ) ;
#9015=CARTESIAN_POINT ( 'NONE',  ( 21.67630575707568852, 5.728324180010714528, -9.603614269126266478 ) ) ;
#9016=AXIS2_PLACEMENT_3D ( 'NONE', #746, #1116, #17220 ) ;
#9017=CARTESIAN_POINT ( 'NONE',  ( -14.25243324638999809, -13.93375672974000068, 0.8660254037843999608 ) ) ;
#9018=CARTESIAN_POINT ( 'NONE',  ( 16.10201719184190949, -5.936034372256892233, -8.493431826325096523 ) ) ;
#9019=CARTESIAN_POINT ( 'NONE',  ( -18.60187077250666832, -5.622357932043938078, 7.315776198232815553 ) ) ;
#9020=CARTESIAN_POINT ( 'NONE',  ( -14.45529013989012057, -12.11766535962171965, 4.011530336787306084 ) ) ;
#9021=CARTESIAN_POINT ( 'NONE',  ( -12.91415807507000046, -6.873022849445000304, -6.789234046460999927 ) ) ;
#9023=ORIENTED_EDGE ( 'NONE', *, *, #23758, .T. ) ;
#9024=CARTESIAN_POINT ( 'NONE',  ( -23.74465998031000069, -6.216878364870000340, 12.50000000000000000 ) ) ;
#9025=CARTESIAN_POINT ( 'NONE',  ( 21.54767801288958395, -5.974488166519072330, -8.885303408042284801 ) ) ;
#9027=ORIENTED_EDGE ( 'NONE', *, *, #1252, .T. ) ;
#9029=CARTESIAN_POINT ( 'NONE',  ( 4.830315656668564550, 14.72903184301115687, -3.766121966294526668 ) ) ;
#9031=B_SPLINE_CURVE_WITH_KNOTS ( 'NONE', 3,
 ( #4528, #16009, #11919, #6585, #2838, #1377, #4657, #23284, #8770, #4778, #21611, #1139, #8535, #15893, #17486, #2716, #12285, #16133, #12162, #19675, #6697, #6821, #14089, #3087, #880, #12043, #6336, #10348, #5028, #19427, #10218, #14214, #23165, #13970, #17736, #10474, #17860, #8645, #23404, #12412, #19796, #13719, #1504, #20378, #5482, #20028 ),
 .UNSPECIFIED., .F., .F.,
 ( 4, 1, 1, 1, 2, 2, 1, 1, 1, 1, 1, 1, 2, 2, 1, 1, 1, 1, 1, 2, 2, 1, 1, 1, 2, 2, 1, 1, 1, 1, 1, 2, 2, 4 ),
 ( 0.000000000000000000, 0.1250000000000003608, 0.1875000000000006661, 0.2187500000000007494, 0.2343750000000008882, 0.2500000000000010547, 0.3750000000000022204, 0.4375000000000028311, 0.4687500000000032196, 0.4843750000000035527, 0.4921875000000037192, 0.4960937500000037748, 0.4980468750000037748, 0.5000000000000037748, 0.5625000000000025535, 0.5937500000000017764, 0.6093750000000015543, 0.6171875000000013323, 0.6210937500000012212, 0.6230468750000011102, 0.6250000000000009992, 0.6875000000000011102, 0.7187500000000012212, 0.7343750000000012212, 0.7421875000000012212, 0.7500000000000012212, 0.8125000000000014433, 0.8437500000000015543, 0.8593750000000015543, 0.8671875000000016653, 0.8710937500000016653, 0.8730468750000015543, 0.8750000000000014433, 1.000000000000000000 ),
 .UNSPECIFIED. ) ;
#9032=CARTESIAN_POINT ( 'NONE',  ( 4.257195002520998806, 12.20674677251999896, -2.334155036774002490 ) ) ;
#9033=ORIENTED_EDGE ( 'NONE', *, *, #6076, .T. ) ;
#9036=CARTESIAN_POINT ( 'NONE',  ( -5.319412312564031353, 16.04959412292968324, 3.038395077758344609 ) ) ;
#9039=ORIENTED_EDGE ( 'NONE', *, *, #18533, .F. ) ;
#9041=CARTESIAN_POINT ( 'NONE',  ( -20.90380581945999694, 9.909073374132001177, -1.964704235543000221 ) ) ;
#9042=CARTESIAN_POINT ( 'NONE',  ( -16.37068540204000300, -7.269710435383999858, -6.508117440121999664 ) ) ;
#9044=CARTESIAN_POINT ( 'NONE',  ( -23.67547148678552560, 4.768064527406466802, 9.453135388948583184 ) ) ;
#9049=ORIENTED_EDGE ( 'NONE', *, *, #19755, .F. ) ;
#9050=CARTESIAN_POINT ( 'NONE',  ( -17.65117920454668266, 8.886717484751601503, 2.388369308413305525 ) ) ;
#9051=CARTESIAN_POINT ( 'NONE',  ( -24.12232999016000079, 1.520060141252000183E-14, 0.000000000000000000 ) ) ;
#9054=B_SPLINE_CURVE_WITH_KNOTS ( 'NONE', 3,
 ( #19984, #23360, #6540, #1338, #23489, #3282, #10664, #8853, #21566, #6654, #6900, #10786, #23615, #10427 ),
 .UNSPECIFIED., .F., .F.,
 ( 4, 2, 2, 2, 2, 2, 4 ),
 ( 0.000000000000000000, 0.2499999999999999445, 0.3749999999999998890, 0.4999999999999998890, 0.6249999999999998890, 0.7499999999999997780, 1.000000000000000000 ),
 .UNSPECIFIED. ) ;
#9056=CARTESIAN_POINT ( 'NONE',  ( 4.069542469406499663, 12.17106568498275720, 2.629390757502099607 ) ) ;
#9058=CARTESIAN_POINT ( 'NONE',  ( -0.9155538765149698888, 11.51860325008744823, -4.724858359221649096 ) ) ;
#9059=EDGE_CURVE ( 'NONE', #9517, #10732, #10902, .T. ) ;
#9060=CARTESIAN_POINT ( 'NONE',  ( -11.04281598264000053, 15.31903517167999951, 1.878299281558999834 ) ) ;
#9064=LINE ( 'NONE', #18383, #15389 ) ;
#9065=CARTESIAN_POINT ( 'NONE',  ( 16.49081408530999937, 8.848325411959001130, 5.124349347825999601 ) ) ;
#9066=CARTESIAN_POINT ( 'NONE',  ( 18.78241513702097976, 7.121959644642507747, 7.638015814842760598 ) ) ;
#9069=AXIS2_PLACEMENT_3D ( 'NONE', #6854, #14249, #5173 ) ;
#9070=CARTESIAN_POINT ( 'NONE',  ( -12.47823091122000072, 7.040259760702999969, -5.593011138739999666 ) ) ;
#9071=CARTESIAN_POINT ( 'NONE',  ( 13.50000000000000355, -9.410104611735745195, -1.703795694468760447 ) ) ;
#9073=DIRECTION ( 'NONE',  ( -1.000000000000000000, 0.000000000000000000, 0.000000000000000000 ) ) ;
#9074=CARTESIAN_POINT ( 'NONE',  ( 23.66558326540000223, 6.907618760750000142, -9.009360667880999429 ) ) ;
#9076=CARTESIAN_POINT ( 'NONE',  ( -7.034000000000000696, 11.50000000000000000, 2.869609411205000113E-11 ) ) ;
#9077=CARTESIAN_POINT ( 'NONE',  ( 24.49999999999999645, -7.300324094424125221, 7.693460009872119088 ) ) ;
#9078=DIRECTION ( 'NONE',  ( 0.000000000000000000, -0.9999999999994555466, 1.043416718096953418E-06 ) ) ;
#9079=AXIS2_PLACEMENT_3D ( 'NONE', #6599, #12058, #4792 ) ;
#9080=CARTESIAN_POINT ( 'NONE',  ( -4.823016552992995365, 12.46847780471999734, 1.104821929769999933 ) ) ;
#9082=CARTESIAN_POINT ( 'NONE',  ( -22.97909504101000167, -8.290368976810999158, 7.428505582751999903 ) ) ;
#9086=ORIENTED_EDGE ( 'NONE', *, *, #6581, .F. ) ;
#9088=CARTESIAN_POINT ( 'NONE',  ( 6.027841067254001928, 13.76213909426999038, 1.750693181843999469 ) ) ;
#9090=CARTESIAN_POINT ( 'NONE',  ( 11.29022434644176975, -2.380282113944267586, -12.49997383652820560 ) ) ;
#9091=CARTESIAN_POINT ( 'NONE',  ( 13.21250000000000036, 0.000000000000000000, 0.000000000000000000 ) ) ;
#9092=CARTESIAN_POINT ( 'NONE',  ( -6.058172502568998752, 16.51671562621000788, -0.9499346773648004172 ) ) ;
#9093=CARTESIAN_POINT ( 'NONE',  ( 12.54206408531000072, 8.432320343758000547, -5.597842903599000053 ) ) ;
#9095=DIRECTION ( 'NONE',  ( -1.000000000000000000, 0.000000000000000000, 0.000000000000000000 ) ) ;
#9099=CARTESIAN_POINT ( 'NONE',  ( -23.75856372112281178, -13.93375672973999890, -3.388131789017201356E-17 ) ) ;
#9103=CARTESIAN_POINT ( 'NONE',  ( 14.42166414075703784, -1.434770972873324002, -10.21765703208912157 ) ) ;
#9105=CARTESIAN_POINT ( 'NONE',  ( 19.64691490199999890, -8.083823404160000337, -7.725524090809999578 ) ) ;
#9108=CARTESIAN_POINT ( 'NONE',  ( 13.73279381853092218, 8.783345170398582979, -2.087887316596209075 ) ) ;
#9109=EDGE_CURVE ( 'NONE', #1172, #709, #6051, .T. ) ;
#9110=CARTESIAN_POINT ( 'NONE',  ( -6.046835300290999804, 16.30334124114000360, 1.000000020649999932 ) ) ;
#9113=AXIS2_PLACEMENT_3D ( 'NONE', #11488, #4213, #18864 ) ;
#9114=CARTESIAN_POINT ( 'NONE',  ( 24.50000000000000711, -10.15712295534905607, 1.516248268602033100 ) ) ;
#9115=ORIENTED_EDGE ( 'NONE', *, *, #22555, .T. ) ;
#9117=CARTESIAN_POINT ( 'NONE',  ( 17.24104166666665705, 7.287850587087861598, -5.600897003789193640 ) ) ;
#9121=CARTESIAN_POINT ( 'NONE',  ( 17.21942445932999988, -10.43099376775999865, 3.766336729935999994 ) ) ;
#9122=CARTESIAN_POINT ( 'NONE',  ( -16.28879905794757832, 6.724608735979642482, 7.932750281745096999 ) ) ;
#9124=ORIENTED_EDGE ( 'NONE', *, *, #11153, .F. ) ;
#9125=CARTESIAN_POINT ( 'NONE',  ( -11.02181256584999858, -14.64514436291000088, -2.564679662907999536 ) ) ;
#9126=FACE_OUTER_BOUND ( 'NONE', #12153, .T. ) ;
#9128=CIRCLE ( 'NONE', #4087, 4.750000000000000000 ) ;
#9130=CARTESIAN_POINT ( 'NONE',  ( 23.32352258632852227, -0.4171737454618665297, -10.59529878620608301 ) ) ;
#9133=CARTESIAN_POINT ( 'NONE',  ( 15.97461056860084661, -8.975192083211494420, -5.171608217064927793 ) ) ;
#9134=CARTESIAN_POINT ( 'NONE',  ( -19.58317126038999945, -9.245977532061999682, 5.315468033165000605 ) ) ;
#9135=CARTESIAN_POINT ( 'NONE',  ( -14.44097954155594721, -12.31212079859721342, 3.674767524707362121 ) ) ;
#9137=CARTESIAN_POINT ( 'NONE',  ( -16.77363468649999945, -9.766024879818999693, 0.2197783339474000119 ) ) ;
#9141=CARTESIAN_POINT ( 'NONE',  ( 21.66117154754112306, -2.170144149905655073, -10.48492122635746959 ) ) ;
#9145=CARTESIAN_POINT ( 'NONE',  ( 0.6124999999999999334, 1.217145837503000065E-14, 0.000000000000000000 ) ) ;
#9149=CARTESIAN_POINT ( 'NONE',  ( -4.396898345509000272, 12.25739909476000733, -2.028097624563999446 ) ) ;
#9150=ORIENTED_EDGE ( 'NONE', *, *, #8672, .F. ) ;
#9151=CARTESIAN_POINT ( 'NONE',  ( 13.80543875730999837, 6.427790461817999734, -6.492639392963999612 ) ) ;
#9154=CARTESIAN_POINT ( 'NONE',  ( -14.45960645816625068, 2.455948253056539965, -12.49996645506552539 ) ) ;
#9156=VECTOR ( 'NONE', #18586, 1000.000000000000227 ) ;
#9157=CARTESIAN_POINT ( 'NONE',  ( -15.61042920454667104, 4.568651703649176277, 7.926930427632896681 ) ) ;
#9158=CARTESIAN_POINT ( 'NONE',  ( -20.15286497918999942, 1.035681084484999959, 10.55014544111999975 ) ) ;
#9159=CARTESIAN_POINT ( 'NONE',  ( -20.23016201347000020, -9.838557159217998560, 0.7066799550067000002 ) ) ;
#9160=CARTESIAN_POINT ( 'NONE',  ( 13.21250000000000036, 0.000000000000000000, 0.000000000000000000 ) ) ;
#9161=DIRECTION ( 'NONE',  ( -0.9865822012466877178, 0.000000000000000000, -0.1632653061223979518 ) ) ;
#9164=CARTESIAN_POINT ( 'NONE',  ( -7.135183041691996131, 15.40308931772999479, 1.043144557813000084 ) ) ;
#9167=CARTESIAN_POINT ( 'NONE',  ( -18.26174577250666786, -8.901978021259040474, -2.392470463651766188 ) ) ;
#9169=CARTESIAN_POINT ( 'NONE',  ( 13.62456398135812030, -0.2661322460768725251, -9.069200149764863994 ) ) ;
#9170=CARTESIAN_POINT ( 'NONE',  ( 5.856952141942437962, 14.44447281020456408, -1.792848595071122597 ) ) ;
#9173=CARTESIAN_POINT ( 'NONE',  ( 3.602888212551376146, 12.02596803873696985, 3.222497887462735022 ) ) ;
#9174=EDGE_LOOP ( 'NONE', ( #10129, #21604, #10627, #19099, #21358 ) ) ;
#9175=CARTESIAN_POINT ( 'NONE',  ( -2.478649635289443598, 11.74284498083996375, -4.136397467743439194 ) ) ;
#9176=CARTESIAN_POINT ( 'NONE',  ( -10.38810889560006778, 15.62418126105870542, 1.271664699463827430 ) ) ;
#9178=FACE_OUTER_BOUND ( 'NONE', #7202, .T. ) ;
#9180=EDGE_CURVE ( 'NONE', #8104, #9388, #17370, .T. ) ;
#9181=CARTESIAN_POINT ( 'NONE',  ( 23.99062354302999722, -6.216878364870000340, 12.50000000000000000 ) ) ;
#9182=CARTESIAN_POINT ( 'NONE',  ( -16.81976253787999909, -9.102909969768001375, 0.000000000000000000 ) ) ;
#9183=CARTESIAN_POINT ( 'NONE',  ( 14.07768908531000207, 0.2086024747513000044, -10.15948369482999958 ) ) ;
#9184=CARTESIAN_POINT ( 'NONE',  ( 18.82077563971644452, 6.007613805412093555, 8.527724857812813752 ) ) ;
#9185=CARTESIAN_POINT ( 'NONE',  ( -24.37124162822026818, 2.557079873875871989, 12.50000271512793049 ) ) ;
#9186=CYLINDRICAL_SURFACE ( 'NONE', #1133, 15.45000000000000107 ) ;
#9188=CARTESIAN_POINT ( 'NONE',  ( 13.50000000000000000, -9.661799839223764508, 1.236133458592524104 ) ) ;
#9189=VECTOR ( 'NONE', #2377, 1000.000000000000000 ) ;
#9192=CARTESIAN_POINT ( 'NONE',  ( 23.75983873544999980, 0.4422497764812000076, -10.81708341766999837 ) ) ;
#9193=EDGE_CURVE ( 'NONE', #16256, #18376, #1378, .T. ) ;
#9195=CARTESIAN_POINT ( 'NONE',  ( -11.04281598264000053, 15.43291325263555436, 0.1613546199214205557 ) ) ;
#9196=CARTESIAN_POINT ( 'NONE',  ( 24.50000000000000000, 0.3475903562124330604, 10.45960510830245482 ) ) ;
#9197=CARTESIAN_POINT ( 'NONE',  ( -4.764492196990996575, 12.47350750427999166, 0.4132957174682002632 ) ) ;
#9205=CARTESIAN_POINT ( 'NONE',  ( 11.78693030655810503, 4.312506568627681780, -12.49999836761436356 ) ) ;
#9206=AXIS2_PLACEMENT_3D ( 'NONE', #13782, #6641, #8227 ) ;
#9209=CARTESIAN_POINT ( 'NONE',  ( 13.09050158531000108, 2.578416522421000057, 9.802228185182000786 ) ) ;
#9212=CARTESIAN_POINT ( 'NONE',  ( -14.13294016288999977, 9.260019365940999947, -2.871107829034000414 ) ) ;
#9214=CONICAL_SURFACE ( 'NONE', #12320, 14.15464499511999996, 0.6126053401530057174 ) ;
#9217=CARTESIAN_POINT ( 'NONE',  ( -10.43420619172003860, 15.58275592125444931, -1.312790953672736682 ) ) ;
#9219=CARTESIAN_POINT ( 'NONE',  ( 14.41906648891345455, -1.524465402106258471, -10.20485689444239519 ) ) ;
#9220=CARTESIAN_POINT ( 'NONE',  ( 24.50000000000000000, 0.000000000000000000, 0.000000000000000000 ) ) ;
#9221=CARTESIAN_POINT ( 'NONE',  ( 24.60268290209999975, -6.843945738500000431, 9.013297814461999735 ) ) ;
#9223=ADVANCED_FACE ( 'NONE', ( #11521 ), #2682, .T. ) ;
#9224=CARTESIAN_POINT ( 'NONE',  ( 13.68370378423180078, 8.311088653021329264, -3.515498294082253228 ) ) ;
#9225=CARTESIAN_POINT ( 'NONE',  ( -6.493754939510261615, 15.47278019132436633, -1.455574667720375803 ) ) ;
#9228=VERTEX_POINT ( 'NONE', #4616 ) ;
#9230=CARTESIAN_POINT ( 'NONE',  ( 24.50000000000000711, -10.20164407018255837, 0.8509029801991366826 ) ) ;
#9232=ORIENTED_EDGE ( 'NONE', *, *, #16595, .F. ) ;
#9233=CARTESIAN_POINT ( 'NONE',  ( -5.372805085453999929, 16.07374366015000078, -2.940844016990000309 ) ) ;
#9235=CARTESIAN_POINT ( 'NONE',  ( 21.34228936713000024, 9.218966921638999779, 0.000000000000000000 ) ) ;
#9237=VECTOR ( 'NONE', #5089, 1000.000000000000000 ) ;
#9238=CARTESIAN_POINT ( 'NONE',  ( 18.56154373921000200, 10.40205886901000021, -3.950313236753000279 ) ) ;
#9239=CARTESIAN_POINT ( 'NONE',  ( -6.142995259236280425, 15.92730771963155689, 1.075595792251097693 ) ) ;
#9244=CARTESIAN_POINT ( 'NONE',  ( -10.91999006584999954, -12.27213681847000082, -8.393598339211999715 ) ) ;
#9245=AXIS2_PLACEMENT_3D ( 'NONE', #16377, #7171, #16615 ) ;
#9247=DIRECTION ( 'NONE',  ( -1.000000000000000000, 0.000000000000000000, 0.000000000000000000 ) ) ;
#9248=CARTESIAN_POINT ( 'NONE',  ( -12.42283980531000154, 12.23011958036999935, -9.372058967585999767 ) ) ;
#9251=CARTESIAN_POINT ( 'NONE',  ( 16.11211489208788450, -5.644912813679614949, -8.690873081026319724 ) ) ;
#9252=CARTESIAN_POINT ( 'NONE',  ( -15.01422961087000019, 1.689195866378999877, -10.88871722812999998 ) ) ;
#9255=ADVANCED_FACE ( 'NONE', ( #21325 ), #10065, .T. ) ;
#9257=CARTESIAN_POINT ( 'NONE',  ( -13.52354911898000012, -2.293961044660999704, 9.402123702338000655 ) ) ;
#9261=CARTESIAN_POINT ( 'NONE',  ( 22.00165215149456444, 8.873424619505614785, -6.013099889673867438 ) ) ;
#9263=CIRCLE ( 'NONE', #7699, 6.125000000000002665 ) ;
#9264=ORIENTED_EDGE ( 'NONE', *, *, #18014, .F. ) ;
#9267=CARTESIAN_POINT ( 'NONE',  ( 4.492400324385998012, 12.36848690438001164, -1.675184738194000378 ) ) ;
#9270=CARTESIAN_POINT ( 'NONE',  ( 15.23137625731000000, -4.902144360783999844, -7.754105707547999771 ) ) ;
#9274=CARTESIAN_POINT ( 'NONE',  ( -14.25243324638999809, 6.216878364870000340, -12.50000000000000000 ) ) ;
#9276=CARTESIAN_POINT ( 'NONE',  ( -14.47125380616164492, -2.070155988435417704, -12.49997628897334501 ) ) ;
#9277=ORIENTED_EDGE ( 'NONE', *, *, #14537, .F. ) ;
#9278=PLANE ( 'NONE',  #8596 ) ;
#9279=CARTESIAN_POINT ( 'NONE',  ( 12.00000000000000178, 3.168049150117523638, -8.572990016710750893 ) ) ;
#9282=EDGE_CURVE ( 'NONE', #13697, #14211, #21588, .T. ) ;
#9284=CARTESIAN_POINT ( 'NONE',  ( -23.93282274426380596, 10.35928047437771404, 2.226158404521125345 ) ) ;
#9286=CARTESIAN_POINT ( 'NONE',  ( -24.12232999016000079, 1.520060141252000183E-14, 0.000000000000000000 ) ) ;
#9287=DIRECTION ( 'NONE',  ( 0.000000000000000000, 1.000000000000000000, 0.000000000000000000 ) ) ;
#9292=CARTESIAN_POINT ( 'NONE',  ( -22.62572616711135254, -6.492281254104476318, -8.331290678700625563 ) ) ;
#9295=CIRCLE ( 'NONE', #22813, 12.50000000000000178 ) ;
#9296=CARTESIAN_POINT ( 'NONE',  ( 2.236616701338915991, 11.69514058084769381, 4.269215119675235037 ) ) ;
#9297=ORIENTED_EDGE ( 'NONE', *, *, #362, .F. ) ;
#9298=CARTESIAN_POINT ( 'NONE',  ( -0.9309833650500990432, 11.51982210469550338, -4.721885681554473635 ) ) ;
#9299=CARTESIAN_POINT ( 'NONE',  ( -11.04281598264000053, 15.31903517167999951, 1.878299281558999834 ) ) ;
#9302=CARTESIAN_POINT ( 'NONE',  ( -23.75393112313999922, 13.93375672974000068, -0.5770173629729000719 ) ) ;
#9303=CARTESIAN_POINT ( 'NONE',  ( 16.71018908530999880, 2.886377165994000293, 9.815223273854998709 ) ) ;
#9304=CARTESIAN_POINT ( 'NONE',  ( 18.13997558517295872, 1.806292539708457934, -10.29261115798856352 ) ) ;
#9306=CARTESIAN_POINT ( 'NONE',  ( -4.900699999999999612, 1.284663064832999817E-14, 0.000000000000000000 ) ) ;
#9307=LINE ( 'NONE', #16442, #3536 ) ;
#9308=CARTESIAN_POINT ( 'NONE',  ( 6.243179582884000212, 1.410249977594731933E-14, 13.77250448649344250 ) ) ;
#9309=EDGE_LOOP ( 'NONE', ( #6070, #23511, #7659 ) ) ;
#9311=CARTESIAN_POINT ( 'NONE',  ( 22.60328865247000252, -1.313042956010000095, 11.24729106410999968 ) ) ;
#9313=ORIENTED_EDGE ( 'NONE', *, *, #8615, .F. ) ;
#9314=CARTESIAN_POINT ( 'NONE',  ( 13.89035753402663254, -9.969457238322348758, -2.796840301697916864 ) ) ;
#9315=CARTESIAN_POINT ( 'NONE',  ( 24.50000000000000355, 3.444092371770813621, 9.698360394283593422 ) ) ;
#9316=CARTESIAN_POINT ( 'NONE',  ( -4.565401903344999290, 12.39645977841000324, 1.432179347221001153 ) ) ;
#9318=EDGE_CURVE ( 'NONE', #10616, #11620, #966, .T. ) ;
#9319=CARTESIAN_POINT ( 'NONE',  ( -21.64241867476000181, 8.060209368933000107, 7.624942817855999699 ) ) ;
#9324=CARTESIAN_POINT ( 'NONE',  ( 5.358355417570997759, 14.28398881512000607, 2.883859362742000165 ) ) ;
#9325=CARTESIAN_POINT ( 'NONE',  ( 16.05145603379665431, 7.936819607890199357, 4.574351470713802215 ) ) ;
#9328=CARTESIAN_POINT ( 'NONE',  ( 14.73581408531000037, 7.589869243736000470, 6.782654363299000622 ) ) ;
#9330=CARTESIAN_POINT ( 'NONE',  ( -12.37247714714999880, 8.083715232074000667, -4.229267010826999851 ) ) ;
#9331=B_SPLINE_CURVE_WITH_KNOTS ( 'NONE', 3,
 ( #4543, #12300, #7077, #23549, #19687, #23418, #21971, #6960, #1629, #18113, #3104, #6713, #9019, #14104, #16149, #12425, #12771, #14229 ),
 .UNSPECIFIED., .F., .F.,
 ( 4, 2, 2, 2, 2, 2, 2, 2, 4 ),
 ( 0.000000000000000000, 0.1249999999999999722, 0.2500000000000000000, 0.3750000000000000000, 0.5000000000000000000, 0.6250000000000000000, 0.7499999999999998890, 0.8750000000000000000, 1.000000000000000000 ),
 .UNSPECIFIED. ) ;
#9332=FACE_OUTER_BOUND ( 'NONE', #4010, .T. ) ;
#9335=CARTESIAN_POINT ( 'NONE',  ( -10.04701370327999932, 16.31160201366999729, -1.000000000000000000 ) ) ;
#9337=CARTESIAN_POINT ( 'NONE',  ( 14.57889531702554464, 4.053392352543252031, -9.495965673588385059 ) ) ;
#9338=CARTESIAN_POINT ( 'NONE',  ( -17.91572087121334178, 7.301875228516277794, -5.611357487623554796 ) ) ;
#9339=CARTESIAN_POINT ( 'NONE',  ( 20.19755579089999742, 9.974711832087001184, -5.086754361666000257 ) ) ;
#9341=CARTESIAN_POINT ( 'NONE',  ( 13.82849600701260862, 9.024859065751403620, 0.8634124378813970990 ) ) ;
#9342=CARTESIAN_POINT ( 'NONE',  ( 3.163367236287002005, 12.09434266441998673, -3.669474972920002909 ) ) ;
#9343=EDGE_CURVE ( 'NONE', #8899, #6464, #2802, .T. ) ;
#9344=CARTESIAN_POINT ( 'NONE',  ( 19.55914433211999892, -7.278973637726999790, -8.742471291912998765 ) ) ;
#9347=EDGE_LOOP ( 'NONE', ( #23672, #11409, #6434, #14239, #3119 ) ) ;
#9348=CARTESIAN_POINT ( 'NONE',  ( -16.14541243917331315, -2.378020554675936982, -8.849179423685832546 ) ) ;
#9349=CARTESIAN_POINT ( 'NONE',  ( 24.34804274388850587, 9.160073233599486997, 9.134287758352421349 ) ) ;
#9350=DIRECTION ( 'NONE',  ( 0.000000000000000000, 1.000000000000000000, 0.000000000000000000 ) ) ;
#9351=CARTESIAN_POINT ( 'NONE',  ( 18.59537304017000281, 10.74774789134999864, 2.883182032014000029 ) ) ;
#9352=PLANE ( 'NONE',  #19514 ) ;
#9357=CARTESIAN_POINT ( 'NONE',  ( -11.73457006584999895, 14.06883258501999912, 4.808938159164000581 ) ) ;
#9361=CARTESIAN_POINT ( 'NONE',  ( -24.43506354683046311, 9.928196662808350226, 7.803922592516721046 ) ) ;
#9362=CARTESIAN_POINT ( 'NONE',  ( 0.000000000000000000, 17.00000000000000000, 0.000000000000000000 ) ) ;
#9363=CARTESIAN_POINT ( 'NONE',  ( 6.240092085251032650, 13.67838160267347014, 1.680192384702403618 ) ) ;
#9364=CARTESIAN_POINT ( 'NONE',  ( 15.93200848183689722, -9.659035961499510492, -3.741044914201433702 ) ) ;
#9365=CARTESIAN_POINT ( 'NONE',  ( -18.37874916017999638, 9.689337229684999997, 5.438183135797000745 ) ) ;
#9368=B_SPLINE_CURVE_WITH_KNOTS ( 'NONE', 3,
 ( #9611, #2343, #4286, #7796, #9732, #13129, #11437, #18813, #2458, #19048, #13594, #15168, #15282, #3929, #13241, #20991, #159, #22796, #5968, #18696, #20878, #13351, #8033, #4402, #15053, #11793, #1990, #9375, #16747, #20751, #14928, #4162, #11322, #18936, #2105, #9494, #21480, #17857, #10214, #2954, #19670, #21357, #12158, #2711, #4894, #10342, #8280, #8403, #17481, #17607, #17356, #23399, #12281, #23280, #13715, #876, #9969, #17732, #1132, #6332, #3083, #1251, #23035, #15643, #10469, #21111, #21239, #4652, #15771, #4524, #8160, #11915, #759, #14085, #1002, #15527, #8531, #10094, #19170, #6453, #19298, #23160, #15889, #13840, #12039, #19422, #8641, #16005, #6817, #2834, #6693, #6579, #13963, #14209, #22914, #21606, #4773, #19548, #5023, #2579, #10702, #14676, #1498, #20258, #5478, #7403 ),
 .UNSPECIFIED., .F., .F.,
 ( 4, 2, 1, 2, 2, 2, 2, 2, 2, 2, 2, 2, 2, 2, 1, 2, 2, 2, 2, 2, 2, 2, 2, 2, 2, 2, 1, 2, 2, 2, 2, 2, 2, 2, 2, 2, 1, 2, 1, 2, 2, 2, 2, 2, 2, 2, 2, 2, 1, 2, 2, 2, 2, 2, 2, 4 ),
 ( 0.000000000000000000, 0.01562500000000000000, 0.03125000000000000000, 0.04687500000000000000, 0.06250000000000000000, 0.07812500000000000000, 0.09375000000000000000, 0.1250000000000000000, 0.1562500000000000000, 0.1718750000000000000, 0.1875000000000000000, 0.2031250000000000000, 0.2187500000000000000, 0.2343750000000000000, 0.2500000000000000000, 0.2656250000000000000, 0.2812500000000000000, 0.2968750000000000000, 0.3125000000000000000, 0.3437500000000000000, 0.3750000000000000000, 0.3906250000000000000, 0.4062500000000000000, 0.4218750000000000000, 0.4375000000000000000, 0.4531250000000000000, 0.4687500000000000000, 0.4843750000000000000, 0.5000000000000000000, 0.5156250000000000000, 0.5312500000000000000, 0.5625000000000000000, 0.5937500000000000000, 0.6093750000000000000, 0.6250000000000000000, 0.6406250000000000000, 0.6562500000000000000, 0.6718750000000000000, 0.6875000000000000000, 0.7031250000000000000, 0.7187500000000000000, 0.7343750000000000000, 0.7500000000000000000, 0.7812500000000000000, 0.8125000000000000000, 0.8281250000000000000, 0.8437500000000000000, 0.8593750000000000000, 0.8750000000000000000, 0.8906250000000000000, 0.9062500000000000000, 0.9218750000000000000, 0.9375000000000000000, 0.9531250000000000000, 0.9687500000000000000, 1.000000000000000000 ),
 .UNSPECIFIED. ) ;
#9369=CARTESIAN_POINT ( 'NONE',  ( -14.01132597738000030, -2.550904266876999671, 10.45586863968000024 ) ) ;
#9374=CARTESIAN_POINT ( 'NONE',  ( 20.27087574806811432, 10.03231373101404600, -3.158548254409779599 ) ) ;
#9375=CARTESIAN_POINT ( 'NONE',  ( -18.16722892299935310, 2.522433974171974569, 10.24789558780088328 ) ) ;
#9377=( BOUNDED_CURVE ( )  B_SPLINE_CURVE ( 3, ( #21373, #4789, #3222, #19565, #2969, #10359, #17748, #6709, #23416, #14102 ),
 .UNSPECIFIED., .F., .F. ) 
 B_SPLINE_CURVE_WITH_KNOTS ( ( 4, 1, 1, 1, 1, 1, 1, 4 ),
 ( 0.000000000000000000, 0.07930571573750974657, 0.2537389680230056066, 0.4205310468338411267, 0.5688359795437202271, 0.7038386765312832916, 0.8425724330419954722, 1.000000000000000000 ),
 .UNSPECIFIED. ) 
 CURVE ( )  GEOMETRIC_REPRESENTATION_ITEM ( )  RATIONAL_B_SPLINE_CURVE ( ( 1.254793930016049108, 1.254793930016049108, 1.254793930016048886, 1.254793930016049108, 1.254793930016049108, 1.254793930016049108, 1.254793930016049108, 1.254793930016049108, 1.254793930016049108, 1.254793930016049108 ) ) 
 REPRESENTATION_ITEM ( '' )  );
#9379=CARTESIAN_POINT ( 'NONE',  ( -4.787147458302001723, 13.37298724219999002, 4.939277822045997191 ) ) ;
#9380=CARTESIAN_POINT ( 'NONE',  ( -13.99999999999999467, -10.14973060463748666, 1.779624900529133580 ) ) ;
#9382=CARTESIAN_POINT ( 'NONE',  ( 17.12250142130999819, -8.875724825267999663, -3.992994992864999926 ) ) ;
#9383=ORIENTED_EDGE ( 'NONE', *, *, #23886, .T. ) ;
#9385=CARTESIAN_POINT ( 'NONE',  ( -4.309862785505534255, 15.29405002130709867, 4.352518930625178584 ) ) ;
#9388=VERTEX_POINT ( 'NONE', #7136 ) ;
#9389=CARTESIAN_POINT ( 'NONE',  ( 22.74058103379666917, 1.211330063708936589, -9.254849841694738899 ) ) ;
#9390=CARTESIAN_POINT ( 'NONE',  ( 4.736790957010000191, 12.61336852909998996, -0.1514267026985999243 ) ) ;
#9391=CARTESIAN_POINT ( 'NONE',  ( -21.01239991986000177, 8.969540160325998102, 3.381244718297999885 ) ) ;
#9392=CARTESIAN_POINT ( 'NONE',  ( -14.43045988485367914, 9.209646829417284408, -9.048410431339574345 ) ) ;
#9395=CARTESIAN_POINT ( 'NONE',  ( -21.07622378627610615, -8.171794258342258033, -6.628154887273959517 ) ) ;
#9399=EDGE_CURVE ( 'NONE', #3069, #3157, #6560, .T. ) ;
#9401=ORIENTED_EDGE ( 'NONE', *, *, #9712, .F. ) ;
#9402=EDGE_CURVE ( 'NONE', #1014, #9699, #23620, .T. ) ;
#9403=CARTESIAN_POINT ( 'NONE',  ( -17.95941243917332741, -2.390205132071402616, -8.894518645773471732 ) ) ;
#9404=CARTESIAN_POINT ( 'NONE',  ( 12.52688711657000020, -6.216878364870000340, -12.50000000000000000 ) ) ;
#9407=CARTESIAN_POINT ( 'NONE',  ( -23.42901741772625712, 3.156775733565070574, 10.10315730872225792 ) ) ;
#9410=CARTESIAN_POINT ( 'NONE',  ( 3.136507135182145412, 11.89683589971509825, 3.669855009401824741 ) ) ;
#9411=ORIENTED_EDGE ( 'NONE', *, *, #7770, .F. ) ;
#9412=CARTESIAN_POINT ( 'NONE',  ( -0.7552438104605452285, 11.50694251763714604, -4.753202236774020761 ) ) ;
#9414=CARTESIAN_POINT ( 'NONE',  ( 24.37705598205755209, 9.806549756205852120, -0.9735673311825817633 ) ) ;
#9415=ADVANCED_FACE ( 'NONE', ( #12721 ), #16788, .T. ) ;
#9417=B_SPLINE_CURVE_WITH_KNOTS ( 'NONE', 3,
 ( #15598, #23477, #13914, #6888, #22985, #8715, #16079, #19619, #8593, #6400, #21185, #2656 ),
 .UNSPECIFIED., .F., .F.,
 ( 4, 2, 2, 2, 2, 4 ),
 ( 0.000000000000000000, 0.2500000000000424660, 0.3750000000000640599, 0.4375000000000685563, 0.5000000000000730527, 1.000000000000000000 ),
 .UNSPECIFIED. ) ;
#9420=CARTESIAN_POINT ( 'NONE',  ( 15.17456408531000100, -6.393444021559000490, 7.935320769223000781 ) ) ;
#9421=CARTESIAN_POINT ( 'NONE',  ( 18.07176995288481081, -0.6453614156608961094, -10.39397914006448431 ) ) ;
#9424=CARTESIAN_POINT ( 'NONE',  ( 17.15614037306000128, 8.095712735332998733, 7.236596325106999572 ) ) ;
#9427=EDGE_LOOP ( 'NONE', ( #2588, #1085, #13935, #20879 ) ) ;
#9429=CARTESIAN_POINT ( 'NONE',  ( 21.36394493738999856, -9.707274230039999452, -5.764439021661999618 ) ) ;
#9432=CARTESIAN_POINT ( 'NONE',  ( 11.59627693011999838, -8.493620999052001963, -2.880788490115999689 ) ) ;
#9433=DIRECTION ( 'NONE',  ( 1.000000000000000000, 0.000000000000000000, 0.000000000000000000 ) ) ;
#9434=CARTESIAN_POINT ( 'NONE',  ( -0.1161258160197999739, 11.43408742862999716, 4.868089096411000405 ) ) ;
#9436=CARTESIAN_POINT ( 'NONE',  ( -22.81201049522999824, -10.99897752496999992, 1.683594084091999843 ) ) ;
#9447=CARTESIAN_POINT ( 'NONE',  ( 14.32350174931000097, 0.2192049860668999761, -10.67495121044000150 ) ) ;
#9448=CARTESIAN_POINT ( 'NONE',  ( -14.41758667332000066, 9.911104062797001291, 4.224474430483999399 ) ) ;
#9453=CARTESIAN_POINT ( 'NONE',  ( -10.08825016236975181, 16.08144774604313199, -1.020021333861736101 ) ) ;
#9455=CARTESIAN_POINT ( 'NONE',  ( 13.97482487491021175, -10.24735112816637184, 1.245669702648658506 ) ) ;
#9458=CARTESIAN_POINT ( 'NONE',  ( 21.81255309151999811, -1.099163774157999818, -11.18733577289999914 ) ) ;
#9460=CARTESIAN_POINT ( 'NONE',  ( 13.60815662951419469, 7.077589705154139210, -5.594308489612157764 ) ) ;
#9462=CARTESIAN_POINT ( 'NONE',  ( -6.678873158505115981, 15.36510622990475738, 1.676819129351728055 ) ) ;
#9463=CARTESIAN_POINT ( 'NONE',  ( 23.03766113620000056, -10.74194406456000017, -4.027689622328000318 ) ) ;
#9464=EDGE_LOOP ( 'NONE', ( #11125, #14662 ) ) ;
#9466=CARTESIAN_POINT ( 'NONE',  ( 12.40357033522256280, -13.79529643152775087, 1.105845675118881211 ) ) ;
#9467=ORIENTED_EDGE ( 'NONE', *, *, #5556, .T. ) ;
#9468=CARTESIAN_POINT ( 'NONE',  ( -16.44774577250665004, -8.856638799171403065, -2.380285886256298777 ) ) ;
#9471=CARTESIAN_POINT ( 'NONE',  ( 16.61041316388000055, 10.47570988103000111, -3.588975773298999972 ) ) ;
#9474=ORIENTED_EDGE ( 'NONE', *, *, #10428, .F. ) ;
#9476=CARTESIAN_POINT ( 'NONE',  ( -10.49795221169000037, 10.03457821036000119, 11.90362028209000123 ) ) ;
#9478=CARTESIAN_POINT ( 'NONE',  ( 17.71428936713000013, 9.125865291226999076, 0.000000000000000000 ) ) ;
#9480=VERTEX_POINT ( 'NONE', #17622 ) ;
#9481=CARTESIAN_POINT ( 'NONE',  ( -5.529771451991000397, 1.198997689148999791E-14, 1.310996564781999865E-13 ) ) ;
#9482=CARTESIAN_POINT ( 'NONE',  ( 19.61728472050814176, -3.208866004501119473, -10.00333024590596054 ) ) ;
#9484=CARTESIAN_POINT ( 'NONE',  ( 15.59175458660710056, -7.210646299692904826, 7.423952708739454565 ) ) ;
#9485=CARTESIAN_POINT ( 'NONE',  ( -17.87080093323000085, -2.119561155269000352, 10.89291255152999938 ) ) ;
#9487=VECTOR ( 'NONE', #22519, 1000.000000000000000 ) ;
#9488=CARTESIAN_POINT ( 'NONE',  ( -19.29271502458999876, -7.174960688273000819, 7.031698840148000507 ) ) ;
#9489=EDGE_CURVE ( 'NONE', #13414, #13163, #9730, .T. ) ;
#9494=CARTESIAN_POINT ( 'NONE',  ( -17.76208048912187110, -9.713398265221545813, 4.231666101567703286 ) ) ;
#9496=CARTESIAN_POINT ( 'NONE',  ( 24.50000000000000000, 0.000000000000000000, 12.50000000000000000 ) ) ;
#9498=DIRECTION ( 'NONE',  ( 0.000000000000000000, -0.5000000000000169864, -0.8660254037844288266 ) ) ;
#9500=CARTESIAN_POINT ( 'NONE',  ( 14.90231375730999908, -9.084442286569000657, 1.213034410125000129 ) ) ;
#9501=ORIENTED_EDGE ( 'NONE', *, *, #2676, .F. ) ;
#9503=CARTESIAN_POINT ( 'NONE',  ( -4.739682122679631959, 15.68822824407284067, 3.880277545986481336 ) ) ;
#9504=CARTESIAN_POINT ( 'NONE',  ( 24.18393254356861632, -13.26880198692879276, 2.017760803068382458 ) ) ;
#9506=VERTEX_POINT ( 'NONE', #8419 ) ;
#9507=CARTESIAN_POINT ( 'NONE',  ( -15.72380420454666528, 7.256715315803072386, 5.576969440672721490 ) ) ;
#9508=CARTESIAN_POINT ( 'NONE',  ( 4.501062182727002536, 12.52238982561000746, 1.504078967853000881 ) ) ;
#9509=CARTESIAN_POINT ( 'NONE',  ( 12.00000000000000178, -4.050809156854140447, -8.703506550480188508 ) ) ;
#9514=LINE ( 'NONE', #4426, #2193 ) ;
#9517=VERTEX_POINT ( 'NONE', #10358 ) ;
#9518=CARTESIAN_POINT ( 'NONE',  ( -18.07278743917332875, -5.613834502798916049, -7.305098395835319280 ) ) ;
#9519=CARTESIAN_POINT ( 'NONE',  ( 24.09204327667999834, -8.784117800967999656, 5.624662619288000265 ) ) ;
#9520=CARTESIAN_POINT ( 'NONE',  ( 13.53123041467663334, -3.132728285495402609, -8.512962057649877679 ) ) ;
#9522=CARTESIAN_POINT ( 'NONE',  ( -22.83993716727533041, -10.41765305974887035, -1.759783978785091296 ) ) ;
#9526=EDGE_LOOP ( 'NONE', ( #2427, #17766, #8928, #8798 ) ) ;
#9528=CARTESIAN_POINT ( 'NONE',  ( 0.5604879404901262907, 11.49595935512666678, -4.779696783358256873 ) ) ;
#9530=DIRECTION ( 'NONE',  ( 0.000000000000000000, 1.000000000000000000, 0.000000000000000000 ) ) ;
#9531=B_SPLINE_CURVE_WITH_KNOTS ( 'NONE', 3,
 ( #11772, #4499, #8506, #19273, #19525, #608, #17331, #4752, #8010, #6309, #13694, #22772, #12136, #19399, #6672, #11654, #15747, #10075 ),
 .UNSPECIFIED., .F., .F.,
 ( 4, 2, 2, 2, 2, 2, 2, 2, 4 ),
 ( 0.000000000000000000, 0.1250000000000000000, 0.2500000000000000000, 0.3750000000000000000, 0.5000000000000000000, 0.6250000000000000000, 0.7500000000000000000, 0.8750000000000000000, 1.000000000000000000 ),
 .UNSPECIFIED. ) ;
#9536=AXIS2_PLACEMENT_3D ( 'NONE', #21547, #15950, #6637 ) ;
#9537=CARTESIAN_POINT ( 'NONE',  ( 12.87112658530999987, 8.616207371593000985, 5.326914196072999985 ) ) ;
#9538=CARTESIAN_POINT ( 'NONE',  ( -19.01635896142999727, -2.665689585159999986, -11.12245455963000040 ) ) ;
#9539=PLANE ( 'NONE',  #10424 ) ;
#9540=CARTESIAN_POINT ( 'NONE',  ( 15.66608580085999947, -10.66676427418000017, 3.898330567911000077 ) ) ;
#9543=CARTESIAN_POINT ( 'NONE',  ( 21.11556404106000073, 9.695547301195000856, -0.01981028907428000058 ) ) ;
#9545=DIRECTION ( 'NONE',  ( 1.000000000000000000, 0.000000000000000000, -2.391341176003999979E-11 ) ) ;
#9546=ORIENTED_EDGE ( 'NONE', *, *, #11594, .T. ) ;
#9548=CARTESIAN_POINT ( 'NONE',  ( 11.64218518496999977, -8.036653071258001546, -4.231765345051999638 ) ) ;
#9549=CARTESIAN_POINT ( 'NONE',  ( 24.49999999999999645, 1.330573465229666574, 10.33004493691498560 ) ) ;
#9550=CARTESIAN_POINT ( 'NONE',  ( -4.663699493647997407, 12.43415402266998981, 1.065227872551999466 ) ) ;
#9553=CARTESIAN_POINT ( 'NONE',  ( -24.46239300412999640, -6.744405939805999672, -8.905960738907999996 ) ) ;
#9558=CARTESIAN_POINT ( 'NONE',  ( -23.50032910583999879, 1.715543117993999783E-14, -9.274346474607714441 ) ) ;
#9562=CARTESIAN_POINT ( 'NONE',  ( 12.56850174931000019, 2.370728120151999629, -10.36336111974000040 ) ) ;
#9563=CARTESIAN_POINT ( 'NONE',  ( -13.19880458549999958, -0.9434914505904000714, -10.69878979702999899 ) ) ;
#9566=CARTESIAN_POINT ( 'NONE',  ( -14.39391695410597549, -4.126581034250158098, 12.49998949084259614 ) ) ;
#9567=EDGE_LOOP ( 'NONE', ( #22373, #19532, #10773 ) ) ;
#9570=CARTESIAN_POINT ( 'NONE',  ( 13.84538782162042381, -8.680617797995118679, 5.551030475077797455 ) ) ;
#9571=CARTESIAN_POINT ( 'NONE',  ( -24.50000000000000000, 1.524685264937999788E-14, 0.000000000000000000 ) ) ;
#9572=CARTESIAN_POINT ( 'NONE',  ( 23.50140112429999917, -0.2660373876970000273, -11.28442596635000150 ) ) ;
#9574=ADVANCED_FACE ( 'NONE', ( #8546 ), #12357, .F. ) ;
#9575=CARTESIAN_POINT ( 'NONE',  ( 11.06619116163201788, -0.4983756420194491166, 12.49999828234741450 ) ) ;
#9576=CARTESIAN_POINT ( 'NONE',  ( 18.74098996950760565, 2.121065158271645323, 10.25986587397817118 ) ) ;
#9580=CARTESIAN_POINT ( 'NONE',  ( -14.48343131230104497, 2.223754299675648305, -8.788885103986384451 ) ) ;
#9581=CARTESIAN_POINT ( 'NONE',  ( 11.70388046505397206, -12.85079422505704017, 2.741654745543806726 ) ) ;
#9582=AXIS2_PLACEMENT_3D ( 'NONE', #2965, #887, #8290 ) ;
#9588=ORIENTED_EDGE ( 'NONE', *, *, #9614, .T. ) ;
#9589=CARTESIAN_POINT ( 'NONE',  ( 15.92243887344999997, -6.551683564218000022, -8.903917471378999693 ) ) ;
#9594=CARTESIAN_POINT ( 'NONE',  ( -13.99999999999999645, -0.2128887255028979741, -9.534676919017003982 ) ) ;
#9595=CARTESIAN_POINT ( 'NONE',  ( -10.09066221169000066, -13.14800539653000122, 8.337798847484000575 ) ) ;
#9596=CARTESIAN_POINT ( 'NONE',  ( -23.74465998031000069, -6.216878364870000340, -12.50000000000000000 ) ) ;
#9597=CARTESIAN_POINT ( 'NONE',  ( -18.99854661335000117, 6.966878364870000340, 12.06698729810999993 ) ) ;
#9598=ORIENTED_EDGE ( 'NONE', *, *, #22219, .T. ) ;
#9599=CARTESIAN_POINT ( 'NONE',  ( -14.49284522991462509, 10.30702784336665978, 7.147655011474417286 ) ) ;
#9600=CARTESIAN_POINT ( 'NONE',  ( 21.07774770046331625, 5.661224168628396392, -7.366763267202135701 ) ) ;
#9601=CARTESIAN_POINT ( 'NONE',  ( 6.142488816234497939, 14.18447672331321741, 0.1076473395637999736 ) ) ;
#9602=CARTESIAN_POINT ( 'NONE',  ( 15.59691868738293863, -7.345342774621501647, 7.289925863788985438 ) ) ;
#9604=CARTESIAN_POINT ( 'NONE',  ( -14.43819794762999997, 5.126061982986000132, 9.736209624113000061 ) ) ;
#9606=CARTESIAN_POINT ( 'NONE',  ( -18.48019363270999804, 4.914628609928000103, -9.714689191606000307 ) ) ;
#9610=DIRECTION ( 'NONE',  ( 0.000000000000000000, 0.9925668416490733836, -0.1217007183987966479 ) ) ;
#9611=CARTESIAN_POINT ( 'NONE',  ( -19.55887123173999953, -9.833822427806001798, 3.504477313184999776 ) ) ;
#9614=EDGE_CURVE ( 'NONE', #19902, #5259, #757, .T. ) ;
#9616=CARTESIAN_POINT ( 'NONE',  ( 6.642812809165002719, 13.49906599351999859, -0.0001514643891326998028 ) ) ;
#9619=CARTESIAN_POINT ( 'NONE',  ( 15.34106375730999972, -1.677480367812999917, -9.021981177529999840 ) ) ;
#9620=VERTEX_POINT ( 'NONE', #20513 ) ;
#9621=CARTESIAN_POINT ( 'NONE',  ( -6.068436532072000844, 15.62980265433002458, -1.260321238843998604 ) ) ;
#9624=ORIENTED_EDGE ( 'NONE', *, *, #16075, .F. ) ;
#9625=CARTESIAN_POINT ( 'NONE',  ( -14.25699038479000080, 13.93375672974000068, -0.1445849984294000079 ) ) ;
#9626=CARTESIAN_POINT ( 'NONE',  ( 21.92720833333332564, -9.233977095127203327, 1.208851722883240276 ) ) ;
#9627=CARTESIAN_POINT ( 'NONE',  ( -4.739674965276999608, 12.61450277301999456, -0.05987925791641996592 ) ) ;
#9629=CARTESIAN_POINT ( 'NONE',  ( -20.20946649501000181, -9.083415843844999671, 0.0004049750149795999896 ) ) ;
#9630=CARTESIAN_POINT ( 'NONE',  ( 18.92362270046332640, -4.611705506703642321, -8.001125271793704030 ) ) ;
#9631=CLOSED_SHELL ( 'NONE', ( #13681, #16223, #1242, #6000, #14287, #21805, #3948, #8508, #1512, #15410, #14149, #22361, #378, #10395, #23451, #8336, #4156, #17570, #6731, #7270, #4366, #3813, #16940, #22106, #16000, #9223, #12105, #17701, #19642, #18796, #11907, #15727, #665, #3787, #23133, #10221, #11046, #4592, #17519, #17224, #21694, #5824, #6230, #19926, #18440, #19267, #20201, #8229, #5813, #11441, #7123, #21864, #10366, #7030, #18278, #23324, #14797, #14852, #23630, #18986, #17525, #15318, #22880, #12960, #8063, #20383, #23309, #13804, #10708, #21925, #17045, #9415, #69, #9662, #8862, #14851, #22423, #19605, #13994, #15934, #16795, #19611, #21085, #21338, #2857, #19118, #17089, #17379, #14076, #5333, #18971, #12200, #5084, #23389, #20491, #5252, #18665, #450, #4288, #1214, #3434, #9255, #9939, #16809, #17796, #22569, #13421, #3487, #1858, #7799, #21409, #16485, #10871, #22414, #8241, #12947, #13503, #16675, #16, #11007, #18297, #14559, #8478, #20663, #21217, #11308, #1027, #17239, #17697, #4080, #11016, #16582, #11788, #18308, #15707, #18425, #3484, #8450, #23870, #12678, #5293, #9574, #16028, #13099, #778, #7938, #16044, #8786, #18593, #943, #21114, #15896, #2162, #18807, #21698, #5072, #5963, #15117, #16633, #20338, #12388, #4067, #10591, #18591, #18083, #7300, #20080, #13133, #22984, #23499, #2585, #10848, #5655, #9955, #19593, #4793, #22640, #11266, #2691 ) ) ;
#9632=CARTESIAN_POINT ( 'NONE',  ( -6.250000000000000000, 16.31160201366999729, -1.000000000001000089 ) ) ;
#9633=CARTESIAN_POINT ( 'NONE',  ( 13.50000000000000000, 0.000000000000000000, 0.000000000000000000 ) ) ;
#9639=CARTESIAN_POINT ( 'NONE',  ( 22.73928674176000087, -5.367530796503000801, -8.899542937657001218 ) ) ;
#9640=CARTESIAN_POINT ( 'NONE',  ( 3.249297074264064555, 13.15931643686085728, -5.930092486474230817 ) ) ;
#9644=CARTESIAN_POINT ( 'NONE',  ( -21.39401291616239931, -4.743783438882505976, 9.554723409011961266 ) ) ;
#9649=ORIENTED_EDGE ( 'NONE', *, *, #9682, .T. ) ;
#9651=CARTESIAN_POINT ( 'NONE',  ( -24.12232999016000079, -13.23032192315998401, 0.000000000000000000 ) ) ;
#9654=EDGE_CURVE ( 'NONE', #20433, #22434, #19251, .T. ) ;
#9657=CARTESIAN_POINT ( 'NONE',  ( 18.71100174931000026, 5.082731606397000057, 9.520742961040999930 ) ) ;
#9658=CARTESIAN_POINT ( 'NONE',  ( -16.78192513375999795, 10.68652398881999943, -3.898064904104000306 ) ) ;
#9659=CARTESIAN_POINT ( 'NONE',  ( 23.96190874292139128, -7.512837009555735968, -5.581780844827100907 ) ) ;
#9660=CARTESIAN_POINT ( 'NONE',  ( 19.39051537306000128, -5.800580820157000161, 8.214924713229001085 ) ) ;
#9662=ADVANCED_FACE ( 'NONE', ( #18574, #15485 ), #19249, .F. ) ;
#9664=CARTESIAN_POINT ( 'NONE',  ( 20.66721036671000178, 8.339588664129999884, -5.894560743941999803 ) ) ;
#9665=CARTESIAN_POINT ( 'NONE',  ( 24.48327518124252933, -10.18191985984368664, 7.364397484155817963 ) ) ;
#9670=CARTESIAN_POINT ( 'NONE',  ( 4.913522824441004744, 12.43887836712999473, 0.2526796349711001310 ) ) ;
#9672=EDGE_CURVE ( 'NONE', #13697, #12220, #3942, .T. ) ;
#9673=CARTESIAN_POINT ( 'NONE',  ( -24.62947754991999716, -9.950913960798999369, -3.563496608132999732 ) ) ;
#9674=ORIENTED_EDGE ( 'NONE', *, *, #21792, .F. ) ;
#9675=CARTESIAN_POINT ( 'NONE',  ( -20.44776253787999920, -9.196011600180998613, 0.000000000000000000 ) ) ;
#9677=CYLINDRICAL_SURFACE ( 'NONE', #3727, 10.59999999999999964 ) ;
#9678=DIRECTION ( 'NONE',  ( -1.000000000000000000, 0.000000000000000000, 0.000000000000000000 ) ) ;
#9680=CARTESIAN_POINT ( 'NONE',  ( 16.39158103379666187, -1.190002857594419705, 9.091921988472257965 ) ) ;
#9681=CARTESIAN_POINT ( 'NONE',  ( 14.76225174930999984, 10.68374474379000105, -0.3265774252310000292 ) ) ;
#9682=EDGE_CURVE ( 'NONE', #19420, #12075, #2519, .T. ) ;
#9683=CARTESIAN_POINT ( 'NONE',  ( -17.62691415960999919, 5.507581498160999622, 8.736692431694999428 ) ) ;
#9684=CARTESIAN_POINT ( 'NONE',  ( 18.26606375730999687, -4.551782674040000032, 7.886397731525000232 ) ) ;
#9685=CARTESIAN_POINT ( 'NONE',  ( 24.32802197706137903, 12.60002805950083982, -3.176111224150924173 ) ) ;
#9686=ORIENTED_EDGE ( 'NONE', *, *, #16764, .T. ) ;
#9689=CARTESIAN_POINT ( 'NONE',  ( 13.84536273287771202, -8.680155482951017021, 5.551750670585463787 ) ) ;
#9694=CARTESIAN_POINT ( 'NONE',  ( 11.78924557931383177, 4.312980057964804104, 12.49999285599082377 ) ) ;
#9695=CARTESIAN_POINT ( 'NONE',  ( 13.50000000000000000, -10.65000000000000036, 0.000000000000000000 ) ) ;
#9696=CARTESIAN_POINT ( 'NONE',  ( -6.694406957049796603, 15.35878686133300342, 1.695873640511939007 ) ) ;
#9698=CARTESIAN_POINT ( 'NONE',  ( 12.28022044529580015, 7.993836135665516096, -11.15426966564930744 ) ) ;
#9699=VERTEX_POINT ( 'NONE', #4728 ) ;
#9707=ORIENTED_EDGE ( 'NONE', *, *, #12067, .F. ) ;
#9708=CARTESIAN_POINT ( 'NONE',  ( 6.159666495275548215, 14.07295743052582360, -0.4000666433572926395 ) ) ;
#9712=EDGE_CURVE ( 'NONE', #14929, #7412, #8598, .T. ) ;
#9713=EDGE_LOOP ( 'NONE', ( #13322, #23821, #16925, #5837, #19940, #23278, #6914, #11916, #22430 ) ) ;
#9714=ORIENTED_EDGE ( 'NONE', *, *, #14150, .F. ) ;
#9716=CARTESIAN_POINT ( 'NONE',  ( -14.00000000000000000, -5.610885045639453672, -8.079343806354058799 ) ) ;
#9717=CARTESIAN_POINT ( 'NONE',  ( -10.80341971169000104, 14.28377837372999970, -6.193755811534000344 ) ) ;
#9721=CARTESIAN_POINT ( 'NONE',  ( -21.65907966340000002, 3.174516240292999836, -9.136279537863000400 ) ) ;
#9722=CARTESIAN_POINT ( 'NONE',  ( -14.25243324638999809, 7.716878364870000340, 11.63397459621999985 ) ) ;
#9723=CARTESIAN_POINT ( 'NONE',  ( 6.158244933928628484, 14.08141442615745653, 0.3795422047411434185 ) ) ;
#9724=CARTESIAN_POINT ( 'NONE',  ( 15.27210601666787149, 3.430796689683968559, 9.762251594826194534 ) ) ;
#9727=CARTESIAN_POINT ( 'NONE',  ( -17.87080258880000017, 5.796842063356000274, 9.195416763971000051 ) ) ;
#9730=B_SPLINE_CURVE_WITH_KNOTS ( 'NONE', 3,
 ( #19563, #774, #1017, #6226, #12173, #12054, #10230, #23049, #8175, #17498 ),
 .UNSPECIFIED., .F., .F.,
 ( 4, 2, 2, 2, 4 ),
 ( 0.000000000000000000, 0.06692748465457198925, 0.1338549693091439785, 0.2007824539637159678, 0.2677099386182879570 ),
 .UNSPECIFIED. ) ;
#9732=CARTESIAN_POINT ( 'NONE',  ( -19.38267422463178491, -10.23251295633816227, -2.712185686795678397 ) ) ;
#9734=VERTEX_POINT ( 'NONE', #1330 ) ;
#9736=CARTESIAN_POINT ( 'NONE',  ( -4.941117876443001933, 15.61713999035001343, 3.125961572582002024 ) ) ;
#9737=CARTESIAN_POINT ( 'NONE',  ( 18.26141666666665131, -8.901969795568348331, 2.392468253058787298 ) ) ;
#9738=CARTESIAN_POINT ( 'NONE',  ( 12.62531392131000096, 8.177682633693001080, 5.055777280222000236 ) ) ;
#9740=CARTESIAN_POINT ( 'NONE',  ( -6.228095582201001790, 16.43254147212998362, -1.007191989855000358 ) ) ;
#9743=ORIENTED_EDGE ( 'NONE', *, *, #12365, .F. ) ;
#9745=CARTESIAN_POINT ( 'NONE',  ( -11.62500000000000000, 1.367011989547999955E-14, 0.000000000000000000 ) ) ;
#9746=CARTESIAN_POINT ( 'NONE',  ( -3.142350709629999628, 12.07584853453000129, 3.567860278848001165 ) ) ;
#9747=DIRECTION ( 'NONE',  ( 1.000000000000000000, 0.000000000000000000, 0.000000000000000000 ) ) ;
#9748=CARTESIAN_POINT ( 'NONE',  ( -23.58178687934999829, -6.109693073218999793, -7.476155833321000088 ) ) ;
#9749=DIRECTION ( 'NONE',  ( -1.000000000000000000, 0.000000000000000000, 0.000000000000000000 ) ) ;
#9750=CARTESIAN_POINT ( 'NONE',  ( -4.628018178257720550, 13.45824813671923437, 5.216489783566583327 ) ) ;
#9751=DIRECTION ( 'NONE',  ( -1.000000000000000000, 0.000000000000000000, 0.000000000000000000 ) ) ;
#9752=CARTESIAN_POINT ( 'NONE',  ( 5.048072026126640743, 14.71121043296684761, 3.475281950094643690 ) ) ;
#9756=FACE_OUTER_BOUND ( 'NONE', #23874, .T. ) ;
#9757=CARTESIAN_POINT ( 'NONE',  ( 3.630616870732635615, 13.24606289761949007, -5.733978109788271382 ) ) ;
#9758=CARTESIAN_POINT ( 'NONE',  ( -23.60559742078757139, -8.658706366674554289, -3.691114709487112844 ) ) ;
#9759=CARTESIAN_POINT ( 'NONE',  ( -22.30440966686241566, 4.682851881239854741, -9.610650805105821703 ) ) ;
#9765=CARTESIAN_POINT ( 'NONE',  ( 24.32771143580656314, 9.033746532951345998, -3.774273071546123681 ) ) ;
#9768=ORIENTED_EDGE ( 'NONE', *, *, #805, .F. ) ;
#9771=CARTESIAN_POINT ( 'NONE',  ( 16.29787674931000296, 5.844090361140000134, -8.997790218903000792 ) ) ;
#9773=CARTESIAN_POINT ( 'NONE',  ( -14.34436095811999934, -2.679964408802999909, 10.98515472083999889 ) ) ;
#9774=CARTESIAN_POINT ( 'NONE',  ( -10.04561490872999840, 16.32684872326999681, 0.9999999999983000265 ) ) ;
#9775=CARTESIAN_POINT ( 'NONE',  ( 19.66181994525999954, -5.517917554610000330, 7.814610069288999483 ) ) ;
#9776=CARTESIAN_POINT ( 'NONE',  ( 13.50000000000000178, -7.092774689729933080, -5.968849012436532320 ) ) ;
#9779=CARTESIAN_POINT ( 'NONE',  ( 22.53195685829999917, 1.853256702191000027, -9.556221255016000171 ) ) ;
#9784=CARTESIAN_POINT ( 'NONE',  ( -1.066174337946000250, 11.54162544571998872, 4.691709464589000511 ) ) ;
#9786=EDGE_CURVE ( 'NONE', #17452, #7412, #14066, .T. ) ;
#9787=CARTESIAN_POINT ( 'NONE',  ( -22.77108459744000157, -5.959070222075999901, -9.395571579996001788 ) ) ;
#9789=DIRECTION ( 'NONE',  ( -1.000000000000000000, 0.000000000000000000, 0.000000000000000000 ) ) ;
#9791=CARTESIAN_POINT ( 'NONE',  ( -23.86847083088467869, 5.679235826614652538, -12.50000000000279599 ) ) ;
#9794=CARTESIAN_POINT ( 'NONE',  ( 16.80728936713000365, -9.102589883624000677, 0.000000000000000000 ) ) ;
#9797=CARTESIAN_POINT ( 'NONE',  ( 13.66537674931000090, -8.233391669162999804, 6.770876163316000174 ) ) ;
#9798=CARTESIAN_POINT ( 'NONE',  ( -14.17369824411999879, 9.412195986946999327, 4.011894131497999005 ) ) ;
#9799=CARTESIAN_POINT ( 'NONE',  ( 18.19293875730999943, -2.463108239980999592, 8.917637382198998708 ) ) ;
#9800=AXIS2_PLACEMENT_3D ( 'NONE', #13947, #5006, #12393 ) ;
#9801=CARTESIAN_POINT ( 'NONE',  ( -14.47125380616081181, 2.070155988425159244, 12.49997628898002944 ) ) ;
#9806=CARTESIAN_POINT ( 'NONE',  ( 14.23170285492579801, -7.372315516923570122, -7.223174187050277695 ) ) ;
#9808=CARTESIAN_POINT ( 'NONE',  ( 4.833250487806001416, 14.92157114608998469, -3.774880232157002524 ) ) ;
#9810=DIRECTION ( 'NONE',  ( -1.000000000000000000, 0.000000000000000000, 0.000000000000000000 ) ) ;
#9811=CARTESIAN_POINT ( 'NONE',  ( 14.39275807839523580, -4.136262847370294260, 8.039618612950896193 ) ) ;
#9812=CARTESIAN_POINT ( 'NONE',  ( 17.98830562607077965, 3.393379461346332171, -9.888719939816333238 ) ) ;
#9813=CARTESIAN_POINT ( 'NONE',  ( 12.00000000000000000, 0.000000000000000000, 1.045589212608000028E-14 ) ) ;
#9820=VERTEX_POINT ( 'NONE', #11121 ) ;
#9822=CARTESIAN_POINT ( 'NONE',  ( -3.055307665906170644, 11.87602316546083969, 3.736655301196532886 ) ) ;
#9826=FACE_OUTER_BOUND ( 'NONE', #8649, .T. ) ;
#9830=ORIENTED_EDGE ( 'NONE', *, *, #15760, .F. ) ;
#9831=VERTEX_POINT ( 'NONE', #20213 ) ;
#9832=CARTESIAN_POINT ( 'NONE',  ( -24.47970833437427984, 10.31330985778130227, -7.136763535915959800 ) ) ;
#9836=ORIENTED_EDGE ( 'NONE', *, *, #12795, .T. ) ;
#9837=CARTESIAN_POINT ( 'NONE',  ( -22.07433482820000137, -2.615545669082999680, -9.865490644338999360 ) ) ;
#9839=CARTESIAN_POINT ( 'NONE',  ( -24.24003052282993309, 9.030352382186375593, 9.358674018443513987 ) ) ;
#9841=CARTESIAN_POINT ( 'NONE',  ( 15.74491607068019938, -9.964074634268969888, 2.836190018388155654 ) ) ;
#9842=CARTESIAN_POINT ( 'NONE',  ( -19.06736070216000201, 2.265016177855000201, -10.89708866536000009 ) ) ;
#9844=CARTESIAN_POINT ( 'NONE',  ( -20.97328328328443092, -5.337166430913867110, -9.061234812632074309 ) ) ;
#9845=CARTESIAN_POINT ( 'NONE',  ( -18.88645432865000018, -8.793774626762999702, -6.438463651166999924 ) ) ;
#9848=ORIENTED_EDGE ( 'NONE', *, *, #13460, .F. ) ;
#9851=AXIS2_PLACEMENT_3D ( 'NONE', #23753, #19659, #7157 ) ;
#9853=EDGE_LOOP ( 'NONE', ( #18071, #8665, #14904 ) ) ;
#9855=CARTESIAN_POINT ( 'NONE',  ( -4.728521406481004163, 15.35552965760000710, 3.489357254952003551 ) ) ;
#9856=VECTOR ( 'NONE', #242, 1000.000000000000000 ) ;
#9858=CARTESIAN_POINT ( 'NONE',  ( 14.27062642131000025, 9.653071988928001446, -0.2951073761277999696 ) ) ;
#9859=ORIENTED_EDGE ( 'NONE', *, *, #14977, .T. ) ;
#9860=CARTESIAN_POINT ( 'NONE',  ( -6.318227646113002471, 16.43048641157998802, -1.007191989855000358 ) ) ;
#9864=CARTESIAN_POINT ( 'NONE',  ( 21.32254166666666606, 5.665264218082834979, 7.371607159753769345 ) ) ;
#9865=CARTESIAN_POINT ( 'NONE',  ( 24.38244769084932528, -4.973698664748710030, 9.391432790414068421 ) ) ;
#9867=CARTESIAN_POINT ( 'NONE',  ( 17.67377246198465812, -10.31525896512351714, -1.350505006071770486 ) ) ;
#9868=DIRECTION ( 'NONE',  ( 1.000000000000000000, 0.000000000000000000, 0.000000000000000000 ) ) ;
#9869=CARTESIAN_POINT ( 'NONE',  ( -14.32799115970092174, 8.244301755411150623, -10.71998578050881790 ) ) ;
#9870=CARTESIAN_POINT ( 'NONE',  ( 23.99062354302999722, -13.93375672974000068, 0.8660254037843999608 ) ) ;
#9871=DIRECTION ( 'NONE',  ( 0.000000000000000000, -1.000000000000000000, 0.000000000000000000 ) ) ;
#9877=CARTESIAN_POINT ( 'NONE',  ( 20.17446287504999702, -7.350134498294000451, 6.461420190107999950 ) ) ;
#9878=CARTESIAN_POINT ( 'NONE',  ( -1.717182781518961976, 12.90331733707204087, -6.468384628374955092 ) ) ;
#9882=DIRECTION ( 'NONE',  ( -1.000000000000000000, 0.000000000000000000, 0.000000000000000000 ) ) ;
#9883=ORIENTED_EDGE ( 'NONE', *, *, #21768, .T. ) ;
#9884=CARTESIAN_POINT ( 'NONE',  ( -18.91245535748801032, -3.755334353860249497, -9.775979986752766138 ) ) ;
#9885=CARTESIAN_POINT ( 'NONE',  ( 24.15736593521746300, 13.39690473052857378, 1.795880342563474397 ) ) ;
#9887=VERTEX_POINT ( 'NONE', #318 ) ;
#9890=CARTESIAN_POINT ( 'NONE',  ( 18.82068924930999998, 1.189837805593999986, 10.72966125727000097 ) ) ;
#9891=CARTESIAN_POINT ( 'NONE',  ( -14.23644303527998822, 0.6063593516544601991, -9.063592691554708480 ) ) ;
#9892=VECTOR ( 'NONE', #18949, 1000.000000000000000 ) ;
#9895=CARTESIAN_POINT ( 'NONE',  ( 16.34364037305999773, -5.328133213713000416, -9.435500363287999903 ) ) ;
#9896=DIRECTION ( 'NONE',  ( 1.000000000000000000, 0.000000000000000000, 0.000000000000000000 ) ) ;
#9898=CARTESIAN_POINT ( 'NONE',  ( -10.04281598263999875, 21.50000000000000000, 1.000000000000000000 ) ) ;
#9899=CARTESIAN_POINT ( 'NONE',  ( 23.41720236907999819, -1.131410883462000028, 9.692640973934999238 ) ) ;
#9900=B_SPLINE_CURVE_WITH_KNOTS ( 'NONE', 3,
 ( #7140, #23368, #21808, #21403, #19218, #4447, #15817, #15931, #13757, #4817, #10388, #9891, #17281, #11837, #15454, #10261, #2759, #22841 ),
 .UNSPECIFIED., .F., .F.,
 ( 4, 2, 2, 2, 2, 2, 2, 2, 4 ),
 ( 0.000000000000000000, 0.1250000000000000000, 0.2500000000000000000, 0.3750000000000000000, 0.5000000000000000000, 0.6250000000000000000, 0.7500000000000000000, 0.8750000000000000000, 1.000000000000000000 ),
 .UNSPECIFIED. ) ;
#9903=CARTESIAN_POINT ( 'NONE',  ( 11.61517937764999964, -2.662040662477000108, -8.927692317508000741 ) ) ;
#9905=CARTESIAN_POINT ( 'NONE',  ( 4.604941514899001831, 12.48958726761999571, 1.077474224869999775 ) ) ;
#9907=CARTESIAN_POINT ( 'NONE',  ( -24.10776096368000054, 9.886905199420999324, -5.181215075838999873 ) ) ;
#9908=VERTEX_POINT ( 'NONE', #20557 ) ;
#9910=VERTEX_POINT ( 'NONE', #11603 ) ;
#9912=CARTESIAN_POINT ( 'NONE',  ( 4.749999673578000348, 12.55004296393999930, -4.341645649670000483E-06 ) ) ;
#9914=CARTESIAN_POINT ( 'NONE',  ( 3.482092246234998800, 13.23084471460000167, 5.478241207029996396 ) ) ;
#9916=CONICAL_SURFACE ( 'NONE', #2569, 9.136555860486998526, 0.02565634000431304615 ) ;
#9917=DIRECTION ( 'NONE',  ( 1.000000000000000000, 0.000000000000000000, 0.000000000000000000 ) ) ;
#9918=CARTESIAN_POINT ( 'NONE',  ( 12.12975174931000133, -10.21766741648000121, -2.893652579598999797 ) ) ;
#9919=CARTESIAN_POINT ( 'NONE',  ( -17.87080258880000017, 5.796842063356000274, 9.195416763971000051 ) ) ;
#9920=CARTESIAN_POINT ( 'NONE',  ( 16.43793875730999687, -4.200504661774999704, 8.191206307881000015 ) ) ;
#9921=CARTESIAN_POINT ( 'NONE',  ( 19.05233531832000082, -1.887707665395999879, 10.26617185442000135 ) ) ;
#9927=CARTESIAN_POINT ( 'NONE',  ( 13.77916999064124504, -7.232023062304977046, 7.346102567300633268 ) ) ;
#9929=CARTESIAN_POINT ( 'NONE',  ( -0.7454422758268997029, 13.21307987702999576, -6.061668110315994618 ) ) ;
#9931=CARTESIAN_POINT ( 'NONE',  ( 14.58760727575919880, -8.335758281611482801, 3.616921650321700987 ) ) ;
#9932=CARTESIAN_POINT ( 'NONE',  ( 17.45863886587524760, -10.56286734491478008, -0.7285313845211358608 ) ) ;
#9933=CARTESIAN_POINT ( 'NONE',  ( 13.50000000000000000, 0.000000000000000000, 0.000000000000000000 ) ) ;
#9937=CARTESIAN_POINT ( 'NONE',  ( -2.402048786002945135, 11.81788909627579187, -4.144620335373454978 ) ) ;
#9939=ADVANCED_FACE ( 'NONE', ( #11364 ), #11717, .T. ) ;
#9940=DIRECTION ( 'NONE',  ( 1.000000000000000000, -0.000000000000000000, -0.000000000000000000 ) ) ;
#9941=CARTESIAN_POINT ( 'NONE',  ( -3.805495096816462031, 12.08739645174783739, 2.982851083477900289 ) ) ;
#9943=CARTESIAN_POINT ( 'NONE',  ( 2.390253620507223786, 12.99717099578450430, 6.277524352174514988 ) ) ;
#9944=CARTESIAN_POINT ( 'NONE',  ( 16.21568206723000216, -6.556442847978000366, -8.910386729497998815 ) ) ;
#9945=CARTESIAN_POINT ( 'NONE',  ( -6.166365645201998369, 15.19835549494000304, -2.169414073428999057 ) ) ;
#9950=CARTESIAN_POINT ( 'NONE',  ( -14.00000000000000000, 3.648514493304280126, -8.539308174521250905 ) ) ;
#9952=CARTESIAN_POINT ( 'NONE',  ( -24.11803009771612949, -8.641091274406146994, -10.03259869780779567 ) ) ;
#9955=ADVANCED_FACE ( 'NONE', ( #21034 ), #21567, .F. ) ;
#9956=CARTESIAN_POINT ( 'NONE',  ( -18.91721189367000022, -3.796518214708000105, 8.814796721447999417 ) ) ;
#9959=CARTESIAN_POINT ( 'NONE',  ( 15.77318932640266880, -10.19605645657118487, 1.803564215919225333 ) ) ;
#9960=CARTESIAN_POINT ( 'NONE',  ( -14.55077782637000006, -1.548327575011000157, 10.89675555037999999 ) ) ;
#9962=CARTESIAN_POINT ( 'NONE',  ( -21.35931016950181416, -10.06206865553333607, 3.097961417847729049 ) ) ;
#9969=CARTESIAN_POINT ( 'NONE',  ( -16.66239188288299644, 10.06542107247047113, 2.687320209561217865 ) ) ;
#9970=B_SPLINE_CURVE_WITH_KNOTS ( 'NONE', 3,
 ( #13580, #4504, #15265, #11538, #13222, #13336, #9950, #20734, #7779, #4025, #17337, #18792, #859, #2441, #2203, #8016, #4385, #8144, #15510, #17215, #13457, #9594, #8262, #10079, #612, #15388, #2325, #20974, #22657, #11776, #19278, #2560, #740, #17465, #9716, #19149, #22898, #16979, #6313, #382, #11896, #15626, #17097, #495, #5838, #6066, #15146, #4634, #8746, #10684, #12140, #3065, #23138 ),
 .UNSPECIFIED., .F., .F.,
 ( 4, 1, 1, 1, 1, 1, 2, 2, 1, 1, 1, 1, 1, 1, 2, 2, 1, 1, 1, 2, 2, 1, 1, 1, 2, 2, 1, 1, 1, 1, 2, 2, 1, 1, 1, 1, 2, 2, 4 ),
 ( 0.000000000000000000, 0.1249999999999986122, 0.1874999999999979738, 0.2187499999999976130, 0.2343749999999975020, 0.2421874999999974187, 0.2460937499999973910, 0.2499999999999973355, 0.3124999999999965583, 0.3437499999999961697, 0.3593749999999960032, 0.3671874999999958922, 0.3710937499999958367, 0.3730468749999957812, 0.3740234374999958367, 0.3749999999999958922, 0.4374999999999960587, 0.4687499999999961697, 0.4843749999999962252, 0.4921874999999962808, 0.4999999999999963363, 0.5624999999999965583, 0.5937499999999966693, 0.6093749999999966693, 0.6171874999999966693, 0.6249999999999966693, 0.6874999999999970024, 0.7187499999999972244, 0.7343749999999973355, 0.7421874999999973355, 0.7460937499999973355, 0.7499999999999974465, 0.8124999999999984457, 0.8437499999999988898, 0.8593749999999991118, 0.8671874999999992228, 0.8710937499999993339, 0.8749999999999993339, 1.000000000000000000 ),
 .UNSPECIFIED. ) ;
#9973=CARTESIAN_POINT ( 'NONE',  ( 4.720439035602998601, 14.52233946640999562, -3.835351803237996737 ) ) ;
#9975=CARTESIAN_POINT ( 'NONE',  ( 12.51562642131000125, 9.466654096131000173, 1.662047859332999922 ) ) ;
#9977=CARTESIAN_POINT ( 'NONE',  ( 0.000000000000000000, -1.100000000000000089, 0.000000000000000000 ) ) ;
#9978=AXIS2_PLACEMENT_3D ( 'NONE', #11619, #13416, #453 ) ;
#9981=B_SPLINE_SURFACE_WITH_KNOTS ( 'NONE', 3, 3, ( 
 ( #17411, #10026, #17650, #681, #2630, #1179, #804, #23326, #6739, #11963, #23208, #19469, #6253, #8088, #17779, #8205, #15571, #19592, #13887, #22960, #8572, #6376, #14133, #21160, #922, #6505, #4571, #21290, #19352, #6624, #8449, #14013, #21527, #13637, #4941 ),
 ( #12204, #21033, #10141, #17529, #19090, #8323, #12087, #2503, #15688, #23078, #4702, #2879, #3003, #23447, #17898, #7097, #1299, #20183, #6862, #14374, #21767, #1545, #14255, #8690, #21653, #12682, #23580, #7211, #5180, #14716, #9158, #23690, #3369, #5066, #14488 ),
 ( #12448, #6985, #12562, #12794, #14602, #23924, #19948, #3483, #19832, #8930, #10630, #1652, #3245, #8817, #18018, #21998, #16178, #20069, #16054, #1419, #16299, #10746, #21880, #18140, #5289, #10865, #18249, #9041, #16412, #7335, #3592, #5411, #23803, #10976, #18359 ),
 ( #1770, #16535, #22111, #12327, #19718, #3130, #10515, #4061, #3701, #13017, #11574, #11222, #9748, #17134, #22338, #2235, #5872, #16656, #18478, #20771, #14825, #5633, #5986, #292, #2007, #18951, #20417, #2357, #9391, #11340, #16885, #3826, #7694, #172, #9629 ) ),
 .UNSPECIFIED., .F., .F., .F.,
 ( 4, 4 ),
 ( 4, 1, 1, 1, 1, 1, 1, 1, 1, 1, 1, 1, 1, 1, 1, 1, 1, 1, 1, 1, 1, 1, 1, 1, 1, 1, 1, 1, 1, 1, 1, 1, 4 ),
 ( -0.08408083179837000376, 1.084080831798000188 ),
 ( 0.1936290155325000040, 0.2193222086650999936, 0.2450154017976000076, 0.2707085949301000216, 0.2964017880627000112, 0.3220949811952000252, 0.3477881743278000148, 0.3734813674603000289, 0.3991745605929000185, 0.4248677537254000325, 0.4505609468578999910, 0.4762541399905000361, 0.5019473331230001056, 0.5276405262555999842, 0.5533337193880999427, 0.5790269125207000434, 0.6047201056532000019, 0.6304132987856999604, 0.6561064919182999500, 0.6817996850508000195, 0.7074928781834000091, 0.7331860713158999676, 0.7588792644484000371, 0.7845724575810000267, 0.8102656507134999853, 0.8359588438460999749, 0.8616520369785999334, 0.8873452301112000340, 0.9130384232436999925, 0.9387316163761999510, 0.9644248095088000516, 0.9901180026413000101, 1.015811195773999920 ),
 .UNSPECIFIED. ) ;
#9986=CARTESIAN_POINT ( 'NONE',  ( 12.12543434881680149, 8.197779943787733004, 10.80110243426253014 ) ) ;
#9987=CARTESIAN_POINT ( 'NONE',  ( 24.44127686332184268, -6.767441607451973873, 8.200622886799944666 ) ) ;
#9988=FACE_OUTER_BOUND ( 'NONE', #13767, .T. ) ;
#9989=CARTESIAN_POINT ( 'NONE',  ( 17.95021154713298372, -4.863476692990534644, -9.270487928442411985 ) ) ;
#9992=CARTESIAN_POINT ( 'NONE',  ( 11.01624327026000039, 1.089736728551999927E-14, 0.000000000000000000 ) ) ;
#9993=CARTESIAN_POINT ( 'NONE',  ( 19.90431259713000145, 9.967540672853999695, -5.083098181931998916 ) ) ;
#9995=AXIS2_PLACEMENT_3D ( 'NONE', #23230, #950, #19374 ) ;
#10000=CARTESIAN_POINT ( 'NONE',  ( 23.02223177661903364, 8.095646187396759785, 4.666105312640251412 ) ) ;
#10001=CARTESIAN_POINT ( 'NONE',  ( 24.33785594068000080, -9.240887486209999224, 5.917068627456000485 ) ) ;
#10002=CARTESIAN_POINT ( 'NONE',  ( -1.358858436891593247, 12.86586849937732069, -6.542507879071220778 ) ) ;
#10005=EDGE_CURVE ( 'NONE', #19819, #9734, #14021, .T. ) ;
#10006=CARTESIAN_POINT ( 'NONE',  ( -20.85848541575246884, -7.716069547171855447, -7.142552263296302328 ) ) ;
#10008=EDGE_CURVE ( 'NONE', #20574, #6561, #2790, .T. ) ;
#10012=CARTESIAN_POINT ( 'NONE',  ( -18.07511824061237604, 6.027222043823452502, 8.713521295921685450 ) ) ;
#10015=AXIS2_PLACEMENT_3D ( 'NONE', #9160, #12901, #3703 ) ;
#10022=CARTESIAN_POINT ( 'NONE',  ( 17.56312270046333524, 7.970618670273120543, -4.594122601136384709 ) ) ;
#10025=CARTESIAN_POINT ( 'NONE',  ( 14.43318924931000069, 4.163528467249999920, -9.835102695514999382 ) ) ;
#10026=CARTESIAN_POINT ( 'NONE',  ( -24.48716916290999990, -3.591176638987999770, -10.24322100536999969 ) ) ;
#10027=CARTESIAN_POINT ( 'NONE',  ( -16.37566443781999936, 5.581214954223999491, 9.898954454263000358 ) ) ;
#10028=CARTESIAN_POINT ( 'NONE',  ( 23.85139158929754188, -9.055547910765916697, -2.371671287066565270 ) ) ;
#10029=CARTESIAN_POINT ( 'NONE',  ( 17.08937451746000136, 1.841749366007999988, -9.602221512397999703 ) ) ;
#10030=CARTESIAN_POINT ( 'NONE',  ( -7.034000000000000696, 11.50000000000000000, 0.000000000000000000 ) ) ;
#10032=CARTESIAN_POINT ( 'NONE',  ( 22.00080955183999976, -9.690658177826998454, 0.7515038182808999601 ) ) ;
#10035=ORIENTED_EDGE ( 'NONE', *, *, #14323, .T. ) ;
#10036=CARTESIAN_POINT ( 'NONE',  ( 18.85240113949000218, -1.886779804701000041, 10.26112574610000117 ) ) ;
#10039=CARTESIAN_POINT ( 'NONE',  ( 3.677613186714003835, 12.08831154218000314, 3.066611987921000981 ) ) ;
#10041=CARTESIAN_POINT ( 'NONE',  ( -23.96113936679000034, 9.883381352389999819, -5.179368058338999603 ) ) ;
#10042=CARTESIAN_POINT ( 'NONE',  ( -14.25000000000000000, 0.000000000000000000, 0.000000000000000000 ) ) ;
#10048=DIRECTION ( 'NONE',  ( 0.000000000000000000, 0.9420570860200443430, 0.3354525997505800605 ) ) ;
#10050=CARTESIAN_POINT ( 'NONE',  ( -19.13034275784999849, -9.231395905450000328, -6.758791263612999423 ) ) ;
#10051=AXIS2_PLACEMENT_3D ( 'NONE', #6923, #21709, #1356 ) ;
#10052=CARTESIAN_POINT ( 'NONE',  ( 17.31543875730999815, 3.351454173900000111, -8.598433847594998625 ) ) ;
#10055=CARTESIAN_POINT ( 'NONE',  ( 19.08782216824772959, -8.814560846539785999, 5.694643456270070736 ) ) ;
#10058=CARTESIAN_POINT ( 'NONE',  ( 4.284596121176959649, 14.56923866457215588, -4.377423833532463782 ) ) ;
#10059=CARTESIAN_POINT ( 'NONE',  ( -10.04701370327999932, 16.31160201366999729, -1.000000000000000000 ) ) ;
#10060=CARTESIAN_POINT ( 'NONE',  ( -12.06624327026013077, 13.93375672974000068, 0.000000000000000000 ) ) ;
#10062=CARTESIAN_POINT ( 'NONE',  ( 11.53663804754310718, -3.465671449079424704, 12.49990775414663702 ) ) ;
#10063=CARTESIAN_POINT ( 'NONE',  ( 17.12411249101483079, -4.802526802559668795, 9.264146113958686257 ) ) ;
#10065=PLANE ( 'NONE',  #11970 ) ;
#10069=CARTESIAN_POINT ( 'NONE',  ( 11.85409292833336892, -8.571431512456976876, 10.15389364928055471 ) ) ;
#10073=CARTESIAN_POINT ( 'NONE',  ( -23.74465998031000069, -7.716878364870000340, -11.63397459621999985 ) ) ;
#10075=CARTESIAN_POINT ( 'NONE',  ( -20.25016455292000117, -8.657612072530000091, 3.085311466348000131 ) ) ;
#10077=ORIENTED_EDGE ( 'NONE', *, *, #9712, .T. ) ;
#10078=ORIENTED_EDGE ( 'NONE', *, *, #7137, .F. ) ;
#10079=CARTESIAN_POINT ( 'NONE',  ( -13.99999999999999645, -1.581653827019005920, -9.457174266960452158 ) ) ;
#10080=CARTESIAN_POINT ( 'NONE',  ( 0.000000000000000000, 20.00000000000000000, 0.000000000000000000 ) ) ;
#10082=ORIENTED_EDGE ( 'NONE', *, *, #21523, .T. ) ;
#10085=CARTESIAN_POINT ( 'NONE',  ( 14.88759896974780972, 10.27467121929758420, -1.078508883751306380 ) ) ;
#10086=CARTESIAN_POINT ( 'NONE',  ( -15.84946274974000069, -10.91352918511999981, 1.678437607090999872 ) ) ;
#10089=CARTESIAN_POINT ( 'NONE',  ( -21.28210479225873542, -10.51966893827426297, 0.3278972208331196181 ) ) ;
#10090=CARTESIAN_POINT ( 'NONE',  ( -13.44269301469999967, -0.9911996677733001526, -11.23901760903999936 ) ) ;
#10094=CARTESIAN_POINT ( 'NONE',  ( -15.50482492894748177, -4.417095855546814498, -9.394177675399193461 ) ) ;
#10097=CARTESIAN_POINT ( 'NONE',  ( 6.588726970868003185, 13.51086646594001195, -0.8681320947235999785 ) ) ;
#10099=CARTESIAN_POINT ( 'NONE',  ( -4.790823927418967898, 13.32134166212725113, -5.557028280688768973 ) ) ;
#10101=CARTESIAN_POINT ( 'NONE',  ( 12.07687642131000061, 2.140746470509000243, -9.358182000212998730 ) ) ;
#10103=CARTESIAN_POINT ( 'NONE',  ( -5.833999999999999631, -11.50000000000000000, 0.000000000000000000 ) ) ;
#10109=CARTESIAN_POINT ( 'NONE',  ( 24.17654558719286229, 2.389057866675304176, 10.34701704806261446 ) ) ;
#10111=CARTESIAN_POINT ( 'NONE',  ( 18.05946651195386110, -1.087382630457392141, -10.35418620074316287 ) ) ;
#10113=EDGE_CURVE ( 'NONE', #4168, #16663, #18928, .T. ) ;
#10114=CARTESIAN_POINT ( 'NONE',  ( -14.49284524109529038, -11.34356441105103919, 5.352320976844065825 ) ) ;
#10115=CARTESIAN_POINT ( 'NONE',  ( 24.45606130522000399, -6.841511667768999772, 9.010092832684000186 ) ) ;
#10117=CARTESIAN_POINT ( 'NONE',  ( -3.666321194958030105, 14.29055989747922339, -4.906588955330460244 ) ) ;
#10120=ORIENTED_EDGE ( 'NONE', *, *, #13203, .F. ) ;
#10121=CARTESIAN_POINT ( 'NONE',  ( 23.13555403315795544, 5.650293567432652431, 7.367300352106260775 ) ) ;
#10122=CARTESIAN_POINT ( 'NONE',  ( 18.68101713701000222, -9.202032660154998212, 4.584888180875999808 ) ) ;
#10123=CARTESIAN_POINT ( 'NONE',  ( -3.418248095344834869, 13.19611224794727100, -5.848127910700672949 ) ) ;
#10124=DIRECTION ( 'NONE',  ( -1.209279329285239001E-08, -0.5796072251201023207, -0.8148959839075015088 ) ) ;
#10125=CARTESIAN_POINT ( 'NONE',  ( -20.29618154032203492, 9.469680736381290487, -4.539250907894071929 ) ) ;
#10126=CARTESIAN_POINT ( 'NONE',  ( -14.00000000000000000, 6.995278287856000254, -5.711120943918999160 ) ) ;
#10128=CARTESIAN_POINT ( 'NONE',  ( 4.940723990893003403, 12.51283213654998505, 0.1566900733660998302 ) ) ;
#10129=ORIENTED_EDGE ( 'NONE', *, *, #7999, .F. ) ;
#10130=CARTESIAN_POINT ( 'NONE',  ( -14.05590007961454013, -7.031665520223276289, 7.590363941843731865 ) ) ;
#10136=ORIENTED_EDGE ( 'NONE', *, *, #10145, .F. ) ;
#10137=CARTESIAN_POINT ( 'NONE',  ( 12.52688711657000020, 13.93375672974000068, -0.8660254037843999608 ) ) ;
#10138=CIRCLE ( 'NONE', #23677, 16.43375672870000415 ) ;
#10139=CARTESIAN_POINT ( 'NONE',  ( 16.95600174931000126, 3.031816831187000183, 10.30986099653000032 ) ) ;
#10140=B_SPLINE_CURVE_WITH_KNOTS ( 'NONE', 3,
 ( #6883, #3023, #18165, #1321, #14279, #23346, #21673, #6765, #18037, #5312, #1443, #16319, #17803, #14156, #1566, #1198, #16202, #23602 ),
 .UNSPECIFIED., .F., .F.,
 ( 4, 2, 2, 2, 2, 2, 2, 2, 4 ),
 ( 0.000000000000000000, 0.1250000000000000000, 0.2500000000000000000, 0.3750000000000000000, 0.5000000000000000000, 0.6250000000000000000, 0.7500000000000000000, 0.8750000000000000000, 1.000000000000000000 ),
 .UNSPECIFIED. ) ;
#10141=CARTESIAN_POINT ( 'NONE',  ( -24.64929215829999976, 0.3828329976861000183, -10.71529421017999972 ) ) ;
#10143=CARTESIAN_POINT ( 'NONE',  ( -15.22293278740000133, 10.31197045934999856, -3.197427357995000108 ) ) ;
#10144=CARTESIAN_POINT ( 'NONE',  ( 22.56966666666665944, 4.658591883815835999, -8.082977972024316671 ) ) ;
#10145=EDGE_CURVE ( 'NONE', #12220, #13163, #16845, .T. ) ;
#10146=CARTESIAN_POINT ( 'NONE',  ( 16.68312451746000136, -9.163211135683999586, -3.377722033148000236 ) ) ;
#10148=B_SPLINE_CURVE_WITH_KNOTS ( 'NONE', 3,
 ( #12436, #14362, #16286, #6847, #7086, #14476, #20053, #21868, #5277, #21983, #17886, #21637 ),
 .UNSPECIFIED., .F., .F.,
 ( 4, 1, 1, 1, 1, 2, 2, 4 ),
 ( 0.000000000000000000, 0.2500000000000041633, 0.3750000000000059952, 0.4375000000000063838, 0.4687500000000064948, 0.4843750000000064393, 0.5000000000000064393, 1.000000000000000000 ),
 .UNSPECIFIED. ) ;
#10150=CARTESIAN_POINT ( 'NONE',  ( 24.36881528991178669, -9.280258940103371046, 8.926120008345273860 ) ) ;
#10151=EDGE_LOOP ( 'NONE', ( #10696, #11913, #11564, #3037 ) ) ;
#10152=CARTESIAN_POINT ( 'NONE',  ( 0.1267126835535345164, 13.69169213017725362, 6.123708248830501688 ) ) ;
#10154=AXIS2_PLACEMENT_3D ( 'NONE', #15628, #613, #742 ) ;
#10155=CARTESIAN_POINT ( 'NONE',  ( -1.048427594716000222, 11.59808701839000200, 4.637028203793000181 ) ) ;
#10157=CARTESIAN_POINT ( 'NONE',  ( -24.42146710634000328, 5.447078518068000363, -9.752648862749000003 ) ) ;
#10158=EDGE_CURVE ( 'NONE', #3791, #12959, #345, .T. ) ;
#10160=DIRECTION ( 'NONE',  ( 0.000000000000000000, -1.000000000000000000, 0.000000000000000000 ) ) ;
#10162=DIRECTION ( 'NONE',  ( -1.000000000000000000, 0.000000000000000000, 0.000000000000000000 ) ) ;
#10163=( BOUNDED_SURFACE ( )  B_SPLINE_SURFACE ( 3, 3, ( 
 ( #2223, #9616, #23164, #2583, #10097, #17485, #15892, #17735, #3086, #879, #6584, #17360, #2715, #19674, #13596, #4896, #11918 ),
 ( #10347, #19303, #13718, #20994, #1137, #10472, #12161, #21113, #14087, #15530, #762, #4404, #11795, #13969, #17859, #23283, #8534 ),
 ( #6335, #15409, #4527, #8163, #10217, #8282, #12042, #12284, #19551, #2957, #1255, #22917, #4656, #6696, #19174, #21484, #9973 ),
 ( #21360, #17611, #15646, #23038, #6457, #13842, #22798, #6213, #21242, #19425, #2837, #1004, #8407, #15774, #4776, #5858, #22324 ) ),
 .UNSPECIFIED., .F., .F., .T. ) 
 B_SPLINE_SURFACE_WITH_KNOTS ( ( 4, 4 ),
 ( 4, 1, 1, 1, 1, 1, 1, 1, 1, 1, 1, 1, 1, 1, 4 ),
 ( 0.000000000000000000, 1.000000000000000000 ),
 ( 0.2368937211084000127, 0.2409453982507999970, 0.2486681467527000200, 0.2559696437135000058, 0.2630400535103000204, 0.2700208015615999657, 0.2769718879389000410, 0.2839229647372999987, 0.2909371157855999979, 0.2981017146652999994, 0.3055324712384000496, 0.3134565545379999763, 0.3221580657204000109, 0.3317495705149000051, 0.3322945160429999767 ),
 .UNSPECIFIED. ) 
 GEOMETRIC_REPRESENTATION_ITEM ( )  RATIONAL_B_SPLINE_SURFACE ( (
 ( 1.093546124775000017, 1.093546124775000017, 1.093546124775000017, 1.093546124775000017, 1.093546124775000017, 1.093546124775000017, 1.093546124775000017, 1.093546124775000017, 1.093546124775000017, 1.093546124775000017, 1.093546124775000017, 1.093546124775000017, 1.093546124775000017, 1.093546124775000017, 1.093546124775000017, 1.093546124775000017, 1.093546124775000017),
 ( 0.9688179584082000639, 0.9688179584082000639, 0.9688179584082000639, 0.9688179584082000639, 0.9688179584082000639, 0.9688179584082000639, 0.9688179584082000639, 0.9688179584082000639, 0.9688179584082000639, 0.9688179584082000639, 0.9688179584082000639, 0.9688179584082000639, 0.9688179584082000639, 0.9688179584082000639, 0.9688179584082000639, 0.9688179584082000639, 0.9688179584082000639),
 ( 0.9688179584082000639, 0.9688179584082000639, 0.9688179584082000639, 0.9688179584082000639, 0.9688179584082000639, 0.9688179584082000639, 0.9688179584082000639, 0.9688179584082000639, 0.9688179584082000639, 0.9688179584082000639, 0.9688179584082000639, 0.9688179584082000639, 0.9688179584082000639, 0.9688179584082000639, 0.9688179584082000639, 0.9688179584082000639, 0.9688179584082000639),
 ( 1.093546124775000017, 1.093546124775000017, 1.093546124775000017, 1.093546124775000017, 1.093546124775000017, 1.093546124775000017, 1.093546124775000017, 1.093546124775000017, 1.093546124775000017, 1.093546124775000017, 1.093546124775000017, 1.093546124775000017, 1.093546124775000017, 1.093546124775000017, 1.093546124775000017, 1.093546124775000017, 1.093546124775000017) ) ) 
 REPRESENTATION_ITEM ( '' )  SURFACE ( )  );
#10165=CARTESIAN_POINT ( 'NONE',  ( -3.194868910741000434, 13.69705038741999026, 5.170042636081004339 ) ) ;
#10169=CARTESIAN_POINT ( 'NONE',  ( -18.92721240987999920, -2.665110294750000275, -11.12003873501999962 ) ) ;
#10170=CARTESIAN_POINT ( 'NONE',  ( 14.90231375730999908, -9.084442286569000657, 1.213034410125000129 ) ) ;
#10172=ORIENTED_EDGE ( 'NONE', *, *, #8184, .F. ) ;
#10173=CARTESIAN_POINT ( 'NONE',  ( -22.04021495466848179, -8.997463528116268705, 2.418937047195946821 ) ) ;
#10175=CARTESIAN_POINT ( 'NONE',  ( -12.25000000000000000, 6.489681479813073750, -13.21205004727046095 ) ) ;
#10176=CARTESIAN_POINT ( 'NONE',  ( 4.120403429707917731, 14.50536380480940046, -4.532139194909468927 ) ) ;
#10178=CARTESIAN_POINT ( 'NONE',  ( -4.105070514359999478, 13.44465293295000485, -4.977031060933996720 ) ) ;
#10181=CARTESIAN_POINT ( 'NONE',  ( 16.34355094967408917, 8.336021693863266080, -6.395580416082841779 ) ) ;
#10182=CARTESIAN_POINT ( 'NONE',  ( 23.99062354302999722, -6.216878364870000340, -12.50000000000000000 ) ) ;
#10183=CARTESIAN_POINT ( 'NONE',  ( 8.124934037954998800, -12.44999999999999929, 0.000000000000000000 ) ) ;
#10184=CARTESIAN_POINT ( 'NONE',  ( 19.90620603379666420, 2.403516248286488910, 8.943079757202132996 ) ) ;
#10185=EDGE_LOOP ( 'NONE', ( #981, #16670 ) ) ;
#10188=CARTESIAN_POINT ( 'NONE',  ( 11.22311500625620795, -9.824279701762014483, 7.983827916374445444 ) ) ;
#10192=CARTESIAN_POINT ( 'NONE',  ( -4.544324455327999779, 13.49053734526000170, 5.132126114358000812 ) ) ;
#10193=CARTESIAN_POINT ( 'NONE',  ( 6.141065375610000210, 14.19649368052000149, -1.893142280157000292E-06 ) ) ;
#10194=CARTESIAN_POINT ( 'NONE',  ( 11.01624327026000039, 1.089736728551999927E-14, 0.000000000000000000 ) ) ;
#10196=ORIENTED_EDGE ( 'NONE', *, *, #12666, .F. ) ;
#10201=CARTESIAN_POINT ( 'NONE',  ( -24.27577904266999909, 0.9982065492062000001, -11.26793000443000103 ) ) ;
#10204=CARTESIAN_POINT ( 'NONE',  ( 15.13684082370412654, 7.510860090511030762, 7.114097475440270379 ) ) ;
#10205=CARTESIAN_POINT ( 'NONE',  ( -17.08006423682000019, 7.985046582893999378, -7.675080017633000296 ) ) ;
#10207=CARTESIAN_POINT ( 'NONE',  ( -20.14975925936147760, 7.687190990672447377, 7.145965227562199651 ) ) ;
#10208=CARTESIAN_POINT ( 'NONE',  ( -4.681494469480999676, 12.59157765981999688, -0.7804412716255002547 ) ) ;
#10212=ORIENTED_EDGE ( 'NONE', *, *, #19952, .T. ) ;
#10214=CARTESIAN_POINT ( 'NONE',  ( -17.53056709833472837, -9.766724693011614278, -4.094736955089503638 ) ) ;
#10215=ORIENTED_EDGE ( 'NONE', *, *, #9682, .F. ) ;
#10216=DIRECTION ( 'NONE',  ( -1.000000000000000000, 0.000000000000000000, 0.000000000000000000 ) ) ;
#10217=CARTESIAN_POINT ( 'NONE',  ( 6.034210908571004062, 14.08836922021000504, -0.7813677579985999211 ) ) ;
#10218=CARTESIAN_POINT ( 'NONE',  ( 12.00000000000000178, 0.6217777569271694116, -8.958706245662780177 ) ) ;
#10220=VECTOR ( 'NONE', #4020, 1000.000000000000000 ) ;
#10221=ADVANCED_FACE ( 'NONE', ( #18561 ), #6552, .F. ) ;
#10222=CARTESIAN_POINT ( 'NONE',  ( 15.25781392131000125, -9.389200645904999476, -2.369324833533999808 ) ) ;
#10225=DIRECTION ( 'NONE',  ( -1.000000000000000000, 0.000000000000000000, 0.000000000000000000 ) ) ;
#10227=ORIENTED_EDGE ( 'NONE', *, *, #22137, .T. ) ;
#10228=DIRECTION ( 'NONE',  ( -1.000000000000000000, 0.000000000000000000, 0.000000000000000000 ) ) ;
#10229=CYLINDRICAL_SURFACE ( 'NONE', #8196, 7.000000000000000000 ) ;
#10230=CARTESIAN_POINT ( 'NONE',  ( -23.28041318627592560, 8.640587636776928093, -3.475811032938793232 ) ) ;
#10231=CARTESIAN_POINT ( 'NONE',  ( -14.00000000000000178, 0.4357667221639321409, 9.714757508063044611 ) ) ;
#10232=CARTESIAN_POINT ( 'NONE',  ( 16.27407322926296018, -0.09559760970984292061, -10.36543711007276869 ) ) ;
#10233=CARTESIAN_POINT ( 'NONE',  ( 11.99999999999999822, -8.403351023270348108, -5.300159557665803156 ) ) ;
#10235=CARTESIAN_POINT ( 'NONE',  ( -14.45529013989012412, 12.11766535962173208, -4.011530336787274997 ) ) ;
#10236=CARTESIAN_POINT ( 'NONE',  ( 21.70285686071999720, 5.756918313552000122, -9.651675814321999169 ) ) ;
#10237=DIRECTION ( 'NONE',  ( -1.000000000000000000, 0.000000000000000000, 0.000000000000000000 ) ) ;
#10238=CIRCLE ( 'NONE', #16411, 7.500000000000000000 ) ;
#10239=CARTESIAN_POINT ( 'NONE',  ( -4.156717377435044547, 13.71198257401902687, -4.893767653246960947 ) ) ;
#10243=CARTESIAN_POINT ( 'NONE',  ( 24.53110687423999892, -10.92244599102000002, -1.095095512714000074 ) ) ;
#10244=CARTESIAN_POINT ( 'NONE',  ( 24.50000000000000000, -2.116736914405999759, 10.36413001332999961 ) ) ;
#10247=CARTESIAN_POINT ( 'NONE',  ( -19.41256116464168358, -9.053821575032303670, 5.280908075822353887 ) ) ;
#10249=CARTESIAN_POINT ( 'NONE',  ( 0.6124999999999999334, 1.217145837503000065E-14, 0.000000000000000000 ) ) ;
#10251=EDGE_CURVE ( 'NONE', #21017, #20281, #15769, .T. ) ;
#10252=CARTESIAN_POINT ( 'NONE',  ( -14.00000000000000000, -8.319952449050001420, 6.066771132503999020 ) ) ;
#10253=DIRECTION ( 'NONE',  ( 1.000000000000000000, 0.000000000000000000, 0.000000000000000000 ) ) ;
#10260=CARTESIAN_POINT ( 'NONE',  ( -5.240876798540814896, 16.01407665191462826, -3.181876338824043415 ) ) ;
#10261=CARTESIAN_POINT ( 'NONE',  ( -14.05911075881999217, 5.716256198029335600, -7.053914683086397908 ) ) ;
#10262=EDGE_CURVE ( 'NONE', #18988, #13308, #23173, .T. ) ;
#10263=CARTESIAN_POINT ( 'NONE',  ( -17.45736661507000065, -2.009541073283000134, -10.67100981108000113 ) ) ;
#10264=CARTESIAN_POINT ( 'NONE',  ( -6.299306890445001805, 15.85649737466999376, 1.061595304832000819 ) ) ;
#10265=CARTESIAN_POINT ( 'NONE',  ( 16.88624951746000136, -4.804895915039999466, -8.508643533405999548 ) ) ;
#10270=CARTESIAN_POINT ( 'NONE',  ( -1.349229317769153669, 13.77424421209987493, 5.987165240414223710 ) ) ;
#10274=CARTESIAN_POINT ( 'NONE',  ( -14.51889506019236187, 1.113324017026137591, -8.974614630071492627 ) ) ;
#10277=VERTEX_POINT ( 'NONE', #22297 ) ;
#10278=CARTESIAN_POINT ( 'NONE',  ( -23.75083293572999921, -13.93375672974000068, 0.6735967263616999823 ) ) ;
#10280=CARTESIAN_POINT ( 'NONE',  ( 2.490830186055004614, 11.74568911763879164, -4.128140691158040276 ) ) ;
#10281=CARTESIAN_POINT ( 'NONE',  ( -1.552755157686999787, 13.31391601496999932, 5.888554406491995685 ) ) ;
#10286=CARTESIAN_POINT ( 'NONE',  ( -9.276082211694999913, 14.45305202397999977, -4.386103535306999923 ) ) ;
#10287=CARTESIAN_POINT ( 'NONE',  ( -15.88025719033000094, -8.846829628555999747, 7.110504558004000053 ) ) ;
#10289=CARTESIAN_POINT ( 'NONE',  ( 14.16093892131000054, 8.852644193975999443, -3.852777470446999697 ) ) ;
#10290=CARTESIAN_POINT ( 'NONE',  ( 18.93357673398348950, 2.325285191727461065, 10.17219493548470943 ) ) ;
#10291=EDGE_LOOP ( 'NONE', ( #8313, #19700, #6040, #20588, #22857, #13518, #18334, #23817, #4568, #11819, #17427 ) ) ;
#10293=DIRECTION ( 'NONE',  ( -1.000000000000000000, 0.000000000000000000, 0.000000000000000000 ) ) ;
#10296=CARTESIAN_POINT ( 'NONE',  ( 2.083048159898164275, 13.90352997106202260, -5.759917838137451618 ) ) ;
#10298=DIRECTION ( 'NONE',  ( 0.000000000000000000, -1.000000000000000000, 0.000000000000000000 ) ) ;
#10302=CARTESIAN_POINT ( 'NONE',  ( 16.23204215805303008, 5.269564841427452073, -8.982820748099108243 ) ) ;
#10305=DIRECTION ( 'NONE',  ( 0.000000000000000000, 0.4098987730065234425, -0.9121310190360518710 ) ) ;
#10308=AXIS2_PLACEMENT_3D ( 'NONE', #13447, #9940, #17204 ) ;
#10309=CARTESIAN_POINT ( 'NONE',  ( -3.792676939738165220, 12.19816298709897140, -2.925173950252105470 ) ) ;
#10313=EDGE_CURVE ( 'NONE', #9228, #12236, #2292, .T. ) ;
#10315=CARTESIAN_POINT ( 'NONE',  ( -2.914577979011814257, 13.09053447596949837, 6.080397015720073739 ) ) ;
#10317=CARTESIAN_POINT ( 'NONE',  ( 6.185781828581297326, 13.94115629030004833, -0.7324217553683136650 ) ) ;
#10319=DIRECTION ( 'NONE',  ( 0.000000000000000000, -1.000000000000000000, 0.000000000000000000 ) ) ;
#10324=CARTESIAN_POINT ( 'NONE',  ( -20.25016455292000117, -8.657612072530000091, 3.085311466348000131 ) ) ;
#10325=EDGE_LOOP ( 'NONE', ( #5742, #15050, #23007, #2841, #13140 ) ) ;
#10326=EDGE_CURVE ( 'NONE', #629, #7062, #7111, .T. ) ;
#10327=CARTESIAN_POINT ( 'NONE',  ( -24.61851251388999984, -10.08336777178000077, -5.147008447691999500 ) ) ;
#10331=CARTESIAN_POINT ( 'NONE',  ( 14.89611160934172318, 10.30233908782160945, -0.7821794371295839321 ) ) ;
#10334=FACE_OUTER_BOUND ( 'NONE', #7572, .T. ) ;
#10335=CARTESIAN_POINT ( 'NONE',  ( -4.741933015551000885, 12.61529762423000456, -0.01097304939024999759 ) ) ;
#10340=VECTOR ( 'NONE', #11658, 1000.000000000000227 ) ;
#10342=CARTESIAN_POINT ( 'NONE',  ( -17.18329701215404626, 0.2739043995376635454, -10.42461585661749091 ) ) ;
#10344=ORIENTED_EDGE ( 'NONE', *, *, #4973, .F. ) ;
#10347=CARTESIAN_POINT ( 'NONE',  ( 6.273483391934002285, 13.70231627968000154, 0.06241200954222003022 ) ) ;
#10348=CARTESIAN_POINT ( 'NONE',  ( 11.99999999999999822, -1.102614627638894174, -8.921479305743723387 ) ) ;
#10349=CIRCLE ( 'NONE', #11114, 12.50000000000000178 ) ;
#10350=CARTESIAN_POINT ( 'NONE',  ( 17.50558333333332328, 8.883175614560848032, 2.387156777129599394 ) ) ;
#10351=CARTESIAN_POINT ( 'NONE',  ( 12.87112658530999987, 8.616207371593000985, 5.326914196072999985 ) ) ;
#10356=EDGE_LOOP ( 'NONE', ( #129, #16840, #139, #7848, #18190, #22250, #2015, #6027, #21474, #3465 ) ) ;
#10357=CARTESIAN_POINT ( 'NONE',  ( 11.06626444616535387, 10.95085460509868369, 6.032555207302821465 ) ) ;
#10358=CARTESIAN_POINT ( 'NONE',  ( -6.249999999202001000, 16.31160201366999729, 0.9999995866763998764 ) ) ;
#10359=CARTESIAN_POINT ( 'NONE',  ( -5.588326156475896589, 14.56718056557104468, -4.654699638219854663 ) ) ;
#10360=CARTESIAN_POINT ( 'NONE',  ( 16.22229514016562035, -1.909916386427916057, -10.18956628747337945 ) ) ;
#10362=CARTESIAN_POINT ( 'NONE',  ( 12.00000000000000000, -8.840148123257950630, -4.669854054429479540 ) ) ;
#10363=CARTESIAN_POINT ( 'NONE',  ( -14.47158023610679756, -11.86027760101404205, 4.457335568564623429 ) ) ;
#10364=AXIS2_PLACEMENT_3D ( 'NONE', #16206, #1325, #1201 ) ;
#10365=CARTESIAN_POINT ( 'NONE',  ( -4.049719616303214309, 13.80515179997299313, -4.863490999083110999 ) ) ;
#10366=ADVANCED_FACE ( 'NONE', ( #22128 ), #14672, .F. ) ;
#10369=CARTESIAN_POINT ( 'NONE',  ( 22.15953394107999941, -5.779992152541000294, 8.618061788542000556 ) ) ;
#10370=CARTESIAN_POINT ( 'NONE',  ( 22.99472057969317973, -10.13472181993574495, 3.079891000904835252 ) ) ;
#10373=CARTESIAN_POINT ( 'NONE',  ( -19.73387766488721340, 0.7360098622191569850, 10.46330882142914653 ) ) ;
#10374=CARTESIAN_POINT ( 'NONE',  ( -14.25243324638999809, -13.93375672974000068, -0.8660254037843999608 ) ) ;
#10375=CIRCLE ( 'NONE', #19244, 7.000000000000000000 ) ;
#10376=CARTESIAN_POINT ( 'NONE',  ( 4.946082664740999668, 12.51487189599001759, -0.1133811337498999705 ) ) ;
#10377=EDGE_LOOP ( 'NONE', ( #5404, #2627, #20565 ) ) ;
#10378=CARTESIAN_POINT ( 'NONE',  ( -15.22817204324037021, -1.771982936837275924, -10.21894444281640624 ) ) ;
#10379=CARTESIAN_POINT ( 'NONE',  ( 17.64450125731000085, 9.220888413547999818, -0.5479559280035000146 ) ) ;
#10384=CARTESIAN_POINT ( 'NONE',  ( -5.194121241778000275, 0.000000000000000000, 0.000000000000000000 ) ) ;
#10386=CARTESIAN_POINT ( 'NONE',  ( -19.30504787661167043, 6.323484023877028015, 6.721981018013264197 ) ) ;
#10387=CARTESIAN_POINT ( 'NONE',  ( 13.00725174931000083, 10.48226630763000067, 1.840397312871999924 ) ) ;
#10388=CARTESIAN_POINT ( 'NONE',  ( -14.29555379409998928, -1.242885911923757858, -8.999946461797254216 ) ) ;
#10389=CARTESIAN_POINT ( 'NONE',  ( -16.84797557115999922, 10.17000433686999905, 3.756487055001000108 ) ) ;
#10390=CARTESIAN_POINT ( 'NONE',  ( -6.137760362496004873, 15.63629344804000887, 1.260435990244000326 ) ) ;
#10391=CARTESIAN_POINT ( 'NONE',  ( 16.81806994525999954, 1.942066464734999887, -10.12485589047999923 ) ) ;
#10395=ADVANCED_FACE ( 'NONE', ( #11238 ), #15823, .F. ) ;
#10396=CARTESIAN_POINT ( 'NONE',  ( 24.48085323735392294, 8.653296529984718433, 5.020612371803464313 ) ) ;
#10398=CARTESIAN_POINT ( 'NONE',  ( 2.808569713089370534, 14.07519307301941147, 5.443121979668293697 ) ) ;
#10402=CARTESIAN_POINT ( 'NONE',  ( -22.41645255698000128, 10.23964721874999917, -4.326993456033999763 ) ) ;
#10405=CARTESIAN_POINT ( 'NONE',  ( -4.836653794536299955, 12.44483666031821834, 0.4214316309137807748 ) ) ;
#10408=CARTESIAN_POINT ( 'NONE',  ( 2.466980964282978750, 11.74073273616931168, -4.142218052624875746 ) ) ;
#10414=CARTESIAN_POINT ( 'NONE',  ( 12.00000000000000000, -10.65000000000000036, 0.000000000000000000 ) ) ;
#10415=CARTESIAN_POINT ( 'NONE',  ( -14.05208405859999843, -9.143870435873997948, 6.637879840603000403 ) ) ;
#10416=CARTESIAN_POINT ( 'NONE',  ( 11.28262625730999957, -8.806575700274999363, 0.9184129047361999643 ) ) ;
#10418=VECTOR ( 'NONE', #21575, 1000.000000000000000 ) ;
#10419=ORIENTED_EDGE ( 'NONE', *, *, #7616, .F. ) ;
#10420=CARTESIAN_POINT ( 'NONE',  ( 5.290856909789264151, 13.79953964304391789, 4.259698828153141825 ) ) ;
#10423=CARTESIAN_POINT ( 'NONE',  ( 2.717593476773952688, 14.04971210407079951, -5.492367343542457370 ) ) ;
#10424=AXIS2_PLACEMENT_3D ( 'NONE', #20923, #2632, #555 ) ;
#10425=VERTEX_POINT ( 'NONE', #7225 ) ;
#10427=CARTESIAN_POINT ( 'NONE',  ( -24.50000000000000000, -10.82531754731000007, 6.250000000000000000 ) ) ;
#10428=EDGE_CURVE ( 'NONE', #13740, #11881, #22787, .T. ) ;
#10429=CARTESIAN_POINT ( 'NONE',  ( 16.52299999999999969, -9.095294458157999529, 0.000000000000000000 ) ) ;
#10430=CARTESIAN_POINT ( 'NONE',  ( -23.74465998031000069, -6.216878364870000340, 12.50000000000000000 ) ) ;
#10431=CARTESIAN_POINT ( 'NONE',  ( 15.86963858528391391, -6.901509964614469972, -7.784720662817159464 ) ) ;
#10432=CARTESIAN_POINT ( 'NONE',  ( -3.870976219244578242, 13.99445802289816321, 4.846937829204491344 ) ) ;
#10438=CARTESIAN_POINT ( 'NONE',  ( 1.252030728491252409, 11.63101246561627278, -4.623972916844822478 ) ) ;
#10439=ORIENTED_EDGE ( 'NONE', *, *, #4448, .F. ) ;
#10442=CARTESIAN_POINT ( 'NONE',  ( 5.509196045612000603, 14.23526548753000576, 2.583477358259002710 ) ) ;
#10444=CARTESIAN_POINT ( 'NONE',  ( 1.662687440517862214, 12.89555417843306806, 6.484250417384837206 ) ) ;
#10446=CARTESIAN_POINT ( 'NONE',  ( 12.50000000000000000, 13.93375672974000068, 0.1442689875826000112 ) ) ;
#10447=CARTESIAN_POINT ( 'NONE',  ( -11.00000000000000000, 1.359357947053999856E-14, 0.000000000000000000 ) ) ;
#10448=CIRCLE ( 'NONE', #23959, 15.43375672974000068 ) ;
#10449=CARTESIAN_POINT ( 'NONE',  ( -19.10482910584000038, 1.458613477275000161E-14, 0.000000000000000000 ) ) ;
#10450=ORIENTED_EDGE ( 'NONE', *, *, #11575, .T. ) ;
#10453=CARTESIAN_POINT ( 'NONE',  ( -10.04281598263999875, 16.43285860070443860, 0.1718092760798937135 ) ) ;
#10455=CARTESIAN_POINT ( 'NONE',  ( -22.48958999300999650, -8.088488029599998796, -7.066540705739000394 ) ) ;
#10456=CARTESIAN_POINT ( 'NONE',  ( 20.64229166666665805, 1.204281607287347011, -9.201003601022879508 ) ) ;
#10457=CARTESIAN_POINT ( 'NONE',  ( 15.07109509836083383, 8.896268110734828483, 5.261584688652965802 ) ) ;
#10462=EDGE_CURVE ( 'NONE', #7012, #9517, #2492, .T. ) ;
#10463=CARTESIAN_POINT ( 'NONE',  ( 4.448835664791996436, 12.50232644074000099, -1.677463259861998290 ) ) ;
#10464=ORIENTED_EDGE ( 'NONE', *, *, #21768, .F. ) ;
#10465=CARTESIAN_POINT ( 'NONE',  ( -16.08338753829999845, -2.146827734392999787, 11.15102392286999944 ) ) ;
#10469=CARTESIAN_POINT ( 'NONE',  ( -16.14148675361209229, -4.939254558134616779, 9.149695053219954133 ) ) ;
#10471=ORIENTED_EDGE ( 'NONE', *, *, #20089, .F. ) ;
#10472=CARTESIAN_POINT ( 'NONE',  ( 6.171933277826004094, 13.72618630928000627, -1.141834261405999973 ) ) ;
#10473=EDGE_CURVE ( 'NONE', #1236, #22071, #17496, .T. ) ;
#10474=CARTESIAN_POINT ( 'NONE',  ( 11.99999999999999822, 2.003559370708953402, -8.770491923202531126 ) ) ;
#10476=CARTESIAN_POINT ( 'NONE',  ( 14.33221009380999966, 6.651214311818000269, -8.775228328761999208 ) ) ;
#10477=CARTESIAN_POINT ( 'NONE',  ( 12.32268908530999951, 2.255737295330999981, -9.860771559977997924 ) ) ;
#10479=CARTESIAN_POINT ( 'NONE',  ( -9.298203992920999639, -13.92019145675999958, -4.121763198284000396 ) ) ;
#10481=FACE_OUTER_BOUND ( 'NONE', #11774, .T. ) ;
#10482=VERTEX_POINT ( 'NONE', #22476 ) ;
#10484=CARTESIAN_POINT ( 'NONE',  ( 23.23527882761811014, -3.583123978552704703, -9.970115068474655118 ) ) ;
#10485=B_SPLINE_CURVE_WITH_KNOTS ( 'NONE', 3,
 ( #21139, #4681, #13506, #10000, #17391, #4554, #10121, #12068, #786, #23786, #8793, #6965, #10727, #23673, #7082, #14357, #21863, #1525, #16155, #7193, #1635, #19815, #23424, #5273 ),
 .UNSPECIFIED., .F., .F.,
 ( 4, 2, 2, 2, 2, 2, 2, 2, 2, 2, 2, 4 ),
 ( 0.000000000000000000, 0.1004975296504320992, 0.2009950593008641706, 0.2512438241260802063, 0.3014925889512962143, 0.4019901186017282302, 0.4522388834269442381, 0.5024876482521603016, 0.6029851779025924285, 0.7034827075530244445, 0.7537314723782405634, 0.8039802372034564604 ),
 .UNSPECIFIED. ) ;
#10487=CARTESIAN_POINT ( 'NONE',  ( 16.80283205072941755, 10.07070901071222124, 2.591683735843758551 ) ) ;
#10488=CARTESIAN_POINT ( 'NONE',  ( -4.820913537080000033, 13.20111002679000123, 5.836439296936000609 ) ) ;
#10489=CARTESIAN_POINT ( 'NONE',  ( -14.29262089642102040, -7.983102671798886441, 11.17286057040532832 ) ) ;
#10491=CARTESIAN_POINT ( 'NONE',  ( -4.303529988270902606, 13.60822715515925907, -4.961366493816785628 ) ) ;
#10496=CARTESIAN_POINT ( 'NONE',  ( 23.95135407356000101, 3.629452715968999765, 10.34366932978999998 ) ) ;
#10497=CARTESIAN_POINT ( 'NONE',  ( 22.68261335940208312, -2.052889571300259064, 10.38301577081636573 ) ) ;
#10501=CARTESIAN_POINT ( 'NONE',  ( 4.978377891991029536, 14.18254257813881125, 3.873879993161618795 ) ) ;
#10503=CARTESIAN_POINT ( 'NONE',  ( 1.438191898982999151, 11.53459387488998722, -4.742439962699002365 ) ) ;
#10505=CARTESIAN_POINT ( 'NONE',  ( -14.72576977311546820, 10.36129416948303827, -0.02468886294351785304 ) ) ;
#10506=CARTESIAN_POINT ( 'NONE',  ( -12.50000000000000000, 1.557342902441000195E-14, 1.045589212608000028E-14 ) ) ;
#10509=CARTESIAN_POINT ( 'NONE',  ( -12.25000000000000000, -15.45000000000000107, 0.000000000000000000 ) ) ;
#10512=VERTEX_POINT ( 'NONE', #306 ) ;
#10514=FACE_OUTER_BOUND ( 'NONE', #9309, .T. ) ;
#10515=CARTESIAN_POINT ( 'NONE',  ( -24.54530698916000020, 7.467341355790000357, 6.161448972441999850 ) ) ;
#10516=CARTESIAN_POINT ( 'NONE',  ( -16.64484522318999993, 5.321837195625000128, 9.439042293465000455 ) ) ;
#10518=CARTESIAN_POINT ( 'NONE',  ( 19.52687451746000136, 7.010897399879999270, 6.912477489258999519 ) ) ;
#10523=CARTESIAN_POINT ( 'NONE',  ( -17.72676253787999912, 9.126185377371999863, 0.000000000000000000 ) ) ;
#10524=CARTESIAN_POINT ( 'NONE',  ( 0.1440416516300269123, 13.69193005210691005, 6.123308775418226269 ) ) ;
#10528=CARTESIAN_POINT ( 'NONE',  ( -19.42939368183000326, -10.43529125724999851, -0.1440759689522999876 ) ) ;
#10529=CARTESIAN_POINT ( 'NONE',  ( -4.797719810903769755, 12.43002135603972924, 0.7136055140974607580 ) ) ;
#10531=CARTESIAN_POINT ( 'NONE',  ( 4.129449150923196754, 12.19149479092433452, -2.525021771999871767 ) ) ;
#10533=EDGE_LOOP ( 'NONE', ( #5195, #5942, #10834, #8735, #16070 ) ) ;
#10534=EDGE_CURVE ( 'NONE', #15169, #4052, #19724, .T. ) ;
#10535=CARTESIAN_POINT ( 'NONE',  ( -24.12232999016000079, 1.520060141252000183E-14, 0.000000000000000000 ) ) ;
#10536=CARTESIAN_POINT ( 'NONE',  ( -13.23956266673000037, 6.512279107760999608, -9.204720484723999618 ) ) ;
#10537=CARTESIAN_POINT ( 'NONE',  ( 17.12250142130999819, -8.875724825267999663, -3.992994992864999926 ) ) ;
#10538=CARTESIAN_POINT ( 'NONE',  ( 18.48965437448689997, 10.24410807905043619, -1.935809810652562524 ) ) ;
#10539=ORIENTED_EDGE ( 'NONE', *, *, #13816, .F. ) ;
#10542=DIRECTION ( 'NONE',  ( 0.5882164119205371966, 0.8087035629619353516, -9.903762298403940582E-17 ) ) ;
#10543=CARTESIAN_POINT ( 'NONE',  ( 4.050551734779913815, 14.47883186787076504, -4.594425583402780511 ) ) ;
#10544=ORIENTED_EDGE ( 'NONE', *, *, #16904, .F. ) ;
#10546=CYLINDRICAL_SURFACE ( 'NONE', #18176, 14.43375672974000068 ) ;
#10549=DIRECTION ( 'NONE',  ( -0.7071067811865474617, -0.7071067811865474617, 0.000000000000000000 ) ) ;
#10550=CARTESIAN_POINT ( 'NONE',  ( 15.95327017899941069, -4.391970926654074070, -9.430978196784264966 ) ) ;
#10551=CARTESIAN_POINT ( 'NONE',  ( -7.834000000000000519, 1.320585629393000037E-14, 0.000000000000000000 ) ) ;
#10554=ORIENTED_EDGE ( 'NONE', *, *, #23442, .T. ) ;
#10555=CARTESIAN_POINT ( 'NONE',  ( -18.99854661335000117, -13.93375672974000068, 0.000000000000000000 ) ) ;
#10557=VERTEX_POINT ( 'NONE', #17149 ) ;
#10560=CARTESIAN_POINT ( 'NONE',  ( 5.048184257089419980, 13.64448757289546066, 4.715755534370476454 ) ) ;
#10562=CARTESIAN_POINT ( 'NONE',  ( 15.90028936713000185, 9.079314476020000413, 0.000000000000000000 ) ) ;
#10568=CARTESIAN_POINT ( 'NONE',  ( 24.24531177150999994, 13.23032192316000000, 0.000000000000000000 ) ) ;
#10569=CARTESIAN_POINT ( 'NONE',  ( -6.250000000003000267, 15.09565008225999883, -3.212814891752000079 ) ) ;
#10570=ORIENTED_EDGE ( 'NONE', *, *, #11615, .T. ) ;
#10571=CARTESIAN_POINT ( 'NONE',  ( -20.70340094334000014, -9.917170701048998893, 2.249121287463999863 ) ) ;
#10573=CARTESIAN_POINT ( 'NONE',  ( 15.15542662814268304, 7.010537146779027395, 7.597953863240286765 ) ) ;
#10577=DIRECTION ( 'NONE',  ( -1.000000000000000000, 0.000000000000000000, 0.000000000000000000 ) ) ;
#10578=CARTESIAN_POINT ( 'NONE',  ( 3.724578230166001980, 12.24861053738000294, -2.969015338948001848 ) ) ;
#10579=ORIENTED_EDGE ( 'NONE', *, *, #6010, .T. ) ;
#10582=ORIENTED_EDGE ( 'NONE', *, *, #10534, .F. ) ;
#10586=ORIENTED_EDGE ( 'NONE', *, *, #10005, .F. ) ;
#10587=CARTESIAN_POINT ( 'NONE',  ( 11.83261479513038061, -13.04738324255308690, -2.401298039148104024 ) ) ;
#10588=CARTESIAN_POINT ( 'NONE',  ( -4.772366215095780184, 13.34838505587969948, -5.491644434773237826 ) ) ;
#10589=B_SPLINE_CURVE_WITH_KNOTS ( 'NONE', 3,
 ( #2975, #4678, #12063, #19449, #17630 ),
 .UNSPECIFIED., .F., .F.,
 ( 4, 1, 4 ),
 ( 0.000000000000000000, 0.5000000000000000000, 1.000000000000000000 ),
 .UNSPECIFIED. ) ;
#10590=CARTESIAN_POINT ( 'NONE',  ( 16.31716997010999748, 10.46811184600000111, -3.586373476968000240 ) ) ;
#10591=ADVANCED_FACE ( 'NONE', ( #7950 ), #4077, .F. ) ;
#10593=CARTESIAN_POINT ( 'NONE',  ( 11.99362658531000037, -8.009633343651000104, -6.163949985837000156 ) ) ;
#10597=CARTESIAN_POINT ( 'NONE',  ( 13.50000000000000000, 9.162136282950783084, -2.282264667262656310 ) ) ;
#10598=DIRECTION ( 'NONE',  ( -1.000000000000000000, 0.000000000000000000, 0.000000000000000000 ) ) ;
#10600=CARTESIAN_POINT ( 'NONE',  ( -23.20138028387000162, 9.293596334485000554, -2.826991214650000028 ) ) ;
#10601=CARTESIAN_POINT ( 'NONE',  ( 11.39490977864433141, 12.26833003003861933, 3.750544030113681426 ) ) ;
#10602=CARTESIAN_POINT ( 'NONE',  ( 21.20567237728856824, -9.515960249491415723, -4.901612566710888963 ) ) ;
#10604=CARTESIAN_POINT ( 'NONE',  ( -5.420127902049621582, 15.54531213489060981, 2.854267850004046814 ) ) ;
#10605=CARTESIAN_POINT ( 'NONE',  ( 16.19937828008823644, -2.727843005219428019, -9.999616570623473422 ) ) ;
#10606=DIRECTION ( 'NONE',  ( -1.000000000000000000, 0.000000000000000000, 0.000000000000000000 ) ) ;
#10608=EDGE_CURVE ( 'NONE', #19829, #11381, #2251, .T. ) ;
#10612=CARTESIAN_POINT ( 'NONE',  ( 21.87815553483999764, 9.951306365835000278, -5.643451686609999740 ) ) ;
#10613=CARTESIAN_POINT ( 'NONE',  ( 24.35664299550522927, 3.038500614219330931, 10.17926622196943498 ) ) ;
#10615=VECTOR ( 'NONE', #19648, 1000.000000000000000 ) ;
#10616=VERTEX_POINT ( 'NONE', #6849 ) ;
#10618=CARTESIAN_POINT ( 'NONE',  ( 4.893783511618616799, 14.39890544002889428, -3.811344258107727256 ) ) ;
#10619=CARTESIAN_POINT ( 'NONE',  ( -3.300528186783000084, 11.98006166429998665, -3.696077710035002628 ) ) ;
#10620=ORIENTED_EDGE ( 'NONE', *, *, #6581, .T. ) ;
#10621=CARTESIAN_POINT ( 'NONE',  ( 17.31543875730999815, 3.351454173900000111, -8.598433847594998625 ) ) ;
#10622=VECTOR ( 'NONE', #15874, 1000.000000000000000 ) ;
#10627=ORIENTED_EDGE ( 'NONE', *, *, #15777, .F. ) ;
#10628=CARTESIAN_POINT ( 'NONE',  ( 11.00000000000000000, -10.59999999999999964, 0.000000000000000000 ) ) ;
#10629=CARTESIAN_POINT ( 'NONE',  ( 12.34912674931000076, -5.416870430593999863, -9.140812312194999123 ) ) ;
#10630=CARTESIAN_POINT ( 'NONE',  ( -23.63377946391999984, -9.915102125873000105, 2.288295221134000190 ) ) ;
#10631=CARTESIAN_POINT ( 'NONE',  ( 11.43887872962712038, -9.287405149881228894, -8.913622445545286155 ) ) ;
#10632=CARTESIAN_POINT ( 'NONE',  ( -4.939568633879000359, 13.53408867494998802, -5.800137320629999316 ) ) ;
#10634=CARTESIAN_POINT ( 'NONE',  ( -24.21590912748918711, 7.621690869234290844, -7.366582963188160527 ) ) ;
#10637=CARTESIAN_POINT ( 'NONE',  ( 14.86016666666666808, -7.910107230074322260, -4.558955418934749204 ) ) ;
#10639=CARTESIAN_POINT ( 'NONE',  ( -17.34884587121334221, 2.386103976833011231, 8.879258109265995458 ) ) ;
#10640=CARTESIAN_POINT ( 'NONE',  ( 3.918815203773234224, 14.42969747532489677, 4.707339579678993857 ) ) ;
#10645=CARTESIAN_POINT ( 'NONE',  ( -4.313940323335201832, 12.25428752138464361, 2.199116708544083476 ) ) ;
#10646=VERTEX_POINT ( 'NONE', #15804 ) ;
#10648=CARTESIAN_POINT ( 'NONE',  ( 2.929890266377786379, 11.84452384940898284, -3.836082332777877912 ) ) ;
#10649=VECTOR ( 'NONE', #10822, 1000.000000000000114 ) ;
#10650=CARTESIAN_POINT ( 'NONE',  ( 11.55866343642402683, -7.053686836476363631, -5.580721502645149990 ) ) ;
#10654=CARTESIAN_POINT ( 'NONE',  ( 15.36750142131000096, -7.843339156370999099, -5.684071587432000250 ) ) ;
#10655=CARTESIAN_POINT ( 'NONE',  ( 18.64504799222103415, 9.813939602435103993, 3.576112584041952314 ) ) ;
#10660=CARTESIAN_POINT ( 'NONE',  ( 13.50000000000000000, -9.675600895433166926, 0.1311100501057143597 ) ) ;
#10661=AXIS2_PLACEMENT_3D ( 'NONE', #9571, #16477, #11159 ) ;
#10664=CARTESIAN_POINT ( 'NONE',  ( -24.27585716844503594, -12.49018833526878147, 3.366221553749007445 ) ) ;
#10665=CARTESIAN_POINT ( 'NONE',  ( 16.22066666666666279, -4.576538324501929544, 7.940613831594722782 ) ) ;
#10666=CARTESIAN_POINT ( 'NONE',  ( -23.86746844839299797, -5.192331206338657523, 8.183175371501549833 ) ) ;
#10667=CARTESIAN_POINT ( 'NONE',  ( -24.50000000000000000, -14.43375672974000068, 0.000000000000000000 ) ) ;
#10669=CARTESIAN_POINT ( 'NONE',  ( -4.889513280961001129, 12.49342386908999281, 0.7528201520557004089 ) ) ;
#10670=ADVANCED_FACE ( 'NONE', ( #6613 ), #5056, .F. ) ;
#10671=DIRECTION ( 'NONE',  ( 0.000000000000000000, 1.000000000000000000, 0.000000000000000000 ) ) ;
#10672=EDGE_LOOP ( 'NONE', ( #13654, #465, #9714, #22083 ) ) ;
#10679=CARTESIAN_POINT ( 'NONE',  ( 5.302309868036999774, 13.73032359673999814, 4.450989051274000019 ) ) ;
#10680=CONICAL_SURFACE ( 'NONE', #11825, 9.152445778720998959, 0.02565634000431304615 ) ;
#10681=CARTESIAN_POINT ( 'NONE',  ( 6.195977518297981490, 13.89472266009280332, -0.8605928538500070557 ) ) ;
#10684=CARTESIAN_POINT ( 'NONE',  ( -14.00000000000000000, -9.461855175648539173, -3.635004795172248393 ) ) ;
#10688=CARTESIAN_POINT ( 'NONE',  ( -19.67520052968999877, 9.945309867329999776, 1.982757173051000077 ) ) ;
#10690=CARTESIAN_POINT ( 'NONE',  ( 14.65641172841788631, 6.408862456806628138, -8.094750487372301961 ) ) ;
#10691=FACE_OUTER_BOUND ( 'NONE', #2217, .T. ) ;
#10692=CARTESIAN_POINT ( 'NONE',  ( 24.63960826817999816, -10.15308605020999977, 2.981009416082999852 ) ) ;
#10694=CARTESIAN_POINT ( 'NONE',  ( -22.90514205544799253, 5.691906622003466865, 7.406426240607752121 ) ) ;
#10695=CARTESIAN_POINT ( 'NONE',  ( -4.722378179075000126, 12.45689350211999979, -0.7786282501865993133 ) ) ;
#10696=ORIENTED_EDGE ( 'NONE', *, *, #4203, .T. ) ;
#10697=TOROIDAL_SURFACE ( 'NONE', #7964, 14.44999999999999929, 2.000000000000000000 ) ;
#10699=EDGE_CURVE ( 'NONE', #15235, #11532, #23194, .T. ) ;
#10700=ORIENTED_EDGE ( 'NONE', *, *, #19465, .T. ) ;
#10702=CARTESIAN_POINT ( 'NONE',  ( -14.28937962731940559, -6.103406805596817364, 8.356759130325041696 ) ) ;
#10704=CARTESIAN_POINT ( 'NONE',  ( 12.28022044528328038, -13.65679895893291196, -1.345730334378181903 ) ) ;
#10706=CARTESIAN_POINT ( 'NONE',  ( 24.35625626386771003, 3.237027092069015843, -12.49999999999999822 ) ) ;
#10708=ADVANCED_FACE ( 'NONE', ( #17887 ), #19282, .T. ) ;
#10709=VERTEX_POINT ( 'NONE', #126 ) ;
#10711=CARTESIAN_POINT ( 'NONE',  ( -10.31642899291999882, 9.736743735031000213, -10.76830904284000034 ) ) ;
#10712=CIRCLE ( 'NONE', #17657, 12.44999999999999929 ) ;
#10713=CARTESIAN_POINT ( 'NONE',  ( 13.50000000000000000, 4.517872873748999929, -7.804362139085999850 ) ) ;
#10714=PLANE ( 'NONE',  #6711 ) ;
#10716=CARTESIAN_POINT ( 'NONE',  ( 23.02937672396094371, -9.233243326448210553, -5.186586685900737237 ) ) ;
#10717=CARTESIAN_POINT ( 'NONE',  ( -14.00000000000000533, 7.443612114797377721, 5.400680299557988562 ) ) ;
#10718=CARTESIAN_POINT ( 'NONE',  ( 17.07981319014894694, 3.655019374395102716, 9.752800675042001544 ) ) ;
#10719=EDGE_CURVE ( 'NONE', #12251, #8738, #23134, .T. ) ;
#10720=CARTESIAN_POINT ( 'NONE',  ( -18.08550596641000396, 9.682332165709999217, 5.434252367816999829 ) ) ;
#10722=AXIS2_PLACEMENT_3D ( 'NONE', #19933, #5164, #5505 ) ;
#10723=CARTESIAN_POINT ( 'NONE',  ( -13.92980981492000048, 8.913287911097999228, 3.799313832512000388 ) ) ;
#10727=CARTESIAN_POINT ( 'NONE',  ( 23.36219854623860925, -1.214243892273371817, 9.213288387738314711 ) ) ;
#10728=CARTESIAN_POINT ( 'NONE',  ( 20.13889713280000038, 11.01791241213000028, -2.895620158417999690 ) ) ;
#10729=CARTESIAN_POINT ( 'NONE',  ( 19.84527499312657639, -2.175409197760720836, -10.28494925254862480 ) ) ;
#10732=VERTEX_POINT ( 'NONE', #9110 ) ;
#10734=CARTESIAN_POINT ( 'NONE',  ( 4.846430159580084052, 14.59246997775862908, -3.777182888792198323 ) ) ;
#10735=CARTESIAN_POINT ( 'NONE',  ( -4.911774959493002690, 12.43823275897999636, 0.1548668838414998805 ) ) ;
#10736=ORIENTED_EDGE ( 'NONE', *, *, #5666, .T. ) ;
#10738=CARTESIAN_POINT ( 'NONE',  ( 17.42512625730999787, 6.303186173173999762, -6.744507379544999459 ) ) ;
#10742=CARTESIAN_POINT ( 'NONE',  ( -23.75083293559999831, -13.93375672974000068, -0.6735967306123999965 ) ) ;
#10743=ORIENTED_EDGE ( 'NONE', *, *, #15869, .F. ) ;
#10746=CARTESIAN_POINT ( 'NONE',  ( -21.86732592927000240, -9.361678282808000517, 3.864640653608000243 ) ) ;
#10748=CARTESIAN_POINT ( 'NONE',  ( -14.00083134239000060, 8.121744576791000370, -4.249165445770000105 ) ) ;
#10750=CARTESIAN_POINT ( 'NONE',  ( -22.67180158262788936, -1.394108788844021118, -10.47118158913528241 ) ) ;
#10752=B_SPLINE_CURVE_WITH_KNOTS ( 'NONE', 3,
 ( #9235, #18098, #5597, #14682, #18326, #7064, #23768, #14561, #21957, #7408, #14789, #12639, #22184, #12979, #18562, #1966, #3786, #11175 ),
 .UNSPECIFIED., .F., .F.,
 ( 4, 2, 2, 2, 2, 2, 2, 2, 4 ),
 ( 0.000000000000000000, 0.1250000000000000000, 0.2500000000000000000, 0.3749999999999999445, 0.4999999999999999445, 0.6250000000000000000, 0.7500000000000000000, 0.8750000000000000000, 1.000000000000000000 ),
 .UNSPECIFIED. ) ;
#10756=ORIENTED_EDGE ( 'NONE', *, *, #11724, .T. ) ;
#10762=CIRCLE ( 'NONE', #23105, 12.44999999999999929 ) ;
#10765=CARTESIAN_POINT ( 'NONE',  ( 0.9483885206027318215, 11.52112569081479698, 4.718712483813342295 ) ) ;
#10767=CARTESIAN_POINT ( 'NONE',  ( 17.95908333333332507, -2.390202921478481457, 8.894510420082752944 ) ) ;
#10768=CARTESIAN_POINT ( 'NONE',  ( 2.835570222853222688, 11.82190223321585520, -3.905115993759757043 ) ) ;
#10769=EDGE_CURVE ( 'NONE', #13583, #1109, #1333, .T. ) ;
#10770=CARTESIAN_POINT ( 'NONE',  ( 24.08098870454836771, -2.879575660560934391, -8.995033484217190178 ) ) ;
#10773=ORIENTED_EDGE ( 'NONE', *, *, #5719, .T. ) ;
#10777=CARTESIAN_POINT ( 'NONE',  ( 14.70937642131000089, 0.7886220128679000130, 9.636901145054999063 ) ) ;
#10778=CARTESIAN_POINT ( 'NONE',  ( 18.45579459229852759, 9.947470068809831645, -3.106797963599987611 ) ) ;
#10779=ORIENTED_EDGE ( 'NONE', *, *, #5925, .T. ) ;
#10782=CARTESIAN_POINT ( 'NONE',  ( 19.05150246751999887, -4.061773497662999333, 10.04047824780999854 ) ) ;
#10783=CARTESIAN_POINT ( 'NONE',  ( 13.50000000000000000, -9.094337642950469203, 3.923034256449659640 ) ) ;
#10786=CARTESIAN_POINT ( 'NONE',  ( -24.48376588670970833, -11.33649700729262300, 5.364757780054595138 ) ) ;
#10790=CARTESIAN_POINT ( 'NONE',  ( -4.155850825563766726, 13.71339692482677108, 4.894222041114647759 ) ) ;
#10791=AXIS2_PLACEMENT_3D ( 'NONE', #1707, #7386, #18199 ) ;
#10792=CARTESIAN_POINT ( 'NONE',  ( -3.747811089796003525, 12.10619433494998631, 3.242694335594999977 ) ) ;
#10801=CARTESIAN_POINT ( 'NONE',  ( 11.22285964975960759, 2.000465806355621545, -12.49999014999358593 ) ) ;
#10804=VECTOR ( 'NONE', #17573, 1000.000000000000000 ) ;
#10813=CARTESIAN_POINT ( 'NONE',  ( -10.81061242803241207, 15.37188199527473209, -1.657872610222045129 ) ) ;
#10815=CARTESIAN_POINT ( 'NONE',  ( 14.81476371884029497, 9.716835099164804035, -3.542462622313707232 ) ) ;
#10818=CARTESIAN_POINT ( 'NONE',  ( 24.27251434224999826, -0.1538460603255000225, 11.30793493386000037 ) ) ;
#10821=CARTESIAN_POINT ( 'NONE',  ( -4.811303441321004293, 12.64225309966998623, 0.1541779168885000495 ) ) ;
#10822=DIRECTION ( 'NONE',  ( 0.5882164119205371966, -0.8087035629619353516, 0.000000000000000000 ) ) ;
#10823=AXIS2_PLACEMENT_3D ( 'NONE', #19963, #12696, #2022 ) ;
#10824=ORIENTED_EDGE ( 'NONE', *, *, #12067, .T. ) ;
#10826=CARTESIAN_POINT ( 'NONE',  ( -24.50000000000000000, -10.82531754731000007, -6.250000000000000000 ) ) ;
#10830=CARTESIAN_POINT ( 'NONE',  ( 11.39490977864411470, -12.26833003003723732, -3.750544030117427763 ) ) ;
#10833=CARTESIAN_POINT ( 'NONE',  ( 17.18559515836999907, -6.254670336401999542, 9.156935761679001473 ) ) ;
#10834=ORIENTED_EDGE ( 'NONE', *, *, #15031, .F. ) ;
#10835=CARTESIAN_POINT ( 'NONE',  ( -11.53092506584999910, 5.630713802624000230, 13.76055599481999892 ) ) ;
#10837=CARTESIAN_POINT ( 'NONE',  ( -14.42499013958043541, -12.50426282925849897, -3.341925919231215403 ) ) ;
#10838=AXIS2_PLACEMENT_3D ( 'NONE', #10249, #19704, #13998 ) ;
#10839=EDGE_CURVE ( 'NONE', #20433, #16718, #5822, .T. ) ;
#10841=CARTESIAN_POINT ( 'NONE',  ( 20.58796606631835857, 0.9461998122939191402, 10.48927542155332304 ) ) ;
#10842=CARTESIAN_POINT ( 'NONE',  ( 12.50000000000000000, -13.93375672974000068, 0.000000000000000000 ) ) ;
#10843=CARTESIAN_POINT ( 'NONE',  ( 16.01298929817072292, -8.180129550563604468, -6.355079070724960033 ) ) ;
#10847=CARTESIAN_POINT ( 'NONE',  ( -18.80493816619999947, -6.461643014194000223, 6.332623921217999552 ) ) ;
#10848=ADVANCED_FACE ( 'NONE', ( #2182 ), #20958, .F. ) ;
#10851=CARTESIAN_POINT ( 'NONE',  ( 20.86671680498296766, -1.970433400296279780, 10.35129057732945412 ) ) ;
#10855=CARTESIAN_POINT ( 'NONE',  ( -14.25243324638999809, -6.216878364870000340, -12.50000000000000000 ) ) ;
#10856=CARTESIAN_POINT ( 'NONE',  ( 0.3698661250554000635, 11.49512849500999323, -4.800726696805998728 ) ) ;
#10857=VERTEX_POINT ( 'NONE', #7762 ) ;
#10862=EDGE_CURVE ( 'NONE', #4095, #4052, #11520, .T. ) ;
#10863=EDGE_LOOP ( 'NONE', ( #10419, #281, #2793, #20002 ) ) ;
#10864=CARTESIAN_POINT ( 'NONE',  ( -15.30809587121333415, -4.564978959981946360, 7.920054021321541349 ) ) ;
#10865=CARTESIAN_POINT ( 'NONE',  ( -21.22497918939999906, 2.624718450046000129, -9.764018522075000206 ) ) ;
#10866=CARTESIAN_POINT ( 'NONE',  ( -19.41764062158999948, 9.069691137161999706, -3.822207856851999708 ) ) ;
#10868=CARTESIAN_POINT ( 'NONE',  ( -23.16076897183521766, -10.23206097900809475, 2.674434693994577561 ) ) ;
#10871=ADVANCED_FACE ( 'NONE', ( #20715 ), #23550, .T. ) ;
#10878=CIRCLE ( 'NONE', #23636, 12.44999999999999929 ) ;
#10879=DIRECTION ( 'NONE',  ( 0.000000000000000000, 0.9999453485888588622, 0.01045465616390955921 ) ) ;
#10880=ORIENTED_EDGE ( 'NONE', *, *, #15777, .T. ) ;
#10881=EDGE_CURVE ( 'NONE', #5259, #16694, #4497, .T. ) ;
#10882=CARTESIAN_POINT ( 'NONE',  ( -2.920465629076966163, 11.84211311063798888, -3.843655616409710873 ) ) ;
#10883=CARTESIAN_POINT ( 'NONE',  ( 24.16322961496833344, 1.753000555242941516, -9.398851739486781653 ) ) ;
#10888=DIRECTION ( 'NONE',  ( 0.000000000000000000, 0.9999173538268769645, -0.01285634146465969990 ) ) ;
#10890=CARTESIAN_POINT ( 'NONE',  ( 18.79425158531000051, -6.072333155528000681, 7.996935486658999892 ) ) ;
#10891=CARTESIAN_POINT ( 'NONE',  ( 18.59376286737137818, 10.28297712058548008, 1.725429498650708160 ) ) ;
#10895=CARTESIAN_POINT ( 'NONE',  ( -12.49507687580999971, 6.705241787176000834, -5.996946098961000615 ) ) ;
#10896=LINE ( 'NONE', #5096, #8532 ) ;
#10899=CARTESIAN_POINT ( 'NONE',  ( 21.00984673308000339, -8.695248534891000247, 7.185696252475000101 ) ) ;
#10902=B_SPLINE_CURVE_WITH_KNOTS ( 'NONE', 3,
 ( #5358, #5704, #7880, #17079, #18901 ),
 .UNSPECIFIED., .F., .F.,
 ( 4, 1, 4 ),
 ( 0.000000000000000000, 0.5000000000000000000, 1.000000000000000000 ),
 .UNSPECIFIED. ) ;
#10903=EDGE_CURVE ( 'NONE', #19902, #19018, #12016, .T. ) ;
#10904=DIRECTION ( 'NONE',  ( 0.000000000000000000, 0.000000000000000000, 1.000000000000000000 ) ) ;
#10905=FACE_OUTER_BOUND ( 'NONE', #21176, .T. ) ;
#10906=CARTESIAN_POINT ( 'NONE',  ( -4.940722032108995521, 12.51282703623000536, -0.1567078306562000589 ) ) ;
#10908=CARTESIAN_POINT ( 'NONE',  ( -24.14868686146999721, -0.7737383780821999180, -11.13665872500999932 ) ) ;
#10912=CARTESIAN_POINT ( 'NONE',  ( 5.805205508519002855, 13.82243867059999509, 2.388040532770999480 ) ) ;
#10913=CARTESIAN_POINT ( 'NONE',  ( 11.48696334737532432, 3.271224437879761027, -12.49992143329918903 ) ) ;
#10914=DIRECTION ( 'NONE',  ( 1.000000000000000000, -0.000000000000000000, -0.000000000000000000 ) ) ;
#10915=CARTESIAN_POINT ( 'NONE',  ( 13.50000000000000178, -0.9241557808115162809, 10.25573529546197804 ) ) ;
#10917=B_SPLINE_CURVE_WITH_KNOTS ( 'NONE', 3,
 ( #13078, #5693, #15234, #11630, #351, #17066, #16825, #20587, #18763, #16705, #18654, #20705, #9801, #11511, #2060, #2174, #13551, #7628, #5812, #463, #2411, #15005, #581, #7867, #22404, #13195, #7986, #15116, #3997, #9566, #2297, #22514 ),
 .UNSPECIFIED., .F., .F.,
 ( 4, 2, 2, 2, 2, 2, 2, 2, 2, 2, 2, 2, 2, 2, 2, 4 ),
 ( 0.000000000000000000, 0.1250000000000000555, 0.1875000000000001943, 0.2187500000000002220, 0.2500000000000002220, 0.3125000000000002220, 0.3437500000000002220, 0.3750000000000002220, 0.5000000000000003331, 0.5625000000000003331, 0.5937500000000003331, 0.6250000000000004441, 0.6875000000000004441, 0.7187500000000004441, 0.7500000000000004441, 1.000000000000000000 ),
 .UNSPECIFIED. ) ;
#10919=CARTESIAN_POINT ( 'NONE',  ( -17.99241677431999875, 4.425129475628999387, -8.746809379632999537 ) ) ;
#10925=CARTESIAN_POINT ( 'NONE',  ( 14.72221008384615182, 8.065344004061731908, -6.473147478577542024 ) ) ;
#10926=CIRCLE ( 'NONE', #14011, 7.000000000000000000 ) ;
#10927=CARTESIAN_POINT ( 'NONE',  ( -18.55817920454666847, -8.909387095795679556, -2.394461597111133155 ) ) ;
#10928=CARTESIAN_POINT ( 'NONE',  ( 19.13319937917999880, -9.753461774593999323, 5.439862873842999491 ) ) ;
#10930=CARTESIAN_POINT ( 'NONE',  ( 14.04262667236427831, 6.000419062831993777, 6.762735978225977718 ) ) ;
#10931=CARTESIAN_POINT ( 'NONE',  ( 4.795731778619003904, 12.63621800153999075, -0.5225435171593996175 ) ) ;
#10934=CARTESIAN_POINT ( 'NONE',  ( -14.86522788937946338, -8.015611292679002631, -4.223672244188741765 ) ) ;
#10935=AXIS2_PLACEMENT_3D ( 'NONE', #4272, #20975, #8512 ) ;
#10938=CARTESIAN_POINT ( 'NONE',  ( -15.61632910584000022, 9.072027496059000384, 0.000000000000000000 ) ) ;
#10939=CARTESIAN_POINT ( 'NONE',  ( 11.48478210364763541, -12.46109695279135288, -3.416571976975812941 ) ) ;
#10940=DIRECTION ( 'NONE',  ( 0.9996708941621513800, -0.02565352539213145919, 0.000000000000000000 ) ) ;
#10941=CARTESIAN_POINT ( 'NONE',  ( 15.05401368519000016, -0.07836042960794999124, 11.03054286538000106 ) ) ;
#10942=CARTESIAN_POINT ( 'NONE',  ( -14.11172255407341325, -5.446421583873537031, 8.794184178919268291 ) ) ;
#10944=CARTESIAN_POINT ( 'NONE',  ( -10.09803613877000039, -2.313608892657999849, 15.04153609805999992 ) ) ;
#10945=CARTESIAN_POINT ( 'NONE',  ( 13.50000000000000000, 7.641056615018084308, -5.228549223296183435 ) ) ;
#10948=CARTESIAN_POINT ( 'NONE',  ( 23.11762048267087977, -7.246916755350970796, -7.729893100918809878 ) ) ;
#10951=CARTESIAN_POINT ( 'NONE',  ( 16.18882540054575259, -3.105308896812054797, -9.887464255232517374 ) ) ;
#10952=CARTESIAN_POINT ( 'NONE',  ( -4.982685754363140873, 13.67876053192405905, 5.582247605641564192 ) ) ;
#10953=CARTESIAN_POINT ( 'NONE',  ( -14.39391672138606992, -12.88860090843611061, 2.676267392864990491 ) ) ;
#10956=EDGE_LOOP ( 'NONE', ( #117, #23371, #15928 ) ) ;
#10958=CARTESIAN_POINT ( 'NONE',  ( 19.67503469114785730, -7.524009671958713952, -7.334830238956850934 ) ) ;
#10960=VERTEX_POINT ( 'NONE', #9195 ) ;
#10961=EDGE_CURVE ( 'NONE', #14047, #2380, #11172, .T. ) ;
#10962=DIRECTION ( 'NONE',  ( 0.000000000000000000, 1.000000000000000000, 0.000000000000000000 ) ) ;
#10965=CARTESIAN_POINT ( 'NONE',  ( -3.196386508574998953, 11.94625779823998357, -3.568797075887999437 ) ) ;
#10967=CARTESIAN_POINT ( 'NONE',  ( 16.35468892131000018, 6.000265896171000257, 7.637201470843999473 ) ) ;
#10968=ORIENTED_EDGE ( 'NONE', *, *, #11634, .T. ) ;
#10969=CARTESIAN_POINT ( 'NONE',  ( -5.050080520837401110, 15.90270261739640922, 3.465883707748838916 ) ) ;
#10974=ORIENTED_EDGE ( 'NONE', *, *, #3651, .F. ) ;
#10975=CARTESIAN_POINT ( 'NONE',  ( -15.87497087121333017, 9.078664753515003127, 1.188521384907375467 ) ) ;
#10976=CARTESIAN_POINT ( 'NONE',  ( -19.99381460464000071, -9.570925607007000124, 1.774722651697000053 ) ) ;
#10978=CARTESIAN_POINT ( 'NONE',  ( -5.542211513735998629, 15.02033096712999338, -2.995715936518001499 ) ) ;
#10979=CARTESIAN_POINT ( 'NONE',  ( -22.13136394192933665, 10.52421200172316951, 1.769957956558704026 ) ) ;
#10981=CARTESIAN_POINT ( 'NONE',  ( -12.25000000000000000, 1.374666032043000015E-14, 0.000000000000000000 ) ) ;
#10984=CARTESIAN_POINT ( 'NONE',  ( 4.787200832998987465, 14.77986595429568162, 3.821410012779939969 ) ) ;
#10985=CARTESIAN_POINT ( 'NONE',  ( 14.46456608149148515, 2.351140429448762337, 8.785231713726679104 ) ) ;
#10986=B_SPLINE_CURVE_WITH_KNOTS ( 'NONE', 3,
 ( #11223, #4062, #13145, #19066, #15429, #13258, #9630, #17015, #3827, #173, #13370, #5873, #20773, #4179, #11456, #8057, #20538, #15302 ),
 .UNSPECIFIED., .F., .F.,
 ( 4, 2, 2, 2, 2, 2, 2, 2, 4 ),
 ( 0.000000000000000000, 0.1250000000000000000, 0.2500000000000000555, 0.3750000000000001110, 0.5000000000000001110, 0.6250000000000001110, 0.7500000000000001110, 0.8750000000000001110, 1.000000000000000000 ),
 .UNSPECIFIED. ) ;
#10990=CARTESIAN_POINT ( 'NONE',  ( 0.8369952473213599919, 11.51240063293612970, 4.739979841301923180 ) ) ;
#10992=CARTESIAN_POINT ( 'NONE',  ( -1.122479358643900360, 11.53522643002050074, -4.684283708769314991 ) ) ;
#10993=CARTESIAN_POINT ( 'NONE',  ( -10.65331237176230950, 15.43888331649234225, 1.511769160805160217 ) ) ;
#10995=ORIENTED_EDGE ( 'NONE', *, *, #2527, .F. ) ;
#10996=EDGE_CURVE ( 'NONE', #6063, #10960, #14268, .T. ) ;
#10999=CARTESIAN_POINT ( 'NONE',  ( 14.84550158531000008, 4.534570621724000716, 9.116298118718001220 ) ) ;
#11000=CARTESIAN_POINT ( 'NONE',  ( 18.61878911107620382, 10.09093427090647666, 2.640026560685321044 ) ) ;
#11004=DIRECTION ( 'NONE',  ( 1.000000000000000000, 0.000000000000000000, 0.000000000000000000 ) ) ;
#11005=CARTESIAN_POINT ( 'NONE',  ( 13.49999999999999645, -9.561895257915249857, -0.9817478549585191283 ) ) ;
#11007=ADVANCED_FACE ( 'NONE', ( #7483 ), #18182, .F. ) ;
#11009=CARTESIAN_POINT ( 'NONE',  ( 23.58278963329000177, -5.861239335239000425, -9.096485928357999740 ) ) ;
#11013=AXIS2_PLACEMENT_3D ( 'NONE', #12376, #14304, #7029 ) ;
#11014=CARTESIAN_POINT ( 'NONE',  ( -4.899115602372003941, 12.43333805657998603, 0.4236866773311000478 ) ) ;
#11016=ADVANCED_FACE ( 'NONE', ( #16449, #5330 ), #8856, .T. ) ;
#11017=CARTESIAN_POINT ( 'NONE',  ( -12.24999999999999822, 13.59206128970241778, -6.344557540553090291 ) ) ;
#11018=VERTEX_POINT ( 'NONE', #692 ) ;
#11023=CARTESIAN_POINT ( 'NONE',  ( 5.182093470520005241, 14.34449281741999727, 3.190697958076003093 ) ) ;
#11025=B_SPLINE_CURVE_WITH_KNOTS ( 'NONE', 3,
 ( #9024, #21748, #5161, #15913, #16280, #18119, #8914, #14469, #19573, #12305, #12661, #21384, #4799, #4919 ),
 .UNSPECIFIED., .F., .F.,
 ( 4, 2, 2, 2, 2, 2, 4 ),
 ( 0.000000000000000000, 0.2500000000000007772, 0.3750000000000008327, 0.5000000000000006661, 0.6250000000000004441, 0.7500000000000003331, 1.000000000000000000 ),
 .UNSPECIFIED. ) ;
#11026=CARTESIAN_POINT ( 'NONE',  ( 18.98579496512684628, -1.886667643284684948, 10.26048715248877485 ) ) ;
#11027=DIRECTION ( 'NONE',  ( -1.000000000000000000, 0.000000000000000000, 0.000000000000000000 ) ) ;
#11028=CARTESIAN_POINT ( 'NONE',  ( 11.81081408531000143, -9.938255359128000066, -0.2191561108886999898 ) ) ;
#11033=B_SPLINE_CURVE_WITH_KNOTS ( 'NONE', 3,
 ( #2728, #19441, #13492, #2477 ),
 .UNSPECIFIED., .F., .F.,
 ( 4, 4 ),
 ( 0.000000000000000000, 1.000000000000000000 ),
 .UNSPECIFIED. ) ;
#11034=CARTESIAN_POINT ( 'NONE',  ( 14.99328936713000004, -9.056039068417000237, 0.000000000000000000 ) ) ;
#11035=CARTESIAN_POINT ( 'NONE',  ( 23.15628936713000030, 9.265517736846000219, 0.000000000000000000 ) ) ;
#11036=ORIENTED_EDGE ( 'NONE', *, *, #14325, .F. ) ;
#11037=CARTESIAN_POINT ( 'NONE',  ( -22.56211168660000155, -2.887064115966999633, -10.88924876608999881 ) ) ;
#11039=CARTESIAN_POINT ( 'NONE',  ( 14.69340912245870001, 7.378059427811160198, -7.245375437766548465 ) ) ;
#11040=FACE_OUTER_BOUND ( 'NONE', #7042, .T. ) ;
#11041=CARTESIAN_POINT ( 'NONE',  ( 23.09738183229000086, -10.55345434226000023, 3.972832674855999890 ) ) ;
#11043=CARTESIAN_POINT ( 'NONE',  ( 13.93170734267679123, 8.120445290024731477, 4.030814257595042527 ) ) ;
#11044=CARTESIAN_POINT ( 'NONE',  ( -6.461264013247827620, 15.49809339140494480, -1.417960285014638444 ) ) ;
#11046=ADVANCED_FACE ( 'NONE', ( #2393 ), #13645, .F. ) ;
#11049=AXIS2_PLACEMENT_3D ( 'NONE', #8093, #6380, #13284 ) ;
#11050=CARTESIAN_POINT ( 'NONE',  ( 24.50000000000000355, -9.703066433905631172, -2.676520811178526582 ) ) ;
#11052=CARTESIAN_POINT ( 'NONE',  ( -16.10762077250664248, -1.189048994148048655, -9.084635008511355636 ) ) ;
#11055=CARTESIAN_POINT ( 'NONE',  ( 14.62545328758000096, 6.656066219229999525, -8.781628413182000159 ) ) ;
#11058=EDGE_CURVE ( 'NONE', #8671, #4782, #13408, .T. ) ;
#11061=CARTESIAN_POINT ( 'NONE',  ( -10.50532613877000010, 15.21613563232000033, 0.2642172441792000614 ) ) ;
#11063=CARTESIAN_POINT ( 'NONE',  ( -14.00000000000000000, 1.396097351027999937E-14, 0.000000000000000000 ) ) ;
#11064=CIRCLE ( 'NONE', #5262, 9.974367097859005327 ) ;
#11065=VERTEX_POINT ( 'NONE', #20687 ) ;
#11066=CARTESIAN_POINT ( 'NONE',  ( -6.250000000000000000, -15.43375672974000068, 0.000000000000000000 ) ) ;
#11067=CARTESIAN_POINT ( 'NONE',  ( 20.51087270046332733, -8.958289992760562370, -2.407343205403928099 ) ) ;
#11069=CARTESIAN_POINT ( 'NONE',  ( 23.99062354302999722, 7.716878364870000340, -11.63397459621999985 ) ) ;
#11070=CARTESIAN_POINT ( 'NONE',  ( 16.02151485735762293, -7.988024155100645451, -6.595574518746330384 ) ) ;
#11071=CARTESIAN_POINT ( 'NONE',  ( -13.62914419562999946, -10.20270304202000133, -2.517845328698999907 ) ) ;
#11077=CARTESIAN_POINT ( 'NONE',  ( 19.95876852777634625, 1.938386817457601108, -10.33238417878841631 ) ) ;
#11078=CARTESIAN_POINT ( 'NONE',  ( -5.833999999999999631, -12.89775331292639926, -5.076083135505105348E-10 ) ) ;
#11079=EDGE_LOOP ( 'NONE', ( #14938, #8142, #16187, #19560, #18680 ) ) ;
#11080=CARTESIAN_POINT ( 'NONE',  ( 5.302309868036999774, 13.73032359673999814, 4.450989051274000019 ) ) ;
#11083=CARTESIAN_POINT ( 'NONE',  ( 4.818401220988001832, 12.41582519560999032, -0.5157391765471998069 ) ) ;
#11084=CARTESIAN_POINT ( 'NONE',  ( 15.45075125730999943, 1.788522226178000052, -9.003565944673999510 ) ) ;
#11092=CARTESIAN_POINT ( 'NONE',  ( -17.72676253787999912, 9.126185377371999863, 0.000000000000000000 ) ) ;
#11093=CARTESIAN_POINT ( 'NONE',  ( 12.00000000000000178, 1.904880462199602054, -9.045477544701622463 ) ) ;
#11094=EDGE_CURVE ( 'NONE', #19490, #9699, #11727, .T. ) ;
#11097=CARTESIAN_POINT ( 'NONE',  ( -21.92548293594716924, 6.766409901490216150, 8.245667780346659370 ) ) ;
#11099=CIRCLE ( 'NONE', #14948, 7.500000000000000000 ) ;
#11100=CARTESIAN_POINT ( 'NONE',  ( 6.117240279542961012, 14.37689077026887041, 0.3699855186153612197 ) ) ;
#11105=CARTESIAN_POINT ( 'NONE',  ( 4.369209802590991565, 13.43978707160767883, -5.263635815137498675 ) ) ;
#11106=CARTESIAN_POINT ( 'NONE',  ( -24.12520316825921896, 4.399791340197258371, -9.646299765070683208 ) ) ;
#11109=CIRCLE ( 'NONE', #4933, 12.50000000000000178 ) ;
#11110=CARTESIAN_POINT ( 'NONE',  ( 2.091802670701738531, 11.66854640885106953, 4.341499821985210339 ) ) ;
#11112=CARTESIAN_POINT ( 'NONE',  ( -2.802233683753186266, 11.81444791271924899, -3.927002317657668051 ) ) ;
#11114=AXIS2_PLACEMENT_3D ( 'NONE', #23290, #6466, #21001 ) ;
#11117=DIRECTION ( 'NONE',  ( 1.000000000000000000, 0.000000000000000000, 0.000000000000000000 ) ) ;
#11118=CARTESIAN_POINT ( 'NONE',  ( 12.76143908531000193, 9.974460201879001175, 1.751222586102000101 ) ) ;
#11119=CARTESIAN_POINT ( 'NONE',  ( 18.31564036859069233, 7.307524194310222043, -7.427871909705804576 ) ) ;
#11121=CARTESIAN_POINT ( 'NONE',  ( -5.372793533988000192, 16.07374366253000275, 2.940837684191000001 ) ) ;
#11124=DIRECTION ( 'NONE',  ( -1.000000000000000000, 0.000000000000000000, 0.000000000000000000 ) ) ;
#11125=ORIENTED_EDGE ( 'NONE', *, *, #4973, .T. ) ;
#11126=CARTESIAN_POINT ( 'NONE',  ( -24.49594166687722208, 11.08137607230481869, 5.806427241679596563 ) ) ;
#11127=CARTESIAN_POINT ( 'NONE',  ( 23.05164232683000236, -7.202366762678000356, 8.056812634288998964 ) ) ;
#11133=CARTESIAN_POINT ( 'NONE',  ( -3.678206510409002483, 12.01686478324999818, 3.158609924971003124 ) ) ;
#11135=EDGE_CURVE ( 'NONE', #12183, #15471, #17182, .T. ) ;
#11139=VERTEX_POINT ( 'NONE', #6264 ) ;
#11141=CARTESIAN_POINT ( 'NONE',  ( 4.722551773131003827, 14.52147321335999663, 3.832747064962003680 ) ) ;
#11142=CARTESIAN_POINT ( 'NONE',  ( 16.16483103379665920, 5.583924645481782356, 7.265765639378300556 ) ) ;
#11143=CARTESIAN_POINT ( 'NONE',  ( -16.89534587121332621, -8.867923303744074559, 2.383057832484115401 ) ) ;
#11146=CARTESIAN_POINT ( 'NONE',  ( 15.94237658530999902, 1.989471272253999778, -10.01494924120000007 ) ) ;
#11149=CARTESIAN_POINT ( 'NONE',  ( -12.71102772709999940, -0.8480750162247000512, -9.618334173012000221 ) ) ;
#11152=CARTESIAN_POINT ( 'NONE',  ( 24.00016455292000117, -9.287173237304083173, 0.000000000000000000 ) ) ;
#11153=EDGE_CURVE ( 'NONE', #12304, #5259, #11705, .T. ) ;
#11155=CARTESIAN_POINT ( 'NONE',  ( -21.01981106612999994, -10.46178610027000033, -4.064235816344999641 ) ) ;
#11157=CARTESIAN_POINT ( 'NONE',  ( 14.42251860313111500, -1.405275611345024434, -10.22176834447581228 ) ) ;
#11158=AXIS2_PLACEMENT_3D ( 'NONE', #3614, #14397, #22458 ) ;
#11159=DIRECTION ( 'NONE',  ( 0.000000000000000000, -0.8660254037844288266, -0.5000000000000169864 ) ) ;
#11160=CARTESIAN_POINT ( 'NONE',  ( 22.36319398042000373, 10.93760387994999839, 2.659607438111999844 ) ) ;
#11162=CARTESIAN_POINT ( 'NONE',  ( 14.12090646444330488, 4.006132324064554773, 8.116375441945786307 ) ) ;
#11166=EDGE_CURVE ( 'NONE', #17463, #3590, #1501, .T. ) ;
#11167=CARTESIAN_POINT ( 'NONE',  ( 11.06626444615592320, 10.69977336184266115, -6.467440677431063101 ) ) ;
#11172=CIRCLE ( 'NONE', #13097, 13.77250448648999637 ) ;
#11173=CARTESIAN_POINT ( 'NONE',  ( 11.64696834793616098, -8.717038812755488308, -3.317893490969420434 ) ) ;
#11174=DIRECTION ( 'NONE',  ( 1.000000000000000000, 0.000000000000000000, 0.000000000000000000 ) ) ;
#11175=CARTESIAN_POINT ( 'NONE',  ( 22.24928936712999672, -9.242242329243000043, 0.000000000000000000 ) ) ;
#11177=TOROIDAL_SURFACE ( 'NONE', #15407, 5.625000000000000000, 0.5000000000000000000 ) ;
#11178=CARTESIAN_POINT ( 'NONE',  ( 16.10288977129999921, -0.1032177031646999976, -11.05906605220000039 ) ) ;
#11179=FACE_BOUND ( 'NONE', #20405, .T. ) ;
#11183=CARTESIAN_POINT ( 'NONE',  ( -10.19985863876999943, 4.116323844992999526, 14.65115941988999992 ) ) ;
#11184=AXIS2_PLACEMENT_3D ( 'NONE', #1036, #12191, #1287 ) ;
#11188=ORIENTED_EDGE ( 'NONE', *, *, #22137, .F. ) ;
#11190=CARTESIAN_POINT ( 'NONE',  ( -14.46758738162251845, 11.92463202973721792, 4.345869468068095820 ) ) ;
#11191=CARTESIAN_POINT ( 'NONE',  ( 20.96437270046331491, 2.410389349752802168, -8.969624798282467282 ) ) ;
#11192=CARTESIAN_POINT ( 'NONE',  ( 6.241414926470116420, 13.66656409111985404, 1.744778710455607618 ) ) ;
#11193=CARTESIAN_POINT ( 'NONE',  ( 16.19032491852358291, -3.051673150441691629, -9.904219964709449542 ) ) ;
#11194=CARTESIAN_POINT ( 'NONE',  ( -17.50947430316999842, -10.99790399745999991, 1.405211504096999908 ) ) ;
#11198=CARTESIAN_POINT ( 'NONE',  ( -15.79874102787999846, 5.047191510808999304, 8.952058016012999886 ) ) ;
#11203=EDGE_CURVE ( 'NONE', #21250, #11018, #20372, .T. ) ;
#11204=CARTESIAN_POINT ( 'NONE',  ( 20.44111605004497534, 10.09892154715089596, 2.954736731020451757 ) ) ;
#11205=CARTESIAN_POINT ( 'NONE',  ( 11.74999999482999868, 0.000000000000000000, 1.045589212608000028E-14 ) ) ;
#11207=ORIENTED_EDGE ( 'NONE', *, *, #19952, .F. ) ;
#11208=CARTESIAN_POINT ( 'NONE',  ( 12.52688711657000020, 7.716878364870000340, 11.63397459621999985 ) ) ;
#11209=CARTESIAN_POINT ( 'NONE',  ( -4.018738216213002090, 13.61287253962000499, 4.587140350181000414 ) ) ;
#11211=AXIS2_PLACEMENT_3D ( 'NONE', #5535, #14617, #12916 ) ;
#11212=CARTESIAN_POINT ( 'NONE',  ( 13.91512625730999986, 8.379890869990997970, -3.647050788746000194 ) ) ;
#11213=PRODUCT_DEFINITION_CONTEXT ( 'detailed design', #8513, 'design' ) ;
#11216=CARTESIAN_POINT ( 'NONE',  ( -5.372793533988000192, 16.07374366253000275, 2.940837684191000001 ) ) ;
#11217=CARTESIAN_POINT ( 'NONE',  ( -14.48633704289933810, 1.427546401368239293, -12.50000676666208221 ) ) ;
#11219=B_SPLINE_CURVE_WITH_KNOTS ( 'NONE', 3,
 ( #9478, #258, #7663, #5952, #15037, #11541, #22433, #13226, #498, #20618 ),
 .UNSPECIFIED., .F., .F.,
 ( 4, 2, 2, 2, 4 ),
 ( 0.000000000000000000, 0.2500000000000001110, 0.5000000000000002220, 0.7500000000000001110, 1.000000000000000000 ),
 .UNSPECIFIED. ) ;
#11220=DIRECTION ( 'NONE',  ( 0.000000000000000000, 0.000000000000000000, -1.000000000000000000 ) ) ;
#11221=CARTESIAN_POINT ( 'NONE',  ( -4.798612374681999526, 12.63734946677000437, 0.4217961273138995937 ) ) ;
#11222=CARTESIAN_POINT ( 'NONE',  ( -23.74237356432000112, -9.140086274078999651, -3.124721474173000058 ) ) ;
#11223=CARTESIAN_POINT ( 'NONE',  ( 18.62128936713000371, -9.149140698829999252, 0.000000000000000000 ) ) ;
#11224=CARTESIAN_POINT ( 'NONE',  ( -4.722737441090003152, 16.04185223773001923, -4.014586937476998685 ) ) ;
#11225=CARTESIAN_POINT ( 'NONE',  ( -21.77107218145970080, 1.618043913735445205, 10.53815187480507198 ) ) ;
#11226=CARTESIAN_POINT ( 'NONE',  ( 5.155714003469999973, 13.97328511022999997, 4.008150528822999270 ) ) ;
#11228=CARTESIAN_POINT ( 'NONE',  ( -6.410055968098999912, 15.31889920838999863, 1.282157099098000463 ) ) ;
#11229=( BOUNDED_CURVE ( )  B_SPLINE_CURVE ( 3, ( #8729, #8605, #15967, #11100, #23361, #6779, #23490, #2483, #2606, #4065, #5990, #8061, #20901, #9752, #2240, #657 ),
 .UNSPECIFIED., .F., .F. ) 
 B_SPLINE_CURVE_WITH_KNOTS ( ( 4, 1, 1, 1, 1, 1, 1, 1, 1, 1, 1, 1, 1, 4 ),
 ( 0.000000000000000000, 0.002937754778506720781, 0.09205143729370196537, 0.1757691448987817595, 0.2560824178855284905, 0.3346853618078635129, 0.4126475807299391785, 0.4905595280248493117, 0.5689923879210118107, 0.6485670012755897496, 0.7300432222292638773, 0.8156447607010655076, 0.9090046746429836233, 1.000000000000000000 ),
 .UNSPECIFIED. ) 
 CURVE ( )  GEOMETRIC_REPRESENTATION_ITEM ( )  RATIONAL_B_SPLINE_CURVE ( ( 1.058246922893853581, 1.058246922893853581, 1.058246922893853581, 1.058246922893853581, 1.058246922893853581, 1.058246922893853581, 1.058246922893853581, 1.058246922893853581, 1.058246922893853581, 1.058246922893853581, 1.058246922893853581, 1.058246922893853581, 1.058246922893853581, 1.058246922893853581, 1.058246922893853581, 1.058246922893853581 ) ) 
 REPRESENTATION_ITEM ( '' )  );
#11232=CARTESIAN_POINT ( 'NONE',  ( -17.43032910583999850, 9.118578311265999048, 0.000000000000000000 ) ) ;
#11233=CARTESIAN_POINT ( 'NONE',  ( 24.03948154624000111, -9.843283099998000552, -0.9867796264882999768 ) ) ;
#11235=CARTESIAN_POINT ( 'NONE',  ( -23.96454491813620180, 8.827218892942170214, -5.864176129446873276 ) ) ;
#11237=CARTESIAN_POINT ( 'NONE',  ( 12.00000000000000000, -8.391897884961000642, -3.194141202603999918 ) ) ;
#11238=FACE_OUTER_BOUND ( 'NONE', #21297, .T. ) ;
#11240=CARTESIAN_POINT ( 'NONE',  ( -0.08431463819058247766, 11.48104257302984088, -4.815429911517862038 ) ) ;
#11241=CARTESIAN_POINT ( 'NONE',  ( 24.38510397947348096, 12.27045979993889802, 3.746940194273108204 ) ) ;
#11242=CARTESIAN_POINT ( 'NONE',  ( 12.52688711657000020, -13.93375672974000068, 0.8660254037843999608 ) ) ;
#11244=CARTESIAN_POINT ( 'NONE',  ( 23.99478584078000054, -7.550251870592999737, 11.73017644753999988 ) ) ;
#11245=CARTESIAN_POINT ( 'NONE',  ( 17.47800158530999681, -7.122204577229999778, -7.372745388647000020 ) ) ;
#11246=CARTESIAN_POINT ( 'NONE',  ( 18.36750925429045012, 8.490495120173470411, -6.047999897081842491 ) ) ;
#11247=CARTESIAN_POINT ( 'NONE',  ( -24.50000000000452971, 0.2564718131585235206, 12.50000000000233946 ) ) ;
#11249=CARTESIAN_POINT ( 'NONE',  ( 14.51551537306000128, -5.756020581778999556, -9.120548154372999150 ) ) ;
#11250=CARTESIAN_POINT ( 'NONE',  ( 13.50000000000000000, -5.669411096634266123, -7.227943221418801301 ) ) ;
#11251=ORIENTED_EDGE ( 'NONE', *, *, #20156, .T. ) ;
#11252=CARTESIAN_POINT ( 'NONE',  ( -23.74465998031000069, 13.93375672974000068, 0.8660254037843999608 ) ) ;
#11253=CARTESIAN_POINT ( 'NONE',  ( 24.11393693976000208, 10.34077239664000025, -3.237760962710000356 ) ) ;
#11256=CARTESIAN_POINT ( 'NONE',  ( -12.49016237973315313, 6.849135750923734278, -5.827197512145549929 ) ) ;
#11259=CARTESIAN_POINT ( 'NONE',  ( 3.786219791712002625, 12.04888752014999653, 3.147501422329002096 ) ) ;
#11262=CARTESIAN_POINT ( 'NONE',  ( -19.63740412539999980, 1.666533117798999930, 10.91439899677999925 ) ) ;
#11266=ADVANCED_FACE ( 'NONE', ( #7343 ), #5301, .T. ) ;
#11270=CYLINDRICAL_SURFACE ( 'NONE', #1060, 4.750000000000000000 ) ;
#11272=DIRECTION ( 'NONE',  ( 0.000000000000000000, 1.000000000000000000, 0.000000000000000000 ) ) ;
#11274=CARTESIAN_POINT ( 'NONE',  ( -15.75798294665000121, 9.136783202530001091, 3.374990494159999965 ) ) ;
#11275=FACE_OUTER_BOUND ( 'NONE', #9347, .T. ) ;
#11279=CARTESIAN_POINT ( 'NONE',  ( -20.33434412369999933, 10.33430737248000142, -4.330206088669999787 ) ) ;
#11281=CARTESIAN_POINT ( 'NONE',  ( 13.86150418236414161, -8.974767284217415764, 5.068416743520222312 ) ) ;
#11283=CARTESIAN_POINT ( 'NONE',  ( 20.56464971682999732, 7.808581107292000389, 8.038765694828999386 ) ) ;
#11285=CARTESIAN_POINT ( 'NONE',  ( 13.69363924190391302, 8.424036582202942824, -3.228120261996942908 ) ) ;
#11286=CARTESIAN_POINT ( 'NONE',  ( -6.281974597825559670, 15.68480551511767729, -1.218664578910494400 ) ) ;
#11288=CARTESIAN_POINT ( 'NONE',  ( 11.39490977864222998, 9.382231423120625635, -8.749413452953497483 ) ) ;
#11292=EDGE_LOOP ( 'NONE', ( #19001, #3549, #22711 ) ) ;
#11296=CARTESIAN_POINT ( 'NONE',  ( 0.000000000000000000, 21.50000000000000000, 0.000000000000000000 ) ) ;
#11297=CARTESIAN_POINT ( 'NONE',  ( 24.19085492956958561, -9.549256642876626344, 0.0002501093553063627687 ) ) ;
#11298=CARTESIAN_POINT ( 'NONE',  ( 16.06906047033999840, -6.554063206097999306, -8.907152100438999298 ) ) ;
#11301=VERTEX_POINT ( 'NONE', #7221 ) ;
#11302=ORIENTED_EDGE ( 'NONE', *, *, #18897, .T. ) ;
#11306=DIRECTION ( 'NONE',  ( -2.971992933571787233E-05, -0.9999999995583628287, -8.164609096927661075E-09 ) ) ;
#11308=ADVANCED_FACE ( 'NONE', ( #5189 ), #23919, .T. ) ;
#11309=CARTESIAN_POINT ( 'NONE',  ( -14.37382028566454650, 13.01774735372515046, 2.452106660089753642 ) ) ;
#11310=CARTESIAN_POINT ( 'NONE',  ( 19.88201599663697294, 5.989684672267420851, -8.637120499181696331 ) ) ;
#11312=CARTESIAN_POINT ( 'NONE',  ( 16.01801534404138394, -8.067232948202645915, -6.498016440650728143 ) ) ;
#11313=CARTESIAN_POINT ( 'NONE',  ( -19.43654966351000013, -9.242645412567998875, 5.313552282507999713 ) ) ;
#11316=CARTESIAN_POINT ( 'NONE',  ( -16.04262945707999677, 5.313593037366000082, 9.424424275870000756 ) ) ;
#11319=ORIENTED_EDGE ( 'NONE', *, *, #22567, .F. ) ;
#11322=CARTESIAN_POINT ( 'NONE',  ( -17.93571553221221393, -5.561216854535629750, 8.842563169821765712 ) ) ;
#11325=CARTESIAN_POINT ( 'NONE',  ( 24.18393254356892896, -4.886968879243103636, 12.50000000000000178 ) ) ;
#11326=CARTESIAN_POINT ( 'NONE',  ( -3.428088622465001567, 14.04569531913998937, 5.080072178502000213 ) ) ;
#11327=EDGE_CURVE ( 'NONE', #20695, #13697, #19959, .T. ) ;
#11329=CARTESIAN_POINT ( 'NONE',  ( 16.68375142130999933, -4.435783964195000095, 8.649968580473998969 ) ) ;
#11330=EDGE_LOOP ( 'NONE', ( #4247, #21867, #5177, #5139 ) ) ;
#11331=B_SPLINE_CURVE_WITH_KNOTS ( 'NONE', 3,
 ( #16818, #20124, #11026, #22161 ),
 .UNSPECIFIED., .F., .F.,
 ( 4, 4 ),
 ( 0.000000000000000000, 1.000000000000000000 ),
 .UNSPECIFIED. ) ;
#11333=CARTESIAN_POINT ( 'NONE',  ( -4.632252426630697251, 15.60046821123447813, 4.007232082546550167 ) ) ;
#11335=B_SPLINE_SURFACE_WITH_KNOTS ( 'NONE', 3, 3, ( 
 ( #114, #9684, #9799, #19375, #8232, #2784, #22627, #2657, #22868, #22747, #10052, #462, #4240, #12112, #6530, #21187, #11862, #706, #9920, #17064, #13666, #11629, #19498, #829, #17435, #20826, #11990, #17185, #18999, #6403, #13915, #4353, #10170, #951, #7865, #15233, #2409, #6038, #15599, #17307, #13426, #580, #19116, #17555, #7985, #15357, #4724, #13550, #8350, #8117, #22986, #13785, #15482, #15714, #21311, #4601, #6282, #6165, #23106, #20946, #11743, #21059, #2530, #4473, #19246, #15842, #10416 ),
 ( #1076, #17807, #5316, #23231, #19744, #3393, #8956, #16080, #1447, #8843, #12355, #15957, #23350, #3154, #10537, #12706, #8594, #21790, #17922, #7121, #3271, #21905, #8475, #1203, #16324, #6768, #14511, #2907, #1327, #23605, #10654, #14040, #6644, #18169, #12233, #19620, #10777, #21678, #14161, #23715, #21556, #10289, #4970, #8716, #14283, #23479, #5090, #6890, #7010, #18042, #16208, #17678, #21433, #4846, #3029, #12470, #19856, #14398, #5205, #12587, #19974, #1572, #22024, #3509, #18623, #16913, #23827 ),
 ( #10890, #317, #7357, #7722, #22135, #7236, #16790, #7591, #18736, #5437, #16560, #18384, #14742, #11245, #18276, #1675, #2030, #12818, #15087, #20440, #9303, #20211, #9065, #3616, #3852, #5546, #14970, #12924, #22484, #5893, #7469, #20098, #16436, #14627, #9420, #85, #5782, #10999, #1795, #20321, #14854, #198, #5659, #3729, #9183, #1914, #22242, #22368, #13166, #20556, #13044, #3970, #11363, #2143, #23950, #9537, #11118, #18504, #16677, #20678, #8322, #17158, #11962, #4325, #6252, #17410, #11716 ),
 ( #4570, #2758, #13636, #9890, #9657, #19351, #4086, #13756, #15453, #17038, #8204, #19088, #2502, #22840, #11481, #4208, #15687, #2263, #6132, #21159, #10139, #17280, #11836, #19217, #22720, #2382, #9771, #13523, #20920, #23077, #18974, #15570, #680, #17528, #21031, #13279, #18858, #20797, #920, #553, #435, #7837, #8087, #10025, #4446, #15207, #22604, #6012, #13398, #11601, #7958, #2629, #15331, #803, #22958, #6375, #10387, #12326, #17897, #21402, #1298, #1178, #10629, #21652, #5065, #19947, #2877 ) ),
 .UNSPECIFIED., .F., .F., .F.,
 ( 4, 4 ),
 ( 4, 1, 1, 1, 1, 1, 1, 1, 1, 1, 1, 1, 1, 1, 1, 1, 1, 1, 1, 1, 1, 1, 1, 1, 1, 1, 1, 1, 1, 1, 1, 1, 1, 1, 1, 1, 1, 1, 1, 1, 1, 1, 1, 1, 1, 1, 1, 1, 1, 1, 1, 1, 1, 1, 1, 1, 1, 1, 1, 1, 1, 1, 1, 1, 4 ),
 ( -0.08331297109794000288, 1.083312971098000066 ),
 ( -0.02000000000000000042, -0.003749999999999999861, 0.01250000000000000069, 0.02875000000000000125, 0.04499999999999999833, 0.06124999999999999889, 0.07749999999999999944, 0.09375000000000000000, 0.1100000000000000006, 0.1262500000000000011, 0.1424999999999999878, 0.1587500000000000022, 0.1749999999999999889, 0.1912500000000000033, 0.2074999999999999900, 0.2237500000000000044, 0.2399999999999999911, 0.2562499999999999778, 0.2725000000000000200, 0.2887500000000000067, 0.3049999999999999933, 0.3212499999999999800, 0.3375000000000000222, 0.3537500000000000089, 0.3699999999999999956, 0.3862499999999999822, 0.4025000000000000244, 0.4187500000000000111, 0.4349999999999999978, 0.4512499999999999845, 0.4675000000000000266, 0.4837500000000000133, 0.5000000000000000000, 0.5162499999999999867, 0.5324999999999999734, 0.5487499999999999600, 0.5649999999999999467, 0.5812500000000000444, 0.5975000000000000311, 0.6137500000000000178, 0.6300000000000000044, 0.6462499999999999911, 0.6624999999999999778, 0.6787499999999999645, 0.6949999999999999512, 0.7112500000000000488, 0.7275000000000000355, 0.7437500000000000222, 0.7600000000000000089, 0.7762499999999999956, 0.7924999999999999822, 0.8087499999999999689, 0.8249999999999999556, 0.8412500000000000533, 0.8575000000000000400, 0.8737500000000000266, 0.8900000000000000133, 0.9062500000000000000, 0.9224999999999999867, 0.9387499999999999734, 0.9549999999999999600, 0.9712499999999999467, 0.9875000000000000444, 1.003749999999999920, 1.020000000000000018 ),
 .UNSPECIFIED. ) ;
#11336=VERTEX_POINT ( 'NONE', #8827 ) ;
#11338=CARTESIAN_POINT ( 'NONE',  ( 22.89174770046333407, 5.689831819425626769, -7.403988410609271931 ) ) ;
#11339=CARTESIAN_POINT ( 'NONE',  ( -4.593072733376997618, 12.55937666042000345, 1.460090207240998694 ) ) ;
#11340=CARTESIAN_POINT ( 'NONE',  ( -20.85181323488999894, 5.829520124619999244, 7.603889561582000134 ) ) ;
#11341=CARTESIAN_POINT ( 'NONE',  ( -14.45561362881575462, 9.532958125092610757, -8.488361093004769486 ) ) ;
#11342=CARTESIAN_POINT ( 'NONE',  ( -4.676113636882003100, 15.28248474626999531, -3.572242236667999560 ) ) ;
#11343=DIRECTION ( 'NONE',  ( 0.000000000000000000, 1.000000000000000000, 0.000000000000000000 ) ) ;
#11346=EDGE_LOOP ( 'NONE', ( #12776, #13917, #4581 ) ) ;
#11347=CARTESIAN_POINT ( 'NONE',  ( -17.39253743917333495, 9.117608502615587085, 1.193619109743944584 ) ) ;
#11348=CARTESIAN_POINT ( 'NONE',  ( 19.98121194148999891, -1.753880888304999885, 9.622565653743999192 ) ) ;
#11351=DIRECTION ( 'NONE',  ( 0.000000000000000000, 0.000000000000000000, 1.000000000000000000 ) ) ;
#11352=CARTESIAN_POINT ( 'NONE',  ( -24.01809766817718739, 7.654457563781243756, -7.454922064010741423 ) ) ;
#11355=ORIENTED_EDGE ( 'NONE', *, *, #11615, .F. ) ;
#11356=CARTESIAN_POINT ( 'NONE',  ( -0.8888509597944463936, 11.51654473730785888, -4.729873641147137597 ) ) ;
#11357=CARTESIAN_POINT ( 'NONE',  ( 24.48327518124253643, 11.46871523476161059, 5.135602515852324856 ) ) ;
#11359=ORIENTED_EDGE ( 'NONE', *, *, #3636, .T. ) ;
#11360=EDGE_CURVE ( 'NONE', #21466, #20461, #14278, .T. ) ;
#11363=CARTESIAN_POINT ( 'NONE',  ( 13.20018908531000079, -1.240977706124000157, 10.06232283554999896 ) ) ;
#11364=FACE_OUTER_BOUND ( 'NONE', #14030, .T. ) ;
#11366=CARTESIAN_POINT ( 'NONE',  ( 13.49989037305999950, 8.681618249821999811, 6.350899454929000321 ) ) ;
#11368=DIRECTION ( 'NONE',  ( -0.9996708941621502698, -0.02565352539217870959, -3.571920101197821240E-14 ) ) ;
#11370=CARTESIAN_POINT ( 'NONE',  ( 23.06310416476999592, 8.733239352628999086, 4.332342072756000029 ) ) ;
#11373=ORIENTED_EDGE ( 'NONE', *, *, #13978, .F. ) ;
#11374=CARTESIAN_POINT ( 'NONE',  ( 11.89873226653999794, -8.042551475384998483, -4.234871351403000084 ) ) ;
#11375=FACE_OUTER_BOUND ( 'NONE', #13605, .T. ) ;
#11376=CARTESIAN_POINT ( 'NONE',  ( 2.369987487222001032, 11.69121506501000951, 4.325025584672001600 ) ) ;
#11378=CARTESIAN_POINT ( 'NONE',  ( -24.60901460102000016, -6.746808026584999674, -8.909132170008000173 ) ) ;
#11380=CARTESIAN_POINT ( 'NONE',  ( -18.73259798496000172, -8.620928137991000995, 3.072238420002000314 ) ) ;
#11381=VERTEX_POINT ( 'NONE', #9404 ) ;
#11384=CARTESIAN_POINT ( 'NONE',  ( 5.091363865865001337, 14.05312055460999687, 3.675988761441002062 ) ) ;
#11386=CARTESIAN_POINT ( 'NONE',  ( 16.27820603379666409, 2.379147093495555421, 8.852401313026854623 ) ) ;
#11388=CARTESIAN_POINT ( 'NONE',  ( 23.99062354302999722, 6.216878364870000340, 12.50000000000000000 ) ) ;
#11389=CIRCLE ( 'NONE', #1725, 15.45000000000000107 ) ;
#11390=CARTESIAN_POINT ( 'NONE',  ( -12.54865546036000090, 9.084388929069001861, -2.336084003038000123 ) ) ;
#11394=VERTEX_POINT ( 'NONE', #22589 ) ;
#11395=CARTESIAN_POINT ( 'NONE',  ( 12.50000000000000000, -13.93375672974000068, -0.1443160066108999939 ) ) ;
#11397=CARTESIAN_POINT ( 'NONE',  ( 14.21677320012310020, -7.733754170777608294, -6.825353183793160028 ) ) ;
#11398=AXIS2_PLACEMENT_3D ( 'NONE', #19065, #9868, #8056 ) ;
#11400=CARTESIAN_POINT ( 'NONE',  ( 18.94965241622000107, -4.614544171587000143, 10.16351295409999977 ) ) ;
#11403=CARTESIAN_POINT ( 'NONE',  ( 14.40647345916092270, -4.520956232057431023, 7.829320738539829350 ) ) ;
#11404=CARTESIAN_POINT ( 'NONE',  ( 24.24531177150999994, 0.000000000000000000, 0.000000000000000000 ) ) ;
#11406=CARTESIAN_POINT ( 'NONE',  ( 12.06371966925150829, 8.266677038032856473, -10.68189384366227479 ) ) ;
#11408=CARTESIAN_POINT ( 'NONE',  ( 12.04708237233491275, -13.35071834206843988, 1.875975938905986684 ) ) ;
#11409=ORIENTED_EDGE ( 'NONE', *, *, #18729, .T. ) ;
#11410=CARTESIAN_POINT ( 'NONE',  ( -16.33437077250664515, -7.269244768974109761, -5.586598368547599058 ) ) ;
#11412=CARTESIAN_POINT ( 'NONE',  ( -23.75391248683000356, -6.466663555194999802, -12.35578645312999946 ) ) ;
#11415=CARTESIAN_POINT ( 'NONE',  ( 16.24951136818999942, -0.1032548074114000153, -11.06308154020999979 ) ) ;
#11420=CARTESIAN_POINT ( 'NONE',  ( 23.99062354302999722, 13.93375672974000068, 0.8660254037843999608 ) ) ;
#11423=FACE_OUTER_BOUND ( 'NONE', #13461, .T. ) ;
#11424=ORIENTED_EDGE ( 'NONE', *, *, #805, .T. ) ;
#11425=CARTESIAN_POINT ( 'NONE',  ( 20.01733333333332965, -8.274956899206415528, 4.125424567703399603 ) ) ;
#11426=CARTESIAN_POINT ( 'NONE',  ( 21.30449770046331182, 9.217997112989703368, -1.206759948112940517 ) ) ;
#11427=CARTESIAN_POINT ( 'NONE',  ( 6.190159225257540143, 13.92116770842173779, 0.7872319910898135653 ) ) ;
#11428=CARTESIAN_POINT ( 'NONE',  ( 15.67523878052337238, -9.013036842459623443, 5.090761818925328974 ) ) ;
#11429=CARTESIAN_POINT ( 'NONE',  ( -14.79952457769999974, 10.86285964459999853, -1.812798036683000102 ) ) ;
#11432=CIRCLE ( 'NONE', #19564, 13.93375672974000068 ) ;
#11433=CARTESIAN_POINT ( 'NONE',  ( -14.37682859208999986, 9.777980407524001549, -3.031781461267000211 ) ) ;
#11435=EDGE_LOOP ( 'NONE', ( #12891, #5074 ) ) ;
#11436=CARTESIAN_POINT ( 'NONE',  ( -24.50000000000000000, -1.873582633960999999, -10.39897383761999983 ) ) ;
#11437=CARTESIAN_POINT ( 'NONE',  ( -19.26691752923823486, -8.287860411292584217, -6.431204527717159891 ) ) ;
#11439=DIRECTION ( 'NONE',  ( -1.000000000000000000, 0.000000000000000000, 0.000000000000000000 ) ) ;
#11440=CARTESIAN_POINT ( 'NONE',  ( -4.278150909564998550, 14.58147911605000679, 4.161691560141001389 ) ) ;
#11441=ADVANCED_FACE ( 'NONE', ( #9756 ), #6303, .F. ) ;
#11444=CARTESIAN_POINT ( 'NONE',  ( 18.00000142131000302, 9.258615172493000145, 3.074095935696000037 ) ) ;
#11446=CIRCLE ( 'NONE', #7184, 7.000000000000000000 ) ;
#11447=CARTESIAN_POINT ( 'NONE',  ( -11.00000000000000000, 7.000000000000000000, 0.000000000000000000 ) ) ;
#11448=EDGE_CURVE ( 'NONE', #4536, #8569, #7655, .T. ) ;
#11451=CARTESIAN_POINT ( 'NONE',  ( -16.63080420454665287, -7.275327887506832347, -5.591273266071538295 ) ) ;
#11452=CARTESIAN_POINT ( 'NONE',  ( -12.50000000000000000, 6.965460728298000781, -5.686777139159000072 ) ) ;
#11453=CARTESIAN_POINT ( 'NONE',  ( 2.851731227921999512, 12.01786460732001238, 3.895295054763002973 ) ) ;
#11454=CARTESIAN_POINT ( 'NONE',  ( 12.00000000000000178, -4.124037653275831161, -8.674183391547163779 ) ) ;
#11456=CARTESIAN_POINT ( 'NONE',  ( 19.37712270046332463, 8.011294138967238965, -4.617566475226050571 ) ) ;
#11457=LINE ( 'NONE', #5988, #23161 ) ;
#11462=ORIENTED_EDGE ( 'NONE', *, *, #6761, .T. ) ;
#11463=CARTESIAN_POINT ( 'NONE',  ( 18.43520447300999976, -8.716575242777999222, 4.343080581981999977 ) ) ;
#11464=CARTESIAN_POINT ( 'NONE',  ( 4.108142509193211112, 13.36663345100772382, -5.448696863470299689 ) ) ;
#11466=DIRECTION ( 'NONE',  ( 0.000000000000000000, 1.000000000000000000, 0.000000000000000000 ) ) ;
#11468=CARTESIAN_POINT ( 'NONE',  ( -22.67927891715234523, -7.913208109210116525, -6.993918658383377007 ) ) ;
#11470=B_SPLINE_CURVE_WITH_KNOTS ( 'NONE', 3,
 ( #7242, #7362, #7016, #21797, #14404, #23485, #12594, #21910, #16565, #6896, #18282, #5212, #14747, #8962, #19980, #1801, #1681, #20326, #22142, #5551, #14291, #10783, #18389, #22031, #16330, #12825, #21684, #14632, #5322, #23721, #9188, #7128, #12477, #12711, #19862, #10660, #20105, #12930, #11005, #3515, #16443, #9071, #5442, #20216, #3622, #20682, #5664, #15092, #6138, #13527, #20560, #9776, #4212, #11250, #20925, #18628 ),
 .UNSPECIFIED., .F., .F.,
 ( 4, 1, 1, 2, 2, 1, 1, 1, 1, 1, 2, 2, 1, 1, 1, 1, 1, 2, 2, 1, 1, 1, 1, 2, 2, 2, 2, 1, 2, 2, 1, 1, 1, 2, 2, 2, 2, 4 ),
 ( 0.000000000000000000, 0.06250000000000063838, 0.09375000000000109635, 0.1093750000000013323, 0.1250000000000015543, 0.1875000000000023870, 0.2187500000000027478, 0.2343750000000028588, 0.2421875000000028588, 0.2460937500000029421, 0.2480468750000029421, 0.2500000000000029976, 0.3125000000000032196, 0.3437500000000032196, 0.3593750000000032752, 0.3671875000000032752, 0.3710937500000032752, 0.3730468750000033307, 0.3750000000000033307, 0.4375000000000032196, 0.4687500000000032196, 0.4843750000000032752, 0.4921875000000033307, 0.4960937500000032752, 0.5000000000000032196, 0.5312500000000033307, 0.5625000000000033307, 0.5937500000000033307, 0.6093750000000033307, 0.6250000000000033307, 0.6875000000000034417, 0.7187500000000035527, 0.7343750000000036637, 0.7421875000000035527, 0.7500000000000035527, 0.8125000000000026645, 0.8750000000000016653, 1.000000000000000000 ),
 .UNSPECIFIED. ) ;
#11472=DIRECTION ( 'NONE',  ( 0.000000000000000000, 1.000000000000000000, 0.000000000000000000 ) ) ;
#11474=CARTESIAN_POINT ( 'NONE',  ( -19.30321267869325652, -10.36687096048695089, 1.553511350694324777 ) ) ;
#11475=CARTESIAN_POINT ( 'NONE',  ( 23.99062354302999722, -6.216878364870000340, -12.50000000000000000 ) ) ;
#11476=AXIS2_PLACEMENT_3D ( 'NONE', #15667, #15552, #901 ) ;
#11478=ORIENTED_EDGE ( 'NONE', *, *, #14977, .F. ) ;
#11479=CARTESIAN_POINT ( 'NONE',  ( -23.74465998031000069, 13.93375672974000068, -0.8660254037843999608 ) ) ;
#11480=AXIS2_PLACEMENT_3D ( 'NONE', #12570, #1555, #23699 ) ;
#11481=CARTESIAN_POINT ( 'NONE',  ( 17.61412674930999955, -9.816082492500997958, -4.416083812485999793 ) ) ;
#11483=CARTESIAN_POINT ( 'NONE',  ( -16.98505548173000079, 5.629683008772999209, -9.891015770318000833 ) ) ;
#11484=DIRECTION ( 'NONE',  ( -1.000000000000000000, 0.000000000000000000, 0.000000000000000000 ) ) ;
#11486=CARTESIAN_POINT ( 'NONE',  ( 13.22858580085999947, 9.111092516355000726, 6.665155751670000406 ) ) ;
#11488=CARTESIAN_POINT ( 'NONE',  ( 11.50000000000000000, 0.000000000000000000, 0.000000000000000000 ) ) ;
#11489=CARTESIAN_POINT ( 'NONE',  ( 22.96884869472000190, 4.899556332588000274, 9.032014534518999938 ) ) ;
#11490=CARTESIAN_POINT ( 'NONE',  ( 23.99999963380687618, 13.93375672974000246, -1.355252715606880543E-17 ) ) ;
#11494=CARTESIAN_POINT ( 'NONE',  ( 2.899213441999003216, 11.80143355452999110, 3.887780554085998652 ) ) ;
#11497=CARTESIAN_POINT ( 'NONE',  ( -21.60149277696999803, -3.745000288986999770, 10.44303877756999910 ) ) ;
#11500=EDGE_CURVE ( 'NONE', #9506, #3318, #1866, .T. ) ;
#11501=CARTESIAN_POINT ( 'NONE',  ( -19.15130138363000611, -9.425786980393212389, 3.359030689042354911 ) ) ;
#11503=CARTESIAN_POINT ( 'NONE',  ( 15.71133103379665208, 7.256459353526666156, -5.576772732782599107 ) ) ;
#11506=CARTESIAN_POINT ( 'NONE',  ( -4.667964586162003826, 13.45633684249999895, 5.273208831630000759 ) ) ;
#11508=CARTESIAN_POINT ( 'NONE',  ( 17.39475174931000012, -10.15246533026000186, 3.558175289345999914 ) ) ;
#11509=CARTESIAN_POINT ( 'NONE',  ( -13.56430720021000091, -8.266217267278999969, 6.000601104121999541 ) ) ;
#11510=CONICAL_SURFACE ( 'NONE', #12674, 9.630770167580999797, 0.9419447502231289571 ) ;
#11511=CARTESIAN_POINT ( 'NONE',  ( -14.47793696890856019, 1.813149206526026624, 12.49999424749803012 ) ) ;
#11516=CARTESIAN_POINT ( 'NONE',  ( 13.84581539899815539, -8.688513243712947087, 5.538713006654606197 ) ) ;
#11517=CARTESIAN_POINT ( 'NONE',  ( 1.945894728673998708, 12.88054714962999903, -6.188039593268000793 ) ) ;
#11519=CARTESIAN_POINT ( 'NONE',  ( 11.40904387244352414, 2.948332260696533869, 12.49995270680734016 ) ) ;
#11520=LINE ( 'NONE', #9695, #22749 ) ;
#11521=FACE_OUTER_BOUND ( 'NONE', #21649, .T. ) ;
#11524=B_SPLINE_CURVE_WITH_KNOTS ( 'NONE', 3,
 ( #1295, #8683, #16050, #23443, #17645, #6620, #4813, #21647, #19588, #8318, #22214, #5408, #9276, #12895, #12676, #16294, #16531, #1767, #23687, #23918, #20294, #5629, #11217, #18596, #5748, #9154, #18246, #7329, #20532, #2001, #3698, #22334 ),
 .UNSPECIFIED., .F., .F.,
 ( 4, 2, 2, 2, 2, 2, 2, 2, 2, 2, 2, 2, 2, 2, 2, 4 ),
 ( 0.000000000000000000, 0.1249999999999995004, 0.1874999999999991396, 0.2187499999999990286, 0.2499999999999988898, 0.3124999999999987788, 0.3437499999999987232, 0.3749999999999987232, 0.4999999999999988898, 0.5624999999999990008, 0.5937499999999990008, 0.6249999999999988898, 0.6874999999999990008, 0.7187499999999991118, 0.7499999999999992228, 1.000000000000000000 ),
 .UNSPECIFIED. ) ;
#11526=CIRCLE ( 'NONE', #11909, 3.000000000000000000 ) ;
#11527=VERTEX_POINT ( 'NONE', #22763 ) ;
#11529=CARTESIAN_POINT ( 'NONE',  ( -5.776078224282449547, 16.26189775706639296, -2.037803783458385976 ) ) ;
#11530=DIRECTION ( 'NONE',  ( 1.000000000000000000, 0.000000000000000000, 0.000000000000000000 ) ) ;
#11531=CARTESIAN_POINT ( 'NONE',  ( 24.00016455292000117, -9.066063387507998783, 2.014468017461000127 ) ) ;
#11532=VERTEX_POINT ( 'NONE', #7881 ) ;
#11533=CARTESIAN_POINT ( 'NONE',  ( 14.47883169068999898, 6.653640265524000341, -8.778428370972001460 ) ) ;
#11538=CARTESIAN_POINT ( 'NONE',  ( -13.99999999999999645, 4.681959665041976137, -7.960623106173056129 ) ) ;
#11539=CARTESIAN_POINT ( 'NONE',  ( -12.12711221169000098, 14.73199291194999994, 5.035616313343000527 ) ) ;
#11541=CARTESIAN_POINT ( 'NONE',  ( 18.00945603379667048, 4.820354688224963269, 7.871655472196390946 ) ) ;
#11542=ORIENTED_EDGE ( 'NONE', *, *, #6119, .F. ) ;
#11543=CARTESIAN_POINT ( 'NONE',  ( -19.25994536489000097, 6.759255884526000457, 6.826644144461000430 ) ) ;
#11544=CARTESIAN_POINT ( 'NONE',  ( -14.32799102833068616, 13.40593186268490911, 1.779780195171070334 ) ) ;
#11545=CARTESIAN_POINT ( 'NONE',  ( 6.149053220390451102, 14.13825405241221667, 0.2391353124664657992 ) ) ;
#11546=CARTESIAN_POINT ( 'NONE',  ( 15.41201067498107058, -1.444056539591619837, 10.25200677523064208 ) ) ;
#11548=CARTESIAN_POINT ( 'NONE',  ( -15.70284115285000226, -10.90955963878999846, 1.677826734307000134 ) ) ;
#11550=CARTESIAN_POINT ( 'NONE',  ( -17.26141154489999963, -10.85036612823000013, 0.2443279951607999767 ) ) ;
#11555=AXIS2_PLACEMENT_3D ( 'NONE', #6227, #650, #2596 ) ;
#11563=CARTESIAN_POINT ( 'NONE',  ( 16.92956408530999823, -4.671063266616000575, 9.108730853067999789 ) ) ;
#11564=ORIENTED_EDGE ( 'NONE', *, *, #6458, .F. ) ;
#11571=CARTESIAN_POINT ( 'NONE',  ( 4.773276884097002792, 12.62757401777001931, 0.6733110646873000649 ) ) ;
#11572=DIRECTION ( 'NONE',  ( 1.000000000000000000, 0.000000000000000000, 0.000000000000000000 ) ) ;
#11574=CARTESIAN_POINT ( 'NONE',  ( -23.90296024929000041, -9.416283900593001022, 2.173132011546999642 ) ) ;
#11575=EDGE_CURVE ( 'NONE', #1524, #8826, #7061, .T. ) ;
#11576=CARTESIAN_POINT ( 'NONE',  ( -18.13088126894000141, 1.446686056264999920E-14, 0.000000000000000000 ) ) ;
#11577=DIRECTION ( 'NONE',  ( -1.000000000000000000, 0.000000000000000000, 0.000000000000000000 ) ) ;
#11583=CARTESIAN_POINT ( 'NONE',  ( -16.67449577250666692, -7.950790078334936339, 4.582403546340589884 ) ) ;
#11584=CARTESIAN_POINT ( 'NONE',  ( 23.45972874556000320, 3.270437186057999934, 9.320145978262999620 ) ) ;
#11585=CARTESIAN_POINT ( 'NONE',  ( -2.450733744771928624, 13.00631661139677497, -6.259151892297924569 ) ) ;
#11590=B_SPLINE_CURVE_WITH_KNOTS ( 'NONE', 3,
 ( #10842, #16860, #18226, #1627, #20159 ),
 .UNSPECIFIED., .F., .F.,
 ( 4, 1, 4 ),
 ( 0.000000000000000000, 0.5000000000000000000, 1.000000000000000000 ),
 .UNSPECIFIED. ) ;
#11591=AXIS2_PLACEMENT_3D ( 'NONE', #8523, #12629, #2946 ) ;
#11592=DIRECTION ( 'NONE',  ( 0.000000000000000000, 1.000000000000000000, 0.000000000000000000 ) ) ;
#11594=EDGE_CURVE ( 'NONE', #9699, #4168, #9263, .T. ) ;
#11595=CARTESIAN_POINT ( 'NONE',  ( -18.24258566398615500, 9.822636663924470213, 3.986703905974770201 ) ) ;
#11596=DIRECTION ( 'NONE',  ( -1.000000000000000000, 0.000000000000000000, 0.000000000000000000 ) ) ;
#11600=DIRECTION ( 'NONE',  ( -1.000000000000000000, 0.000000000000000000, 0.000000000000000000 ) ) ;
#11601=CARTESIAN_POINT ( 'NONE',  ( 13.77506424931000240, -10.16002631551000057, 3.235559929811000046 ) ) ;
#11602=EDGE_CURVE ( 'NONE', #13414, #5364, #12741, .T. ) ;
#11603=CARTESIAN_POINT ( 'NONE',  ( 11.01624327026000039, 12.44999999999999929, 0.000000000000000000 ) ) ;
#11605=CARTESIAN_POINT ( 'NONE',  ( 13.29676537305999950, 10.72359741199000105, -0.7733205501537999682 ) ) ;
#11607=CARTESIAN_POINT ( 'NONE',  ( 8.124934037954998800, 1.125145054518999965E-14, 0.000000000000000000 ) ) ;
#11608=CARTESIAN_POINT ( 'NONE',  ( 21.72950497963999794, -10.21084190113000112, 0.7917905117385000135 ) ) ;
#11611=CARTESIAN_POINT ( 'NONE',  ( 12.38482062235000036, -2.667901244413000139, -8.947351465620000610 ) ) ;
#11613=VECTOR ( 'NONE', #18605, 1000.000000000000114 ) ;
#11614=CARTESIAN_POINT ( 'NONE',  ( 4.258622327748002867, 12.20824998909998804, 2.305144079472002616 ) ) ;
#11615=EDGE_CURVE ( 'NONE', #10557, #20433, #14843, .T. ) ;
#11617=CARTESIAN_POINT ( 'NONE',  ( -24.77609914680000358, -9.954456274527998971, -3.564765137135000206 ) ) ;
#11618=ORIENTED_EDGE ( 'NONE', *, *, #2604, .T. ) ;
#11619=CARTESIAN_POINT ( 'NONE',  ( 11.00000000000000000, 0.000000000000000000, 0.000000000000000000 ) ) ;
#11620=VERTEX_POINT ( 'NONE', #1466 ) ;
#11623=DIRECTION ( 'NONE',  ( 0.000000000000000000, -1.000000000000000000, 0.000000000000000000 ) ) ;
#11627=CARTESIAN_POINT ( 'NONE',  ( 14.43318924931000069, 4.163528467249999920, -9.835102695514999382 ) ) ;
#11628=CARTESIAN_POINT ( 'NONE',  ( -15.79874102787999846, 5.047191510808999304, 8.952058016012999886 ) ) ;
#11629=CARTESIAN_POINT ( 'NONE',  ( 16.10887625731000128, 5.681759715831000257, 7.231772086132999711 ) ) ;
#11630=CARTESIAN_POINT ( 'NONE',  ( -14.37382046149249071, 4.385283932934418871, 12.49975322910802511 ) ) ;
#11634=EDGE_CURVE ( 'NONE', #10960, #1, #22018, .T. ) ;
#11636=CARTESIAN_POINT ( 'NONE',  ( 14.19556169655588818, -8.215741800005648798, -6.232346285851887657 ) ) ;
#11637=CARTESIAN_POINT ( 'NONE',  ( -4.353632028022997424, 13.53541229131999835, -4.749265782704001460 ) ) ;
#11638=CARTESIAN_POINT ( 'NONE',  ( 20.16063042481999901, 5.004994577864000149, -10.01485155063000043 ) ) ;
#11640=CARTESIAN_POINT ( 'NONE',  ( 11.39490977863705012, 2.886098606888460871, 12.49995748308370125 ) ) ;
#11643=CARTESIAN_POINT ( 'NONE',  ( -6.250000012226999857, 15.73199627394999922, 1.185103398761000015 ) ) ;
#11649=CARTESIAN_POINT ( 'NONE',  ( -5.987337191874583908, 16.36486391838442955, -1.335248119225510566 ) ) ;
#11653=CARTESIAN_POINT ( 'NONE',  ( 6.143312206438239720, 14.17910314525702375, -0.1182593359610033257 ) ) ;
#11654=CARTESIAN_POINT ( 'NONE',  ( -20.31751159899667769, -7.761064575021531020, 5.041909840973705315 ) ) ;
#11658=DIRECTION ( 'NONE',  ( -0.8181527231370768760, 0.000000000000000000, -0.5750009753238559673 ) ) ;
#11663=CARTESIAN_POINT ( 'NONE',  ( -22.58843503502000161, -9.116449256743999641, 4.620077567651999395 ) ) ;
#11664=FACE_OUTER_BOUND ( 'NONE', #12971, .T. ) ;
#11665=CARTESIAN_POINT ( 'NONE',  ( 6.157535982278581344, 14.08554119385395964, 0.3695686495852765208 ) ) ;
#11666=CARTESIAN_POINT ( 'NONE',  ( 15.38005428219763893, -0.3122026486411542678, 10.35019470995840507 ) ) ;
#11670=CARTESIAN_POINT ( 'NONE',  ( -13.76743754818000021, -2.422432655768999687, 9.928996171009998761 ) ) ;
#11675=CARTESIAN_POINT ( 'NONE',  ( 18.22028936713000036, -1.652712406954000013, 8.988165862088999702 ) ) ;
#11678=CARTESIAN_POINT ( 'NONE',  ( -5.147424556882004509, 15.83079896314000301, 2.717927425388003027 ) ) ;
#11680=CARTESIAN_POINT ( 'NONE',  ( 17.47800158530999681, -7.122204577229999778, -7.372745388647000020 ) ) ;
#11682=CARTESIAN_POINT ( 'NONE',  ( -6.116766749681998405, 16.13602277433998466, -0.9718497405647000820 ) ) ;
#11683=CARTESIAN_POINT ( 'NONE',  ( 24.34804274388857337, -12.49056186101158872, 3.365712241645715253 ) ) ;
#11688=CARTESIAN_POINT ( 'NONE',  ( -4.811457632815001162, 12.64231287075998900, -0.1525242827666000722 ) ) ;
#11689=CARTESIAN_POINT ( 'NONE',  ( 18.93264468355999952, 0.000000000000000000, 0.000000000000000000 ) ) ;
#11690=CARTESIAN_POINT ( 'NONE',  ( 17.77671462316595807, -9.250044903823519959, -4.891976846289935565 ) ) ;
#11693=CARTESIAN_POINT ( 'NONE',  ( -4.820913537080000033, 13.20111002679000123, 5.836439296936000609 ) ) ;
#11697=EDGE_CURVE ( 'NONE', #23530, #20521, #21212, .T. ) ;
#11700=CARTESIAN_POINT ( 'NONE',  ( 23.84623061267999944, -8.327348115725000000, 5.332256611120000045 ) ) ;
#11701=CARTESIAN_POINT ( 'NONE',  ( 2.743213193691274032, 13.05670274646432105, -6.153260231641096922 ) ) ;
#11705=B_SPLINE_CURVE_WITH_KNOTS ( 'NONE', 3,
 ( #22380, #22969, #2641, #10036 ),
 .UNSPECIFIED., .F., .F.,
 ( 4, 4 ),
 ( 0.000000000000000000, 1.000000000000000000 ),
 .UNSPECIFIED. ) ;
#11706=AXIS2_PLACEMENT_3D ( 'NONE', #21617, #5033, #12985 ) ;
#11707=CARTESIAN_POINT ( 'NONE',  ( -10.04701370329000021, 16.31160201364000173, 0.9999999999983000265 ) ) ;
#11709=CARTESIAN_POINT ( 'NONE',  ( -17.48898225880079238, -10.32045256900975971, 1.544200643038546872 ) ) ;
#11713=FACE_OUTER_BOUND ( 'NONE', #10863, .T. ) ;
#11714=ORIENTED_EDGE ( 'NONE', *, *, #12377, .T. ) ;
#11715=DIRECTION ( 'NONE',  ( 0.000000000000000000, 0.9145998131564575528, -0.4043602128970813503 ) ) ;
#11716=CARTESIAN_POINT ( 'NONE',  ( 11.77425158531000093, -9.807789133420998340, 1.022826625653000088 ) ) ;
#11717=PLANE ( 'NONE',  #13135 ) ;
#11718=CARTESIAN_POINT ( 'NONE',  ( -10.04351714999000045, 16.35737901937999794, 1.000000000001999956 ) ) ;
#11719=CARTESIAN_POINT ( 'NONE',  ( 13.43171080085999947, 2.637024924671000470, 10.98238284665000108 ) ) ;
#11722=CARTESIAN_POINT ( 'NONE',  ( -5.625000000000000000, 21.50000000000000000, -1.676174921084000144E-09 ) ) ;
#11723=CARTESIAN_POINT ( 'NONE',  ( 24.30244787985000343, 0.3995280882934000299, -9.774475514773000029 ) ) ;
#11724=EDGE_CURVE ( 'NONE', #7720, #3069, #3036, .T. ) ;
#11726=ORIENTED_EDGE ( 'NONE', *, *, #8054, .F. ) ;
#11727=LINE ( 'NONE', #19101, #22359 ) ;
#11729=CARTESIAN_POINT ( 'NONE',  ( 4.150310933805998914, 12.32001967052000424, 2.267141452629003240 ) ) ;
#11731=CARTESIAN_POINT ( 'NONE',  ( -22.10274641431000120, 10.93051552941000004, 1.976840160283999781 ) ) ;
#11732=ORIENTED_EDGE ( 'NONE', *, *, #18428, .F. ) ;
#11733=CARTESIAN_POINT ( 'NONE',  ( -23.16929462096833703, 9.265295224643226746, 1.607743681355135241E-05 ) ) ;
#11738=CARTESIAN_POINT ( 'NONE',  ( 5.043056616458001962, 13.80554412637000006, 4.028432506473001773 ) ) ;
#11740=CARTESIAN_POINT ( 'NONE',  ( 12.78787674931000140, 8.861872729009999006, -5.882981327196000088 ) ) ;
#11741=AXIS2_PLACEMENT_3D ( 'NONE', #16758, #21877, #14598 ) ;
#11742=CARTESIAN_POINT ( 'NONE',  ( -18.88645432865000018, -8.793774626762999702, -6.438463651166999924 ) ) ;
#11743=CARTESIAN_POINT ( 'NONE',  ( 11.83106375730999993, 2.025755645688000151, -8.855592440447001223 ) ) ;
#11750=CARTESIAN_POINT ( 'NONE',  ( 14.21171828542962423, -7.852796259521285016, -6.687517491369988853 ) ) ;
#11752=CARTESIAN_POINT ( 'NONE',  ( -3.787113239318998570, 13.89839096013999509, -4.743087660284001750 ) ) ;
#11753=CARTESIAN_POINT ( 'NONE',  ( 19.12053096800999796, 0.006299968456938000866, 10.67181407054999909 ) ) ;
#11756=CARTESIAN_POINT ( 'NONE',  ( 11.22311500623200153, 2.002057944010465107, 12.49998975379359756 ) ) ;
#11757=CARTESIAN_POINT ( 'NONE',  ( 18.07193721978578793, 6.079758669371162050, -8.513683897598470551 ) ) ;
#11759=CARTESIAN_POINT ( 'NONE',  ( -21.54962077250665686, -1.207329456531916589, -9.224287454130459807 ) ) ;
#11761=CARTESIAN_POINT ( 'NONE',  ( 24.50000000000000711, -11.08150693382694030, -5.806266966183555311 ) ) ;
#11763=CARTESIAN_POINT ( 'NONE',  ( 11.31235608933860526, -12.07787442533556899, 4.080443649533860295 ) ) ;
#11764=EDGE_LOOP ( 'NONE', ( #12604, #373, #1205 ) ) ;
#11765=CARTESIAN_POINT ( 'NONE',  ( -5.902050209366081823, 16.32236802668609243, -1.677094527035041693 ) ) ;
#11768=EDGE_CURVE ( 'NONE', #10482, #4536, #1578, .T. ) ;
#11772=CARTESIAN_POINT ( 'NONE',  ( -21.05832910583999862, 9.211679941677999750, 0.000000000000000000 ) ) ;
#11773=CARTESIAN_POINT ( 'NONE',  ( 17.71428936713000013, 9.125865291226999076, 0.000000000000000000 ) ) ;
#11774=EDGE_LOOP ( 'NONE', ( #4637, #7517, #11424, #15325 ) ) ;
#11776=CARTESIAN_POINT ( 'NONE',  ( -14.00000000000000000, -4.254780838336652771, -8.767722819108374921 ) ) ;
#11778=CARTESIAN_POINT ( 'NONE',  ( -24.50000000000000000, -10.82531754731000007, -6.250000000000000000 ) ) ;
#11779=VERTEX_POINT ( 'NONE', #19990 ) ;
#11780=CARTESIAN_POINT ( 'NONE',  ( -20.28814577853999523, -8.980834437001998793, -3.489049909224000157 ) ) ;
#11782=DIRECTION ( 'NONE',  ( 1.000000000000000000, 0.000000000000000000, 0.000000000000000000 ) ) ;
#11783=CARTESIAN_POINT ( 'NONE',  ( 15.87393906135570276, -10.20432133770710159, -1.800441640727369563 ) ) ;
#11784=CARTESIAN_POINT ( 'NONE',  ( -16.57211600987000111, 9.781171088540000724, 5.166091611002999961 ) ) ;
#11787=CARTESIAN_POINT ( 'NONE',  ( -20.38137539109145280, 10.48768805034149487, -0.5609562679966193510 ) ) ;
#11788=ADVANCED_FACE ( 'NONE', ( #22153 ), #18475, .F. ) ;
#11791=VERTEX_POINT ( 'NONE', #11979 ) ;
#11793=CARTESIAN_POINT ( 'NONE',  ( -18.28298561839290670, 6.265330369647709396, 8.380266679069755753 ) ) ;
#11795=CARTESIAN_POINT ( 'NONE',  ( 5.325462603570996656, 13.97134787008000067, -3.325730261421003142 ) ) ;
#11800=CARTESIAN_POINT ( 'NONE',  ( 13.83187642131000139, 0.1979999634357000049, -9.644016179210000317 ) ) ;
#11801=EDGE_LOOP ( 'NONE', ( #20036, #9883, #20318, #23205, #3110, #9115, #12767 ) ) ;
#11805=VERTEX_POINT ( 'NONE', #8073 ) ;
#11807=CARTESIAN_POINT ( 'NONE',  ( 11.49999999537000051, -6.999999995366000149, -1.987954085830999545E-09 ) ) ;
#11808=CARTESIAN_POINT ( 'NONE',  ( 23.91181431106168631, 9.664920907709271702, 4.394489354301833295 ) ) ;
#11811=CARTESIAN_POINT ( 'NONE',  ( 17.66192372649435427, -10.35977045958544807, -0.9250195969887425873 ) ) ;
#11813=CARTESIAN_POINT ( 'NONE',  ( -14.45561362881484335, -9.532958125082343415, 8.488361093024359150 ) ) ;
#11814=CARTESIAN_POINT ( 'NONE',  ( 24.43180435030999931, -9.516463450214999398, 5.130367153252000101 ) ) ;
#11819=ORIENTED_EDGE ( 'NONE', *, *, #18114, .F. ) ;
#11820=CARTESIAN_POINT ( 'NONE',  ( 19.06751900412999845, -6.585038314783999702, -7.908837097906999958 ) ) ;
#11821=CARTESIAN_POINT ( 'NONE',  ( 1.979184699210071896, 12.93672951579921815, -6.401123758412539999 ) ) ;
#11822=CARTESIAN_POINT ( 'NONE',  ( 8.124934037954998800, -14.44999999999999929, 0.000000000000000000 ) ) ;
#11823=CARTESIAN_POINT ( 'NONE',  ( -20.13552329019880460, 10.43394003992358599, 1.146997921864789882 ) ) ;
#11825=AXIS2_PLACEMENT_3D ( 'NONE', #12719, #23364, #23494 ) ;
#11827=ORIENTED_EDGE ( 'NONE', *, *, #15224, .T. ) ;
#11828=CARTESIAN_POINT ( 'NONE',  ( -17.62853844494577871, -8.423990400856537164, 6.160666632630097617 ) ) ;
#11829=DIRECTION ( 'NONE',  ( -1.000000000000000000, 0.000000000000000000, 0.000000000000000000 ) ) ;
#11832=CARTESIAN_POINT ( 'NONE',  ( -14.25000000000000000, 0.000000000000000000, 0.000000000000000000 ) ) ;
#11835=CARTESIAN_POINT ( 'NONE',  ( 16.95845603379666855, -7.957157342237437092, -4.586073407758718190 ) ) ;
#11836=CARTESIAN_POINT ( 'NONE',  ( 16.73662674931000183, 9.294473935295998857, 5.382749556855999984 ) ) ;
#11837=CARTESIAN_POINT ( 'NONE',  ( -14.14777689704998487, 3.317162000593086635, -8.454068354355397830 ) ) ;
#11838=CARTESIAN_POINT ( 'NONE',  ( 18.51344355829000321, -6.966878364870000340, 12.06698729810999993 ) ) ;
#11839=FACE_OUTER_BOUND ( 'NONE', #11079, .T. ) ;
#11840=CARTESIAN_POINT ( 'NONE',  ( 13.56806994526000132, 10.19277579189000171, -0.7351067978804000091 ) ) ;
#11842=AXIS2_PLACEMENT_3D ( 'NONE', #3579, #19820, #10962 ) ;
#11843=B_SPLINE_CURVE_WITH_KNOTS ( 'NONE', 3,
 ( #20017, #3659, #8761, #8887, #12857, #16124, #7056, #14441, #18212, #6938, #17966, #14334, #19789, #23873, #3438, #1370, #20255, #16369 ),
 .UNSPECIFIED., .F., .F.,
 ( 4, 2, 2, 2, 2, 2, 2, 2, 4 ),
 ( 0.000000000000000000, 0.1250000000000000833, 0.2500000000000001665, 0.3750000000000002220, 0.5000000000000002220, 0.6250000000000002220, 0.7500000000000001110, 0.8750000000000001110, 1.000000000000000000 ),
 .UNSPECIFIED. ) ;
#11845=CARTESIAN_POINT ( 'NONE',  ( 22.88605506260999789, 9.630491853314000039, -1.482563043280999970 ) ) ;
#11848=CARTESIAN_POINT ( 'NONE',  ( 2.374386521520468918, 13.96624173149727000, 5.647372986366287151 ) ) ;
#11850=CARTESIAN_POINT ( 'NONE',  ( -3.143058089422002599, 11.99907213748002022, 3.545075994667000518 ) ) ;
#11852=CARTESIAN_POINT ( 'NONE',  ( -22.26983096010000196, 10.23598255321000039, -4.325444529497999291 ) ) ;
#11857=VECTOR ( 'NONE', #6804, 1000.000000000000114 ) ;
#11859=CARTESIAN_POINT ( 'NONE',  ( -14.25243324638999809, 7.716878364870000340, 11.63397459621999985 ) ) ;
#11861=CARTESIAN_POINT ( 'NONE',  ( -16.61126241975999918, -1.906005702182999917, -10.12158796435999975 ) ) ;
#11862=CARTESIAN_POINT ( 'NONE',  ( 16.65731375730999986, -8.692770150473998925, 3.046645682941000022 ) ) ;
#11863=CARTESIAN_POINT ( 'NONE',  ( 18.93668626432143753, 2.220822707206575597, 10.19564009161587492 ) ) ;
#11865=CARTESIAN_POINT ( 'NONE',  ( 21.19112270046331403, 8.051969607661357387, -4.641010349315714656 ) ) ;
#11867=CIRCLE ( 'NONE', #630, 11.50000000000000000 ) ;
#11869=CARTESIAN_POINT ( 'NONE',  ( 3.240158297419062361, 14.20012988688566402, -5.197965063808845265 ) ) ;
#11871=AXIS2_PLACEMENT_3D ( 'NONE', #5540, #18733, #9530 ) ;
#11872=CARTESIAN_POINT ( 'NONE',  ( -2.059766911846999893, 13.39089224444999360, -5.755068626256005793 ) ) ;
#11874=EDGE_CURVE ( 'NONE', #11018, #19420, #3884, .T. ) ;
#11875=CARTESIAN_POINT ( 'NONE',  ( 11.97297107871654731, -4.846971342278104444, 12.50004942866789470 ) ) ;
#11876=CARTESIAN_POINT ( 'NONE',  ( 18.15556881350096319, 8.256286803634841576, -6.419835422307386352 ) ) ;
#11878=CARTESIAN_POINT ( 'NONE',  ( -14.25395417760000072, -13.93375672974000068, 0.7213694211268999457 ) ) ;
#11879=DIRECTION ( 'NONE',  ( -1.000000000000000000, 0.000000000000000000, 0.000000000000000000 ) ) ;
#11881=VERTEX_POINT ( 'NONE', #10126 ) ;
#11882=CARTESIAN_POINT ( 'NONE',  ( -24.50000000000000355, -4.232391308703559396, -9.760415500123547972 ) ) ;
#11883=CARTESIAN_POINT ( 'NONE',  ( 4.749999673578000348, 12.55004296393999930, -4.341645649670000483E-06 ) ) ;
#11885=CARTESIAN_POINT ( 'NONE',  ( -5.458329129694160287, 16.11242751627741043, -2.784599576127760656 ) ) ;
#11887=CARTESIAN_POINT ( 'NONE',  ( 2.707574462781773050, 13.05161192232940870, 6.163505927546630403 ) ) ;
#11888=AXIS2_PLACEMENT_3D ( 'NONE', #17178, #18647, #13300 ) ;
#11890=DIRECTION ( 'NONE',  ( 0.000000000000000000, 1.000000000000000000, 0.000000000000000000 ) ) ;
#11896=CARTESIAN_POINT ( 'NONE',  ( -14.00000000000000355, -7.692389098372126810, -6.335209552320772985 ) ) ;
#11898=CARTESIAN_POINT ( 'NONE',  ( -10.04281598263999875, 20.50000000000000000, -1.000000000000000000 ) ) ;
#11901=CARTESIAN_POINT ( 'NONE',  ( -23.27390197746000311, 9.786885249677000687, 3.008867104030000128 ) ) ;
#11904=CARTESIAN_POINT ( 'NONE',  ( 15.66712465133541698, -8.871746670583112504, 5.331234943396478521 ) ) ;
#11905=CARTESIAN_POINT ( 'NONE',  ( -17.62205418190999850, -9.739724721154001230, -5.304212073993999077 ) ) ;
#11906=LINE ( 'NONE', #15636, #6034 ) ;
#11907=ADVANCED_FACE ( 'NONE', ( #4805 ), #741, .F. ) ;
#11908=CARTESIAN_POINT ( 'NONE',  ( -19.58358649291538711, -9.522198621325964396, 4.381512970191762335 ) ) ;
#11909=AXIS2_PLACEMENT_3D ( 'NONE', #18242, #21518, #6976 ) ;
#11910=B_SPLINE_CURVE_WITH_KNOTS ( 'NONE', 3,
 ( #6212, #2714, #13968, #21359, #4775 ),
 .UNSPECIFIED., .F., .F.,
 ( 4, 1, 4 ),
 ( 0.000000000000000000, 0.5000000000000000000, 1.000000000000000000 ),
 .UNSPECIFIED. ) ;
#11911=CARTESIAN_POINT ( 'NONE',  ( -17.09903927815000202, -2.106860712391000146, -11.18744719158000045 ) ) ;
#11913=ORIENTED_EDGE ( 'NONE', *, *, #8518, .T. ) ;
#11915=CARTESIAN_POINT ( 'NONE',  ( -15.79421666743139063, -10.31181917561241868, -1.322403086089456226 ) ) ;
#11916=ORIENTED_EDGE ( 'NONE', *, *, #6245, .T. ) ;
#11917=CARTESIAN_POINT ( 'NONE',  ( -24.12232999016000079, 1.520060141252000183E-14, 0.000000000000000000 ) ) ;
#11918=CARTESIAN_POINT ( 'NONE',  ( 5.081337163470998952, 13.95839723273002342, -4.282365589915004378 ) ) ;
#11919=CARTESIAN_POINT ( 'NONE',  ( 12.00000000000000000, -7.784405687158085563, -4.546983378751352056 ) ) ;
#11921=EDGE_CURVE ( 'NONE', #14445, #709, #18164, .T. ) ;
#11922=CARTESIAN_POINT ( 'NONE',  ( 15.80625142131000160, 5.282396774718000287, -8.133049213409000444 ) ) ;
#11923=EDGE_CURVE ( 'NONE', #13362, #4875, #8674, .T. ) ;
#11925=CARTESIAN_POINT ( 'NONE',  ( 11.00000000000000000, 0.000000000000000000, 0.000000000000000000 ) ) ;
#11926=VECTOR ( 'NONE', #22070, 1000.000000000000000 ) ;
#11931=CARTESIAN_POINT ( 'NONE',  ( 21.05799999999999983, 9.211671496174000495, 0.000000000000000000 ) ) ;
#11934=CARTESIAN_POINT ( 'NONE',  ( 18.09556522515502763, 0.2122117348836315975, -10.42041577245926121 ) ) ;
#11936=CARTESIAN_POINT ( 'NONE',  ( 12.00000000000000000, -9.392874664203999302, -3.575135015595999999 ) ) ;
#11938=CARTESIAN_POINT ( 'NONE',  ( -14.49454819745151823, -10.30763366377482804, 7.146668779541629490 ) ) ;
#11939=CARTESIAN_POINT ( 'NONE',  ( 24.57842594718999862, -9.519849028365999999, 5.132192201719999680 ) ) ;
#11940=EDGE_CURVE ( 'NONE', #12473, #4875, #5345, .T. ) ;
#11945=ORIENTED_EDGE ( 'NONE', *, *, #20942, .F. ) ;
#11946=CARTESIAN_POINT ( 'NONE',  ( 21.05259007015999728, -8.871572192553999869, -6.301471715339999946 ) ) ;
#11947=CARTESIAN_POINT ( 'NONE',  ( 1.757374578699382184, 12.90728621817367028, -6.460611937468210719 ) ) ;
#11948=CARTESIAN_POINT ( 'NONE',  ( 5.625000000000000000, 22.00000000000000000, 0.000000000000000000 ) ) ;
#11950=CARTESIAN_POINT ( 'NONE',  ( -19.65354853982566397, -2.165949038814164673, 10.25715202507329948 ) ) ;
#11952=CARTESIAN_POINT ( 'NONE',  ( -2.801175654530000614, 11.78395597969999464, -4.055686653598001179 ) ) ;
#11955=CARTESIAN_POINT ( 'NONE',  ( -19.21947896700662639, -10.37017577041856242, -1.473655227643129839 ) ) ;
#11958=VERTEX_POINT ( 'NONE', #23432 ) ;
#11960=CARTESIAN_POINT ( 'NONE',  ( 17.22299770046334189, -1.193049601325050224, -9.113257778775379236 ) ) ;
#11962=CARTESIAN_POINT ( 'NONE',  ( 12.10331408531000008, -5.154040300995999857, -8.697259314724000490 ) ) ;
#11963=CARTESIAN_POINT ( 'NONE',  ( -23.25600457815999889, -7.940956846984001061, 7.903779492682001084 ) ) ;
#11964=CARTESIAN_POINT ( 'NONE',  ( -14.47646183292000011, -10.21069195510999883, -0.7742164398386000013 ) ) ;
#11966=CARTESIAN_POINT ( 'NONE',  ( 17.02119494526000310, 8.035509840822999905, -6.467739846315000207 ) ) ;
#11970=AXIS2_PLACEMENT_3D ( 'NONE', #22762, #843, #3046 ) ;
#11971=CARTESIAN_POINT ( 'NONE',  ( 5.155702020191999857, 13.97328941143999970, -4.008166040501000893 ) ) ;
#11973=CARTESIAN_POINT ( 'NONE',  ( 1.455334549417839130, 13.79506959216120343, 5.949608132610088695 ) ) ;
#11976=AXIS2_PLACEMENT_3D ( 'NONE', #19291, #22222, #13020 ) ;
#11977=CARTESIAN_POINT ( 'NONE',  ( 2.299232923512000593, 11.73080725892999787, 4.209277167837999656 ) ) ;
#11979=CARTESIAN_POINT ( 'NONE',  ( -4.649999999999999467, 20.00000000000000000, 0.000000000000000000 ) ) ;
#11981=ORIENTED_EDGE ( 'NONE', *, *, #13868, .F. ) ;
#11982=CARTESIAN_POINT ( 'NONE',  ( 15.52237270046331830, 2.373835617566403489, -8.833607132019553276 ) ) ;
#11983=DIRECTION ( 'NONE',  ( -1.000000000000000000, 2.869195662841999727E-10, -3.826635294907999820E-14 ) ) ;
#11984=CARTESIAN_POINT ( 'NONE',  ( -0.4432754260544001790, 13.79882529351002241, 6.151150798201001635 ) ) ;
#11988=CARTESIAN_POINT ( 'NONE',  ( -12.23630863876999975, 8.849960763674998176, -12.38048805091999860 ) ) ;
#11989=CARTESIAN_POINT ( 'NONE',  ( -15.47399649439000058, -8.448196802485998802, -7.562854223976000156 ) ) ;
#11990=CARTESIAN_POINT ( 'NONE',  ( 15.56043875731000092, 5.001549981505999831, -7.700678710662999471 ) ) ;
#11991=CARTESIAN_POINT ( 'NONE',  ( 18.94629248412468314, 1.889948409553210196, 10.26455889571793811 ) ) ;
#11993=CARTESIAN_POINT ( 'NONE',  ( -22.11582036142275243, -8.073955378484633627, 4.653000851119870163 ) ) ;
#11995=CARTESIAN_POINT ( 'NONE',  ( -12.35782654106666634, 6.613167033160651798, -13.46344878000693335 ) ) ;
#11996=CARTESIAN_POINT ( 'NONE',  ( 1.271172506183420259, 13.76972512329144571, -5.992853696390493923 ) ) ;
#11998=B_SPLINE_CURVE_WITH_KNOTS ( 'NONE', 3,
 ( #21984, #23680, #16524, #14815, #10855 ),
 .UNSPECIFIED., .F., .F.,
 ( 4, 1, 4 ),
 ( 0.000000000000000000, 0.5000000000000000000, 1.000000000000000000 ),
 .UNSPECIFIED. ) ;
#11999=CARTESIAN_POINT ( 'NONE',  ( 5.267432092546001421, 13.90546002103000056, -3.709299984792997495 ) ) ;
#12000=CARTESIAN_POINT ( 'NONE',  ( 21.26191220262000314, -10.18341492801999948, 4.724734105908999560 ) ) ;
#12002=CARTESIAN_POINT ( 'NONE',  ( -23.85040575352566350, -5.911899685930855242, 7.659340654891490630 ) ) ;
#12003=CARTESIAN_POINT ( 'NONE',  ( 15.98114737690458931, -3.455263148493648462, -9.811776265688715526 ) ) ;
#12004=CARTESIAN_POINT ( 'NONE',  ( 12.52688711657000020, -7.716878364870000340, -11.63397459621999985 ) ) ;
#12007=( BOUNDED_SURFACE ( )  B_SPLINE_SURFACE ( 3, 3, ( 
 ( #6032, #11506, #108, #7860, #13422, #20821, #4232, #18994, #2404, #22742, #6159, #20347, #3754 ),
 ( #15593, #22981, #2778, #15478, #2524, #22862, #4347, #8470, #4595, #9914, #12106, #11738, #6276 ),
 ( #13659, #8342, #6396, #10165, #3022, #10281, #1070, #1197, #21055, #17548, #17671, #17302, #15836 ),
 ( #19613, #4719, #15708, #4468, #13779, #21180, #11984, #6639, #23226, #2653, #945, #23099, #19112 ) ),
 .UNSPECIFIED., .F., .F., .T. ) 
 B_SPLINE_SURFACE_WITH_KNOTS ( ( 4, 4 ),
 ( 4, 1, 1, 1, 1, 1, 1, 1, 1, 1, 4 ),
 ( 0.000000000000000000, 1.000000000000000000 ),
 ( 0.2731447329273000157, 0.2887972725788000017, 0.3269706604050000021, 0.3700588552437000245, 0.4191490422699000185, 0.4751505887952999774, 0.5373493534070999944, 0.6034834658143000130, 0.6714119343383999627, 0.7375481631143000483, 0.7972330670102999450 ),
 .UNSPECIFIED. ) 
 GEOMETRIC_REPRESENTATION_ITEM ( )  RATIONAL_B_SPLINE_SURFACE ( (
 ( 1.179586311108000052, 1.179586311108000052, 1.179586311108000052, 1.179586311108000052, 1.179586311108000052, 1.179586311108000052, 1.179586311108000052, 1.179586311108000052, 1.179586311108000052, 1.179586311108000052, 1.179586311108000052, 1.179586311108000052, 1.179586311108000052),
 ( 0.9401378962973999664, 0.9401378962973999664, 0.9401378962973999664, 0.9401378962973999664, 0.9401378962973999664, 0.9401378962973999664, 0.9401378962973999664, 0.9401378962973999664, 0.9401378962973999664, 0.9401378962973999664, 0.9401378962973999664, 0.9401378962973999664, 0.9401378962973999664),
 ( 0.9401378962973999664, 0.9401378962973999664, 0.9401378962973999664, 0.9401378962973999664, 0.9401378962973999664, 0.9401378962973999664, 0.9401378962973999664, 0.9401378962973999664, 0.9401378962973999664, 0.9401378962973999664, 0.9401378962973999664, 0.9401378962973999664, 0.9401378962973999664),
 ( 1.179586311108000052, 1.179586311108000052, 1.179586311108000052, 1.179586311108000052, 1.179586311108000052, 1.179586311108000052, 1.179586311108000052, 1.179586311108000052, 1.179586311108000052, 1.179586311108000052, 1.179586311108000052, 1.179586311108000052, 1.179586311108000052) ) ) 
 REPRESENTATION_ITEM ( '' )  SURFACE ( )  );
#12008=CARTESIAN_POINT ( 'NONE',  ( 19.52828936713000019, 9.172416106433001204, 0.000000000000000000 ) ) ;
#12009=ORIENTED_EDGE ( 'NONE', *, *, #4500, .F. ) ;
#12010=CARTESIAN_POINT ( 'NONE',  ( -24.50000000000000711, -9.452605432706508992, -4.381486995578353749 ) ) ;
#12011=CARTESIAN_POINT ( 'NONE',  ( -4.749965457312494088, 12.54998638856619486, -0.6287771473730588978 ) ) ;
#12012=ORIENTED_EDGE ( 'NONE', *, *, #15854, .T. ) ;
#12015=CARTESIAN_POINT ( 'NONE',  ( -1.216511548453131253, 12.85264031799866835, 6.568461162512661211 ) ) ;
#12016=B_SPLINE_CURVE_WITH_KNOTS ( 'NONE', 3,
 ( #21916, #7368, #9077, #14867, #12600, #22149, #5671, #1927, #12830, #5560, #20111, #1462, #13059, #16337 ),
 .UNSPECIFIED., .F., .F.,
 ( 4, 1, 1, 1, 1, 1, 1, 2, 2, 4 ),
 ( 0.000000000000000000, 0.2499999999999956701, 0.3749999999999936162, 0.4374999999999925060, 0.4687499999999916178, 0.4843749999999909517, 0.4921874999999909517, 0.4960937499999911737, 0.4999999999999914513, 1.000000000000000000 ),
 .UNSPECIFIED. ) ;
#12017=CARTESIAN_POINT ( 'NONE',  ( 15.67432937369000001, -6.527804446355999879, 8.913017593376000747 ) ) ;
#12019=CARTESIAN_POINT ( 'NONE',  ( 24.50000000000000000, 4.174438572590999431E-14, -12.50000000000000000 ) ) ;
#12022=ORIENTED_EDGE ( 'NONE', *, *, #21424, .T. ) ;
#12025=CARTESIAN_POINT ( 'NONE',  ( -6.706871426378296697, 15.26719126503497215, -2.301088630243747879 ) ) ;
#12026=ORIENTED_EDGE ( 'NONE', *, *, #17664, .F. ) ;
#12027=PLANE ( 'NONE',  #9016 ) ;
#12028=CARTESIAN_POINT ( 'NONE',  ( 24.00034722001000276, 6.716786536054000223, -12.21137788280000080 ) ) ;
#12029=CARTESIAN_POINT ( 'NONE',  ( 14.97832412782650380, 10.09172200828920474, 2.218384077932363141 ) ) ;
#12030=CARTESIAN_POINT ( 'NONE',  ( -16.21078937980000134, -1.833411044341999974, 10.89860299424000090 ) ) ;
#12032=CARTESIAN_POINT ( 'NONE',  ( -20.30417001384837761, 10.26022708029042008, 2.230831165255982018 ) ) ;
#12033=CARTESIAN_POINT ( 'NONE',  ( 4.725446626782000337, 12.53698071169998762, -0.1085052580315999798 ) ) ;
#12037=ORIENTED_EDGE ( 'NONE', *, *, #362, .T. ) ;
#12039=CARTESIAN_POINT ( 'NONE',  ( -15.01285897352482301, 9.893965164599533679, -3.127973572333462293 ) ) ;
#12042=CARTESIAN_POINT ( 'NONE',  ( 5.921804960513004090, 14.11680711012999367, -1.397333608379999204 ) ) ;
#12043=CARTESIAN_POINT ( 'NONE',  ( 12.00000000000000355, -1.539276415234435369, -8.846422256191463163 ) ) ;
#12044=CARTESIAN_POINT ( 'NONE',  ( -19.69192920454666051, 8.018450232194952676, -4.621400420351030824 ) ) ;
#12046=CARTESIAN_POINT ( 'NONE',  ( 13.28343892131000104, -9.177482186369001482, 2.922696180057999804 ) ) ;
#12047=ORIENTED_EDGE ( 'NONE', *, *, #2289, .T. ) ;
#12048=CARTESIAN_POINT ( 'NONE',  ( 5.699442596042000098, 1.578914512950999657E-14, 0.000000000000000000 ) ) ;
#12051=ORIENTED_EDGE ( 'NONE', *, *, #11921, .F. ) ;
#12053=CARTESIAN_POINT ( 'NONE',  ( 11.48696334737391034, 9.189637287616163164, 9.082924181322448831 ) ) ;
#12054=CARTESIAN_POINT ( 'NONE',  ( -23.30805980735596350, 8.264335043300832240, -4.289310384929161835 ) ) ;
#12055=CARTESIAN_POINT ( 'NONE',  ( 24.50000000000000000, 0.000000000000000000, 0.000000000000000000 ) ) ;
#12056=CARTESIAN_POINT ( 'NONE',  ( 16.45228901489213058, 5.938338979451788013, -8.534682244571794030 ) ) ;
#12058=DIRECTION ( 'NONE',  ( -1.000000000000000000, 0.000000000000000000, 0.000000000000000000 ) ) ;
#12059=CARTESIAN_POINT ( 'NONE',  ( -14.48092000065305385, 9.982182315252655869, -7.710362946291708930 ) ) ;
#12060=CARTESIAN_POINT ( 'NONE',  ( 20.63850044899999858, -5.380123924041000372, 9.833381923714000550 ) ) ;
#12062=CARTESIAN_POINT ( 'NONE',  ( -4.111914283818391525, 13.74838725675451379, -4.878539065083999482 ) ) ;
#12063=CARTESIAN_POINT ( 'NONE',  ( 12.49102043323999922, 6.966843713870000343, -12.06700730386999965 ) ) ;
#12067=EDGE_CURVE ( 'NONE', #4069, #2201, #14558, .T. ) ;
#12068=CARTESIAN_POINT ( 'NONE',  ( 23.17332811867109754, 4.643914442280755672, 8.043476694703691976 ) ) ;
#12069=CARTESIAN_POINT ( 'NONE',  ( 23.75810313999999934, 9.259900066636999938, 5.856734761124000599 ) ) ;
#12070=CARTESIAN_POINT ( 'NONE',  ( 12.52688711657000020, 6.216878364870000340, -12.50000000000000000 ) ) ;
#12071=DIRECTION ( 'NONE',  ( -1.000000000000000000, 0.000000000000000000, 0.000000000000000000 ) ) ;
#12073=CARTESIAN_POINT ( 'NONE',  ( 4.846185023065524788, 14.59761631344303545, 3.777028798763933715 ) ) ;
#12074=CARTESIAN_POINT ( 'NONE',  ( -3.690048612459000843, 12.01986709263998598, -3.260388994065002155 ) ) ;
#12075=VERTEX_POINT ( 'NONE', #11080 ) ;
#12076=CARTESIAN_POINT ( 'NONE',  ( -15.89804173673989318, -6.399027050157823027, 8.374265193961687004 ) ) ;
#12078=ADVANCED_FACE ( 'NONE', ( #18348 ), #23791, .F. ) ;
#12079=CARTESIAN_POINT ( 'NONE',  ( 23.99062354302999722, 13.93375672974000068, 0.8660254037843999608 ) ) ;
#12083=ORIENTED_EDGE ( 'NONE', *, *, #19584, .T. ) ;
#12084=CARTESIAN_POINT ( 'NONE',  ( 17.52533103379666812, 7.293684496933804162, -5.605380383579831260 ) ) ;
#12086=CARTESIAN_POINT ( 'NONE',  ( -5.101723131807428757, 15.93850954079848670, -3.397737009563421839 ) ) ;
#12087=CARTESIAN_POINT ( 'NONE',  ( -24.00694541842999996, 8.257142182343001124, 6.813018789841999379 ) ) ;
#12088=CARTESIAN_POINT ( 'NONE',  ( -15.83232383131000276, -8.056602140089001551, -7.212379830447999574 ) ) ;
#12089=CARTESIAN_POINT ( 'NONE',  ( -6.124356664509996051, 15.85446180679002559, 1.061635727481998748 ) ) ;
#12090=CARTESIAN_POINT ( 'NONE',  ( 16.00556994525999954, -5.082985426985000110, 8.943222925845001114 ) ) ;
#12091=CARTESIAN_POINT ( 'NONE',  ( -14.25395396059999875, -13.93375672974000068, -0.7213900596348999938 ) ) ;
#12092=CARTESIAN_POINT ( 'NONE',  ( -14.25699038479000080, 13.93375672974000068, 0.1445756673977000029 ) ) ;
#12093=EDGE_CURVE ( 'NONE', #22144, #11065, #11998, .T. ) ;
#12095=VERTEX_POINT ( 'NONE', #21869 ) ;
#12096=CARTESIAN_POINT ( 'NONE',  ( -3.371625728408081279, 14.23819322435518053, 5.124742718149488674 ) ) ;
#12099=CARTESIAN_POINT ( 'NONE',  ( -19.96237077250665237, -7.343695055788383108, -5.643813670142061589 ) ) ;
#12101=DIRECTION ( 'NONE',  ( 1.000000000000000000, 0.000000000000000000, 0.000000000000000000 ) ) ;
#12105=ADVANCED_FACE ( 'NONE', ( #18466 ), #21119, .F. ) ;
#12106=CARTESIAN_POINT ( 'NONE',  ( 4.505994758382000143, 13.58051267175999044, 4.661972778555996122 ) ) ;
#12109=CARTESIAN_POINT ( 'NONE',  ( -10.59977471169000118, 14.06013194402999922, 6.685927415084999659 ) ) ;
#12110=CARTESIAN_POINT ( 'NONE',  ( -14.86460545047999915, 10.81390249068999942, -3.353128725732000159 ) ) ;
#12112=CARTESIAN_POINT ( 'NONE',  ( 16.98637625730999900, -6.405805545913000110, -6.631092424295999876 ) ) ;
#12113=CARTESIAN_POINT ( 'NONE',  ( 18.93537196294775882, 2.265043017815088433, 10.18579095625258546 ) ) ;
#12115=CARTESIAN_POINT ( 'NONE',  ( -22.66395956040253523, 6.970187874413995566, 6.113416044038686437 ) ) ;
#12118=CARTESIAN_POINT ( 'NONE',  ( 2.248479345707985910, 13.93831621736242532, -5.697544554129113870 ) ) ;
#12124=CARTESIAN_POINT ( 'NONE',  ( 16.53869133500922572, 10.41447537069648099, 0.2212634277976356645 ) ) ;
#12127=CARTESIAN_POINT ( 'NONE',  ( 19.56608103379665664, 9.173385915083406061, 1.200666460651664158 ) ) ;
#12130=CARTESIAN_POINT ( 'NONE',  ( 12.06371966929668282, -8.266677037995437516, 10.68189384375242668 ) ) ;
#12134=CARTESIAN_POINT ( 'NONE',  ( 2.972536222373345360, 13.09994088774743481, 6.061060134369011365 ) ) ;
#12135=CARTESIAN_POINT ( 'NONE',  ( 14.59162398661999838, 0.2593516755336999768, -11.01510379984999943 ) ) ;
#12136=CARTESIAN_POINT ( 'NONE',  ( -20.48587921418834057, -3.712447563501607206, 8.482500515389572726 ) ) ;
#12137=AXIS2_PLACEMENT_3D ( 'NONE', #4144, #2329, #11306 ) ;
#12138=DIRECTION ( 'NONE',  ( -0.8181527231370768760, -7.041731039369663653E-17, 0.5750009753238559673 ) ) ;
#12140=CARTESIAN_POINT ( 'NONE',  ( -14.00000000000000355, -9.891701185583293920, -2.661512775288601418 ) ) ;
#12142=CARTESIAN_POINT ( 'NONE',  ( 12.52688711657000020, -7.716878364870000340, 11.63397459621999985 ) ) ;
#12144=ORIENTED_EDGE ( 'NONE', *, *, #346, .F. ) ;
#12145=CARTESIAN_POINT ( 'NONE',  ( -20.43318916570999733, -0.1401826590115999860, -10.68367857704999935 ) ) ;
#12146=CARTESIAN_POINT ( 'NONE',  ( -24.50000000000000000, -10.82531754731000007, 6.250000000000000000 ) ) ;
#12147=CARTESIAN_POINT ( 'NONE',  ( 21.05799999999999983, 9.211671496174000495, 0.000000000000000000 ) ) ;
#12148=CARTESIAN_POINT ( 'NONE',  ( 15.23661952948198817, 4.575606413770517022, 9.271423793378714251 ) ) ;
#12149=CARTESIAN_POINT ( 'NONE',  ( -16.93344263992999998, 7.982151262181000462, -7.672296569841999592 ) ) ;
#12151=FACE_OUTER_BOUND ( 'NONE', #5680, .T. ) ;
#12152=CARTESIAN_POINT ( 'NONE',  ( -4.735820586438997282, 12.61288540589000640, -0.3245998379664998823 ) ) ;
#12153=EDGE_LOOP ( 'NONE', ( #13294, #6333, #21845, #9297, #5452 ) ) ;
#12154=CARTESIAN_POINT ( 'NONE',  ( -24.50000000000000000, -9.995791495354000133, -2.484784171996999635 ) ) ;
#12156=ORIENTED_EDGE ( 'NONE', *, *, #18300, .T. ) ;
#12158=CARTESIAN_POINT ( 'NONE',  ( -17.32799288139599980, -4.762660099403713154, -9.278735530162990131 ) ) ;
#12161=CARTESIAN_POINT ( 'NONE',  ( 6.104584092870004142, 13.74269313579999974, -1.459638886711001282 ) ) ;
#12162=CARTESIAN_POINT ( 'NONE',  ( 12.00000000000000355, -3.246823130105976674, -8.379510835762300047 ) ) ;
#12163=CARTESIAN_POINT ( 'NONE',  ( -19.84309587121332896, 4.623588645206304193, -8.021742693057086981 ) ) ;
#12164=CIRCLE ( 'NONE', #20656, 3.000000000000000000 ) ;
#12165=CARTESIAN_POINT ( 'NONE',  ( 13.20018908531000079, -1.240977706124000157, 10.06232283554999896 ) ) ;
#12166=ORIENTED_EDGE ( 'NONE', *, *, #3618, .F. ) ;
#12167=CARTESIAN_POINT ( 'NONE',  ( -9.603671492921000308, -7.945443728446001330, 12.15033259826000034 ) ) ;
#12171=ORIENTED_EDGE ( 'NONE', *, *, #22099, .F. ) ;
#12172=CARTESIAN_POINT ( 'NONE',  ( 11.18574820343528131, 11.70054794219022476, 4.734095432790576652 ) ) ;
#12173=CARTESIAN_POINT ( 'NONE',  ( -23.36335304951608904, 7.300808882634314934, -5.780451761111838671 ) ) ;
#12175=CARTESIAN_POINT ( 'NONE',  ( 16.24398043996313845, -1.141157097763910278, -10.31439134400806346 ) ) ;
#12176=CARTESIAN_POINT ( 'NONE',  ( 11.99999999999999822, -8.124792819186978932, -5.670701520036931065 ) ) ;
#12177=CARTESIAN_POINT ( 'NONE',  ( -14.49454883410026085, -11.27877807214812833, 5.464517788383423280 ) ) ;
#12179=CARTESIAN_POINT ( 'NONE',  ( -3.937744478194991515, 13.91798078350775292, -4.847309677219109325 ) ) ;
#12180=CARTESIAN_POINT ( 'NONE',  ( -24.50000000000293099, 10.69708164072063461, -6.472111105570566458 ) ) ;
#12183=VERTEX_POINT ( 'NONE', #22565 ) ;
#12185=CARTESIAN_POINT ( 'NONE',  ( 24.19716673756000347, 3.808960480925000169, 10.85543100556000162 ) ) ;
#12187=DIRECTION ( 'NONE',  ( 1.000000000000000000, 0.000000000000000000, 0.000000000000000000 ) ) ;
#12190=CARTESIAN_POINT ( 'NONE',  ( -20.67105079060898376, -1.821131150673523491, -10.35028598315374815 ) ) ;
#12191=DIRECTION ( 'NONE',  ( -1.000000000000000000, 0.000000000000000000, 0.000000000000000000 ) ) ;
#12192=CARTESIAN_POINT ( 'NONE',  ( -1.474518126777998983, 11.62008507038000715, -4.742463282491001131 ) ) ;
#12195=CARTESIAN_POINT ( 'NONE',  ( -16.06550916011372721, -0.7239279268763375574, 10.37154066821624099 ) ) ;
#12199=PLANE ( 'NONE',  #2078 ) ;
#12200=ADVANCED_FACE ( 'NONE', ( #278 ), #10163, .F. ) ;
#12202=CARTESIAN_POINT ( 'NONE',  ( -23.74465998031000069, 6.216878364870000340, -12.50000000000000000 ) ) ;
#12203=CARTESIAN_POINT ( 'NONE',  ( -4.421389682918046127, 15.40904240291348692, -4.239377148695758990 ) ) ;
#12204=CARTESIAN_POINT ( 'NONE',  ( -24.80987884326999904, -5.066946248634999428, -8.838305289106999751 ) ) ;
#12205=CARTESIAN_POINT ( 'NONE',  ( -18.33593844434000175, -7.737619111796999682, 6.870299314828000270 ) ) ;
#12207=CARTESIAN_POINT ( 'NONE',  ( 13.43312451745999958, 0.8166441206667999220, -8.872015940503999332 ) ) ;
#12208=FACE_BOUND ( 'NONE', #8281, .T. ) ;
#12209=CARTESIAN_POINT ( 'NONE',  ( 23.99062354302999722, -13.93375672974000068, 0.8660254037843999608 ) ) ;
#12210=EDGE_CURVE ( 'NONE', #21237, #5409, #17384, .T. ) ;
#12211=CARTESIAN_POINT ( 'NONE',  ( 15.31366666666666276, 4.564816387457174329, -7.920276097247842095 ) ) ;
#12213=CARTESIAN_POINT ( 'NONE',  ( -3.102235637044312266, 14.15615357930589191, 5.289215628019240611 ) ) ;
#12215=CIRCLE ( 'NONE', #8333, 1.000000000000000888 ) ;
#12216=CARTESIAN_POINT ( 'NONE',  ( -19.77341243917331681, -2.402389709466869139, -8.939857867861107366 ) ) ;
#12217=CARTESIAN_POINT ( 'NONE',  ( -14.50464602252369772, 1.560506203883582632, -8.906515074185010761 ) ) ;
#12219=CARTESIAN_POINT ( 'NONE',  ( -3.794133490988780721, 12.08388102651774965, 2.997060710912608172 ) ) ;
#12220=VERTEX_POINT ( 'NONE', #7550 ) ;
#12223=CARTESIAN_POINT ( 'NONE',  ( 2.616450853603692117, 11.77236066036824091, -4.051655692838156853 ) ) ;
#12225=CARTESIAN_POINT ( 'NONE',  ( 11.51452871203068717, -7.818510255363073647, -4.442849280847243065 ) ) ;
#12231=CARTESIAN_POINT ( 'NONE',  ( -15.67712684235999987, -11.34047394370000106, -0.3014134449561000073 ) ) ;
#12233=CARTESIAN_POINT ( 'NONE',  ( 14.92875142131000210, -6.069959421551999412, 7.533852356441999909 ) ) ;
#12235=B_SPLINE_CURVE_WITH_KNOTS ( 'NONE', 3,
 ( #10244, #21632, #12546, #19575, #10613, #8795, #8307, #15672, #1032, #13871, #16035, #1163, #21274, #15800, #23559, #8557, #17997, #19697, #19453, #23061, #1402, #19932, #23192, #4801, #2980, #16157, #6609, #906, #5051, #3350, #17512, #12307, #12433, #21386, #6489, #10370, #23306, #6723, #14114, #6967, #21509, #3113, #10497, #17882, #1283, #14811, #1636, #12662, #18121, #22205, #16282, #5739, #1754, #8916, #12882, #9261, #13001, #20402, #18585, #9141, #9025, #13128, #7549, #22094, #16519, #3466, #5504, #3575, #7314, #158, #7428, #5619, #22323, #10851, #23906, #3808, #23675, #1989, #14927, #3687, #14703, #7195, #18233, #11204, #14585, #16395, #7083, #9374, #20524, #23787, #20283, #21979, #5393, #12778, #11077, #18461, #20169, #10729, #16746, #1527, #1874, #10958, #18344, #16637, #46, #14470, #21865, #5274, #20050, #2220, #18812, #2805, #2103, #16997, #4491, #19392 ),
 .UNSPECIFIED., .F., .F.,
 ( 4, 2, 2, 2, 2, 2, 1, 2, 2, 2, 2, 2, 2, 2, 2, 2, 2, 2, 2, 2, 2, 2, 2, 2, 2, 2, 2, 2, 2, 2, 2, 2, 2, 2, 2, 2, 2, 2, 2, 2, 2, 2, 2, 2, 2, 2, 2, 2, 2, 2, 2, 2, 1, 2, 2, 2, 2, 2, 4 ),
 ( 0.000000000000000000, 0.01562499999999999653, 0.03124999999999999306, 0.04687499999999998612, 0.06249999999999998612, 0.07812499999999997224, 0.09374999999999997224, 0.1093749999999999584, 0.1249999999999999584, 0.1406249999999999722, 0.1562499999999999722, 0.1718749999999999722, 0.1874999999999999445, 0.2031249999999999445, 0.2187499999999999445, 0.2343749999999999445, 0.2499999999999999445, 0.2656249999999999445, 0.2812499999999999445, 0.2968749999999999445, 0.3124999999999999445, 0.3281249999999999445, 0.3437499999999999445, 0.3593749999999999445, 0.3749999999999998890, 0.3906249999999998890, 0.4062499999999999445, 0.4375000000000000000, 0.4687500000000000555, 0.5000000000000001110, 0.5312500000000001110, 0.5625000000000001110, 0.5937500000000001110, 0.6093750000000001110, 0.6250000000000001110, 0.6406250000000001110, 0.6562500000000001110, 0.6718750000000001110, 0.6875000000000001110, 0.7031250000000001110, 0.7187500000000001110, 0.7343750000000001110, 0.7500000000000000000, 0.7656250000000000000, 0.7812500000000000000, 0.7968750000000000000, 0.8125000000000000000, 0.8281250000000000000, 0.8437500000000000000, 0.8593750000000000000, 0.8750000000000000000, 0.8906250000000000000, 0.9062500000000000000, 0.9218750000000000000, 0.9375000000000000000, 0.9531250000000000000, 0.9687500000000000000, 0.9843750000000000000, 1.000000000000000000 ),
 .UNSPECIFIED. ) ;
#12236=VERTEX_POINT ( 'NONE', #17231 ) ;
#12237=CARTESIAN_POINT ( 'NONE',  ( -22.45604469182422136, 1.209830229891543540, 9.246699917977114325 ) ) ;
#12239=CARTESIAN_POINT ( 'NONE',  ( -15.46516243917332822, 7.923575937676545777, 4.567008865628563896 ) ) ;
#12240=CARTESIAN_POINT ( 'NONE',  ( -23.68078907432000335, -9.459496811531000304, -9.754788243598999975E-09 ) ) ;
#12241=EDGE_LOOP ( 'NONE', ( #8773, #6955, #19919, #8148, #13990 ) ) ;
#12243=CARTESIAN_POINT ( 'NONE',  ( 5.302302355349000074, 1.402151973163523525E-14, 14.43375672973994917 ) ) ;
#12245=EDGE_CURVE ( 'NONE', #20167, #1386, #23578, .T. ) ;
#12247=CARTESIAN_POINT ( 'NONE',  ( 16.28779655386367509, 6.890083051547521542, -7.810293348495036092 ) ) ;
#12248=CARTESIAN_POINT ( 'NONE',  ( -3.688226731973703654, 14.24897469870492372, 4.890359035125574572 ) ) ;
#12249=CARTESIAN_POINT ( 'NONE',  ( -21.96532910583999865, -9.234955349282000014, 0.000000000000000000 ) ) ;
#12250=CARTESIAN_POINT ( 'NONE',  ( 20.39749770046332955, -9.194721705386330157, 1.203713204382251600 ) ) ;
#12251=VERTEX_POINT ( 'NONE', #15406 ) ;
#12253=VECTOR ( 'NONE', #19847, 1000.000000000000227 ) ;
#12254=CARTESIAN_POINT ( 'NONE',  ( 11.55284350197085885, -9.059841367792975220, 9.307687628814361958 ) ) ;
#12256=VERTEX_POINT ( 'NONE', #4045 ) ;
#12258=CARTESIAN_POINT ( 'NONE',  ( 4.816292305294004983, 14.93029986592002345, 3.795759443924001442 ) ) ;
#12259=CARTESIAN_POINT ( 'NONE',  ( 6.220855133530989178, 13.78415744763224815, -1.220025851734428901 ) ) ;
#12260=CARTESIAN_POINT ( 'NONE',  ( -14.25243324638999809, -6.216878364870000340, -12.50000000000000000 ) ) ;
#12265=DIRECTION ( 'NONE',  ( 0.000000000000000000, -1.000000000000000000, 0.000000000000000000 ) ) ;
#12268=CARTESIAN_POINT ( 'NONE',  ( -19.11937752606000274, -10.08460061511999939, 1.755720681344000056 ) ) ;
#12270=CARTESIAN_POINT ( 'NONE',  ( 23.99478584078000054, 6.383504859171999612, -12.40379814865999997 ) ) ;
#12271=CARTESIAN_POINT ( 'NONE',  ( 14.88923352241194031, 10.28052023608410792, -1.022339429599108618 ) ) ;
#12274=CARTESIAN_POINT ( 'NONE',  ( 13.58272190881292474, 6.554870883473079779, -6.201906958780953438 ) ) ;
#12275=CARTESIAN_POINT ( 'NONE',  ( 4.721753426476999138, 12.53551098956998544, 0.1045195479194000188 ) ) ;
#12277=CARTESIAN_POINT ( 'NONE',  ( -24.18402430578868945, -7.007993001692642387, -7.183753820344653818 ) ) ;
#12279=ORIENTED_EDGE ( 'NONE', *, *, #1258, .T. ) ;
#12280=CARTESIAN_POINT ( 'NONE',  ( 23.99062354302999722, 6.216878364870000340, 12.50000000000000000 ) ) ;
#12281=CARTESIAN_POINT ( 'NONE',  ( -16.83602692597334638, 9.825331796457355438, -3.486094970374975510 ) ) ;
#12284=CARTESIAN_POINT ( 'NONE',  ( 5.843331730810001901, 14.13764455460000136, -1.695804390486001401 ) ) ;
#12285=CARTESIAN_POINT ( 'NONE',  ( 12.00000000000000178, -3.594391383428954700, -8.228416206764714858 ) ) ;
#12286=CONICAL_SURFACE ( 'NONE', #3001, 13.23032192316000000, 1.235249617460683957 ) ;
#12287=CARTESIAN_POINT ( 'NONE',  ( 14.15175919596000043, 0.2590669823852999598, -11.00306018672999997 ) ) ;
#12288=CARTESIAN_POINT ( 'NONE',  ( 16.49081408530999937, 8.848325411959001130, 5.124349347825999601 ) ) ;
#12290=CARTESIAN_POINT ( 'NONE',  ( -10.11278399292000074, 14.51541005890999969, 0.2520496489101999860 ) ) ;
#12292=( LENGTH_UNIT ( ) NAMED_UNIT ( * ) SI_UNIT ( .MILLI., .METRE. ) );
#12298=CARTESIAN_POINT ( 'NONE',  ( 17.36346904825625259, -6.105277895300214475, 8.468900842036610754 ) ) ;
#12299=AXIS2_PLACEMENT_3D ( 'NONE', #17033, #11596, #2025 ) ;
#12300=CARTESIAN_POINT ( 'NONE',  ( -19.20653743917332434, 9.164159317821958695, 1.199712597205233600 ) ) ;
#12302=CARTESIAN_POINT ( 'NONE',  ( -4.306867197362858946, 13.60612586508986688, -4.963187192049142382 ) ) ;
#12304=VERTEX_POINT ( 'NONE', #11675 ) ;
#12305=CARTESIAN_POINT ( 'NONE',  ( -24.41513307468991201, -2.047838742126371958, 12.49997210310724327 ) ) ;
#12306=CARTESIAN_POINT ( 'NONE',  ( 20.22702460548000047, -1.851192937421999751, 10.15609432501999976 ) ) ;
#12307=CARTESIAN_POINT ( 'NONE',  ( 23.16496088167180645, -10.13946258324673444, -3.077221131437410495 ) ) ;
#12312=CARTESIAN_POINT ( 'NONE',  ( 4.852688899486731877, 14.56075982391421597, 3.781543657204870623 ) ) ;
#12313=VECTOR ( 'NONE', #19342, 1000.000000000000000 ) ;
#12314=CARTESIAN_POINT ( 'NONE',  ( 3.260899927695999345, 11.89447923387001183, -3.718744492640997379 ) ) ;
#12316=CARTESIAN_POINT ( 'NONE',  ( -14.89323719649020283, 8.655513120188558673, -5.700961162800999737 ) ) ;
#12320=AXIS2_PLACEMENT_3D ( 'NONE', #20423, #19866, #5525 ) ;
#12326=CARTESIAN_POINT ( 'NONE',  ( 12.89756424930999934, 10.41448860350999972, -2.177620798092000598 ) ) ;
#12327=CARTESIAN_POINT ( 'NONE',  ( -25.02706704405999716, 5.409545006709000070, -8.044608227789000310 ) ) ;
#12328=CARTESIAN_POINT ( 'NONE',  ( -15.08585287682999976, 4.592917106262999205, 9.171186875826000673 ) ) ;
#12330=CARTESIAN_POINT ( 'NONE',  ( 19.93312451746000136, -5.235254289062000410, 7.414295425348999657 ) ) ;
#12333=FACE_OUTER_BOUND ( 'NONE', #1375, .T. ) ;
#12334=CARTESIAN_POINT ( 'NONE',  ( 14.89795833333333164, -7.239947641283004387, -5.563765923746745834 ) ) ;
#12336=CARTESIAN_POINT ( 'NONE',  ( 23.93192965267665073, -8.373336412066850087, 4.179851967670701107 ) ) ;
#12337=CARTESIAN_POINT ( 'NONE',  ( -2.320455940937359962, 13.95415153313363454, 5.669042681536121897 ) ) ;
#12340=AXIS2_PLACEMENT_3D ( 'NONE', #10667, #23728, #18055 ) ;
#12341=EDGE_CURVE ( 'NONE', #21964, #8871, #9368, .T. ) ;
#12342=CARTESIAN_POINT ( 'NONE',  ( -20.41143800761999927, 10.68499263730999971, 2.863133627322999697 ) ) ;
#12345=CARTESIAN_POINT ( 'NONE',  ( -4.359756007405287903, 12.27018733399866868, 2.109445806361383013 ) ) ;
#12346=VERTEX_POINT ( 'NONE', #19792 ) ;
#12348=CARTESIAN_POINT ( 'NONE',  ( -24.50000000000453682, -0.2564718131638233367, -12.50000000000233946 ) ) ;
#12349=CARTESIAN_POINT ( 'NONE',  ( -10.64039927319732826, 15.44563189339511133, 1.499887593842308853 ) ) ;
#12354=CARTESIAN_POINT ( 'NONE',  ( -16.28651788626999775, 5.579994563924000062, 9.896790535726999849 ) ) ;
#12355=CARTESIAN_POINT ( 'NONE',  ( 17.56125142131000061, 3.538711643716999866, -9.078802261343000168 ) ) ;
#12356=CARTESIAN_POINT ( 'NONE',  ( 18.49749537389288179, 10.29274632983991289, -1.665592463132857137 ) ) ;
#12357=CONICAL_SURFACE ( 'NONE', #1902, 9.136555860486998526, 0.02565634000431304615 ) ;
#12362=CARTESIAN_POINT ( 'NONE',  ( -2.129837485869429337, 13.91293410602873415, -5.743800140878768445 ) ) ;
#12365=EDGE_CURVE ( 'NONE', #3930, #8569, #16488, .T. ) ;
#12367=CARTESIAN_POINT ( 'NONE',  ( -24.41513307469365657, 11.84921275893194093, -4.476505678047745462 ) ) ;
#12370=CARTESIAN_POINT ( 'NONE',  ( 16.65020012662924742, 9.567642578645610740, 4.135108216434137951 ) ) ;
#12371=CARTESIAN_POINT ( 'NONE',  ( -3.834781054353642027, 14.03942942280233552, 4.850192126058685993 ) ) ;
#12372=CARTESIAN_POINT ( 'NONE',  ( -4.915212978806001054, 12.43953049402999511, 0.1288957748261999048 ) ) ;
#12376=CARTESIAN_POINT ( 'NONE',  ( 18.93264468355999952, 0.000000000000000000, 0.000000000000000000 ) ) ;
#12377=EDGE_CURVE ( 'NONE', #5826, #19902, #3344, .T. ) ;
#12382=CYLINDRICAL_SURFACE ( 'NONE', #3569, 12.44999999999999929 ) ;
#12383=CARTESIAN_POINT ( 'NONE',  ( -2.915062434927890855, 13.09062905184296355, 6.080193266496893401 ) ) ;
#12386=DIRECTION ( 'NONE',  ( 0.000000000000000000, 1.000000000000000000, 0.000000000000000000 ) ) ;
#12388=ADVANCED_FACE ( 'NONE', ( #7167, #3321 ), #21726, .F. ) ;
#12393=DIRECTION ( 'NONE',  ( 0.000000000000000000, 0.5000000000000169864, -0.8660254037844288266 ) ) ;
#12395=CARTESIAN_POINT ( 'NONE',  ( -23.34642367104000016, 6.759604227058999548, 8.376683203238998843 ) ) ;
#12396=CARTESIAN_POINT ( 'NONE',  ( 20.15099999999999980, -9.188396088570998543, 0.000000000000000000 ) ) ;
#12397=CARTESIAN_POINT ( 'NONE',  ( 15.05994471934696222, 9.084270234149091294, 4.927946041152025280 ) ) ;
#12398=DIRECTION ( 'NONE',  ( 0.000000000000000000, 1.000000000000000000, 0.000000000000000000 ) ) ;
#12400=CARTESIAN_POINT ( 'NONE',  ( -23.13201460959644606, 9.263705172255090048, 1.213526924431011178 ) ) ;
#12401=CARTESIAN_POINT ( 'NONE',  ( -4.287094022045000230, 12.36933742260000280, -1.995563538544997240 ) ) ;
#12405=EDGE_LOOP ( 'NONE', ( #14768, #23469, #21082, #17246 ) ) ;
#12412=CARTESIAN_POINT ( 'NONE',  ( 12.00000000000000533, 3.282172266231635493, -8.358364226753291604 ) ) ;
#12414=CARTESIAN_POINT ( 'NONE',  ( 12.43237658531000100, 5.753414546153999609, -8.323445001914000940 ) ) ;
#12417=CARTESIAN_POINT ( 'NONE',  ( -5.194121241777001075, 12.44999999999999929, 0.000000000000000000 ) ) ;
#12418=CARTESIAN_POINT ( 'NONE',  ( 13.50000000000000000, 9.050782136005169676, -2.623848385460896271 ) ) ;
#12419=CARTESIAN_POINT ( 'NONE',  ( 21.05799999999999983, 9.211671496174000495, 0.000000000000000000 ) ) ;
#12421=CARTESIAN_POINT ( 'NONE',  ( 11.53663804754501321, 9.092401935531025714, 9.251313393131750829 ) ) ;
#12422=CARTESIAN_POINT ( 'NONE',  ( 22.35284124051811716, 2.717056027886565417, 10.21878362023675635 ) ) ;
#12423=CARTESIAN_POINT ( 'NONE',  ( -14.00000000000000178, 5.842258123726868035, 7.306472440924601131 ) ) ;
#12424=CARTESIAN_POINT ( 'NONE',  ( 16.27435937805609356, -0.08560440561706507412, -10.36554760290414734 ) ) ;
#12425=CARTESIAN_POINT ( 'NONE',  ( -18.41291243917333631, -8.905853451295076439, 2.393251276420213181 ) ) ;
#12428=B_SPLINE_CURVE_WITH_KNOTS ( 'NONE', 3,
 ( #16819, #3641, #5686, #2169, #3993, #5573 ),
 .UNSPECIFIED., .F., .F.,
 ( 4, 1, 1, 4 ),
 ( 0.000000000000000000, 0.3333333333333000081, 0.6666666666667000474, 1.000000000000000000 ),
 .UNSPECIFIED. ) ;
#12429=DIRECTION ( 'NONE',  ( -0.9996708941621516020, 0.02565352539211874019, 0.000000000000000000 ) ) ;
#12431=ORIENTED_EDGE ( 'NONE', *, *, #6587, .F. ) ;
#12432=CARTESIAN_POINT ( 'NONE',  ( 23.23091206975999867, -5.927610222709999377, -9.828413730229001999 ) ) ;
#12433=CARTESIAN_POINT ( 'NONE',  ( 23.10821411434546846, -10.53956942713338485, -1.043342762108328881 ) ) ;
#12434=DIRECTION ( 'NONE',  ( 0.000000000000000000, 0.9899013191676121481, -0.1417581684074016302 ) ) ;
#12435=VERTEX_POINT ( 'NONE', #6942 ) ;
#12436=CARTESIAN_POINT ( 'NONE',  ( 23.99062354302999722, -7.716878364870000340, -11.63397459621999985 ) ) ;
#12437=CARTESIAN_POINT ( 'NONE',  ( -5.425547005761002239, 14.33167101788998110, 5.123586822884999670 ) ) ;
#12438=CARTESIAN_POINT ( 'NONE',  ( -4.656229534563997241, 12.40715657742001454, -1.679150298895001114 ) ) ;
#12441=ORIENTED_EDGE ( 'NONE', *, *, #18014, .T. ) ;
#12442=DIRECTION ( 'NONE',  ( 0.000000000000000000, 1.000000000000000000, 0.000000000000000000 ) ) ;
#12444=CARTESIAN_POINT ( 'NONE',  ( 11.50000000000000000, 7.000000000000000000, 0.000000000000000000 ) ) ;
#12446=CARTESIAN_POINT ( 'NONE',  ( -10.04281598261999875, 16.38798294977999959, -1.000000000000000000 ) ) ;
#12447=CARTESIAN_POINT ( 'NONE',  ( -12.28892333464999886, 12.23011958036999935, -9.372058967585999767 ) ) ;
#12448=CARTESIAN_POINT ( 'NONE',  ( -25.07905962863999960, -4.825123054982000781, -8.416491615424000372 ) ) ;
#12450=CARTESIAN_POINT ( 'NONE',  ( -14.41041139552000061, -8.718623938206999213, 6.329101201815000799 ) ) ;
#12451=FACE_OUTER_BOUND ( 'NONE', #22212, .T. ) ;
#12452=CARTESIAN_POINT ( 'NONE',  ( -24.08723349875008068, 10.05054684006879917, -3.366032446606162853 ) ) ;
#12454=DIRECTION ( 'NONE',  ( 0.000000000000000000, 1.000000000000000000, 0.000000000000000000 ) ) ;
#12455=CARTESIAN_POINT ( 'NONE',  ( 24.28255857085268943, -8.769700062105057370, 9.810433925293667201 ) ) ;
#12456=ORIENTED_EDGE ( 'NONE', *, *, #21817, .F. ) ;
#12457=CARTESIAN_POINT ( 'NONE',  ( 23.24497483482962679, 8.949111925071910889, 2.821285790844791475 ) ) ;
#12458=CARTESIAN_POINT ( 'NONE',  ( 3.157813948402969473, 14.17377548709831814, 5.253260371035572085 ) ) ;
#12460=CARTESIAN_POINT ( 'NONE',  ( -20.74560709917999901, 6.919428769260999701, -8.642269477009000056 ) ) ;
#12461=CARTESIAN_POINT ( 'NONE',  ( -4.280167514080574165, 12.24264458569462732, 2.262784844200641743 ) ) ;
#12464=CARTESIAN_POINT ( 'NONE',  ( 4.423996544771463313, 12.29285732557641708, -1.971860468088503016 ) ) ;
#12465=CARTESIAN_POINT ( 'NONE',  ( 24.11388506871679738, -1.064351356577731833, -9.431612009895189885 ) ) ;
#12467=ORIENTED_EDGE ( 'NONE', *, *, #18579, .T. ) ;
#12469=CARTESIAN_POINT ( 'NONE',  ( -15.27086614641999951, -1.548365329537000123, -11.22688807791999999 ) ) ;
#12470=CARTESIAN_POINT ( 'NONE',  ( 12.62531392131000096, 8.177682633693001080, 5.055777280222000236 ) ) ;
#12471=CARTESIAN_POINT ( 'NONE',  ( 18.60941832878186020, 10.17571512187342719, 2.300618295382859113 ) ) ;
#12473=VERTEX_POINT ( 'NONE', #10826 ) ;
#12474=CARTESIAN_POINT ( 'NONE',  ( -22.87210175995843642, 9.258583067823760615, -6.329161777784410158E-06 ) ) ;
#12477=CARTESIAN_POINT ( 'NONE',  ( 13.50000000000000178, -9.667143133194834093, 1.150750041508975974 ) ) ;
#12478=AXIS2_PLACEMENT_3D ( 'NONE', #3185, #23637, #7150 ) ;
#12480=CARTESIAN_POINT ( 'NONE',  ( 18.75008227645999881, 0.000000000000000000, 0.000000000000000000 ) ) ;
#12483=CARTESIAN_POINT ( 'NONE',  ( -23.76509227919060407, -8.602129290516417726, 4.230010080241071613 ) ) ;
#12484=CARTESIAN_POINT ( 'NONE',  ( 14.14125231517192383, -4.302439909528064987, -9.420726477911008701 ) ) ;
#12485=CARTESIAN_POINT ( 'NONE',  ( 24.50000000000000000, -10.82531754731000007, 6.250000000000000000 ) ) ;
#12486=CARTESIAN_POINT ( 'NONE',  ( 2.372479547917001330, 11.76473980360000837, 4.356678035347999689 ) ) ;
#12492=ORIENTED_EDGE ( 'NONE', *, *, #13472, .F. ) ;
#12494=FACE_OUTER_BOUND ( 'NONE', #22207, .T. ) ;
#12495=CARTESIAN_POINT ( 'NONE',  ( -19.42565315260486614, -9.827978956737730698, 3.502397672827030739 ) ) ;
#12497=CARTESIAN_POINT ( 'NONE',  ( -5.694829656253005190, 15.68676470074999685, -2.067368767709001798 ) ) ;
#12500=ORIENTED_EDGE ( 'NONE', *, *, #18250, .F. ) ;
#12503=DIRECTION ( 'NONE',  ( -0.9996708941621507138, -0.02565352539215873945, -1.663606736649919489E-14 ) ) ;
#12506=CARTESIAN_POINT ( 'NONE',  ( -19.74772222328000026, 7.504538301275000656, 7.579212376565000575 ) ) ;
#12508=CARTESIAN_POINT ( 'NONE',  ( 15.14946676811930892, 7.172451777050300237, 7.444582818315895523 ) ) ;
#12510=CARTESIAN_POINT ( 'NONE',  ( 24.30943970833000023, -6.839077597037000800, 9.006887850905000548 ) ) ;
#12512=CARTESIAN_POINT ( 'NONE',  ( -22.58373927040480211, -4.100154767907044473, 8.316095026788374867 ) ) ;
#12513=CARTESIAN_POINT ( 'NONE',  ( 4.436770113162001650, 12.42462873132999057, -1.662129547883000047 ) ) ;
#12515=ORIENTED_EDGE ( 'NONE', *, *, #3366, .T. ) ;
#12518=ORIENTED_EDGE ( 'NONE', *, *, #21424, .F. ) ;
#12521=ORIENTED_EDGE ( 'NONE', *, *, #491, .T. ) ;
#12524=DIRECTION ( 'NONE',  ( 0.000000000000000000, 1.000000000000000000, 0.000000000000000000 ) ) ;
#12525=CARTESIAN_POINT ( 'NONE',  ( 14.87356278734000092, 6.387809963882999931, 8.986984594874000365 ) ) ;
#12526=ORIENTED_EDGE ( 'NONE', *, *, #1948, .T. ) ;
#12527=CARTESIAN_POINT ( 'NONE',  ( -11.91164815959000123, 4.681446530594000066, -13.43333759439000019 ) ) ;
#12528=CARTESIAN_POINT ( 'NONE',  ( 13.50000000000000000, 9.584206265642421840, 0.6392395819158175341 ) ) ;
#12530=EDGE_CURVE ( 'NONE', #2558, #16650, #7669, .T. ) ;
#12531=VERTEX_POINT ( 'NONE', #22530 ) ;
#12533=CARTESIAN_POINT ( 'NONE',  ( 23.73532679364096154, 10.43134061897112552, -1.947531773972139835 ) ) ;
#12536=CARTESIAN_POINT ( 'NONE',  ( 17.60422380272236964, -10.38553041900061835, 1.163297858921190642 ) ) ;
#12537=CARTESIAN_POINT ( 'NONE',  ( -17.90484265138000097, 4.662643172107000744, 10.07117353495000067 ) ) ;
#12538=CARTESIAN_POINT ( 'NONE',  ( -14.33281102374373184, -13.40129170500426348, 1.788281879885561754 ) ) ;
#12540=CARTESIAN_POINT ( 'NONE',  ( -17.38302573041000088, 5.218320932965999859, 8.277968099418000492 ) ) ;
#12544=CARTESIAN_POINT ( 'NONE',  ( 21.10515180059999807, -11.40348565785000012, 0.5907356610812999342 ) ) ;
#12546=CARTESIAN_POINT ( 'NONE',  ( 24.44176314649520165, -0.04959099671479073879, 10.63117537983664107 ) ) ;
#12549=ORIENTED_EDGE ( 'NONE', *, *, #11166, .F. ) ;
#12551=CARTESIAN_POINT ( 'NONE',  ( 4.921741273393275051, 14.32471902143299758, -3.831972585562755995 ) ) ;
#12552=CARTESIAN_POINT ( 'NONE',  ( -4.833494752206995315, 12.42175356251998330, 0.1521745567910999519 ) ) ;
#12553=ORIENTED_EDGE ( 'NONE', *, *, #18678, .F. ) ;
#12558=VERTEX_POINT ( 'NONE', #4128 ) ;
#12559=LINE ( 'NONE', #14131, #18632 ) ;
#12560=CIRCLE ( 'NONE', #8704, 4.750000000000000000 ) ;
#12561=CARTESIAN_POINT ( 'NONE',  ( -4.894724768791110847, 15.80180785695556267, -3.682445206660954540 ) ) ;
#12562=CARTESIAN_POINT ( 'NONE',  ( -24.91847294367000032, 0.3645929728760000099, -10.20369181617000010 ) ) ;
#12563=CARTESIAN_POINT ( 'NONE',  ( -16.16755505407000371, -1.332106624616000046, -9.660193477322000177 ) ) ;
#12564=CARTESIAN_POINT ( 'NONE',  ( 19.09283333333333132, 8.004919495498239002, -4.613892360491747446 ) ) ;
#12565=CARTESIAN_POINT ( 'NONE',  ( -23.08356359459203233, -10.56989946170757122, -0.1237766064311238562 ) ) ;
#12569=ORIENTED_EDGE ( 'NONE', *, *, #17943, .T. ) ;
#12570=CARTESIAN_POINT ( 'NONE',  ( -61.30710721978000066, 16.31160201366999729, 2.000000000000000000 ) ) ;
#12573=CARTESIAN_POINT ( 'NONE',  ( -24.36619054344396673, -4.196740350062569291, -9.738563182048725508 ) ) ;
#12576=CARTESIAN_POINT ( 'NONE',  ( 3.929826322352642620, 12.12559072794920745, 2.830479342495737960 ) ) ;
#12578=CARTESIAN_POINT ( 'NONE',  ( 18.29920833333331842, -9.140875464714465437, 1.196664747960662245 ) ) ;
#12583=CARTESIAN_POINT ( 'NONE',  ( 11.91174123157076004, 2.862535089823035062, -8.618805975702651168 ) ) ;
#12584=ORIENTED_EDGE ( 'NONE', *, *, #17943, .F. ) ;
#12586=CARTESIAN_POINT ( 'NONE',  ( -16.29067920454665241, 2.379230875366821873, -8.852713068186144341 ) ) ;
#12587=CARTESIAN_POINT ( 'NONE',  ( 12.18656392131000210, 5.460236994095999385, -7.899338765649998706 ) ) ;
#12588=CARTESIAN_POINT ( 'NONE',  ( 18.71070319846496233, 8.742660180748359267, 5.685782510781925758 ) ) ;
#12591=CARTESIAN_POINT ( 'NONE',  ( -24.49594166687865382, 0.5121745395634360598, 12.49996680834482454 ) ) ;
#12592=CARTESIAN_POINT ( 'NONE',  ( 11.00000000000000000, -7.000000000000000000, 0.000000000000000000 ) ) ;
#12593=CARTESIAN_POINT ( 'NONE',  ( -12.49650014189999858, 7.040626845934999878, -5.593302763177000259 ) ) ;
#12594=CARTESIAN_POINT ( 'NONE',  ( 13.50000000000000000, -6.542208323345639620, 7.794097110268465300 ) ) ;
#12598=CARTESIAN_POINT ( 'NONE',  ( -14.25699038479000080, 13.93375672974000068, 0.000000000000000000 ) ) ;
#12600=CARTESIAN_POINT ( 'NONE',  ( 24.50000000000000355, -6.132195556898603073, 8.621549258802161830 ) ) ;
#12602=CARTESIAN_POINT ( 'NONE',  ( -1.099366357925000148, 11.57595430713999818, 4.853237177371000577 ) ) ;
#12603=CARTESIAN_POINT ( 'NONE',  ( -24.42716110443999966, -9.258832120292998624, -5.480706378555000313 ) ) ;
#12604=ORIENTED_EDGE ( 'NONE', *, *, #2096, .T. ) ;
#12607=ORIENTED_EDGE ( 'NONE', *, *, #14737, .F. ) ;
#12610=DIRECTION ( 'NONE',  ( -1.000000000000000000, 0.000000000000000000, 0.000000000000000000 ) ) ;
#12612=CARTESIAN_POINT ( 'NONE',  ( -19.49229789055419459, -9.829589521208637493, 3.502971628430095130 ) ) ;
#12613=CIRCLE ( 'NONE', #7557, 7.500000000000000000 ) ;
#12614=CARTESIAN_POINT ( 'NONE',  ( 6.225185179353265319, 13.76374128849115941, -1.297207482702341652 ) ) ;
#12618=CARTESIAN_POINT ( 'NONE',  ( -17.17989538244000158, -1.375580078895000113, 9.682594755839000200 ) ) ;
#12621=VERTEX_POINT ( 'NONE', #131 ) ;
#12623=CARTESIAN_POINT ( 'NONE',  ( -21.63275631497000262, 9.168463912656999781, 5.549645297457000304 ) ) ;
#12625=CARTESIAN_POINT ( 'NONE',  ( 14.42874905160420340, -1.189975876054675474, -10.24990194960133216 ) ) ;
#12627=CARTESIAN_POINT ( 'NONE',  ( 22.47397007865999896, -6.123241711276000920, 9.448760031808999926 ) ) ;
#12629=DIRECTION ( 'NONE',  ( -1.000000000000000000, 0.000000000000000000, 0.000000000000000000 ) ) ;
#12632=VERTEX_POINT ( 'NONE', #16966 ) ;
#12635=ORIENTED_EDGE ( 'NONE', *, *, #12530, .F. ) ;
#12638=CARTESIAN_POINT ( 'NONE',  ( 16.78754166666665526, -5.593745091089892263, -7.278544301236070879 ) ) ;
#12639=CARTESIAN_POINT ( 'NONE',  ( 21.94695603379666338, -4.650544061505227589, 8.069014881146078011 ) ) ;
#12640=CARTESIAN_POINT ( 'NONE',  ( 17.90739874975000134, -0.4687343941967000438, -11.09907540322000052 ) ) ;
#12641=( BOUNDED_SURFACE ( )  B_SPLINE_SURFACE ( 3, 3, ( 
 ( #1102, #18065, #16349, #14185, #14310, #21702, #8867, #23505, #8617, #21582, #8502, #14533, #16237, #21927, #19767, #3177, #12258 ),
 ( #5112, #7034, #8740, #16103, #5339, #6916, #6668, #12727, #23628, #19643, #10442, #9324, #11023, #3752, #7742, #11141, #18755 ),
 ( #16583, #3989, #7258, #22159, #5570, #16698, #22047, #9088, #5456, #10912, #14993, #18527, #16459, #11384, #7494, #1818, #14761 ),
 ( #14879, #12948, #107, #22504, #3530, #22266, #16815, #14651, #13186, #23850, #20345, #22391, #20467, #5682, #2165, #340, #1936 ) ),
 .UNSPECIFIED., .F., .F., .T. ) 
 B_SPLINE_SURFACE_WITH_KNOTS ( ( 4, 4 ),
 ( 4, 1, 1, 1, 1, 1, 1, 1, 1, 1, 1, 1, 1, 1, 4 ),
 ( 0.000000000000000000, 1.000000000000000000 ),
 ( 0.2369161175745000125, 0.2385325641787000017, 0.2467937715444999958, 0.2545547496928000086, 0.2620001226550999762, 0.2692869410311000133, 0.2765143615464999982, 0.2837371216738999724, 0.2910081725563999910, 0.2983850687121999967, 0.3059382517664999690, 0.3138738688366000118, 0.3225287194381999956, 0.3320773268852000304, 0.3323108935713000034 ),
 .UNSPECIFIED. ) 
 GEOMETRIC_REPRESENTATION_ITEM ( )  RATIONAL_B_SPLINE_SURFACE ( (
 ( 1.093547071729999987, 1.093547071729999987, 1.093547071729999987, 1.093547071729999987, 1.093547071729999987, 1.093547071729999987, 1.093547071729999987, 1.093547071729999987, 1.093547071729999987, 1.093547071729999987, 1.093547071729999987, 1.093547071729999987, 1.093547071729999987, 1.093547071729999987, 1.093547071729999987, 1.093547071729999987, 1.093547071729999987),
 ( 0.9688176427565999838, 0.9688176427565999838, 0.9688176427565999838, 0.9688176427565999838, 0.9688176427565999838, 0.9688176427565999838, 0.9688176427565999838, 0.9688176427565999838, 0.9688176427565999838, 0.9688176427565999838, 0.9688176427565999838, 0.9688176427565999838, 0.9688176427565999838, 0.9688176427565999838, 0.9688176427565999838, 0.9688176427565999838, 0.9688176427565999838),
 ( 0.9688176427565999838, 0.9688176427565999838, 0.9688176427565999838, 0.9688176427565999838, 0.9688176427565999838, 0.9688176427565999838, 0.9688176427565999838, 0.9688176427565999838, 0.9688176427565999838, 0.9688176427565999838, 0.9688176427565999838, 0.9688176427565999838, 0.9688176427565999838, 0.9688176427565999838, 0.9688176427565999838, 0.9688176427565999838, 0.9688176427565999838),
 ( 1.093547071729999987, 1.093547071729999987, 1.093547071729999987, 1.093547071729999987, 1.093547071729999987, 1.093547071729999987, 1.093547071729999987, 1.093547071729999987, 1.093547071729999987, 1.093547071729999987, 1.093547071729999987, 1.093547071729999987, 1.093547071729999987, 1.093547071729999987, 1.093547071729999987, 1.093547071729999987, 1.093547071729999987) ) ) 
 REPRESENTATION_ITEM ( '' )  SURFACE ( )  );
#12642=ORIENTED_EDGE ( 'NONE', *, *, #4203, .F. ) ;
#12644=CARTESIAN_POINT ( 'NONE',  ( -11.12363506584999939, -14.39414658121999935, 3.723758764729999893 ) ) ;
#12645=CARTESIAN_POINT ( 'NONE',  ( 13.50000000000000178, 5.245049793575820019, -7.438478054735814915 ) ) ;
#12648=EDGE_CURVE ( 'NONE', #3390, #1236, #1820, .T. ) ;
#12649=FACE_OUTER_BOUND ( 'NONE', #10291, .T. ) ;
#12650=CARTESIAN_POINT ( 'NONE',  ( 20.67620982502827687, -2.254432935689778983, 10.28453417332591258 ) ) ;
#12652=CARTESIAN_POINT ( 'NONE',  ( 16.12378973994088938, -5.293627507836296431, -8.912173777944857989 ) ) ;
#12653=CARTESIAN_POINT ( 'NONE',  ( -19.35014917163000092, -7.793226253172000462, 6.938245049636000417 ) ) ;
#12656=CARTESIAN_POINT ( 'NONE',  ( -17.01752311569999776, -10.30819550402000040, 0.2320531645540999943 ) ) ;
#12661=CARTESIAN_POINT ( 'NONE',  ( -24.43506354683022508, -1.794296882945331628, 12.50003182001101365 ) ) ;
#12662=CARTESIAN_POINT ( 'NONE',  ( 22.48399967376405684, 5.010257334270587393, 9.319128840364694355 ) ) ;
#12666=EDGE_CURVE ( 'NONE', #5222, #17203, #6753, .T. ) ;
#12667=DIRECTION ( 'NONE',  ( -1.000000000000000000, 0.000000000000000000, 0.000000000000000000 ) ) ;
#12668=DIRECTION ( 'NONE',  ( 0.000000000000000000, 1.000000000000000000, 0.000000000000000000 ) ) ;
#12670=CARTESIAN_POINT ( 'NONE',  ( -4.838624173045001697, 12.42376152392000321, -0.01103063371175000071 ) ) ;
#12674=AXIS2_PLACEMENT_3D ( 'NONE', #20941, #1440, #8838 ) ;
#12676=CARTESIAN_POINT ( 'NONE',  ( -14.48091997122309138, -1.686280348636405968, -12.50000494027439046 ) ) ;
#12678=ADVANCED_FACE ( 'NONE', ( #23125 ), #18127, .F. ) ;
#12680=CARTESIAN_POINT ( 'NONE',  ( -19.27137435357334283, 5.489963247718526063, 7.417229561569652851 ) ) ;
#12682=CARTESIAN_POINT ( 'NONE',  ( -20.95579840402999849, 2.757578367990000334, -10.25841757755000039 ) ) ;
#12683=CARTESIAN_POINT ( 'NONE',  ( -14.33938192233999942, -0.8520670991562999674, -9.663538843295999214 ) ) ;
#12685=CARTESIAN_POINT ( 'NONE',  ( -24.50000000000000000, -1.873582633960999999, -10.39897383761999983 ) ) ;
#12687=CARTESIAN_POINT ( 'NONE',  ( -7.078629509575005585, 15.37751798353000865, 1.431388464268000815 ) ) ;
#12689=EDGE_LOOP ( 'NONE', ( #20117, #17389, #19029, #11732, #3865 ) ) ;
#12690=CARTESIAN_POINT ( 'NONE',  ( 23.49157400021077180, 3.736182324670829669, 8.508904909832841312 ) ) ;
#12691=CARTESIAN_POINT ( 'NONE',  ( 2.980299236784382355, 14.12173736862491147, 5.353969783937538196 ) ) ;
#12692=CARTESIAN_POINT ( 'NONE',  ( 13.81123111472108711, 5.253611299945564639, -7.402707599910051783 ) ) ;
#12694=CARTESIAN_POINT ( 'NONE',  ( 5.822189159540518411, 14.45422085624546149, -1.902041274716720354 ) ) ;
#12696=DIRECTION ( 'NONE',  ( 1.000000000000000000, 0.000000000000000000, 0.000000000000000000 ) ) ;
#12697=ORIENTED_EDGE ( 'NONE', *, *, #23312, .F. ) ;
#12698=CARTESIAN_POINT ( 'NONE',  ( -2.579645516591716259, 11.76412175278740158, -4.075715327416034484 ) ) ;
#12699=CARTESIAN_POINT ( 'NONE',  ( -10.64810398754049281, 15.44157726471785530, 1.506975047069119222 ) ) ;
#12700=CARTESIAN_POINT ( 'NONE',  ( 11.84553914498074612, 0.8330063648739851612, -8.962484781899275887 ) ) ;
#12705=VECTOR ( 'NONE', #3414, 1000.000000000000000 ) ;
#12706=CARTESIAN_POINT ( 'NONE',  ( 17.01281392131000203, -9.720744103539999514, -0.4165551917177999774 ) ) ;
#12707=CARTESIAN_POINT ( 'NONE',  ( 18.82877641267331370, 5.758514806318896895, 8.698589068941570801 ) ) ;
#12710=CARTESIAN_POINT ( 'NONE',  ( -12.50725636293000065, 6.705474853889000997, -5.997154546401000097 ) ) ;
#12711=CARTESIAN_POINT ( 'NONE',  ( 13.50000000000000000, -9.682388338819057694, 0.8738273617125053017 ) ) ;
#12714=CARTESIAN_POINT ( 'NONE',  ( 21.81229861174000106, -4.409328772385999962, -9.829213302973000665 ) ) ;
#12715=AXIS2_PLACEMENT_3D ( 'NONE', #14727, #22122, #3378 ) ;
#12717=DIRECTION ( 'NONE',  ( -1.000000000000000000, 0.000000000000000000, 0.000000000000000000 ) ) ;
#12718=CIRCLE ( 'NONE', #11555, 10.59999999999999964 ) ;
#12719=CARTESIAN_POINT ( 'NONE',  ( 18.75008227645999881, 0.000000000000000000, 0.000000000000000000 ) ) ;
#12721=FACE_OUTER_BOUND ( 'NONE', #21079, .T. ) ;
#12722=CARTESIAN_POINT ( 'NONE',  ( -23.98160231569000445, 5.441259261708000672, -9.742227938132998588 ) ) ;
#12727=CARTESIAN_POINT ( 'NONE',  ( 5.849408608611998517, 14.13599281491000248, 1.675474256364998693 ) ) ;
#12729=CARTESIAN_POINT ( 'NONE',  ( 6.189313035766128124, 13.92501040246023791, -0.7765889110677386409 ) ) ;
#12731=AXIS2_PLACEMENT_3D ( 'NONE', #2309, #361, #18774 ) ;
#12733=CARTESIAN_POINT ( 'NONE',  ( -16.97676503447000229, -7.308902056012999360, 6.489539471208999544 ) ) ;
#12735=CYLINDRICAL_SURFACE ( 'NONE', #12478, 7.000000000000000000 ) ;
#12737=ORIENTED_EDGE ( 'NONE', *, *, #20951, .T. ) ;
#12738=CARTESIAN_POINT ( 'NONE',  ( -19.47751044566000189, -9.410400067285001668, 6.038396183999999778 ) ) ;
#12740=CARTESIAN_POINT ( 'NONE',  ( 14.75769395697458641, 8.804643041191516417, -5.399440270566639555 ) ) ;
#12741=CIRCLE ( 'NONE', #8881, 9.274346474608000435 ) ;
#12742=DIRECTION ( 'NONE',  ( 1.000000000000000000, 0.000000000000000000, 0.000000000000000000 ) ) ;
#12743=CARTESIAN_POINT ( 'NONE',  ( 21.11529060572999938, -10.17976386977000125, 4.723040569265999800 ) ) ;
#12746=CARTESIAN_POINT ( 'NONE',  ( 13.69763181055747658, 8.467209252517251983, -3.113060745664182338 ) ) ;
#12751=CARTESIAN_POINT ( 'NONE',  ( -14.91309832688787829, -8.601256312377522306, -2.840204793172258491 ) ) ;
#12753=B_SPLINE_CURVE_WITH_KNOTS ( 'NONE', 3,
 ( #17562, #11995, #16085, #957 ),
 .UNSPECIFIED., .F., .F.,
 ( 4, 4 ),
 ( 0.000000000000000000, 1.000000000000000000 ),
 .UNSPECIFIED. ) ;
#12754=CONICAL_SURFACE ( 'NONE', #19321, 9.787173237795000702, 0.7982263333994560339 ) ;
#12756=CARTESIAN_POINT ( 'NONE',  ( -15.76749577250665268, 7.930452343988175556, -4.570681609295893288 ) ) ;
#12759=LINE ( 'NONE', #9007, #21634 ) ;
#12760=CARTESIAN_POINT ( 'NONE',  ( 13.97130829811999853, -6.225248563364000454, -9.070390281432999302 ) ) ;
#12761=CARTESIAN_POINT ( 'NONE',  ( -15.14443833155225860, 1.225503469059798345, -10.30197729002023443 ) ) ;
#12763=CARTESIAN_POINT ( 'NONE',  ( -9.079811138770001122, 14.12775011938999903, -4.287383359707000352 ) ) ;
#12764=DIRECTION ( 'NONE',  ( -0.000000000000000000, 0.8660254037844288266, 0.5000000000000169864 ) ) ;
#12767=ORIENTED_EDGE ( 'NONE', *, *, #22831, .T. ) ;
#12768=CARTESIAN_POINT ( 'NONE',  ( 23.64708303493075903, 9.358955864019327109, -4.992123380202468041 ) ) ;
#12769=DIRECTION ( 'NONE',  ( 1.000000000000000000, 0.000000000000000000, 0.000000000000000000 ) ) ;
#12770=CARTESIAN_POINT ( 'NONE',  ( 16.10813149828275925, -5.761241547484484471, -8.613496363008477985 ) ) ;
#12771=CARTESIAN_POINT ( 'NONE',  ( -18.37512077250666565, -9.142823527519007953, 1.196665853474645713 ) ) ;
#12774=CARTESIAN_POINT ( 'NONE',  ( -12.71102772709999940, -0.8480750162247000512, -9.618334173012000221 ) ) ;
#12776=ORIENTED_EDGE ( 'NONE', *, *, #5842, .F. ) ;
#12778=CARTESIAN_POINT ( 'NONE',  ( 20.01551529510171434, 3.913198373954541509, -9.761947581437320665 ) ) ;
#12783=CARTESIAN_POINT ( 'NONE',  ( -5.708827511056002280, 14.62924567951000121, 4.675388362802000763 ) ) ;
#12785=CARTESIAN_POINT ( 'NONE',  ( -1.453122705278999671, 11.52960387473001447, -4.636509077308001103 ) ) ;
#12787=CARTESIAN_POINT ( 'NONE',  ( 18.30262625730999915, -5.463569446885998993, 7.195226492777999638 ) ) ;
#12791=PLANE ( 'NONE',  #4397 ) ;
#12792=ORIENTED_EDGE ( 'NONE', *, *, #5645, .T. ) ;
#12793=CARTESIAN_POINT ( 'NONE',  ( 22.96733103379666829, 7.405359927155213740, -5.691203335971525945 ) ) ;
#12794=CARTESIAN_POINT ( 'NONE',  ( -24.75788625869999748, 5.695182633683000262, -8.469459980026998736 ) ) ;
#12795=EDGE_CURVE ( 'NONE', #15500, #22071, #14647, .T. ) ;
#12796=CARTESIAN_POINT ( 'NONE',  ( -17.58946748986000230, 9.198462325352998903, -3.355076284083000182 ) ) ;
#12797=CYLINDRICAL_SURFACE ( 'NONE', #10015, 12.44999999999999929 ) ;
#12799=CARTESIAN_POINT ( 'NONE',  ( -24.03576324725467117, 10.56622451174204791, -1.538538087633267493 ) ) ;
#12801=CARTESIAN_POINT ( 'NONE',  ( -23.74465998031000069, 13.93375672974000068, -0.8660254037843999608 ) ) ;
#12804=CARTESIAN_POINT ( 'NONE',  ( -14.25243324638999809, 7.716878364870000340, 11.63397459621999985 ) ) ;
#12806=CARTESIAN_POINT ( 'NONE',  ( 14.65123321485445729, -3.417938325912019515, 8.433851502399324573 ) ) ;
#12810=CARTESIAN_POINT ( 'NONE',  ( 3.768907243589071143, 12.07611331052141068, 3.028204989709172068 ) ) ;
#12811=ORIENTED_EDGE ( 'NONE', *, *, #19797, .F. ) ;
#12812=CARTESIAN_POINT ( 'NONE',  ( 0.9507570701814898051, 11.52082522333564185, -4.719524835566960341 ) ) ;
#12816=DIRECTION ( 'NONE',  ( 0.000000000000000000, -1.000000000000000000, 0.000000000000000000 ) ) ;
#12818=CARTESIAN_POINT ( 'NONE',  ( 17.03925158531000150, -7.718145806856000490, 6.728824147386999854 ) ) ;
#12819=CARTESIAN_POINT ( 'NONE',  ( 18.56467270447140905, 10.41527438795320215, 0.6637449761490703537 ) ) ;
#12824=CARTESIAN_POINT ( 'NONE',  ( 24.00016455292000117, 0.000000000000000000, 0.000000000000000000 ) ) ;
#12825=CARTESIAN_POINT ( 'NONE',  ( 13.49999999999999822, -9.280155195632126208, 3.398040422365634416 ) ) ;
#12826=ORIENTED_EDGE ( 'NONE', *, *, #2163, .F. ) ;
#12828=CARTESIAN_POINT ( 'NONE',  ( 24.01968146971000095, 10.82136356335000116, 3.464147784671999908 ) ) ;
#12829=LINE ( 'NONE', #20222, #22034 ) ;
#12830=CARTESIAN_POINT ( 'NONE',  ( 24.50000000000000355, -5.745916189485869019, 8.881438032232539470 ) ) ;
#12831=CARTESIAN_POINT ( 'NONE',  ( 24.50000000000000000, -2.116736914405999759, 10.36413001332999961 ) ) ;
#12832=CARTESIAN_POINT ( 'NONE',  ( -4.911757422161000974, 12.43820115989000463, -0.1548696107648001308 ) ) ;
#12840=CARTESIAN_POINT ( 'NONE',  ( 11.83261479512859005, -4.444106517313184845, -12.50001436053571346 ) ) ;
#12842=CARTESIAN_POINT ( 'NONE',  ( 15.61599999999999966, 9.072019050554999353, 0.000000000000000000 ) ) ;
#12843=CARTESIAN_POINT ( 'NONE',  ( 14.95518908531000157, 0.8306535110907999897, 10.15076156001000207 ) ) ;
#12845=CARTESIAN_POINT ( 'NONE',  ( -13.92980981492000048, 8.913287911097999228, 3.799313832512000388 ) ) ;
#12849=CARTESIAN_POINT ( 'NONE',  ( -21.70527800856000056, 4.716435154626999804, 10.20496424891999965 ) ) ;
#12851=CARTESIAN_POINT ( 'NONE',  ( 14.42389269608120550, -1.357837271329138895, -10.22827832841361584 ) ) ;
#12853=CARTESIAN_POINT ( 'NONE',  ( 24.74930449899000351, -6.846379809230999314, 9.016502796240001061 ) ) ;
#12855=CARTESIAN_POINT ( 'NONE',  ( 13.90630400283265189, 8.447665157146255765, 3.286514732384385962 ) ) ;
#12857=CARTESIAN_POINT ( 'NONE',  ( -21.54372087121332058, 7.376325515330552030, -5.668572789218019103 ) ) ;
#12858=ORIENTED_EDGE ( 'NONE', *, *, #11327, .T. ) ;
#12861=CARTESIAN_POINT ( 'NONE',  ( -16.52332910583999848, -9.095302903661998783, 0.000000000000000000 ) ) ;
#12862=CARTESIAN_POINT ( 'NONE',  ( 11.10357421856111770, -11.32461805837665914, -5.385126951711886711 ) ) ;
#12863=DIRECTION ( 'NONE',  ( 1.000000000000000000, 0.000000000000000000, 0.000000000000000000 ) ) ;
#12864=CARTESIAN_POINT ( 'NONE',  ( 18.74199463705999946, 10.75162630220000182, 2.884222835622999526 ) ) ;
#12865=CARTESIAN_POINT ( 'NONE',  ( -14.22336750299141350, -1.721665810523229201, 10.20748740977781743 ) ) ;
#12868=CARTESIAN_POINT ( 'NONE',  ( -9.698120065846001836, -12.55614823169000083, 7.962473021397999062 ) ) ;
#12870=CARTESIAN_POINT ( 'NONE',  ( -14.46758738162252200, -11.92463202973427450, -4.345869468076080544 ) ) ;
#12872=CARTESIAN_POINT ( 'NONE',  ( 22.97054755148782235, -10.09263782147366406, -3.219215513880642643 ) ) ;
#12874=CARTESIAN_POINT ( 'NONE',  ( 24.36881528991178669, 9.280258940103371046, -8.926120008345273860 ) ) ;
#12875=CARTESIAN_POINT ( 'NONE',  ( 15.98668428079841419, -8.741113912782290996, -5.559642979276560482 ) ) ;
#12876=CARTESIAN_POINT ( 'NONE',  ( -14.65290298080999953, 10.85889821503999997, -1.812136570545000103 ) ) ;
#12877=CARTESIAN_POINT ( 'NONE',  ( -14.25243324638999809, -13.93375672974000068, 0.8660254037843999608 ) ) ;
#12878=CARTESIAN_POINT ( 'NONE',  ( -17.42378381163999990, -1.451785825221999948, 10.21952336923999916 ) ) ;
#12882=CARTESIAN_POINT ( 'NONE',  ( 22.05839891882162362, 9.896157607257229927, -4.111721767579475717 ) ) ;
#12884=VERTEX_POINT ( 'NONE', #15106 ) ;
#12886=CARTESIAN_POINT ( 'NONE',  ( 4.959031697897713364, 14.24213067552161860, -3.859769780926356475 ) ) ;
#12887=CARTESIAN_POINT ( 'NONE',  ( -4.686714857457999983, 12.36493082504999030, -1.218571946898999281 ) ) ;
#12889=EDGE_CURVE ( 'NONE', #16623, #20307, #642, .T. ) ;
#12890=CARTESIAN_POINT ( 'NONE',  ( 12.37950125730999851, 7.739157895793999487, 4.784640364371000487 ) ) ;
#12891=ORIENTED_EDGE ( 'NONE', *, *, #18467, .T. ) ;
#12892=CARTESIAN_POINT ( 'NONE',  ( -4.793505211713778635, 15.72902665353115914, 3.813309186838572451 ) ) ;
#12893=VECTOR ( 'NONE', #1235, 1000.000000000000000 ) ;
#12895=CARTESIAN_POINT ( 'NONE',  ( -14.47793696890909310, -1.813149206532627122, -12.49999424749392318 ) ) ;
#12896=EDGE_LOOP ( 'NONE', ( #20145, #2999, #4228, #3505, #9674, #14877 ) ) ;
#12897=DIRECTION ( 'NONE',  ( 0.000000000000000000, -1.000000000000000000, 0.000000000000000000 ) ) ;
#12898=CARTESIAN_POINT ( 'NONE',  ( 12.00000000000000000, -2.131481067915950600, -9.235415327618111903 ) ) ;
#12900=CARTESIAN_POINT ( 'NONE',  ( -17.79259783783000159, 4.846286003622000571, -8.514261148733998752 ) ) ;
#12901=DIRECTION ( 'NONE',  ( -1.000000000000000000, 0.000000000000000000, 0.000000000000000000 ) ) ;
#12902=CARTESIAN_POINT ( 'NONE',  ( -23.23797434907875115, -9.160276637173986103, 5.282797156801545491 ) ) ;
#12904=CARTESIAN_POINT ( 'NONE',  ( 15.88054166666666767, 5.579441265691143848, 7.259931729532359768 ) ) ;
#12905=CARTESIAN_POINT ( 'NONE',  ( -6.460109682835006417, 15.34437729315000176, 0.9342512191726000115 ) ) ;
#12907=( BOUNDED_SURFACE ( )  B_SPLINE_SURFACE ( 3, 3, ( 
 ( #2668, #2794, #588, #8240, #4610, #20710, #4119, #22633, #2305, #4482, #13559, #7873 ),
 ( #11999, #20954, #15607, #8125, #15242, #11517, #19383, #18895, #6174, #2417, #10178, #11637 ),
 ( #15725, #4359, #17565, #717, #5928, #13434, #20836, #9929, #11872, #13313, #11752, #19255 ),
 ( #22875, #9808, #7991, #17192, #22755, #19125, #17444, #2537, #17314, #15490, #838, #6292 ) ),
 .UNSPECIFIED., .F., .F., .T. ) 
 B_SPLINE_SURFACE_WITH_KNOTS ( ( 4, 4 ),
 ( 4, 1, 1, 1, 1, 1, 1, 1, 1, 4 ),
 ( 0.000000000000000000, 1.000000000000000000 ),
 ( 0.2029331708080999996, 0.2146186482909000215, 0.2811902510222000218, 0.3470065005328999974, 0.4101739155435999984, 0.4723427673776999791, 0.5359290704369999991, 0.6036851897885999740, 0.6764911258172999764, 0.7270516473460000295 ),
 .UNSPECIFIED. ) 
 GEOMETRIC_REPRESENTATION_ITEM ( )  RATIONAL_B_SPLINE_SURFACE ( (
 ( 1.179588279202000045, 1.179588279202000045, 1.179588279202000045, 1.179588279202000045, 1.179588279202000045, 1.179588279202000045, 1.179588279202000045, 1.179588279202000045, 1.179588279202000045, 1.179588279202000045, 1.179588279202000045, 1.179588279202000045),
 ( 0.9401372402659999850, 0.9401372402659999850, 0.9401372402659999850, 0.9401372402659999850, 0.9401372402659999850, 0.9401372402659999850, 0.9401372402659999850, 0.9401372402659999850, 0.9401372402659999850, 0.9401372402659999850, 0.9401372402659999850, 0.9401372402659999850),
 ( 0.9401372402659999850, 0.9401372402659999850, 0.9401372402659999850, 0.9401372402659999850, 0.9401372402659999850, 0.9401372402659999850, 0.9401372402659999850, 0.9401372402659999850, 0.9401372402659999850, 0.9401372402659999850, 0.9401372402659999850, 0.9401372402659999850),
 ( 1.179588279202000045, 1.179588279202000045, 1.179588279202000045, 1.179588279202000045, 1.179588279202000045, 1.179588279202000045, 1.179588279202000045, 1.179588279202000045, 1.179588279202000045, 1.179588279202000045, 1.179588279202000045, 1.179588279202000045) ) ) 
 REPRESENTATION_ITEM ( '' )  SURFACE ( )  );
#12910=CARTESIAN_POINT ( 'NONE',  ( -18.18616243917333009, -7.984589140717944566, -4.602174676763225669 ) ) ;
#12912=CARTESIAN_POINT ( 'NONE',  ( 14.40234370370382422, 4.168452611431005650, 8.082017270204577386 ) ) ;
#12913=CARTESIAN_POINT ( 'NONE',  ( -21.92954041657237596, 10.88116636271459647, 1.967860641670612587 ) ) ;
#12916=DIRECTION ( 'NONE',  ( 0.000000000000000000, 0.9420570860200443430, 0.3354525997505800605 ) ) ;
#12919=CARTESIAN_POINT ( 'NONE',  ( 0.8312882252666201621, 11.51171045331395959, -4.741665037663635118 ) ) ;
#12924=CARTESIAN_POINT ( 'NONE',  ( 15.94237658530999902, 1.989471272253999778, -10.01494924120000007 ) ) ;
#12925=CARTESIAN_POINT ( 'NONE',  ( 18.02254691115746255, -2.403045170833804978, -10.14401436518803656 ) ) ;
#12929=CARTESIAN_POINT ( 'NONE',  ( -12.49041039833999989, 7.040504484191000500, -5.593205555032000120 ) ) ;
#12930=CARTESIAN_POINT ( 'NONE',  ( 13.50000000000000000, -9.612102684847110723, -0.6144775398871813454 ) ) ;
#12931=VERTEX_POINT ( 'NONE', #9675 ) ;
#12932=CARTESIAN_POINT ( 'NONE',  ( 5.155714003469999973, 13.97328511022999997, 4.008150528822999270 ) ) ;
#12933=CARTESIAN_POINT ( 'NONE',  ( 20.65574852876999756, 3.825724961307999994, 10.60128487009999887 ) ) ;
#12935=ORIENTED_EDGE ( 'NONE', *, *, #10961, .T. ) ;
#12938=VECTOR ( 'NONE', #20896, 1000.000000000000000 ) ;
#12939=CARTESIAN_POINT ( 'NONE',  ( -1.956099473965003055, 11.60247837895001766, 4.451137785169001937 ) ) ;
#12941=CARTESIAN_POINT ( 'NONE',  ( -19.97157321695999954, 10.67346343640000050, 2.860045257361000015 ) ) ;
#12942=ORIENTED_EDGE ( 'NONE', *, *, #10313, .F. ) ;
#12943=CARTESIAN_POINT ( 'NONE',  ( -11.00000000000000000, -7.000000000000000000, 0.000000000000000000 ) ) ;
#12947=ADVANCED_FACE ( 'NONE', ( #16811 ), #302, .T. ) ;
#12948=CARTESIAN_POINT ( 'NONE',  ( 6.642413157096004106, 13.49915274099000229, -0.03986506147346999263 ) ) ;
#12951=CARTESIAN_POINT ( 'NONE',  ( -5.833999999999999631, 1.198997689148999791E-14, 1.310996564781999865E-13 ) ) ;
#12952=CARTESIAN_POINT ( 'NONE',  ( -14.70932910584000020, -9.048752088456000209, 0.000000000000000000 ) ) ;
#12953=CARTESIAN_POINT ( 'NONE',  ( 17.61412674930999955, -9.816082492500997958, -4.416083812485999793 ) ) ;
#12954=ORIENTED_EDGE ( 'NONE', *, *, #6458, .T. ) ;
#12955=CARTESIAN_POINT ( 'NONE',  ( -15.96111329461999695, 9.155832847151000209, -3.339520933045000195 ) ) ;
#12959=VERTEX_POINT ( 'NONE', #12943 ) ;
#12960=ADVANCED_FACE ( 'NONE', ( #5679, #217 ), #5801, .T. ) ;
#12961=CARTESIAN_POINT ( 'NONE',  ( -22.39074495098999762, 3.695816561226999752, -10.63704688588000025 ) ) ;
#12964=CARTESIAN_POINT ( 'NONE',  ( 14.78385631704689551, 9.271102238192243661, -4.553591355444472022 ) ) ;
#12966=CARTESIAN_POINT ( 'NONE',  ( 24.87166914097000259, -9.526620184668999514, 5.135842298655000526 ) ) ;
#12968=CARTESIAN_POINT ( 'NONE',  ( 13.70420460113422401, 8.535173263265548371, -2.924258408944889531 ) ) ;
#12970=CARTESIAN_POINT ( 'NONE',  ( 11.06619116165479255, 11.07450388076360248, -5.818393174638943677 ) ) ;
#12971=EDGE_LOOP ( 'NONE', ( #16619, #5814, #13273, #4030 ) ) ;
#12972=CARTESIAN_POINT ( 'NONE',  ( -14.81254764687445302, -7.118814266998854556, -5.616278725454130871 ) ) ;
#12973=B_SPLINE_CURVE_WITH_KNOTS ( 'NONE', 3,
 ( #800, #8200, #2379, #15085 ),
 .UNSPECIFIED., .F., .F.,
 ( 4, 4 ),
 ( 0.8921488906972279143, 1.000000000000000000 ),
 .UNSPECIFIED. ) ;
#12975=CARTESIAN_POINT ( 'NONE',  ( 11.97297107869919941, -13.24884602490436336, 2.052424400535947324 ) ) ;
#12977=CARTESIAN_POINT ( 'NONE',  ( 19.75000000000000000, -1.659811535170000019, 9.026773995975998943 ) ) ;
#12978=DIRECTION ( 'NONE',  ( 0.000000000000000000, 1.000000000000000000, 0.000000000000000000 ) ) ;
#12979=CARTESIAN_POINT ( 'NONE',  ( 22.06033103379666116, -7.386747355451507069, 5.676899510572770424 ) ) ;
#12980=CARTESIAN_POINT ( 'NONE',  ( 17.83974014782999973, -10.67906364485000026, -3.053789962008000014 ) ) ;
#12981=CARTESIAN_POINT ( 'NONE',  ( -23.75388191523000003, -7.467918500480999811, 11.77771164093999978 ) ) ;
#12983=ORIENTED_EDGE ( 'NONE', *, *, #16640, .F. ) ;
#12984=CARTESIAN_POINT ( 'NONE',  ( -9.901765065845999914, -2.260336335250999973, 14.69519359487999921 ) ) ;
#12985=DIRECTION ( 'NONE',  ( 1.000000000000000000, 0.000000000000000000, 0.000000000000000000 ) ) ;
#12986=CARTESIAN_POINT ( 'NONE',  ( -14.49454882815139989, -10.37180012737783308, -7.035449704340302368 ) ) ;
#12989=CARTESIAN_POINT ( 'NONE',  ( -24.27585716846455099, 9.160327548063252223, 9.133709619345506070 ) ) ;
#12990=CARTESIAN_POINT ( 'NONE',  ( 19.26430968566658919, -10.49064719816144198, -0.3961187825285560904 ) ) ;
#12992=CARTESIAN_POINT ( 'NONE',  ( 6.243179582884000212, 13.63341776306000064, 1.952383140737000033 ) ) ;
#12993=CARTESIAN_POINT ( 'NONE',  ( 16.18807664608717545, -3.132089813987705806, -9.878995028433909198 ) ) ;
#12994=CARTESIAN_POINT ( 'NONE',  ( -18.74007579025000325, 8.211845105499000042, -7.499515029571000468 ) ) ;
#12996=CARTESIAN_POINT ( 'NONE',  ( -16.00187137585000130, 9.645521962609000965, 3.562832264799999926 ) ) ;
#12999=ORIENTED_EDGE ( 'NONE', *, *, #9180, .F. ) ;
#13001=CARTESIAN_POINT ( 'NONE',  ( 21.88815861684361863, 5.936906186455843226, -8.917737836111772509 ) ) ;
#13002=LINE ( 'NONE', #14704, #9156 ) ;
#13004=CARTESIAN_POINT ( 'NONE',  ( -5.458617562394002753, 14.91827681947001771, 3.239474778739999117 ) ) ;
#13005=CIRCLE ( 'NONE', #10308, 12.89775331292476857 ) ;
#13006=AXIS2_PLACEMENT_3D ( 'NONE', #415, #2358, #18601 ) ;
#13008=CARTESIAN_POINT ( 'NONE',  ( 18.54843892131000160, -5.767951301206999837, 7.596080989717999721 ) ) ;
#13010=CARTESIAN_POINT ( 'NONE',  ( -4.246233029694164607, 15.22475462804525037, 4.414853621744755152 ) ) ;
#13011=FACE_OUTER_BOUND ( 'NONE', #9567, .T. ) ;
#13012=VERTEX_POINT ( 'NONE', #7376 ) ;
#13014=CARTESIAN_POINT ( 'NONE',  ( 22.43824770046333938, -7.394682124757493646, -5.682679906726310293 ) ) ;
#13015=CARTESIAN_POINT ( 'NONE',  ( -0.1118455922670000408, 11.62596257264000421, 4.769745589915999062 ) ) ;
#13017=CARTESIAN_POINT ( 'NONE',  ( -24.06354693424999880, -6.852501536825999828, 6.820264521660000412 ) ) ;
#13018=CARTESIAN_POINT ( 'NONE',  ( -19.21451027362000019, 9.383283592320998068, 2.951452985934999607 ) ) ;
#13020=DIRECTION ( 'NONE',  ( 0.000000000000000000, 1.000000000000000000, 0.000000000000000000 ) ) ;
#13022=VECTOR ( 'NONE', #1996, 1000.000000000000000 ) ;
#13024=EDGE_CURVE ( 'NONE', #2137, #11779, #20055, .T. ) ;
#13025=CARTESIAN_POINT ( 'NONE',  ( 0.000000000000000000, 21.50000000000000000, 0.000000000000000000 ) ) ;
#13026=VERTEX_POINT ( 'NONE', #13065 ) ;
#13027=CARTESIAN_POINT ( 'NONE',  ( -17.46812077250666562, 9.119548119916148110, -1.193619109744021412 ) ) ;
#13029=B_SPLINE_CURVE_WITH_KNOTS ( 'NONE', 3,
 ( #16307, #20192, #12336, #21776, #5300, #3601, #1187, #17789, #5075, #14143, #19840, #19728, #12690, #20081, #16422, #17906, #21662, #6872, #12457, #8939, #8698 ),
 .UNSPECIFIED., .F., .F.,
 ( 4, 2, 2, 2, 2, 2, 2, 2, 2, 1, 4 ),
 ( 0.000000000000000000, 0.1250000000000000833, 0.2500000000000001110, 0.3750000000000001110, 0.5000000000000001110, 0.5625000000000001110, 0.6250000000000002220, 0.7500000000000001110, 0.8125000000000001110, 0.8750000000000000000, 1.000000000000000000 ),
 .UNSPECIFIED. ) ;
#13031=CARTESIAN_POINT ( 'NONE',  ( -23.80388666801320596, 10.58805584965292645, -0.3166584334353429453 ) ) ;
#13035=CARTESIAN_POINT ( 'NONE',  ( 3.749887601161898232, 12.07028453061897544, 3.051358318113421397 ) ) ;
#13037=CARTESIAN_POINT ( 'NONE',  ( 0.3785172659374461679, 11.48892188479672072, -4.796579582458316615 ) ) ;
#13044=CARTESIAN_POINT ( 'NONE',  ( 13.41956408531000022, -7.835164430201999153, 6.443409769539999665 ) ) ;
#13045=CARTESIAN_POINT ( 'NONE',  ( 17.73336492619503701, -9.837232967517808291, -3.444572193406692850 ) ) ;
#13054=CARTESIAN_POINT ( 'NONE',  ( 20.92705310096999582, 3.648664467165000147, 10.11050619795000038 ) ) ;
#13055=EDGE_CURVE ( 'NONE', #12531, #6719, #23931, .T. ) ;
#13058=ORIENTED_EDGE ( 'NONE', *, *, #18997, .F. ) ;
#13059=CARTESIAN_POINT ( 'NONE',  ( 24.50000000000000000, -3.407821508741362138, 10.10044300661528460 ) ) ;
#13060=DIRECTION ( 'NONE',  ( 0.000000000000000000, 1.000000000000000000, 0.000000000000000000 ) ) ;
#13061=CARTESIAN_POINT ( 'NONE',  ( 2.943303094549000853, 11.81758645637001415, 3.952898282072999425 ) ) ;
#13063=CARTESIAN_POINT ( 'NONE',  ( 12.50448585038000004, 13.93375672974000068, -0.4329886192124000055 ) ) ;
#13065=CARTESIAN_POINT ( 'NONE',  ( -23.74465998031000069, 7.716878364870000340, 11.63397459621999985 ) ) ;
#13069=EDGE_CURVE ( 'NONE', #1109, #11394, #13775, .T. ) ;
#13070=CARTESIAN_POINT ( 'NONE',  ( 16.08924770046332853, 7.264394122832348977, 5.582553128935895614 ) ) ;
#13078=CARTESIAN_POINT ( 'NONE',  ( -14.25243324638999809, 6.216878364870000340, 12.50000000000000000 ) ) ;
#13079=ORIENTED_EDGE ( 'NONE', *, *, #10881, .F. ) ;
#13080=CARTESIAN_POINT ( 'NONE',  ( -22.90484515781000141, -11.18753571154999982, -1.400055669627999988 ) ) ;
#13082=CARTESIAN_POINT ( 'NONE',  ( 4.829987487923999900, 14.79876397742000016, -3.766541047082999860 ) ) ;
#13084=CARTESIAN_POINT ( 'NONE',  ( -18.14247087121333735, 1.196138244234068893, -9.136853272523239866 ) ) ;
#13085=CARTESIAN_POINT ( 'NONE',  ( 19.50029330511999959, -8.080914015124001537, -7.722743123546000454 ) ) ;
#13086=EDGE_CURVE ( 'NONE', #21017, #4023, #19489, .T. ) ;
#13088=CARTESIAN_POINT ( 'NONE',  ( 14.17388432423843980, 2.487224340016167545, 8.704718658459677627 ) ) ;
#13090=DIRECTION ( 'NONE',  ( 0.000000000000000000, -1.000000000000000000, 0.000000000000000000 ) ) ;
#13091=VECTOR ( 'NONE', #939, 1000.000000000000114 ) ;
#13093=CARTESIAN_POINT ( 'NONE',  ( 11.36701043059670013, 9.445581393796846470, -8.639701956129112403 ) ) ;
#13095=CARTESIAN_POINT ( 'NONE',  ( 11.90008533511401012, -13.14613689767216620, 2.230302227742338328 ) ) ;
#13097=AXIS2_PLACEMENT_3D ( 'NONE', #20453, #5218, #3741 ) ;
#13099=ADVANCED_FACE ( 'NONE', ( #4834 ), #3073, .F. ) ;
#13103=CARTESIAN_POINT ( 'NONE',  ( 13.72319879834999945, -6.784451854297000040, 8.651728039901000145 ) ) ;
#13106=CLOSED_SHELL ( 'NONE', ( #322, #23403, #4008, #23108 ) ) ;
#13107=VERTEX_POINT ( 'NONE', #23221 ) ;
#13109=CARTESIAN_POINT ( 'NONE',  ( -11.31990613876999952, -14.73339388177000231, 3.811521877444000062 ) ) ;
#13111=CARTESIAN_POINT ( 'NONE',  ( 16.80728936713000365, -9.102589883624000677, 0.000000000000000000 ) ) ;
#13114=CARTESIAN_POINT ( 'NONE',  ( -14.45529025083970964, 9.532921455391518251, 8.488438081448235195 ) ) ;
#13115=CARTESIAN_POINT ( 'NONE',  ( 19.17606592695706169, -10.11566850997402156, 2.778547194757770455 ) ) ;
#13117=CARTESIAN_POINT ( 'NONE',  ( 16.13030374810696443, -5.090882584321414939, -9.031255120879867704 ) ) ;
#13118=CARTESIAN_POINT ( 'NONE',  ( -13.89620800253999988, -10.81410884553999985, 1.946053687578000124 ) ) ;
#13123=CARTESIAN_POINT ( 'NONE',  ( -12.86025400554999898, 8.992670415662999517, -4.704867779684000162 ) ) ;
#13126=B_SPLINE_CURVE_WITH_KNOTS ( 'NONE', 3,
 ( #5015, #12400, #8396, #21350, #19661, #10694, #15762, #23522, #19785, #5245, #23271, #12512, #23152, #14078, #3194, #1490, #6685, #19540, #21472, #6573 ),
 .UNSPECIFIED., .F., .F.,
 ( 4, 2, 2, 2, 2, 2, 2, 2, 2, 4 ),
 ( 0.2677099386182879570, 0.3592461962910020179, 0.4507824539637160788, 0.5423187116364300842, 0.6338549693091439785, 0.7253912269818580949, 0.7711593558182151531, 0.8169274846545721003, 0.9084637423272861056, 1.000000000000000000 ),
 .UNSPECIFIED. ) ;
#13128=CARTESIAN_POINT ( 'NONE',  ( 21.49093124556538470, -7.629915688256811102, -7.503604758355795212 ) ) ;
#13129=CARTESIAN_POINT ( 'NONE',  ( -19.32479587693500989, -9.395654797978956196, -4.657724768059325449 ) ) ;
#13130=AXIS2_PLACEMENT_3D ( 'NONE', #9145, #18125, #12668 ) ;
#13133=ADVANCED_FACE ( 'NONE', ( #15588 ), #19288, .T. ) ;
#13134=CARTESIAN_POINT ( 'NONE',  ( -13.99999999999999645, -10.04553844607464264, 2.270358494041115449 ) ) ;
#13135=AXIS2_PLACEMENT_3D ( 'NONE', #11838, #18737, #17282 ) ;
#13136=CARTESIAN_POINT ( 'NONE',  ( 18.21937642130999890, 4.597142045420999246, 8.611084490720001483 ) ) ;
#13138=CARTESIAN_POINT ( 'NONE',  ( -14.25546272797000036, 7.467346636043999730, -11.77804180703000014 ) ) ;
#13140=ORIENTED_EDGE ( 'NONE', *, *, #15763, .F. ) ;
#13141=DIRECTION ( 'NONE',  ( -1.000000000000000000, 0.000000000000000000, 0.000000000000000000 ) ) ;
#13142=CARTESIAN_POINT ( 'NONE',  ( -4.814347747396997335, 12.64342941097000939, -0.06095846195990003991 ) ) ;
#13143=AXIS2_PLACEMENT_3D ( 'NONE', #14046, #21439, #4852 ) ;
#13144=CARTESIAN_POINT ( 'NONE',  ( 12.00000000000000000, 4.372713938407501111, -7.949045871140958397 ) ) ;
#13145=CARTESIAN_POINT ( 'NONE',  ( 18.69687270046333083, -8.912950770672923184, -2.395158628008459800 ) ) ;
#13148=CARTESIAN_POINT ( 'NONE',  ( 5.278705197451656339, 13.81926695668341942, -4.223825586974010449 ) ) ;
#13151=ORIENTED_EDGE ( 'NONE', *, *, #3639, .T. ) ;
#13152=CARTESIAN_POINT ( 'NONE',  ( -17.58149577250666695, 7.971127812682293090, -4.594125483385558262 ) ) ;
#13153=CARTESIAN_POINT ( 'NONE',  ( 24.23273247979999923, -6.599590995379000624, -6.390628695050000196 ) ) ;
#13154=CARTESIAN_POINT ( 'NONE',  ( 14.58901083706679991, -1.542589092830730646, 8.966384590779057362 ) ) ;
#13155=PLANE ( 'NONE',  #18863 ) ;
#13156=CARTESIAN_POINT ( 'NONE',  ( -22.92026629233681234, -10.50598538670077176, 1.170518972298471239 ) ) ;
#13158=DIRECTION ( 'NONE',  ( 0.9999999999999941158, 7.061425694895919264E-12, -1.088544838354987623E-07 ) ) ;
#13160=CARTESIAN_POINT ( 'NONE',  ( 0.6509447386268639724, 11.50075708578391698, -4.768141952204850043 ) ) ;
#13163=VERTEX_POINT ( 'NONE', #11733 ) ;
#13165=FACE_OUTER_BOUND ( 'NONE', #2281, .T. ) ;
#13166=CARTESIAN_POINT ( 'NONE',  ( 13.63893908531000143, -10.12407100975999974, -0.7263252697377000633 ) ) ;
#13167=CARTESIAN_POINT ( 'NONE',  ( -19.28553974680000138, -2.542569097918999876, -10.60900310786000134 ) ) ;
#13169=CARTESIAN_POINT ( 'NONE',  ( 17.35926537306000128, 1.492411638035999966, 10.76125290731000028 ) ) ;
#13173=CARTESIAN_POINT ( 'NONE',  ( 22.07214134601000310, 11.17751647723999930, -1.720558685957000122 ) ) ;
#13174=CARTESIAN_POINT ( 'NONE',  ( -14.09989322724901051, 9.032303263851988007, 3.309274488355915889E-05 ) ) ;
#13177=DIRECTION ( 'NONE',  ( 0.000000000000000000, -1.000000000000000000, -4.004361744935000256E-13 ) ) ;
#13179=CARTESIAN_POINT ( 'NONE',  ( 4.447198537830002074, 12.27562294272000720, 1.915162380135998044 ) ) ;
#13181=CARTESIAN_POINT ( 'NONE',  ( -23.62697027523000060, 8.705873425905000573, 6.965082319091999707 ) ) ;
#13186=CARTESIAN_POINT ( 'NONE',  ( 6.269600329294999774, 13.58666533272000088, 2.205063801677000335 ) ) ;
#13188=CARTESIAN_POINT ( 'NONE',  ( 16.73170603379667298, -8.863736118548766640, 2.382193237844414835 ) ) ;
#13191=CARTESIAN_POINT ( 'NONE',  ( 14.21381424931000126, -3.754242569768000415, -9.992333729823998922 ) ) ;
#13193=CARTESIAN_POINT ( 'NONE',  ( -14.01132597738000030, -2.550904266876999671, 10.45586863968000024 ) ) ;
#13195=CARTESIAN_POINT ( 'NONE',  ( -14.45960645816968082, -2.455948252940329812, 12.49996645506771920 ) ) ;
#13197=CARTESIAN_POINT ( 'NONE',  ( -22.04801147977000042, 11.23783126569999880, -0.5540781968215000575 ) ) ;
#13199=CARTESIAN_POINT ( 'NONE',  ( 14.20401836875051060, -8.028458463233919318, -6.472791156920650657 ) ) ;
#13201=CARTESIAN_POINT ( 'NONE',  ( 24.93285146195000124, -10.16030646464000142, 2.983129374812000023 ) ) ;
#13203=EDGE_CURVE ( 'NONE', #11791, #20267, #316, .T. ) ;
#13204=CARTESIAN_POINT ( 'NONE',  ( 14.36820406744966760, -3.431467036491389511, 8.367050089429785231 ) ) ;
#13205=CARTESIAN_POINT ( 'NONE',  ( 16.98472650148946883, 0.04247749959640340772, 10.43385324419452509 ) ) ;
#13207=CARTESIAN_POINT ( 'NONE',  ( -6.838539683285000059, 15.31903379280000088, 1.878299112549000061 ) ) ;
#13208=CARTESIAN_POINT ( 'NONE',  ( 18.97939153144000102, -4.829087144285000299, 10.28159918154000074 ) ) ;
#13209=ORIENTED_EDGE ( 'NONE', *, *, #7834, .F. ) ;
#13215=CARTESIAN_POINT ( 'NONE',  ( -14.00000000000000000, 9.030549305586312414, 0.000000000000000000 ) ) ;
#13216=CARTESIAN_POINT ( 'NONE',  ( 14.65928258853999999, 10.53691696905000086, -3.227074023763999655 ) ) ;
#13217=LINE ( 'NONE', #20611, #10220 ) ;
#13218=EDGE_CURVE ( 'NONE', #21240, #19135, #21175, .T. ) ;
#13221=ORIENTED_EDGE ( 'NONE', *, *, #23927, .T. ) ;
#13222=CARTESIAN_POINT ( 'NONE',  ( -13.99999999999999645, 4.101844789563358518, -8.303384789743008199 ) ) ;
#13224=CARTESIAN_POINT ( 'NONE',  ( -12.22893471169000001, 15.49542151714999960, -1.510114813732999828 ) ) ;
#13226=CARTESIAN_POINT ( 'NONE',  ( 18.13595603379667054, 1.025616415363163503, 9.176462519624685399 ) ) ;
#13229=CARTESIAN_POINT ( 'NONE',  ( 21.03995603379664914, 4.638822124460471485, -8.048677146799199988 ) ) ;
#13231=CARTESIAN_POINT ( 'NONE',  ( 15.49672992670417848, -4.362109857448412065, 9.420198599912847470 ) ) ;
#13232=CARTESIAN_POINT ( 'NONE',  ( -16.09820950105999771, 4.896146317806000070, 9.904571738106000112 ) ) ;
#13235=CIRCLE ( 'NONE', #4352, 4.750000000000000000 ) ;
#13236=CARTESIAN_POINT ( 'NONE',  ( -18.52095171394000062, 10.52702611403999988, -4.436598560839000172 ) ) ;
#13240=CARTESIAN_POINT ( 'NONE',  ( -11.04281598264000053, 1.359882291614000008E-14, 0.000000000000000000 ) ) ;
#13241=CARTESIAN_POINT ( 'NONE',  ( -18.80389074766395652, 6.775504899648727708, -8.189869853558933599 ) ) ;
#13242=EDGE_LOOP ( 'NONE', ( #10227, #5640, #16949, #2807 ) ) ;
#13243=CARTESIAN_POINT ( 'NONE',  ( 8.124934037954998800, 1.125145054518999965E-14, 0.000000000000000000 ) ) ;
#13244=CARTESIAN_POINT ( 'NONE',  ( -4.988174690688001789, 14.11622277100999234, 4.390520985612999638 ) ) ;
#13245=CARTESIAN_POINT ( 'NONE',  ( -13.99999999999999822, -9.985610030060415809, 2.514921185572130735 ) ) ;
#13247=CARTESIAN_POINT ( 'NONE',  ( 18.10968892130999919, 7.460570333748000493, 6.290326521484000288 ) ) ;
#13251=CARTESIAN_POINT ( 'NONE',  ( -6.018858921593000844, 16.12697589426997880, -0.9718497405647000820 ) ) ;
#13255=CARTESIAN_POINT ( 'NONE',  ( 23.15628936713000030, 9.265517736846000219, 0.000000000000000000 ) ) ;
#13256=CARTESIAN_POINT ( 'NONE',  ( -0.1133183553920999731, 11.65492397528000978, 4.844731806490002235 ) ) ;
#13257=CARTESIAN_POINT ( 'NONE',  ( 12.00000000000000000, -0.6870795729671005381, -9.379734039196923945 ) ) ;
#13258=CARTESIAN_POINT ( 'NONE',  ( 18.88583103379665928, -5.626836121677762925, -7.321603354489151450 ) ) ;
#13263=CARTESIAN_POINT ( 'NONE',  ( 23.99062354302999722, -6.216878364870000340, 12.50000000000000000 ) ) ;
#13265=VERTEX_POINT ( 'NONE', #11237 ) ;
#13266=CARTESIAN_POINT ( 'NONE',  ( 23.31903954243999877, 10.35114991066999934, -1.095165573133999981 ) ) ;
#13267=CARTESIAN_POINT ( 'NONE',  ( 3.328927207363430174, 13.17665712429451652, -5.891523500073148512 ) ) ;
#13269=DIRECTION ( 'NONE',  ( 1.000000000000000000, 5.653314293126999632E-09, -4.083276203493999756E-09 ) ) ;
#13270=CARTESIAN_POINT ( 'NONE',  ( -23.34868829266476808, 0.2602095544171842967, 10.57497587573962861 ) ) ;
#13272=DIRECTION ( 'NONE',  ( -1.000000000000000000, 0.000000000000000000, 0.000000000000000000 ) ) ;
#13273=ORIENTED_EDGE ( 'NONE', *, *, #20978, .F. ) ;
#13274=CARTESIAN_POINT ( 'NONE',  ( -18.82872164579986674, -0.8013280645230316246, -10.43343868322613943 ) ) ;
#13275=DIRECTION ( 'NONE',  ( -1.000000000000000000, 0.000000000000000000, 0.000000000000000000 ) ) ;
#13279=CARTESIAN_POINT ( 'NONE',  ( 15.31068924931000019, -3.145391809039999931, 10.23054077443999965 ) ) ;
#13281=LINE ( 'NONE', #15090, #18911 ) ;
#13282=CARTESIAN_POINT ( 'NONE',  ( 15.46296080085999947, -5.609029392994999696, 9.868489697990998621 ) ) ;
#13284=DIRECTION ( 'NONE',  ( -1.000000000000000000, 0.000000000000000000, 0.000000000000000000 ) ) ;
#13285=CARTESIAN_POINT ( 'NONE',  ( 19.21557844680999949, -0.06227916920583000115, 10.25955241042999866 ) ) ;
#13290=DIRECTION ( 'NONE',  ( -1.000000000000000000, 0.000000000000000000, 0.000000000000000000 ) ) ;
#13291=CARTESIAN_POINT ( 'NONE',  ( -3.628081332548001026, 12.07241784922001315, 3.129844478951998799 ) ) ;
#13293=CARTESIAN_POINT ( 'NONE',  ( -23.43942278056000106, -2.880430617476999799, 10.76542036194000040 ) ) ;
#13294=ORIENTED_EDGE ( 'NONE', *, *, #5542, .F. ) ;
#13298=CARTESIAN_POINT ( 'NONE',  ( -20.01879387067656424, -9.049182457752882769, 3.224885811638896982 ) ) ;
#13300=DIRECTION ( 'NONE',  ( 0.000000000000000000, 1.000000000000000000, 0.000000000000000000 ) ) ;
#13302=CARTESIAN_POINT ( 'NONE',  ( 16.29787674931000296, 5.844090361140000134, -8.997790218903000792 ) ) ;
#13304=AXIS2_PLACEMENT_3D ( 'NONE', #12048, #6702, #21367 ) ;
#13305=CARTESIAN_POINT ( 'NONE',  ( -15.63636876114000351, -8.424167882059999002, 6.770715351507000435 ) ) ;
#13307=CARTESIAN_POINT ( 'NONE',  ( 23.99062354302999722, 13.93375672974000068, -0.8660254037843999608 ) ) ;
#13308=VERTEX_POINT ( 'NONE', #20995 ) ;
#13309=DIRECTION ( 'NONE',  ( 0.000000000000000000, 1.000000000000000000, 0.000000000000000000 ) ) ;
#13311=CARTESIAN_POINT ( 'NONE',  ( 13.58082059198365776, -0.8793308655295314358, 10.28020606850954088 ) ) ;
#13313=CARTESIAN_POINT ( 'NONE',  ( -3.167057169673002104, 13.68010474867000603, -5.212571554903001392 ) ) ;
#13314=CARTESIAN_POINT ( 'NONE',  ( 19.79353649888999911, -8.086732793196000912, -7.728305058073000389 ) ) ;
#13316=CARTESIAN_POINT ( 'NONE',  ( 14.40372725440316870, -4.444427729678738892, 7.873048769373896860 ) ) ;
#13317=CARTESIAN_POINT ( 'NONE',  ( -14.00000000000000000, 6.995278287856000254, -5.711120943918999160 ) ) ;
#13322=ORIENTED_EDGE ( 'NONE', *, *, #5853, .T. ) ;
#13324=ORIENTED_EDGE ( 'NONE', *, *, #11094, .T. ) ;
#13328=VERTEX_POINT ( 'NONE', #4405 ) ;
#13329=AXIS2_PLACEMENT_3D ( 'NONE', #3543, #7274, #12742 ) ;
#13330=CARTESIAN_POINT ( 'NONE',  ( 15.20063528206999948, -0.07838933043231000042, 11.03455842080999894 ) ) ;
#13331=CARTESIAN_POINT ( 'NONE',  ( -6.133957692552824525, 15.94870493351765006, 1.066878949731052684 ) ) ;
#13335=ORIENTED_EDGE ( 'NONE', *, *, #11768, .F. ) ;
#13336=CARTESIAN_POINT ( 'NONE',  ( -13.99999999999999645, 3.801362129166840909, -8.462681129871283403 ) ) ;
#13337=CARTESIAN_POINT ( 'NONE',  ( -12.02528971169000016, 11.32897754936000112, 10.67910005269999907 ) ) ;
#13339=PLANE ( 'NONE',  #17148 ) ;
#13341=CARTESIAN_POINT ( 'NONE',  ( -14.38789236265103177, 12.88903867674593684, 2.675117728956161400 ) ) ;
#13342=CARTESIAN_POINT ( 'NONE',  ( 6.165272352932655409, 14.04219028581453443, 0.4745907567973399188 ) ) ;
#13343=CARTESIAN_POINT ( 'NONE',  ( 15.63618592470433022, -8.281329406721820163, 6.227711793688024855 ) ) ;
#13344=CARTESIAN_POINT ( 'NONE',  ( -14.83356629584000075, 7.743367107227999924, -7.832546484073001025 ) ) ;
#13347=CARTESIAN_POINT ( 'NONE',  ( -14.78308928803000022, -1.400056168502999965, -10.15245659134999912 ) ) ;
#13351=CARTESIAN_POINT ( 'NONE',  ( -18.45662066148324953, 9.913592205210392194, 3.361782804926630064 ) ) ;
#13352=ORIENTED_EDGE ( 'NONE', *, *, #18437, .T. ) ;
#13353=CARTESIAN_POINT ( 'NONE',  ( -5.483104808914001538, 16.58388603771001613, 3.024255283996999832 ) ) ;
#13354=FACE_OUTER_BOUND ( 'NONE', #17712, .T. ) ;
#13357=CARTESIAN_POINT ( 'NONE',  ( 17.34187642131000118, -3.686089773936000125, -9.013740861256998471 ) ) ;
#13359=CONICAL_SURFACE ( 'NONE', #3715, 13.23032192316000000, 1.093540295016705466 ) ;
#13362=VERTEX_POINT ( 'NONE', #20198 ) ;
#13363=CARTESIAN_POINT ( 'NONE',  ( -12.50000000000000000, 6.668552375895999695, -6.032891668653000750 ) ) ;
#13364=B_SPLINE_CURVE_WITH_KNOTS ( 'NONE', 3,
 ( #2594, #4669, #17497, #9986, #15297, #8293, #22688, #15541, #22929, #6346, #2967, #12421, #12053, #6707, #23177, #1388, #3219, #14225, #8545, #6595, #6956, #10357, #23545, #6832, #21370, #12172, #13979, #14099, #21738, #21494, #10601, #4787, #5151, #19562, #1268, #1150, #8418, #17746, #19438, #8655, #2848, #8781 ),
 .UNSPECIFIED., .F., .F.,
 ( 4, 2, 1, 2, 2, 2, 1, 2, 2, 2, 2, 2, 2, 2, 2, 1, 2, 2, 2, 1, 2, 2, 4 ),
 ( 0.000000000000000000, 0.06250000000000038858, 0.09375000000000058287, 0.1093750000000009159, 0.1250000000000012490, 0.1875000000000026090, 0.2187500000000032752, 0.2343750000000035805, 0.2500000000000038303, 0.3125000000000036082, 0.3750000000000033862, 0.5000000000000028866, 0.5625000000000024425, 0.6250000000000021094, 0.6875000000000016653, 0.7187500000000014433, 0.7343750000000013323, 0.7500000000000012212, 0.8125000000000003331, 0.8437500000000000000, 0.8593749999999998890, 0.8749999999999997780, 1.000000000000000000 ),
 .UNSPECIFIED. ) ;
#13365=CARTESIAN_POINT ( 'NONE',  ( 21.54929166666666163, -1.207328351017986412, 9.224279008625865472 ) ) ;
#13366=CARTESIAN_POINT ( 'NONE',  ( 4.570970069156997440, 12.55112336938002038, 1.530869126733999108 ) ) ;
#13367=CARTESIAN_POINT ( 'NONE',  ( -13.99999999999999822, -2.102368047938235840, 9.650932645709392688 ) ) ;
#13369=CARTESIAN_POINT ( 'NONE',  ( 12.00000000000000000, -4.187907907339877944, -8.648131877027614323 ) ) ;
#13370=CARTESIAN_POINT ( 'NONE',  ( 19.15037270046332196, 2.398204772357335646, -8.924285576194829872 ) ) ;
#13371=CARTESIAN_POINT ( 'NONE',  ( -6.215630469039999717, 16.31160401236000368, -1.000000000001000089 ) ) ;
#13372=CARTESIAN_POINT ( 'NONE',  ( 5.607894170315999460, 13.81677657626999967, 3.376581585463999780 ) ) ;
#13373=CARTESIAN_POINT ( 'NONE',  ( 5.290861247900399356, 13.79131577112301876, -4.285521124256567838 ) ) ;
#13375=EDGE_CURVE ( 'NONE', #18008, #3010, #17750, .T. ) ;
#13379=CARTESIAN_POINT ( 'NONE',  ( 21.33396847639999905, 9.703104815872000799, 1.500914832134000010 ) ) ;
#13380=CARTESIAN_POINT ( 'NONE',  ( -1.476145454422083558, 12.87712156297896371, -6.520379654891271137 ) ) ;
#13381=AXIS2_PLACEMENT_3D ( 'NONE', #18700, #9498, #22452 ) ;
#13383=AXIS2_PLACEMENT_3D ( 'NONE', #17627, #17752, #15548 ) ;
#13384=CARTESIAN_POINT ( 'NONE',  ( -23.58967566784923164, 8.020275622323017828, 6.913969526970511481 ) ) ;
#13387=ORIENTED_EDGE ( 'NONE', *, *, #11058, .T. ) ;
#13388=CARTESIAN_POINT ( 'NONE',  ( -18.80081040857043462, 0.2165797905031099924, -10.46343287096509833 ) ) ;
#13390=CARTESIAN_POINT ( 'NONE',  ( 24.50000000000000000, 10.82531754731000007, 6.250000000000000000 ) ) ;
#13391=AXIS2_PLACEMENT_3D ( 'NONE', #11205, #21980, #7429 ) ;
#13392=EDGE_CURVE ( 'NONE', #13265, #8938, #9031, .T. ) ;
#13395=ORIENTED_EDGE ( 'NONE', *, *, #19013, .F. ) ;
#13398=CARTESIAN_POINT ( 'NONE',  ( 13.88475174931000033, -10.63832449705000016, -0.7632376485559000390 ) ) ;
#13399=CARTESIAN_POINT ( 'NONE',  ( -13.93810026219000164, -11.26370332044000122, -0.8539229629768000374 ) ) ;
#13400=CARTESIAN_POINT ( 'NONE',  ( -10.04281598263999875, 16.40330333352000025, 0.9999999999983999466 ) ) ;
#13401=CARTESIAN_POINT ( 'NONE',  ( 15.12489037305999950, 10.79910518316000001, -0.2491780114572999805 ) ) ;
#13403=DIRECTION ( 'NONE',  ( 1.000000000000000000, 0.000000000000000000, 0.000000000000000000 ) ) ;
#13404=CARTESIAN_POINT ( 'NONE',  ( 24.56229061411000458, 9.827592947978999405, 3.145925499939000503 ) ) ;
#13408=LINE ( 'NONE', #4335, #1886 ) ;
#13410=CARTESIAN_POINT ( 'NONE',  ( -4.833442993138002741, 12.42174073273999646, -0.1521763619671000767 ) ) ;
#13412=CARTESIAN_POINT ( 'NONE',  ( 24.29519417982890772, -9.695549469153794675, -1.137487036544780006 ) ) ;
#13413=CARTESIAN_POINT ( 'NONE',  ( -21.78904027164999846, 8.063099807893998161, 7.627676736206999486 ) ) ;
#13414=VERTEX_POINT ( 'NONE', #20263 ) ;
#13416=DIRECTION ( 'NONE',  ( -1.000000000000000000, 0.000000000000000000, 0.000000000000000000 ) ) ;
#13417=ORIENTED_EDGE ( 'NONE', *, *, #8194, .F. ) ;
#13418=CARTESIAN_POINT ( 'NONE',  ( -23.97728971656852082, 5.151501960897337362, -12.49974207332436116 ) ) ;
#13421=ADVANCED_FACE ( 'NONE', ( #20148 ), #1848, .T. ) ;
#13422=CARTESIAN_POINT ( 'NONE',  ( -2.932110437813000292, 12.98378357228998681, 6.429187290204003702 ) ) ;
#13424=CARTESIAN_POINT ( 'NONE',  ( 15.31068924931000019, -3.145391809039999931, 10.23054077443999965 ) ) ;
#13425=CARTESIAN_POINT ( 'NONE',  ( -12.86025400554999898, 8.992670415662999517, -4.704867779684000162 ) ) ;
#13426=CARTESIAN_POINT ( 'NONE',  ( 14.02481375730999957, 9.137735611494999688, -0.2793723515763000265 ) ) ;
#13427=CARTESIAN_POINT ( 'NONE',  ( 24.35625626386761056, 12.44383109334005866, -3.446652305529492200 ) ) ;
#13432=CARTESIAN_POINT ( 'NONE',  ( 13.59953730933185589, -1.556863950183797751, 10.19646127995974361 ) ) ;
#13434=CARTESIAN_POINT ( 'NONE',  ( 1.774480129771998538, 13.34308553469999659, -5.838396592341002389 ) ) ;
#13435=CARTESIAN_POINT ( 'NONE',  ( -24.50000000000000000, 14.43375672974000068, 0.000000000000000000 ) ) ;
#13437=CARTESIAN_POINT ( 'NONE',  ( 11.12576011242912699, 1.246535810083129636, 12.50000754954551141 ) ) ;
#13441=CARTESIAN_POINT ( 'NONE',  ( 24.37173283531061330, -12.35285683711744653, -3.604224339486718609 ) ) ;
#13444=AXIS2_PLACEMENT_3D ( 'NONE', #6498, #10253, #2751 ) ;
#13445=ORIENTED_EDGE ( 'NONE', *, *, #22210, .T. ) ;
#13447=CARTESIAN_POINT ( 'NONE',  ( -5.833999999999999631, 1.198997689148999791E-14, 1.310996564781999865E-13 ) ) ;
#13450=CARTESIAN_POINT ( 'NONE',  ( 24.06553262398158921, -9.296743367502696032, 1.372136975361484268 ) ) ;
#13453=AXIS2_PLACEMENT_3D ( 'NONE', #4612, #13798, #14050 ) ;
#13456=ORIENTED_EDGE ( 'NONE', *, *, #18250, .T. ) ;
#13457=CARTESIAN_POINT ( 'NONE',  ( -14.00000000000000355, 0.5659072664207758230, -9.465469235123730840 ) ) ;
#13458=FACE_OUTER_BOUND ( 'NONE', #18515, .T. ) ;
#13459=CARTESIAN_POINT ( 'NONE',  ( -23.74465998031000069, -7.716878364870000340, -11.63397459621999985 ) ) ;
#13460=EDGE_CURVE ( 'NONE', #14183, #10512, #16962, .T. ) ;
#13461=EDGE_LOOP ( 'NONE', ( #9401, #5567, #17005, #29 ) ) ;
#13462=CARTESIAN_POINT ( 'NONE',  ( -18.63160066766000256, -9.081568620942999104, 1.581064911138999829 ) ) ;
#13463=CARTESIAN_POINT ( 'NONE',  ( -14.43045961913871622, 12.44097983993677659, 3.451577511309273039 ) ) ;
#13465=CARTESIAN_POINT ( 'NONE',  ( 15.75487062095969470, -10.05329925375477806, 2.473809878897430092 ) ) ;
#13467=CARTESIAN_POINT ( 'NONE',  ( -15.66879943471000125, -9.824257856382001108, -5.029609084265999286 ) ) ;
#13470=CARTESIAN_POINT ( 'NONE',  ( -17.30216962611999776, -8.848728181206000798, -7.171245711509000920 ) ) ;
#13471=AXIS2_PLACEMENT_3D ( 'NONE', #9051, #7107, #18259 ) ;
#13472=EDGE_CURVE ( 'NONE', #22434, #17213, #10752, .T. ) ;
#13479=ORIENTED_EDGE ( 'NONE', *, *, #987, .F. ) ;
#13480=CARTESIAN_POINT ( 'NONE',  ( -3.317497142792999121, 13.45106591520001160, 5.148782710378998040 ) ) ;
#13481=AXIS2_PLACEMENT_3D ( 'NONE', #822, #22976, #15348 ) ;
#13482=CARTESIAN_POINT ( 'NONE',  ( 15.03843892131000004, -8.433581200277000534, 4.746982932527000543 ) ) ;
#13483=ORIENTED_EDGE ( 'NONE', *, *, #15743, .T. ) ;
#13487=EDGE_CURVE ( 'NONE', #4084, #5502, #23540, .T. ) ;
#13490=CARTESIAN_POINT ( 'NONE',  ( 21.77604166666666075, -7.380913445605565393, 5.672416130782132804 ) ) ;
#13491=CARTESIAN_POINT ( 'NONE',  ( -4.447536355888999537, 12.50584014757999185, 1.859842023822999568 ) ) ;
#13492=CARTESIAN_POINT ( 'NONE',  ( -12.49618567022092641, 6.982953552602237046, -5.700977629478201969 ) ) ;
#13494=CARTESIAN_POINT ( 'NONE',  ( 17.86344468463383350, -7.381542623598233099, -7.407332015522091417 ) ) ;
#13495=CARTESIAN_POINT ( 'NONE',  ( 23.99062354302999722, 6.216878364870000340, -12.50000000000000000 ) ) ;
#13496=CARTESIAN_POINT ( 'NONE',  ( -21.35476253787999923, 9.219287007783998789, 0.000000000000000000 ) ) ;
#13497=CARTESIAN_POINT ( 'NONE',  ( -4.820916185790466102, 13.26632684913112037, 5.688929395781997300 ) ) ;
#13499=CARTESIAN_POINT ( 'NONE',  ( -14.00000000000000000, 1.396097351027999937E-14, 0.000000000000000000 ) ) ;
#13503=ADVANCED_FACE ( 'NONE', ( #14340, #8896 ), #23534, .T. ) ;
#13505=ORIENTED_EDGE ( 'NONE', *, *, #14246, .F. ) ;
#13506=CARTESIAN_POINT ( 'NONE',  ( 22.94668360559225562, 9.017902059207619558, 2.425039471787421075 ) ) ;
#13507=CARTESIAN_POINT ( 'NONE',  ( 3.536817740288733525, 13.22384477141398129, -5.784969809341429681 ) ) ;
#13513=ORIENTED_EDGE ( 'NONE', *, *, #8054, .T. ) ;
#13515=CARTESIAN_POINT ( 'NONE',  ( -17.40524854711295433, -10.32373598890054467, -1.469896786939441924 ) ) ;
#13516=CARTESIAN_POINT ( 'NONE',  ( 0.000000000000000000, 22.00000000000000000, 0.000000000000000000 ) ) ;
#13518=ORIENTED_EDGE ( 'NONE', *, *, #21552, .F. ) ;
#13522=CARTESIAN_POINT ( 'NONE',  ( 17.67649770046333657, 9.124895482576970807, -1.194572973190361820 ) ) ;
#13523=CARTESIAN_POINT ( 'NONE',  ( 16.18818924931000325, 2.089945795291999975, -10.52064088945999920 ) ) ;
#13524=CARTESIAN_POINT ( 'NONE',  ( -19.48867009477000067, -8.807317413567998798, -6.448376625637000537 ) ) ;
#13525=CARTESIAN_POINT ( 'NONE',  ( 23.81455253808871930, -9.280040243854974946, -1.185412662895561242 ) ) ;
#13526=CARTESIAN_POINT ( 'NONE',  ( 13.09364037305999950, 7.670935586994999333, -7.523170208358000544 ) ) ;
#13527=CARTESIAN_POINT ( 'NONE',  ( 13.50000000000000178, -7.987118333487818411, -4.877847799884814428 ) ) ;
#13529=CARTESIAN_POINT ( 'NONE',  ( 21.90655408178999863, -8.810107392619000777, -5.231571157656000004 ) ) ;
#13533=CARTESIAN_POINT ( 'NONE',  ( 12.40372306987999984, 5.542563168401000162, -7.077615733026999756 ) ) ;
#13535=CIRCLE ( 'NONE', #13922, 0.9999999999999992228 ) ;
#13536=CARTESIAN_POINT ( 'NONE',  ( -4.723119614623001894, 12.53615931869001621, -0.05929000460447006460 ) ) ;
#13537=LINE ( 'NONE', #15219, #5369 ) ;
#13538=CARTESIAN_POINT ( 'NONE',  ( -23.29280118367000085, -2.879402575693999822, 10.76157691598000099 ) ) ;
#13541=ORIENTED_EDGE ( 'NONE', *, *, #22654, .T. ) ;
#13542=CARTESIAN_POINT ( 'NONE',  ( 0.6284882100611323130, 11.57509495284122458, 4.749874987833288209 ) ) ;
#13544=FACE_OUTER_BOUND ( 'NONE', #21901, .T. ) ;
#13546=CARTESIAN_POINT ( 'NONE',  ( 12.89756424930999934, 10.41448860350999972, -2.177620798092000598 ) ) ;
#13549=CARTESIAN_POINT ( 'NONE',  ( -12.75178580833000019, 5.886008164689000566, -8.319303600761999817 ) ) ;
#13550=CARTESIAN_POINT ( 'NONE',  ( 13.25700125730999979, -8.207589172378998654, -3.980341215395999832 ) ) ;
#13551=CARTESIAN_POINT ( 'NONE',  ( -14.49999964368427818, 0.5192523986245470846, 12.50000205182227297 ) ) ;
#13552=ORIENTED_EDGE ( 'NONE', *, *, #20092, .T. ) ;
#13555=CARTESIAN_POINT ( 'NONE',  ( 13.85371245318831157, -8.834497878575451324, 5.305004613496619115 ) ) ;
#13558=B_SPLINE_CURVE_WITH_KNOTS ( 'NONE', 3,
 ( #11226, #16768, #13372, #2360, #22696, #22584 ),
 .UNSPECIFIED., .F., .F.,
 ( 4, 1, 1, 4 ),
 ( 0.000000000000000000, 0.3333333333333000081, 0.6666666666667000474, 1.000000000000000000 ),
 .UNSPECIFIED. ) ;
#13559=CARTESIAN_POINT ( 'NONE',  ( -4.480219250449000157, 13.39360627083002164, -5.444853299477003361 ) ) ;
#13562=EDGE_CURVE ( 'NONE', #11958, #1386, #12759, .T. ) ;
#13563=CARTESIAN_POINT ( 'NONE',  ( 11.72559253309398386, 4.116598456381781901, 12.49995860919340274 ) ) ;
#13565=CARTESIAN_POINT ( 'NONE',  ( 17.57014765749539720, -9.538208588764241824, -4.608418869076832181 ) ) ;
#13566=DIRECTION ( 'NONE',  ( 1.000000000000000000, 0.000000000000000000, 0.000000000000000000 ) ) ;
#13567=CARTESIAN_POINT ( 'NONE',  ( -21.09612077250664086, 9.212649750328886000, -1.205806084666599665 ) ) ;
#13568=CARTESIAN_POINT ( 'NONE',  ( 23.99999963380712131, 13.93375672974000246, -0.09624782609426597857 ) ) ;
#13575=CARTESIAN_POINT ( 'NONE',  ( 15.13297668014999964, 10.44537513801999928, 3.552586481088999992 ) ) ;
#13576=CARTESIAN_POINT ( 'NONE',  ( -5.847212767158005420, 15.04942523385998498, -2.909050744206997496 ) ) ;
#13578=EDGE_LOOP ( 'NONE', ( #8597, #13335, #23109, #10743, #10620, #10450 ) ) ;
#13579=EDGE_LOOP ( 'NONE', ( #11036, #14367, #2532, #2161, #22043, #12518, #4553, #17967 ) ) ;
#13580=CARTESIAN_POINT ( 'NONE',  ( -14.00000000000000000, 6.995278287856000254, -5.711120943918999160 ) ) ;
#13582=DIRECTION ( 'NONE',  ( 1.000000000000000000, 0.000000000000000000, 0.000000000000000000 ) ) ;
#13583=VERTEX_POINT ( 'NONE', #15257 ) ;
#13586=CARTESIAN_POINT ( 'NONE',  ( 15.75898575427667581, -10.08917934536900418, 2.323824035917134712 ) ) ;
#13587=CARTESIAN_POINT ( 'NONE',  ( -17.44139086687999907, -4.785270692951000271, -9.999417235773998769 ) ) ;
#13589=CARTESIAN_POINT ( 'NONE',  ( -20.20122951085723884, 8.831040645199459860, 5.673307061337953705 ) ) ;
#13590=CARTESIAN_POINT ( 'NONE',  ( -13.97056789615000127, 4.578996057282999743, 9.143398144881999201 ) ) ;
#13592=ORIENTED_EDGE ( 'NONE', *, *, #20459, .F. ) ;
#13594=CARTESIAN_POINT ( 'NONE',  ( -19.09328248614785650, -3.188221648232169692, -9.986957848427829632 ) ) ;
#13596=CARTESIAN_POINT ( 'NONE',  ( 5.193778049067001135, 13.91699130313997657, -4.147951301185004880 ) ) ;
#13598=CARTESIAN_POINT ( 'NONE',  ( -19.80530420454666540, 5.641336654966718100, -7.340471888469334516 ) ) ;
#13599=CARTESIAN_POINT ( 'NONE',  ( 17.69737658530999980, -0.08473977435852000917, -10.25642497589999991 ) ) ;
#13601=B_SPLINE_CURVE_WITH_KNOTS ( 'NONE', 3,
 ( #21075, #23119, #4487, #2922, #475, #22999, #13802, #6417, #965, #8364, #1586, #19635, #3045, #10790, #5104, #15969, #16338, #1217, #23729, #14174, #16093, #8608, #21692, #4984, #14411, #1463, #8857, #7134, #6659, #14525, #10432, #21917, #14053, #5331, #17822, #21574, #12371, #3408, #12248, #17695 ),
 .UNSPECIFIED., .F., .F.,
 ( 4, 2, 2, 1, 2, 2, 2, 2, 1, 1, 2, 2, 2, 2, 2, 2, 2, 2, 1, 2, 2, 4 ),
 ( 0.000000000000000000, 0.1249999999999819311, 0.1874999999999721334, 0.2187499999999676370, 0.2343749999999661382, 0.2499999999999646394, 0.3749999999999477085, 0.4374999999999382161, 0.4687499999999327205, 0.4843749999999300559, 0.4921874999999286682, 0.4999999999999273359, 0.5624999999999176215, 0.5937499999999141798, 0.6093749999999130695, 0.6249999999999118483, 0.6874999999999157341, 0.7187499999999187317, 0.7343749999999219513, 0.7421874999999236167, 0.7499999999999251710, 1.000000000000000000 ),
 .UNSPECIFIED. ) ;
#13602=CARTESIAN_POINT ( 'NONE',  ( 18.22028936713000036, -1.652712406954000013, 8.988165862088999702 ) ) ;
#13604=CARTESIAN_POINT ( 'NONE',  ( 0.6124999999999999334, 1.217145837503000065E-14, 0.000000000000000000 ) ) ;
#13605=EDGE_LOOP ( 'NONE', ( #14888, #6168, #5908, #10995 ) ) ;
#13608=CARTESIAN_POINT ( 'NONE',  ( 23.97064348353488228, 8.656922289499620504, 6.324528327562126684 ) ) ;
#13609=CARTESIAN_POINT ( 'NONE',  ( 19.52828936713000019, 9.172416106433001204, 0.000000000000000000 ) ) ;
#13610=CARTESIAN_POINT ( 'NONE',  ( 17.66745306301536544, -10.34082436438601427, -1.123769564641571295 ) ) ;
#13612=CARTESIAN_POINT ( 'NONE',  ( -14.42499036736162843, 9.146326703434647598, -9.158041868011997266 ) ) ;
#13613=CARTESIAN_POINT ( 'NONE',  ( -5.470519282017996865, 16.57663645147999532, -3.044056508385000193 ) ) ;
#13614=CARTESIAN_POINT ( 'NONE',  ( 11.99999999337999945, 7.499999993379000252, 2.839929970532000182E-09 ) ) ;
#13619=CARTESIAN_POINT ( 'NONE',  ( -17.12799577250666516, 4.588264514863035437, 7.960958945508470386 ) ) ;
#13620=CARTESIAN_POINT ( 'NONE',  ( 18.29451526988999888, 2.173595297473000176, 9.280136552624998814 ) ) ;
#13621=CARTESIAN_POINT ( 'NONE',  ( -4.400811355473761566, 13.44820252045024844, -5.243297503433447915 ) ) ;
#13624=CARTESIAN_POINT ( 'NONE',  ( -19.54644303974366082, -5.739935299888772491, 8.770143196517862449 ) ) ;
#13629=CARTESIAN_POINT ( 'NONE',  ( -16.98657998867568253, 0.2181174425927162597, -10.41649861509676356 ) ) ;
#13632=EDGE_LOOP ( 'NONE', ( #21331, #12012, #15785, #5097, #6796 ) ) ;
#13635=DIRECTION ( 'NONE',  ( 0.000000000000000000, -1.000000000000000000, 0.000000000000000000 ) ) ;
#13636=CARTESIAN_POINT ( 'NONE',  ( 18.93037674931000325, -2.874963284959999754, 10.40852167983000065 ) ) ;
#13637=CARTESIAN_POINT ( 'NONE',  ( -19.45545303391000047, -10.54334799148000101, 1.955063380522000127 ) ) ;
#13638=CARTESIAN_POINT ( 'NONE',  ( -19.89493079071000281, -7.185997981995999595, 7.042515753137999823 ) ) ;
#13640=CARTESIAN_POINT ( 'NONE',  ( 16.07233580085999947, -5.589751863050000047, -9.898928778229000969 ) ) ;
#13641=DIRECTION ( 'NONE',  ( 0.000000000000000000, -1.000000000000000000, 0.000000000000000000 ) ) ;
#13643=PLANE ( 'NONE',  #18390 ) ;
#13644=CARTESIAN_POINT ( 'NONE',  ( 19.95901395809000078, -10.16568956861999951, -0.7466314648695999701 ) ) ;
#13645=B_SPLINE_SURFACE_WITH_KNOTS ( 'NONE', 3, 3, ( 
 ( #4219, #6144, #18869, #11611, #14983, #22494, #5903 ),
 ( #13533, #4096, #2042, #2274, #6022, #11374, #20809 ),
 ( #17048, #328, #18745, #22730, #7733, #9548, #9432 ),
 ( #15465, #562, #16926, #9903, #15098, #5793, #16803 ) ),
 .UNSPECIFIED., .F., .F., .F.,
 ( 4, 4 ),
 ( 4, 1, 1, 1, 4 ),
 ( 0.5752948794218999407, 1.078423528826000011 ),
 ( 0.9199548376994000076, 0.9403585065211000904, 0.9607621753428000622, 0.9811658441645999540, 1.001569512986000055 ),
 .UNSPECIFIED. ) ;
#13648=CARTESIAN_POINT ( 'NONE',  ( -12.50000000000000000, 6.606768802097000126, -6.099810110451000966 ) ) ;
#13650=CARTESIAN_POINT ( 'NONE',  ( 4.778589274750996374, 12.47906568194001764, 0.2464885544182001953 ) ) ;
#13653=CARTESIAN_POINT ( 'NONE',  ( -20.93315459384999855, -5.137598072637000080, -9.812497494458000347 ) ) ;
#13654=ORIENTED_EDGE ( 'NONE', *, *, #9318, .T. ) ;
#13656=ORIENTED_EDGE ( 'NONE', *, *, #4685, .T. ) ;
#13658=CARTESIAN_POINT ( 'NONE',  ( -11.00000000000000000, -10.59999999999999964, 0.000000000000000000 ) ) ;
#13659=CARTESIAN_POINT ( 'NONE',  ( -4.023597209795000573, 13.98887489068000356, 4.533200346611999443 ) ) ;
#13665=CARTESIAN_POINT ( 'NONE',  ( -14.78308928803000022, -1.400056168502999965, -10.15245659134999912 ) ) ;
#13666=CARTESIAN_POINT ( 'NONE',  ( 16.21856375731000099, 2.595497835609000159, 8.825947828509001170 ) ) ;
#13667=CARTESIAN_POINT ( 'NONE',  ( 24.40278699097224901, 2.659935282767430298, 12.50000000000000000 ) ) ;
#13669=CARTESIAN_POINT ( 'NONE',  ( 19.67611389298096114, -1.127737984101849555, -10.44857563443030557 ) ) ;
#13670=CARTESIAN_POINT ( 'NONE',  ( 12.50000000000000000, -13.93375672974000068, 0.000000000000000000 ) ) ;
#13672=CARTESIAN_POINT ( 'NONE',  ( 4.036236897996232642, 14.47342755007821147, -4.607006349117426680 ) ) ;
#13675=CARTESIAN_POINT ( 'NONE',  ( -24.24003052284538029, 12.62002563675921962, -3.141177558926625313 ) ) ;
#13677=CARTESIAN_POINT ( 'NONE',  ( -12.50000000000000000, 1.554281285377000029E-14, -7.500000000000916600 ) ) ;
#13678=CARTESIAN_POINT ( 'NONE',  ( 17.62590205330530679, -8.442047657051244158, -6.393466172490128940 ) ) ;
#13681=ADVANCED_FACE ( 'NONE', ( #2435 ), #23089, .F. ) ;
#13683=EDGE_LOOP ( 'NONE', ( #845, #22121, #7426, #17313, #5213 ) ) ;
#13684=CARTESIAN_POINT ( 'NONE',  ( -7.034000000000000696, 1.310788454998999989E-14, 0.000000000000000000 ) ) ;
#13686=CARTESIAN_POINT ( 'NONE',  ( 11.40904387243762663, -9.351110459859503621, 8.803306989946506178 ) ) ;
#13687=ORIENTED_EDGE ( 'NONE', *, *, #17020, .F. ) ;
#13690=CARTESIAN_POINT ( 'NONE',  ( 2.689850711658643867, 13.04840579188256200, 6.170289802015100022 ) ) ;
#13693=CARTESIAN_POINT ( 'NONE',  ( 6.141454963614990881, 14.19352208129948956, -0.05101708110013205427 ) ) ;
#13694=CARTESIAN_POINT ( 'NONE',  ( -20.58689978330333759, -0.5797656323877646845, 9.243770522370594378 ) ) ;
#13696=EDGE_CURVE ( 'NONE', #4476, #20167, #4707, .T. ) ;
#13697=VERTEX_POINT ( 'NONE', #16971 ) ;
#13700=CARTESIAN_POINT ( 'NONE',  ( -23.74465998031000069, 7.716878364870000340, -11.63397459621999985 ) ) ;
#13705=CARTESIAN_POINT ( 'NONE',  ( 6.157250470212304982, 14.08721296600253403, 0.3655245610725118000 ) ) ;
#13706=CARTESIAN_POINT ( 'NONE',  ( 15.88689183704831898, -10.11250081917797949, -2.234254655284192648 ) ) ;
#13707=CARTESIAN_POINT ( 'NONE',  ( -18.52537075707000014, 9.692839761673001320, 5.440148519787000758 ) ) ;
#13709=CARTESIAN_POINT ( 'NONE',  ( -19.76373237314461306, -5.167322758071764888, 9.127427723831647910 ) ) ;
#13710=CARTESIAN_POINT ( 'NONE',  ( -24.24721944463121304, -7.815463711320101758, -6.401738435092275026 ) ) ;
#13715=CARTESIAN_POINT ( 'NONE',  ( -16.74920940442816075, 10.40545465073398645, -0.4181688731950466420 ) ) ;
#13717=FACE_OUTER_BOUND ( 'NONE', #19015, .T. ) ;
#13718=CARTESIAN_POINT ( 'NONE',  ( 6.273195954926005236, 13.70238338811998702, -0.1819524851944001598 ) ) ;
#13719=CARTESIAN_POINT ( 'NONE',  ( 12.00000000000000000, 3.342026269744088562, -8.334540845168532996 ) ) ;
#13722=CARTESIAN_POINT ( 'NONE',  ( 12.18656392131000210, 5.460236994095999385, -7.899338765649998706 ) ) ;
#13724=CARTESIAN_POINT ( 'NONE',  ( 18.58787270046333262, -9.148283161302634525, 1.058975758512214815 ) ) ;
#13731=CONICAL_SURFACE ( 'NONE', #2514, 7.249999994591000529, 0.7853981633972997312 ) ;
#13733=CARTESIAN_POINT ( 'NONE',  ( 18.35290878106735946, 8.176867920054682770, -6.464955659164507651 ) ) ;
#13735=CARTESIAN_POINT ( 'NONE',  ( -14.25243324638999809, -7.716878364870000340, 11.63397459621999985 ) ) ;
#13736=CARTESIAN_POINT ( 'NONE',  ( 21.92332918976000045, 10.92587188921000063, 2.656753488603999624 ) ) ;
#13740=VERTEX_POINT ( 'NONE', #13215 ) ;
#13741=CARTESIAN_POINT ( 'NONE',  ( 18.54032793388999778, 2.288377001679999800, 9.770195530030999720 ) ) ;
#13742=CARTESIAN_POINT ( 'NONE',  ( 2.011763616992924941, 12.94111840506035271, -6.392243311745070322 ) ) ;
#13744=CARTESIAN_POINT ( 'NONE',  ( -20.59072166554749828, 1.091684521857474444, -10.45463456709096661 ) ) ;
#13746=DIRECTION ( 'NONE',  ( 0.000000000000000000, 1.000000000000000000, 0.000000000000000000 ) ) ;
#13750=CARTESIAN_POINT ( 'NONE',  ( -16.73537885361223232, 8.099390186838867578, -6.548858784556899515 ) ) ;
#13753=ORIENTED_EDGE ( 'NONE', *, *, #3936, .F. ) ;
#13755=CARTESIAN_POINT ( 'NONE',  ( 24.19085492956958561, -9.549256642876626344, 0.0002501093553063627687 ) ) ;
#13756=CARTESIAN_POINT ( 'NONE',  ( 18.38193924931000112, 10.76489784149000251, -0.6396482201651000343 ) ) ;
#13757=CARTESIAN_POINT ( 'NONE',  ( -14.38421993232999085, -3.906483176905686694, -8.205166477479426845 ) ) ;
#13759=CARTESIAN_POINT ( 'NONE',  ( -14.81667209146000097, 4.829413564942999670, 9.643273172525999470 ) ) ;
#13760=CARTESIAN_POINT ( 'NONE',  ( 22.49408333333332521, 2.420664364967175075, -9.007858475302045420 ) ) ;
#13761=CARTESIAN_POINT ( 'NONE',  ( 18.91749951746000136, 2.321179906104000157, -9.550167091796001984 ) ) ;
#13765=CARTESIAN_POINT ( 'NONE',  ( 22.79179959256000387, 9.200607065852999256, 4.564250555339000037 ) ) ;
#13767=EDGE_LOOP ( 'NONE', ( #12954, #16999, #12697, #16903 ) ) ;
#13768=CARTESIAN_POINT ( 'NONE',  ( -0.5828398938954729713, 13.70670201154066348, 6.100149040538799916 ) ) ;
#13771=CARTESIAN_POINT ( 'NONE',  ( -4.720280981314001423, 12.53503187393000751, -0.1499689402456999276 ) ) ;
#13773=EDGE_CURVE ( 'NONE', #22774, #6663, #21735, .T. ) ;
#13774=CARTESIAN_POINT ( 'NONE',  ( -24.25438256056000341, 9.890429046451000517, -5.183062093339000143 ) ) ;
#13775=LINE ( 'NONE', #8338, #13091 ) ;
#13777=CARTESIAN_POINT ( 'NONE',  ( 15.40899770046332051, -1.186956113863760320, -9.066706963569007627 ) ) ;
#13779=CARTESIAN_POINT ( 'NONE',  ( -2.386616373980000372, 14.08111751881002327, 5.671222873807000298 ) ) ;
#13782=CARTESIAN_POINT ( 'NONE',  ( 13.50000000000000000, 0.000000000000000000, 0.000000000000000000 ) ) ;
#13784=CARTESIAN_POINT ( 'NONE',  ( -13.84895371062999914, -11.26122607477999971, -0.8537354506236000118 ) ) ;
#13785=CARTESIAN_POINT ( 'NONE',  ( 12.81825125731000092, -4.388733341911000174, 7.983506680731000671 ) ) ;
#13786=CARTESIAN_POINT ( 'NONE',  ( 23.99062354302999722, 6.216878364870000340, 12.50000000000000000 ) ) ;
#13791=CIRCLE ( 'NONE', #16108, 1.000000757558000553 ) ;
#13793=CARTESIAN_POINT ( 'NONE',  ( 3.076789502295112833, 14.15080769385439652, -5.296133739446251099 ) ) ;
#13794=ORIENTED_EDGE ( 'NONE', *, *, #20978, .T. ) ;
#13797=PLANE ( 'NONE',  #16973 ) ;
#13798=DIRECTION ( 'NONE',  ( 1.000000000000000000, 0.000000000000000000, 0.000000000000000000 ) ) ;
#13799=CARTESIAN_POINT ( 'NONE',  ( 11.32654380050958309, 2.569587902822825232, 12.49997024370573939 ) ) ;
#13800=CARTESIAN_POINT ( 'NONE',  ( 16.78958611615448149, 6.561663190455382377, 8.105752677713512711 ) ) ;
#13802=CARTESIAN_POINT ( 'NONE',  ( -4.348907022798502275, 13.58078079707876995, 4.987290125177318956 ) ) ;
#13803=CARTESIAN_POINT ( 'NONE',  ( -21.47403743917331909, 1.207329456531927248, -9.222347836830195433 ) ) ;
#13804=ADVANCED_FACE ( 'NONE', ( #2810 ), #8422, .T. ) ;
#13805=CARTESIAN_POINT ( 'NONE',  ( 24.40278699097225612, -12.15528518867914620, -3.946428472716975833 ) ) ;
#13806=ORIENTED_EDGE ( 'NONE', *, *, #21675, .F. ) ;
#13808=CARTESIAN_POINT ( 'NONE',  ( 11.07373617190885184, -10.57520287780550206, 6.683140124596108400 ) ) ;
#13810=CARTESIAN_POINT ( 'NONE',  ( -14.25243324638999809, 6.216878364870000340, -12.50000000000000000 ) ) ;
#13812=CARTESIAN_POINT ( 'NONE',  ( 4.133705205700141327, 13.37470319316354406, 5.426825399075087653 ) ) ;
#13814=CARTESIAN_POINT ( 'NONE',  ( 6.150813686940276526, 14.12672329618388467, -0.2685225048143122795 ) ) ;
#13815=CARTESIAN_POINT ( 'NONE',  ( -6.454293914649997355, 15.34141787428001180, -0.9747575175365998934 ) ) ;
#13816=EDGE_CURVE ( 'NONE', #20493, #17324, #21563, .T. ) ;
#13818=ORIENTED_EDGE ( 'NONE', *, *, #1722, .F. ) ;
#13824=EDGE_CURVE ( 'NONE', #17699, #12075, #16233, .T. ) ;
#13825=AXIS2_PLACEMENT_3D ( 'NONE', #676, #8083, #15567 ) ;
#13827=EDGE_CURVE ( 'NONE', #17905, #11381, #21165, .T. ) ;
#13829=CARTESIAN_POINT ( 'NONE',  ( 24.00034722001000276, 7.216970193741999218, -11.92259671338999993 ) ) ;
#13830=CARTESIAN_POINT ( 'NONE',  ( 14.98923988655635497, 9.998246065564853069, 2.609326537872780793 ) ) ;
#13831=CARTESIAN_POINT ( 'NONE',  ( -15.09276777146999926, 10.87078250371000010, -1.814120968959000102 ) ) ;
#13832=CARTESIAN_POINT ( 'NONE',  ( -20.35564026534377291, 10.49329004425314693, 0.3800888360172406943 ) ) ;
#13833=CARTESIAN_POINT ( 'NONE',  ( -4.588558270747998158, 12.55560619728998972, -1.211727637559999904 ) ) ;
#13835=CARTESIAN_POINT ( 'NONE',  ( -24.37360972231626377, -9.140674791923824927, -4.597026942064932342 ) ) ;
#13840=CARTESIAN_POINT ( 'NONE',  ( -15.09967649506999798, 8.662012103627256820, -5.976300280193180825 ) ) ;
#13841=ORIENTED_EDGE ( 'NONE', *, *, #21994, .F. ) ;
#13842=CARTESIAN_POINT ( 'NONE',  ( 6.037827715737003054, 14.51810667922999087, -1.086417744412999653 ) ) ;
#13843=CARTESIAN_POINT ( 'NONE',  ( -4.701368215507619297, 13.42162485236267599, -5.311323292224679804 ) ) ;
#13844=CARTESIAN_POINT ( 'NONE',  ( -24.50000000000000000, -0.9970802404058677348, -10.51200122757351174 ) ) ;
#13845=CARTESIAN_POINT ( 'NONE',  ( 13.17375142130999954, -7.436937191241000278, 6.115943375764999246 ) ) ;
#13846=EDGE_LOOP ( 'NONE', ( #8947, #19746, #18350, #21577, #7885 ) ) ;
#13850=CARTESIAN_POINT ( 'NONE',  ( 12.52688711657000020, 13.93375672974000068, 0.8660254037843999608 ) ) ;
#13852=EDGE_LOOP ( 'NONE', ( #22621, #11981, #18905, #6982 ) ) ;
#13854=CARTESIAN_POINT ( 'NONE',  ( 21.36033333333333317, 4.643197203103720305, 8.055763831365723604 ) ) ;
#13856=CARTESIAN_POINT ( 'NONE',  ( -14.00000000000000355, -1.769624730688005076, 9.693260132994977241 ) ) ;
#13857=CARTESIAN_POINT ( 'NONE',  ( 16.57009594051854506, 8.851926291245774792, -5.490978545969712243 ) ) ;
#13860=CARTESIAN_POINT ( 'NONE',  ( -14.33281102374372473, 13.40129170500425460, -1.788281879885584624 ) ) ;
#13861=CARTESIAN_POINT ( 'NONE',  ( 22.80413863851999778, -10.54592076045000049, 3.969997482439000525 ) ) ;
#13862=LINE ( 'NONE', #19192, #2466 ) ;
#13864=B_SPLINE_CURVE_WITH_KNOTS ( 'NONE', 3,
 ( #16918, #17042, #440, #22608 ),
 .UNSPECIFIED., .F., .F.,
 ( 4, 4 ),
 ( 0.000000000000000000, 1.000000000000000000 ),
 .UNSPECIFIED. ) ;
#13865=CARTESIAN_POINT ( 'NONE',  ( -3.830485454497844611, 14.04491027079380494, -4.850755123483903475 ) ) ;
#13866=CARTESIAN_POINT ( 'NONE',  ( -5.833999999999999631, 1.296092693409999996E-14, 0.000000000000000000 ) ) ;
#13868=EDGE_CURVE ( 'NONE', #20307, #21964, #1223, .T. ) ;
#13870=CARTESIAN_POINT ( 'NONE',  ( 20.80677740615999838, -8.429461903092001052, -5.987368277389999882 ) ) ;
#13871=CARTESIAN_POINT ( 'NONE',  ( 24.12965592620283672, 9.344095902241738472, 5.044035288470976042 ) ) ;
#13874=CARTESIAN_POINT ( 'NONE',  ( -20.69782716562949432, -2.778284679047643646, -10.13681908816563926 ) ) ;
#13876=CARTESIAN_POINT ( 'NONE',  ( 4.829979889486999411, 12.47095937650998820, -1.110733291722999283 ) ) ;
#13877=ORIENTED_EDGE ( 'NONE', *, *, #3336, .T. ) ;
#13879=CARTESIAN_POINT ( 'NONE',  ( -16.23297658348885264, 5.081863263689504251, 9.076500965692741119 ) ) ;
#13880=CARTESIAN_POINT ( 'NONE',  ( -5.833999999999999631, 11.50000000000000000, 0.000000000000000000 ) ) ;
#13883=EDGE_LOOP ( 'NONE', ( #16013, #2966, #15875, #23942 ) ) ;
#13884=CARTESIAN_POINT ( 'NONE',  ( 17.18520603379667477, -2.385239382193358182, -8.875070924070865175 ) ) ;
#13886=DIRECTION ( 'NONE',  ( 0.000000000000000000, 0.000000000000000000, -1.000000000000000000 ) ) ;
#13887=CARTESIAN_POINT ( 'NONE',  ( -21.81072441343999913, 5.248549362552000552, 9.854325464458000283 ) ) ;
#13888=CARTESIAN_POINT ( 'NONE',  ( -14.67959218088999940, -8.291367167875000277, 6.018862870213999905 ) ) ;
#13889=CARTESIAN_POINT ( 'NONE',  ( -6.225556268444002228, 15.63956656239001575, 1.260315956371999446 ) ) ;
#13890=CARTESIAN_POINT ( 'NONE',  ( 13.50083285078999928, 2.897491670606999747, -8.682224649056999866 ) ) ;
#13891=CARTESIAN_POINT ( 'NONE',  ( -14.25699038479000080, -13.93375672974000068, 0.000000000000000000 ) ) ;
#13892=CARTESIAN_POINT ( 'NONE',  ( -4.544324455327999779, 13.49053734526000170, 5.132126114358000812 ) ) ;
#13893=AXIS2_PLACEMENT_3D ( 'NONE', #11296, #12978, #22647 ) ;
#13896=CARTESIAN_POINT ( 'NONE',  ( -2.409957067094174565, 13.97492973469119448, 5.631351995472492433 ) ) ;
#13900=CIRCLE ( 'NONE', #11976, 2.000000000000000000 ) ;
#13902=CARTESIAN_POINT ( 'NONE',  ( -21.24686073652000218, -9.675487687114999957, -5.408659645178999220 ) ) ;
#13907=CARTESIAN_POINT ( 'NONE',  ( 4.343596930150846802, 12.26443547612926110, -2.147542669209427491 ) ) ;
#13913=CARTESIAN_POINT ( 'NONE',  ( -9.377904711694998952, 11.69296112842000035, -10.27916260946000193 ) ) ;
#13914=CARTESIAN_POINT ( 'NONE',  ( -6.062127672058159611, 16.18558825329198214, -1.005394117991464276 ) ) ;
#13915=CARTESIAN_POINT ( 'NONE',  ( 15.12168875731000028, -7.425874990359000449, -5.381511109182000041 ) ) ;
#13916=CARTESIAN_POINT ( 'NONE',  ( 19.00748459915545752, -0.3300499044338658927, 10.45037867241294371 ) ) ;
#13917=ORIENTED_EDGE ( 'NONE', *, *, #14846, .F. ) ;
#13920=CARTESIAN_POINT ( 'NONE',  ( -15.42737077250666644, 7.250632197270348911, 5.572294543148784030 ) ) ;
#13922=AXIS2_PLACEMENT_3D ( 'NONE', #19627, #3035, #1209 ) ;
#13927=CARTESIAN_POINT ( 'NONE',  ( -5.990165124597438329, 16.36624069022721528, 1.318159437083336272 ) ) ;
#13928=CARTESIAN_POINT ( 'NONE',  ( 15.64662100204322215, -10.36655533400305274, -0.7640403907738141376 ) ) ;
#13931=CARTESIAN_POINT ( 'NONE',  ( -11.04281598264000053, 1.359882291614000008E-14, 0.000000000000000000 ) ) ;
#13932=ORIENTED_EDGE ( 'NONE', *, *, #9654, .F. ) ;
#13933=CARTESIAN_POINT ( 'NONE',  ( -24.50000000000000000, -8.081477262649000792, -6.807253044743999837 ) ) ;
#13934=CARTESIAN_POINT ( 'NONE',  ( 11.83261479513829784, -8.603276725215390996, 10.09871632141666176 ) ) ;
#13935=ORIENTED_EDGE ( 'NONE', *, *, #13024, .F. ) ;
#13936=B_SPLINE_CURVE_WITH_KNOTS ( 'NONE', 3,
 ( #14613, #16544, #2017, #23936, #14728, #20309, #3714, #11105, #22472, #19074, #5882, #8188, #11464, #2368, #9757, #13507, #2246, #13267, #9640, #17143, #15076, #17024, #2743, #21141, #11701, #15310, #423, #2489, #540, #20906, #13742, #21019, #11821, #11947, #7823, #4310, #4431, #20661, #2613, #18842, #6360, #4556, #20782, #15194, #19199, #4188, #22590, #4072, #7945, #22705, #6114, #17393, #10002, #13380, #9878, #17264, #5995, #11585, #663, #788, #7707, #18960, #19332, #15556, #22943, #8069, #10123, #22825, #300, #15438, #6239, #13621, #8668 ),
 .UNSPECIFIED., .F., .F.,
 ( 4, 2, 2, 1, 1, 1, 2, 2, 2, 2, 1, 1, 1, 2, 2, 2, 2, 1, 1, 2, 2, 2, 1, 1, 2, 2, 2, 1, 1, 1, 2, 2, 2, 2, 2, 2, 2, 2, 2, 2, 2, 2, 4 ),
 ( 0.000000000000000000, 0.06249999999999331091, 0.09374999999999010514, 0.1093749999999885647, 0.1171874999999877598, 0.1210937499999874684, 0.1230468749999873851, 0.1249999999999873157, 0.1874999999999849842, 0.2187499999999837907, 0.2343749999999832079, 0.2421874999999829026, 0.2460937499999827083, 0.2480468749999827915, 0.2499999999999828471, 0.3124999999999827915, 0.3437499999999828471, 0.3593749999999827915, 0.3671874999999826805, 0.3710937499999827915, 0.3749999999999828471, 0.4374999999999854006, 0.4687499999999866773, 0.4843749999999872879, 0.4921874999999875655, 0.4999999999999878986, 0.5624999999999898970, 0.5937499999999908962, 0.6093749999999914513, 0.6171874999999916733, 0.6210937499999917843, 0.6249999999999918954, 0.6874999999999938938, 0.7187499999999948930, 0.7499999999999958922, 0.8124999999999978906, 0.8203124999999980016, 0.8281249999999982236, 0.8437499999999984457, 0.8749999999999986677, 0.9062499999999990008, 0.9374999999999993339, 1.000000000000000000 ),
 .UNSPECIFIED. ) ;
#13937=EDGE_CURVE ( 'NONE', #2137, #379, #8806, .T. ) ;
#13940=CARTESIAN_POINT ( 'NONE',  ( 0.6306621565982972744, 12.81494453417391810, 6.641634381469641468 ) ) ;
#13941=CARTESIAN_POINT ( 'NONE',  ( 6.156111259623703091, 14.09394095567527572, -0.3492167251953930962 ) ) ;
#13943=CARTESIAN_POINT ( 'NONE',  ( 24.28255857084583624, -4.111234970449187287, -12.50000000000000533 ) ) ;
#13945=DIRECTION ( 'NONE',  ( 0.000000000000000000, 1.000000000000000000, 0.000000000000000000 ) ) ;
#13947=CARTESIAN_POINT ( 'NONE',  ( 0.000000000000000000, -14.43375672974000068, 0.000000000000000000 ) ) ;
#13950=CARTESIAN_POINT ( 'NONE',  ( -23.17505693544000422, 0.9177324661394998806, 10.72000274858999980 ) ) ;
#13951=CYLINDRICAL_SURFACE ( 'NONE', #18668, 10.65000000000000036 ) ;
#13952=CARTESIAN_POINT ( 'NONE',  ( 20.33995833333332470, -7.351623071504412188, -5.649588876138436966 ) ) ;
#13953=CARTESIAN_POINT ( 'NONE',  ( 15.07770949396983617, 8.779094814448228590, 5.457277787253644874 ) ) ;
#13954=CARTESIAN_POINT ( 'NONE',  ( -14.76548285955000139, 9.865459827462000675, 4.892865777766999713 ) ) ;
#13956=DIRECTION ( 'NONE',  ( 1.000000000000000000, 0.000000000000000000, 0.000000000000000000 ) ) ;
#13957=CARTESIAN_POINT ( 'NONE',  ( 1.367099767897999918, 11.70857751387000434, -4.578439149374998962 ) ) ;
#13963=CARTESIAN_POINT ( 'NONE',  ( -14.63664971349574273, 5.615217594154322533, 8.712278466216046624 ) ) ;
#13964=B_SPLINE_CURVE_WITH_KNOTS ( 'NONE', 3,
 ( #652, #6103, #17626, #4301, #17751 ),
 .UNSPECIFIED., .F., .F.,
 ( 4, 1, 4 ),
 ( 0.000000000000000000, 0.5000000000000000000, 1.000000000000000000 ),
 .UNSPECIFIED. ) ;
#13966=ORIENTED_EDGE ( 'NONE', *, *, #3324, .T. ) ;
#13967=EDGE_CURVE ( 'NONE', #7090, #20281, #11109, .T. ) ;
#13968=CARTESIAN_POINT ( 'NONE',  ( -23.76320767093000086, 6.967315680849999637, -12.06673481360999922 ) ) ;
#13969=CARTESIAN_POINT ( 'NONE',  ( 5.100994270091002036, 14.04962196135000418, -3.662671701414000225 ) ) ;
#13970=CARTESIAN_POINT ( 'NONE',  ( 12.00000000000000000, 0.9388500350608516287, -8.930124715774828914 ) ) ;
#13971=CARTESIAN_POINT ( 'NONE',  ( 24.18393254356921318, 4.886968879241179842, -12.50000000000000000 ) ) ;
#13972=CARTESIAN_POINT ( 'NONE',  ( 12.76143908531000193, 9.974460201879001175, 1.751222586102000101 ) ) ;
#13974=CARTESIAN_POINT ( 'NONE',  ( -8.687268992921000077, 13.47714631021000109, -4.089943008506000233 ) ) ;
#13978=EDGE_CURVE ( 'NONE', #21807, #22775, #20016, .T. ) ;
#13979=CARTESIAN_POINT ( 'NONE',  ( 11.22311500625409941, 11.82633764590034708, 4.516161837427946857 ) ) ;
#13982=CARTESIAN_POINT ( 'NONE',  ( 16.27456687147326164, -0.07827200606447888565, -10.36562678650456881 ) ) ;
#13983=LINE ( 'NONE', #19567, #3302 ) ;
#13985=CARTESIAN_POINT ( 'NONE',  ( -14.43045988485397935, -9.209646829420966796, 9.048410431333177684 ) ) ;
#13987=CARTESIAN_POINT ( 'NONE',  ( -4.038094091498922289, 13.81604646495375555, -4.860948425493686997 ) ) ;
#13990=ORIENTED_EDGE ( 'NONE', *, *, #2278, .T. ) ;
#13991=CARTESIAN_POINT ( 'NONE',  ( 18.60474491173999922, 0.1088057166755999894, 10.28239292309999797 ) ) ;
#13992=DIRECTION ( 'NONE',  ( -1.000000000000000000, 0.000000000000000000, 0.000000000000000000 ) ) ;
#13994=ADVANCED_FACE ( 'NONE', ( #458 ), #11270, .F. ) ;
#13995=CARTESIAN_POINT ( 'NONE',  ( -20.21585241526053522, 10.35035534361658272, -1.764829101647155563 ) ) ;
#13996=CARTESIAN_POINT ( 'NONE',  ( -24.47970833437434024, -11.33727345183922708, -5.363206565890020094 ) ) ;
#13998=DIRECTION ( 'NONE',  ( 0.000000000000000000, 1.000000000000000000, 0.000000000000000000 ) ) ;
#14000=FACE_OUTER_BOUND ( 'NONE', #18087, .T. ) ;
#14001=CIRCLE ( 'NONE', #7806, 10.30000000000000426 ) ;
#14006=B_SPLINE_SURFACE_WITH_KNOTS ( 'NONE', 3, 3, ( 
 ( #21394, #18281, #20215, #12593 ),
 ( #19979, #12710, #3621, #12929 ),
 ( #18388, #21796, #22030, #5211 ),
 ( #1680, #10895, #8848, #9070 ) ),
 .UNSPECIFIED., .F., .F., .F.,
 ( 4, 4 ),
 ( 4, 4 ),
 ( 0.9881930060304000563, 1.000231509685999942 ),
 ( 0.9965732490345999839, 1.000616174089999921 ),
 .UNSPECIFIED. ) ;
#14011=AXIS2_PLACEMENT_3D ( 'NONE', #7751, #20827, #5923 ) ;
#14012=CARTESIAN_POINT ( 'NONE',  ( -12.53497940801999988, 6.430159825535999296, -13.55186498671000095 ) ) ;
#14013=CARTESIAN_POINT ( 'NONE',  ( -19.72309750885000312, -4.915363752585999890, 9.961952662738001507 ) ) ;
#14014=CARTESIAN_POINT ( 'NONE',  ( -13.59789000363999989, 6.208834040094999729, -8.775712258748999517 ) ) ;
#14016=CARTESIAN_POINT ( 'NONE',  ( 13.63624951745999958, 6.911022695730999921, -6.778078827992000122 ) ) ;
#14018=CARTESIAN_POINT ( 'NONE',  ( -14.25394832655999977, 13.93375672974000068, 0.7219259138221999494 ) ) ;
#14019=CARTESIAN_POINT ( 'NONE',  ( 24.37173283531060619, -9.297778257491829734, 8.895775660514537719 ) ) ;
#14020=ORIENTED_EDGE ( 'NONE', *, *, #820, .T. ) ;
#14021=B_SPLINE_CURVE_WITH_KNOTS ( 'NONE', 3,
 ( #3485, #18251, #18360, #1772, #16536, #7336, #18479, #14717, #22113, #5521, #1892, #7446, #22220, #20419, #10631, #22073, #23402, #6947, #21955, #18325, #19794, #16008, #3326, #12862, #3205, #14681, #14212, #3664, #23655, #6820, #10830, #7170, #10939, #1730, #21841, #16263, #18216, #10587, #1503, #17975, #10704, #1376 ),
 .UNSPECIFIED., .F., .F.,
 ( 4, 2, 1, 2, 2, 2, 1, 2, 2, 2, 2, 2, 2, 2, 2, 1, 2, 2, 2, 1, 2, 2, 4 ),
 ( 0.000000000000000000, 0.06249999999999979183, 0.09374999999999969469, 0.1093749999999996392, 0.1249999999999995837, 0.1874999999999995282, 0.2187499999999993616, 0.2343749999999991673, 0.2499999999999989730, 0.3124999999999987788, 0.3749999999999986677, 0.4999999999999984457, 0.5624999999999983347, 0.6249999999999982236, 0.6874999999999981126, 0.7187499999999982236, 0.7343749999999983347, 0.7499999999999983347, 0.8124999999999988898, 0.8437499999999992228, 0.8593749999999993339, 0.8749999999999995559, 1.000000000000000000 ),
 .UNSPECIFIED. ) ;
#14022=CARTESIAN_POINT ( 'NONE',  ( -2.122180917233752240, 13.91146394560632515, 5.745605564203374982 ) ) ;
#14025=CARTESIAN_POINT ( 'NONE',  ( -19.24432910583999856, 9.165129126472001175, 0.000000000000000000 ) ) ;
#14026=CARTESIAN_POINT ( 'NONE',  ( -14.34305601391669427, 6.095070058083463138, -6.708088486029590847 ) ) ;
#14029=CARTESIAN_POINT ( 'NONE',  ( -4.758298526560081676, 12.41512346299555425, 0.9316463370115228848 ) ) ;
#14030=EDGE_LOOP ( 'NONE', ( #9836, #14587, #9277, #17240 ) ) ;
#14031=CARTESIAN_POINT ( 'NONE',  ( -5.194121241778000275, 1.198997689148931003E-14, -12.44999999999999929 ) ) ;
#14032=CARTESIAN_POINT ( 'NONE',  ( 3.890492083747782104, 12.11396562357843720, -2.873055849959892605 ) ) ;
#14034=B_SPLINE_CURVE_WITH_KNOTS ( 'NONE', 3,
 ( #4940, #21766, #18450, #18017, #3129, #4816, #1418, #6623, #8816, #8688, #16177, #21526, #23579, #19468, #12203, #16053, #3002, #23446, #17778, #23207, #6984, #14373, #5179, #12561, #3676, #12086, #10260, #17649 ),
 .UNSPECIFIED., .F., .F.,
 ( 4, 2, 2, 1, 1, 2, 2, 2, 1, 1, 2, 2, 2, 2, 2, 4 ),
 ( 0.000000000000000000, 0.1250000000000167089, 0.1875000000000248412, 0.2187500000000285327, 0.2343750000000297540, 0.2421875000000298650, 0.2500000000000299760, 0.3750000000000260347, 0.4375000000000237588, 0.4687500000000231482, 0.4843750000000227596, 0.5000000000000224265, 0.6250000000000169864, 0.6875000000000139888, 0.7500000000000108802, 1.000000000000000000 ),
 .UNSPECIFIED. ) ;
#14035=CARTESIAN_POINT ( 'NONE',  ( 11.71313497180072183, -3.220258825039508110, -8.401516397519381840 ) ) ;
#14037=CARTESIAN_POINT ( 'NONE',  ( -10.29430721169000051, -2.366881450064000081, 15.38787860124999973 ) ) ;
#14038=CARTESIAN_POINT ( 'NONE',  ( 11.47028936713000036, -8.379193606113998882, -3.189305674207999708 ) ) ;
#14039=VECTOR ( 'NONE', #19526, 1000.000000000000000 ) ;
#14040=CARTESIAN_POINT ( 'NONE',  ( 15.25781392131000125, -9.389200645904999476, -2.369324833533999808 ) ) ;
#14041=LINE ( 'NONE', #23351, #3951 ) ;
#14045=CARTESIAN_POINT ( 'NONE',  ( -15.61632910584000022, 9.072027496059000384, 0.000000000000000000 ) ) ;
#14046=CARTESIAN_POINT ( 'NONE',  ( 24.50000000000000000, 0.000000000000000000, 0.000000000000000000 ) ) ;
#14047=VERTEX_POINT ( 'NONE', #5806 ) ;
#14049=CARTESIAN_POINT ( 'NONE',  ( -3.000000000000000000, 17.00000000000000000, 0.000000000000000000 ) ) ;
#14050=DIRECTION ( 'NONE',  ( 0.000000000000000000, 0.9780930753991020632, 0.2081680471550005351 ) ) ;
#14052=CARTESIAN_POINT ( 'NONE',  ( 16.20416496014759034, 4.371488613225747777, -9.447241867773790602 ) ) ;
#14053=CARTESIAN_POINT ( 'NONE',  ( -3.850316308734367254, 14.01983185593565651, 4.848505112072696299 ) ) ;
#14055=CARTESIAN_POINT ( 'NONE',  ( -24.37124162823073448, -9.546779961752369204, 8.464497487801450504 ) ) ;
#14058=DIRECTION ( 'NONE',  ( 0.000000000000000000, 1.000000000000000000, 0.000000000000000000 ) ) ;
#14062=CARTESIAN_POINT ( 'NONE',  ( 2.058318499670220625, 12.94702448370908776, 6.380432469888065228 ) ) ;
#14063=CARTESIAN_POINT ( 'NONE',  ( 6.202279051248352992, 13.86702088811886036, -0.9424181477496827997 ) ) ;
#14064=CARTESIAN_POINT ( 'NONE',  ( -5.978103862651994227, 15.83376621642000792, -0.9317320578097998407 ) ) ;
#14066=B_SPLINE_CURVE_WITH_KNOTS ( 'NONE', 3,
 ( #8959, #11247, #12591, #2032, #22028, #5208, #9185, #5548, #16679, #7472 ),
 .UNSPECIFIED., .F., .F.,
 ( 4, 2, 2, 2, 4 ),
 ( 0.000000000000000000, 0.1250000000000000000, 0.2500000000000000000, 0.5000000000000001110, 1.000000000000000000 ),
 .UNSPECIFIED. ) ;
#14068=FACE_OUTER_BOUND ( 'NONE', #9464, .T. ) ;
#14072=CARTESIAN_POINT ( 'NONE',  ( -19.16110032286999854, -4.005958525575000095, 9.301206193175998393 ) ) ;
#14073=CARTESIAN_POINT ( 'NONE',  ( 21.02020833333332561, 9.210701687524210257, -1.205804979152639733 ) ) ;
#14074=CARTESIAN_POINT ( 'NONE',  ( 15.06774083095429440, 8.954513157289483161, 5.161873896049346655 ) ) ;
#14075=FACE_OUTER_BOUND ( 'NONE', #16522, .T. ) ;
#14076=ADVANCED_FACE ( 'NONE', ( #3991 ), #12007, .F. ) ;
#14077=CARTESIAN_POINT ( 'NONE',  ( -12.25000000000000000, -13.93375672974000068, 0.000000000000000000 ) ) ;
#14078=CARTESIAN_POINT ( 'NONE',  ( -22.52702113186910893, -5.641063948273841611, 7.354633707470615178 ) ) ;
#14079=CARTESIAN_POINT ( 'NONE',  ( 4.628885738981002085, 12.57105835719000275, -1.073190880219000221 ) ) ;
#14080=EDGE_LOOP ( 'NONE', ( #9383, #20948, #4481, #3612 ) ) ;
#14081=CARTESIAN_POINT ( 'NONE',  ( -15.47399649439000058, -8.448196802485998802, -7.562854223976000156 ) ) ;
#14085=CARTESIAN_POINT ( 'NONE',  ( -15.67845997203782105, -8.965097180577222602, -5.248789696445946618 ) ) ;
#14087=CARTESIAN_POINT ( 'NONE',  ( 5.922047466466997534, 13.79009778142999920, -2.080318915485001252 ) ) ;
#14088=EDGE_CURVE ( 'NONE', #7062, #8639, #14210, .T. ) ;
#14089=CARTESIAN_POINT ( 'NONE',  ( 12.00000000000000000, -1.672630921217244993, -8.822341735481002090 ) ) ;
#14090=CARTESIAN_POINT ( 'NONE',  ( 18.99010413682999854, -5.601003484193999959, 8.806426514188000709 ) ) ;
#14092=CARTESIAN_POINT ( 'NONE',  ( 16.05206408531000051, 5.563243567929000655, -8.565419716155998842 ) ) ;
#14094=CARTESIAN_POINT ( 'NONE',  ( -8.992736492921000746, -0.04910128871962000235, -14.51750318222000047 ) ) ;
#14095=DIRECTION ( 'NONE',  ( -1.000000000000000000, 0.000000000000000000, 0.000000000000000000 ) ) ;
#14098=CARTESIAN_POINT ( 'NONE',  ( -24.00109171669999952, -9.333314996567999344, -0.6894523598369000084 ) ) ;
#14099=CARTESIAN_POINT ( 'NONE',  ( 11.29022434644395467, 12.01543594605562504, 4.188602139394846269 ) ) ;
#14101=DIRECTION ( 'NONE',  ( -1.000000000000000000, 0.000000000000000000, 0.000000000000000000 ) ) ;
#14102=CARTESIAN_POINT ( 'NONE',  ( -6.250000000003001155, 15.09565008225999883, -3.212814891752000079 ) ) ;
#14103=CARTESIAN_POINT ( 'NONE',  ( 17.52130432638741198, -9.628271833752394926, 4.056250497054570303 ) ) ;
#14104=CARTESIAN_POINT ( 'NONE',  ( -18.52628743917332699, -7.314404681686845322, 5.620986415498060218 ) ) ;
#14107=AXIS2_PLACEMENT_3D ( 'NONE', #2971, #17380, #1156 ) ;
#14113=CARTESIAN_POINT ( 'NONE',  ( 20.47283726948000293, -1.948504986539999928, 10.68962299628999979 ) ) ;
#14114=CARTESIAN_POINT ( 'NONE',  ( 22.85285366138076313, -7.483697671837180820, 7.491427571326791046 ) ) ;
#14116=ORIENTED_EDGE ( 'NONE', *, *, #5008, .F. ) ;
#14117=DIRECTION ( 'NONE',  ( 0.7071067811865474617, 0.7071067811865474617, 0.000000000000000000 ) ) ;
#14118=CARTESIAN_POINT ( 'NONE',  ( 4.852182833551873742, 14.56344984251652619, 3.781189165742629754 ) ) ;
#14120=CARTESIAN_POINT ( 'NONE',  ( 4.896390829840998826, 12.43229641542999886, -0.5248650586911998150 ) ) ;
#14122=CARTESIAN_POINT ( 'NONE',  ( -15.03279338263535436, 5.021830743698944666, -9.069083216823218052 ) ) ;
#14124=ORIENTED_EDGE ( 'NONE', *, *, #23419, .T. ) ;
#14125=CIRCLE ( 'NONE', #564, 12.50000000000000000 ) ;
#14130=EDGE_LOOP ( 'NONE', ( #8555, #23761, #20555, #4218 ) ) ;
#14131=CARTESIAN_POINT ( 'NONE',  ( 11.74999999482999868, 0.000000000000000000, -7.249999994832990069 ) ) ;
#14132=CARTESIAN_POINT ( 'NONE',  ( -12.21107666535000114, 9.613013645102999050, -12.04164784824000023 ) ) ;
#14133=CARTESIAN_POINT ( 'NONE',  ( -21.16837767356999578, -10.99666358480999939, -1.827877429396000064 ) ) ;
#14135=CARTESIAN_POINT ( 'NONE',  ( -16.50776531261999835, -8.025729601713999628, 6.450400044432999636 ) ) ;
#14136=CARTESIAN_POINT ( 'NONE',  ( -5.988267586462001191, 16.12301021452999805, 0.9718889544497001376 ) ) ;
#14138=CARTESIAN_POINT ( 'NONE',  ( 16.20869494526000310, -9.667040997353000265, 3.533098828328999907 ) ) ;
#14140=DIRECTION ( 'NONE',  ( 0.000000000000000000, 0.000000000000000000, 1.000000000000000000 ) ) ;
#14141=CARTESIAN_POINT ( 'NONE',  ( 15.08691666666666187, -2.371145242616797599, -8.822626156915163165 ) ) ;
#14143=CARTESIAN_POINT ( 'NONE',  ( 23.56203090460532934, 1.574364913339408867, 9.158349804732198507 ) ) ;
#14144=CARTESIAN_POINT ( 'NONE',  ( -2.218848708602919384, 13.93185214957625817, 5.709114769721670868 ) ) ;
#14148=CARTESIAN_POINT ( 'NONE',  ( -22.75062164853999747, 0.1503650050700000018, -11.12440192913999937 ) ) ;
#14149=ADVANCED_FACE ( 'NONE', ( #13544 ), #11510, .F. ) ;
#14150=EDGE_CURVE ( 'NONE', #4798, #2581, #19849, .T. ) ;
#14151=CARTESIAN_POINT ( 'NONE',  ( -4.511714276356390663, 12.32404474554762785, 1.769770020287825263 ) ) ;
#14154=CARTESIAN_POINT ( 'NONE',  ( -24.49594166687865027, -0.5121745395713884763, -12.49996680834449947 ) ) ;
#14155=CARTESIAN_POINT ( 'NONE',  ( 24.06454052246407826, -3.752188697602235390, -8.644687579573476555 ) ) ;
#14156=CARTESIAN_POINT ( 'NONE',  ( -21.16580420454666367, 7.368390746024480187, 5.662792393064417062 ) ) ;
#14157=VECTOR ( 'NONE', #18336, 1000.000000000000000 ) ;
#14159=CARTESIAN_POINT ( 'NONE',  ( -17.91156067002999919, -1.604197317876000062, 11.29338059605000133 ) ) ;
#14161=CARTESIAN_POINT ( 'NONE',  ( 14.49000142131000146, 7.205444258087999820, 6.439089808501999634 ) ) ;
#14162=CARTESIAN_POINT ( 'NONE',  ( 24.28255857084583624, 4.111234970449187287, 12.50000000000000533 ) ) ;
#14164=CARTESIAN_POINT ( 'NONE',  ( 5.302311171175275284, 13.76370502379775118, 4.348021967961785528 ) ) ;
#14166=CARTESIAN_POINT ( 'NONE',  ( -14.74712077250667086, -9.049721897106270063, 1.184478878552067682 ) ) ;
#14167=CARTESIAN_POINT ( 'NONE',  ( 4.071856426817071828, 14.48689095887983846, -4.575612886981444305 ) ) ;
#14168=ORIENTED_EDGE ( 'NONE', *, *, #3038, .F. ) ;
#14171=DIRECTION ( 'NONE',  ( 1.000000000000000000, 0.000000000000000000, 0.000000000000000000 ) ) ;
#14172=CARTESIAN_POINT ( 'NONE',  ( -5.695156607585949438, 16.22280606751403198, 2.279197634692520680 ) ) ;
#14173=CARTESIAN_POINT ( 'NONE',  ( 16.12053336643119295, 1.488762681687257672, -10.30218658287923716 ) ) ;
#14174=CARTESIAN_POINT ( 'NONE',  ( -4.066544995498063031, 13.78971146288197325, 4.867452680521627606 ) ) ;
#14175=CARTESIAN_POINT ( 'NONE',  ( 4.942518863364997017, 12.51350827579999958, 0.2556867146312000183 ) ) ;
#14176=CARTESIAN_POINT ( 'NONE',  ( -23.50032910583999879, 1.512442827330999945E-14, 0.000000000000000000 ) ) ;
#14178=EDGE_CURVE ( 'NONE', #7012, #1, #6397, .T. ) ;
#14180=CIRCLE ( 'NONE', #2183, 9.274346474608000435 ) ;
#14182=CIRCLE ( 'NONE', #13006, 3.000000000000000000 ) ;
#14183=VERTEX_POINT ( 'NONE', #8709 ) ;
#14185=CARTESIAN_POINT ( 'NONE',  ( 6.124486376501002916, 14.49660437619998810, 0.3689214650952001295 ) ) ;
#14186=CARTESIAN_POINT ( 'NONE',  ( -0.4921054408743313346, 12.81188039431768644, 6.647493645939474227 ) ) ;
#14188=CARTESIAN_POINT ( 'NONE',  ( -6.012535197899005368, 16.49418337425001013, -1.225408514526999282 ) ) ;
#14190=AXIS2_PLACEMENT_3D ( 'NONE', #19333, #12187, #8308 ) ;
#14192=CARTESIAN_POINT ( 'NONE',  ( -12.24999999999999822, 13.59206128970241778, -6.344557540553090291 ) ) ;
#14193=DIRECTION ( 'NONE',  ( 0.000000000000000000, 1.000000000000000000, 0.000000000000000000 ) ) ;
#14194=DIRECTION ( 'NONE',  ( 0.000000000000000000, -1.000000000000000000, 0.000000000000000000 ) ) ;
#14196=CARTESIAN_POINT ( 'NONE',  ( -23.24757862902999861, -5.490534083007999833, 9.858273392202999474 ) ) ;
#14199=CARTESIAN_POINT ( 'NONE',  ( 14.88837544317048511, 10.27747569187551235, -1.051874237603601436 ) ) ;
#14201=DIRECTION ( 'NONE',  ( 0.000000000000000000, 1.000000000000000000, 0.000000000000000000 ) ) ;
#14203=CARTESIAN_POINT ( 'NONE',  ( -4.725411482781997741, 12.53696406558999143, -0.01086751525878999931 ) ) ;
#14209=CARTESIAN_POINT ( 'NONE',  ( -14.57877136579895705, 3.775861415940093835, 9.652007294606121945 ) ) ;
#14210=CIRCLE ( 'NONE', #7243, 12.44999999999999574 ) ;
#14211=VERTEX_POINT ( 'NONE', #16201 ) ;
#14212=CARTESIAN_POINT ( 'NONE',  ( 11.22311500625338354, -11.82633764589515302, -4.516161837439471860 ) ) ;
#14214=CARTESIAN_POINT ( 'NONE',  ( 12.00000000000000000, 0.7795197778698420565, -8.945416492546511833 ) ) ;
#14215=CONICAL_SURFACE ( 'NONE', #6065, 9.630770167580999797, 0.9419447502231289571 ) ;
#14219=CARTESIAN_POINT ( 'NONE',  ( 13.74862658530999937, -9.135377135809001459, -4.430325866828999537 ) ) ;
#14223=PLANE ( 'NONE',  #17111 ) ;
#14225=CARTESIAN_POINT ( 'NONE',  ( 11.22285964980139283, 9.825076113690533575, 7.982449282869310103 ) ) ;
#14226=CARTESIAN_POINT ( 'NONE',  ( 22.44108499922769795, -0.4819289312304581574, 10.56690249824243466 ) ) ;
#14227=CARTESIAN_POINT ( 'NONE',  ( 17.03668726726226268, 5.064517129654977801, 9.097274685846976183 ) ) ;
#14229=CARTESIAN_POINT ( 'NONE',  ( -18.33732910583999853, -9.141853718868999223, 0.000000000000000000 ) ) ;
#14232=CARTESIAN_POINT ( 'NONE',  ( -4.475682853278175166, 13.51377492745002229, -5.070986449459744527 ) ) ;
#14234=VERTEX_POINT ( 'NONE', #14277 ) ;
#14236=CARTESIAN_POINT ( 'NONE',  ( 23.61741393687999846, 8.209328251910999796, -8.036582473515998970 ) ) ;
#14239=ORIENTED_EDGE ( 'NONE', *, *, #14088, .F. ) ;
#14241=CARTESIAN_POINT ( 'NONE',  ( 4.871525856247341579, 14.47411258586163285, 3.795094578399595520 ) ) ;
#14242=AXIS2_PLACEMENT_3D ( 'NONE', #5910, #22261, #20694 ) ;
#14243=CARTESIAN_POINT ( 'NONE',  ( 0.3813121960981003533, 11.52964601297000335, -4.965239699173999988 ) ) ;
#14245=B_SPLINE_CURVE_WITH_KNOTS ( 'NONE', 3,
 ( #16763, #530, #13144, #15184, #15068, #9279, #20299, #22579, #11093, #5756, #7563, #7934, #14943, #22462, #15301, #3945, #4178, #13257, #20650, #1891, #59, #17014, #20537, #7444, #12898, #413, #18710, #5520, #2120, #9509, #11454, #18830, #7812, #13369, #8298, #23183, #2852, #2731, #8549, #21376, #8178, #15427, #17502, #15546, #19322, #12176, #19443, #10233, #10362, #22814, #11936 ),
 .UNSPECIFIED., .F., .F.,
 ( 4, 1, 1, 2, 2, 1, 1, 1, 1, 1, 2, 2, 1, 1, 1, 1, 1, 2, 2, 1, 1, 1, 1, 1, 2, 2, 1, 1, 1, 2, 2, 2, 1, 2, 2, 4 ),
 ( 0.000000000000000000, 0.06250000000000245637, 0.09375000000000369149, 0.1093750000000042744, 0.1250000000000048572, 0.1875000000000070499, 0.2187500000000081324, 0.2343750000000086597, 0.2421875000000089095, 0.2460937500000090206, 0.2480468750000090761, 0.2500000000000091038, 0.3125000000000100475, 0.3437500000000105471, 0.3593750000000108247, 0.3671875000000109912, 0.3710937500000111022, 0.3730468750000111022, 0.3750000000000111022, 0.4375000000000130451, 0.4687500000000140443, 0.4843750000000145439, 0.4921875000000148770, 0.4960937500000149325, 0.4980468750000149880, 0.5000000000000149880, 0.5625000000000126565, 0.5937500000000114353, 0.6093750000000108802, 0.6171875000000106581, 0.6250000000000105471, 0.7500000000000069944, 0.8125000000000053291, 0.8437500000000044409, 0.8750000000000035527, 1.000000000000000000 ),
 .UNSPECIFIED. ) ;
#14246=EDGE_CURVE ( 'NONE', #23264, #18727, #15652, .T. ) ;
#14247=CARTESIAN_POINT ( 'NONE',  ( 17.53481375730999758, 8.357543471651000644, -3.927243979254000372 ) ) ;
#14249=DIRECTION ( 'NONE',  ( -1.000000000000000000, 0.000000000000000000, 0.000000000000000000 ) ) ;
#14251=DIRECTION ( 'NONE',  ( 0.000000000000000000, 0.000000000000000000, 1.000000000000000000 ) ) ;
#14252=VERTEX_POINT ( 'NONE', #22238 ) ;
#14253=CARTESIAN_POINT ( 'NONE',  ( -18.79994503103667469, -7.728185936305688841, 5.020550006176206281 ) ) ;
#14254=CARTESIAN_POINT ( 'NONE',  ( -11.96502059198000012, 13.67685060524999940, -6.159850446377999056 ) ) ;
#14255=CARTESIAN_POINT ( 'NONE',  ( -21.43755845894000345, -10.49164694751999960, -1.743970444100000128 ) ) ;
#14258=CARTESIAN_POINT ( 'NONE',  ( 24.50000000000000000, -9.344098705406999272, -3.489386534399999906 ) ) ;
#14260=AXIS2_PLACEMENT_3D ( 'NONE', #10042, #12101, #17298 ) ;
#14261=DIRECTION ( 'NONE',  ( 0.000000000000000000, 0.9512662730843030046, -0.3083706822840010520 ) ) ;
#14262=CARTESIAN_POINT ( 'NONE',  ( 24.43449445986659896, -9.725059455069036574, 8.155702917191968382 ) ) ;
#14265=CARTESIAN_POINT ( 'NONE',  ( -12.50000000000000000, 1.557342902441000195E-14, 0.000000000000000000 ) ) ;
#14268=CIRCLE ( 'NONE', #20064, 15.43375672974000068 ) ;
#14271=CIRCLE ( 'NONE', #17771, 4.750000000000000000 ) ;
#14272=CARTESIAN_POINT ( 'NONE',  ( 0.03709750155276533845, 11.48001782603875576, 4.817879853919041722 ) ) ;
#14274=CARTESIAN_POINT ( 'NONE',  ( 6.243179582884000212, 1.148189900220999940E-14, 0.000000000000000000 ) ) ;
#14275=EDGE_CURVE ( 'NONE', #8479, #1455, #16672, .T. ) ;
#14276=CARTESIAN_POINT ( 'NONE',  ( 3.408454823722866678, 11.96990078945976954, -3.424875488495797704 ) ) ;
#14277=CARTESIAN_POINT ( 'NONE',  ( 11.00000000000000000, 7.000000000000000000, 0.000000000000000000 ) ) ;
#14278=CIRCLE ( 'NONE', #8106, 7.500000000000000000 ) ;
#14279=CARTESIAN_POINT ( 'NONE',  ( -20.63672087121333476, -7.357712943626705027, 5.654268963819235161 ) ) ;
#14282=CARTESIAN_POINT ( 'NONE',  ( -13.03643231875999930, 10.05168146521000061, -2.584826834016999531 ) ) ;
#14283=CARTESIAN_POINT ( 'NONE',  ( 13.83187642131000139, 0.1979999634357000049, -9.644016179210000317 ) ) ;
#14284=CARTESIAN_POINT ( 'NONE',  ( 18.84514110817610089, 5.243717532068479237, 9.030486612376559918 ) ) ;
#14286=ORIENTED_EDGE ( 'NONE', *, *, #14735, .F. ) ;
#14287=ADVANCED_FACE ( 'NONE', ( #4081 ), #18456, .T. ) ;
#14288=CARTESIAN_POINT ( 'NONE',  ( 5.239091540984079920, 13.88197682617082762, 4.112037740998657043 ) ) ;
#14291=CARTESIAN_POINT ( 'NONE',  ( 13.50000000000000000, -9.063837456487554789, 4.006327031784646664 ) ) ;
#14293=EDGE_LOOP ( 'NONE', ( #3330, #14346, #19059, #2344 ) ) ;
#14297=CARTESIAN_POINT ( 'NONE',  ( -12.50000000000000000, 6.739397414018897692, -5.973639980163532925 ) ) ;
#14298=CARTESIAN_POINT ( 'NONE',  ( 14.81030506489262777, 9.856952506639157008, 3.248035065178327851 ) ) ;
#14301=CARTESIAN_POINT ( 'NONE',  ( -4.861444494134998351, 12.41891182900000601, 0.7440676659160004869 ) ) ;
#14302=CARTESIAN_POINT ( 'NONE',  ( 20.28412270046332821, -8.031631873314140080, 4.629288412270770259 ) ) ;
#14303=ORIENTED_EDGE ( 'NONE', *, *, #17844, .F. ) ;
#14304=DIRECTION ( 'NONE',  ( 1.000000000000000000, 0.000000000000000000, 0.000000000000000000 ) ) ;
#14309=EDGE_CURVE ( 'NONE', #2155, #17483, #3013, .T. ) ;
#14310=CARTESIAN_POINT ( 'NONE',  ( 6.093726023679999493, 14.50411598793998635, 0.7125610185517002870 ) ) ;
#14311=CARTESIAN_POINT ( 'NONE',  ( 11.39490977864336330, -2.886098606921414955, -12.49995748308249865 ) ) ;
#14313=AXIS2_PLACEMENT_3D ( 'NONE', #7148, #9095, #16468 ) ;
#14314=CARTESIAN_POINT ( 'NONE',  ( 6.235934676345907590, 13.70700678873121880, -1.537716637499378258 ) ) ;
#14320=CARTESIAN_POINT ( 'NONE',  ( -24.50000000000000000, 7.216878364870000340, 12.50000000000000000 ) ) ;
#14323=EDGE_CURVE ( 'NONE', #3318, #9734, #6005, .T. ) ;
#14324=CARTESIAN_POINT ( 'NONE',  ( -20.94728937253999845, -10.43362079082000093, 2.366296559912000053 ) ) ;
#14325=EDGE_CURVE ( 'NONE', #1, #16256, #20553, .T. ) ;
#14326=CARTESIAN_POINT ( 'NONE',  ( 23.99478584078000054, 7.550251870592999737, -11.73017644753999988 ) ) ;
#14327=CARTESIAN_POINT ( 'NONE',  ( 15.02841901554468684, 9.563305402470449579, 3.947719917943012025 ) ) ;
#14328=DIRECTION ( 'NONE',  ( 1.000000000000000000, 0.000000000000000000, 0.000000000000000000 ) ) ;
#14329=CARTESIAN_POINT ( 'NONE',  ( 18.68066617734999824, 0.006293508795006000009, 10.66027559447000073 ) ) ;
#14331=CARTESIAN_POINT ( 'NONE',  ( 13.60016193201688139, 6.912966986891127874, -5.794099676471392790 ) ) ;
#14332=CARTESIAN_POINT ( 'NONE',  ( -4.574431393056000772, 12.47762465527999076, -1.200270365199999523 ) ) ;
#14334=CARTESIAN_POINT ( 'NONE',  ( -21.95942920454664815, -4.650705262963104047, -8.069294568062584716 ) ) ;
#14335=ORIENTED_EDGE ( 'NONE', *, *, #19884, .F. ) ;
#14337=CARTESIAN_POINT ( 'NONE',  ( 24.50000000000000000, -9.344098705406999272, -3.489386534399999906 ) ) ;
#14338=ORIENTED_EDGE ( 'NONE', *, *, #20674, .F. ) ;
#14340=FACE_BOUND ( 'NONE', #16242, .T. ) ;
#14341=CARTESIAN_POINT ( 'NONE',  ( 24.36165043081789960, 3.174800876238617953, -12.50000000000000000 ) ) ;
#14343=CARTESIAN_POINT ( 'NONE',  ( -11.33465399291999987, 5.498006771546000593, 13.43624142368999941 ) ) ;
#14344=FACE_OUTER_BOUND ( 'NONE', #13846, .T. ) ;
#14346=ORIENTED_EDGE ( 'NONE', *, *, #17780, .T. ) ;
#14347=DIRECTION ( 'NONE',  ( -1.000000000000000000, 0.000000000000000000, 0.000000000000000000 ) ) ;
#14348=CARTESIAN_POINT ( 'NONE',  ( 20.99977027363030047, -10.24898389550873290, 2.455023892489411885 ) ) ;
#14349=CARTESIAN_POINT ( 'NONE',  ( -13.99999999999999467, -0.2201081049113881583, 9.776473952568711212 ) ) ;
#14350=CARTESIAN_POINT ( 'NONE',  ( 16.25882916898783392, -0.6197948286024473896, -10.35986595345727146 ) ) ;
#14351=CARTESIAN_POINT ( 'NONE',  ( -4.886147650005925769, 13.44678367007931818, 5.723089997228743009 ) ) ;
#14354=CARTESIAN_POINT ( 'NONE',  ( -18.60180781823000018, -9.793299576559000741, 0.7034231180304000297 ) ) ;
#14356=ORIENTED_EDGE ( 'NONE', *, *, #7178, .T. ) ;
#14357=CARTESIAN_POINT ( 'NONE',  ( 23.47552080277744935, -4.670392666604991305, 8.100843789317771382 ) ) ;
#14358=CARTESIAN_POINT ( 'NONE',  ( 11.53663804755082190, 12.55807338460112454, -3.248594360998799502 ) ) ;
#14359=DIRECTION ( 'NONE',  ( 0.000000000000000000, 1.000000000000000000, 0.000000000000000000 ) ) ;
#14361=ORIENTED_EDGE ( 'NONE', *, *, #15236, .F. ) ;
#14362=CARTESIAN_POINT ( 'NONE',  ( 24.07420734439589083, -7.985988878874604069, -11.16786151310754960 ) ) ;
#14364=CARTESIAN_POINT ( 'NONE',  ( 2.398621549960997967, 11.68146935173001033, -4.243417778616998426 ) ) ;
#14365=EDGE_LOOP ( 'NONE', ( #4924, #10974, #7968, #12467, #2486 ) ) ;
#14366=CARTESIAN_POINT ( 'NONE',  ( 18.19293875730999943, -2.463108239980999592, 8.917637382198998708 ) ) ;
#14367=ORIENTED_EDGE ( 'NONE', *, *, #11634, .F. ) ;
#14372=DIRECTION ( 'NONE',  ( 0.7071067811866525998, 0.000000000000000000, -0.7071067811864425456 ) ) ;
#14373=CARTESIAN_POINT ( 'NONE',  ( -4.792894583204066805, 15.72849393113409633, -3.814013712966466407 ) ) ;
#14374=CARTESIAN_POINT ( 'NONE',  ( -21.91931851383999685, -0.7111562311954999771, 10.62484833929000061 ) ) ;
#14375=CARTESIAN_POINT ( 'NONE',  ( -17.99572818580000089, -1.813981674565000146, -9.633252329321001284 ) ) ;
#14376=CARTESIAN_POINT ( 'NONE',  ( -4.850296048403001770, 13.26922248379001523, -5.932245385413001948 ) ) ;
#14377=CARTESIAN_POINT ( 'NONE',  ( -22.74900695987042099, -4.110693411953544540, -9.728987031145388542 ) ) ;
#14379=DIRECTION ( 'NONE',  ( -1.000000000000000000, 0.000000000000000000, 0.000000000000000000 ) ) ;
#14380=EDGE_CURVE ( 'NONE', #8826, #4536, #7831, .T. ) ;
#14382=EDGE_LOOP ( 'NONE', ( #7207, #16965, #17703, #14417 ) ) ;
#14385=AXIS2_PLACEMENT_3D ( 'NONE', #18357, #11220, #12897 ) ;
#14386=CARTESIAN_POINT ( 'NONE',  ( 4.829987487923999900, 14.79876397742000016, -3.766541047082999860 ) ) ;
#14388=CARTESIAN_POINT ( 'NONE',  ( -3.673647344300186468, 12.04674575989788465, 3.146065391725001881 ) ) ;
#14391=CARTESIAN_POINT ( 'NONE',  ( 4.834782059083999606, 12.44497316928999808, -0.3759403457470999466 ) ) ;
#14392=EDGE_CURVE ( 'NONE', #19829, #5746, #19411, .T. ) ;
#14393=CARTESIAN_POINT ( 'NONE',  ( 24.26191870746986012, 6.808678168838079969, -6.906054575474446011 ) ) ;
#14395=VERTEX_POINT ( 'NONE', #18851 ) ;
#14396=FACE_OUTER_BOUND ( 'NONE', #8763, .T. ) ;
#14397=DIRECTION ( 'NONE',  ( -1.000000000000000000, 0.000000000000000000, 0.000000000000000000 ) ) ;
#14398=CARTESIAN_POINT ( 'NONE',  ( 12.40593892130999976, 9.405156509668998410, -1.966610333673999955 ) ) ;
#14399=CARTESIAN_POINT ( 'NONE',  ( 18.72471403812598467, 8.467466865290406375, 6.090674659130430157 ) ) ;
#14402=CARTESIAN_POINT ( 'NONE',  ( -6.042815982636000172, 21.50000000000000000, -1.000000000000000000 ) ) ;
#14403=CARTESIAN_POINT ( 'NONE',  ( 18.50983580085999947, 11.40398223831000024, 0.8544022015744000553 ) ) ;
#14404=CARTESIAN_POINT ( 'NONE',  ( 13.50000000000000533, -6.340245170342347691, 7.979342322378518482 ) ) ;
#14407=CARTESIAN_POINT ( 'NONE',  ( 24.55082877617000037, -5.845823156057000425, 8.945057363882000345 ) ) ;
#14408=EDGE_CURVE ( 'NONE', #20281, #7389, #6969, .T. ) ;
#14409=CARTESIAN_POINT ( 'NONE',  ( -23.95278192272984086, -1.063754273011168205, 9.723242869295845026 ) ) ;
#14410=CARTESIAN_POINT ( 'NONE',  ( 13.61158555497621947, -7.958227948172696742, 6.606147741580802979 ) ) ;
#14411=CARTESIAN_POINT ( 'NONE',  ( -3.978825713501787931, 13.87455081233140497, 4.851109908756392919 ) ) ;
#14412=CARTESIAN_POINT ( 'NONE',  ( -4.573911348824003298, 12.37758549377001671, 1.892950700447998402 ) ) ;
#14413=DIRECTION ( 'NONE',  ( 0.000000000000000000, 1.000000000000000000, 0.000000000000000000 ) ) ;
#14415=FACE_OUTER_BOUND ( 'NONE', #15179, .T. ) ;
#14417=ORIENTED_EDGE ( 'NONE', *, *, #16936, .T. ) ;
#14421=CARTESIAN_POINT ( 'NONE',  ( 12.06371966923812522, -5.117452910095027896, -12.50009924164533182 ) ) ;
#14423=CARTESIAN_POINT ( 'NONE',  ( 19.58133333333332970, 3.621958592900809126, 8.534357609150490021 ) ) ;
#14425=VERTEX_POINT ( 'NONE', #13880 ) ;
#14427=PLANE ( 'NONE',  #14784 ) ;
#14428=DIRECTION ( 'NONE',  ( 0.000000000000000000, 1.000000000000000000, 0.000000000000000000 ) ) ;
#14429=ORIENTED_EDGE ( 'NONE', *, *, #2403, .T. ) ;
#14430=CARTESIAN_POINT ( 'NONE',  ( -20.09045569450000102, 9.845892643941999367, -4.125506862962999399 ) ) ;
#14432=CARTESIAN_POINT ( 'NONE',  ( 14.60105817408460638, 4.787368022142956647, -9.159926853143835146 ) ) ;
#14433=CARTESIAN_POINT ( 'NONE',  ( -7.834000000000000519, 10.59999999999999964, 0.000000000000000000 ) ) ;
#14434=CARTESIAN_POINT ( 'NONE',  ( 20.45495348602999997, 1.509263456234000156, 11.10181671682000015 ) ) ;
#14437=CARTESIAN_POINT ( 'NONE',  ( 13.60079008836671477, 6.926023288026004643, -5.778502639464679014 ) ) ;
#14439=CARTESIAN_POINT ( 'NONE',  ( -6.504405627207126450, 15.46487054860210364, -1.467966815537356196 ) ) ;
#14441=CARTESIAN_POINT ( 'NONE',  ( -21.73267920454664903, 2.415784607553221441, -8.988730734449054793 ) ) ;
#14445=VERTEX_POINT ( 'NONE', #8197 ) ;
#14447=CARTESIAN_POINT ( 'NONE',  ( 17.01429166666665083, 1.192094632364767870, -9.107901970610145170 ) ) ;
#14451=CARTESIAN_POINT ( 'NONE',  ( 18.44875144328999994, 10.74386948049999901, 2.882141228404999644 ) ) ;
#14452=ORIENTED_EDGE ( 'NONE', *, *, #3651, .T. ) ;
#14453=CARTESIAN_POINT ( 'NONE',  ( -9.385278638770000015, -0.05147163365328999429, -15.21832980031999938 ) ) ;
#14454=CARTESIAN_POINT ( 'NONE',  ( 13.50000000000000000, 5.478253366763097709, 8.484493166734903724 ) ) ;
#14456=ORIENTED_EDGE ( 'NONE', *, *, #16439, .F. ) ;
#14458=CARTESIAN_POINT ( 'NONE',  ( 21.91162244696776540, 10.46836026662980679, -2.349396852667112956 ) ) ;
#14460=CARTESIAN_POINT ( 'NONE',  ( 16.10403698457205834, -5.878893883532452236, -8.533248856027976004 ) ) ;
#14462=CARTESIAN_POINT ( 'NONE',  ( -4.900699999999999612, 1.284663064832999817E-14, 0.000000000000000000 ) ) ;
#14466=CARTESIAN_POINT ( 'NONE',  ( -18.43943555148999991, -2.412201287215999912, -10.06532802039999908 ) ) ;
#14469=CARTESIAN_POINT ( 'NONE',  ( -24.33938584177210984, -2.815218398150926671, 12.49992678696526127 ) ) ;
#14470=CARTESIAN_POINT ( 'NONE',  ( 19.44804762184721270, -10.50094980715322635, 0.1342334127711540259 ) ) ;
#14471=FACE_OUTER_BOUND ( 'NONE', #15723, .T. ) ;
#14472=B_SPLINE_CURVE_WITH_KNOTS ( 'NONE', 3,
 ( #13602, #17367, #4409, #19180, #4170, #2589, #18943, #768, #13724, #21122 ),
 .UNSPECIFIED., .F., .F.,
 ( 4, 2, 2, 2, 4 ),
 ( 0.000000000000000000, 0.2500000000000001110, 0.5000000000000001110, 0.7500000000000001110, 1.000000000000000000 ),
 .UNSPECIFIED. ) ;
#14476=CARTESIAN_POINT ( 'NONE',  ( 24.34804274388851297, -9.160073233599486997, -9.134287758352421349 ) ) ;
#14477=CARTESIAN_POINT ( 'NONE',  ( 4.926165394784816520, 14.31396120642910930, -3.835254638722358500 ) ) ;
#14478=CARTESIAN_POINT ( 'NONE',  ( -4.917002979092000459, 12.44024335427998906, -0.01122529268158000207 ) ) ;
#14480=DIRECTION ( 'NONE',  ( 0.000000000000000000, 1.000000000000000000, 0.000000000000000000 ) ) ;
#14481=CIRCLE ( 'NONE', #2098, 15.43375672974000068 ) ;
#14482=ORIENTED_EDGE ( 'NONE', *, *, #23448, .F. ) ;
#14483=CARTESIAN_POINT ( 'NONE',  ( -4.123153084920957667, 15.07815051851633825, 4.529465602894293674 ) ) ;
#14486=CARTESIAN_POINT ( 'NONE',  ( -15.15692920454666570, -7.916761560459355529, 4.562790735126731612 ) ) ;
#14488=CARTESIAN_POINT ( 'NONE',  ( -19.67110492428000157, -10.05584626669999970, 0.0004483298532730999866 ) ) ;
#14490=CARTESIAN_POINT ( 'NONE',  ( 18.63933333333331888, -4.608031391969340085, -7.994750628324704955 ) ) ;
#14491=CARTESIAN_POINT ( 'NONE',  ( -22.77474208561820390, -4.966028226955915947, -9.323134938704122021 ) ) ;
#14494=FACE_OUTER_BOUND ( 'NONE', #21220, .T. ) ;
#14496=EDGE_LOOP ( 'NONE', ( #5802, #19080, #3779, #1542, #8458 ) ) ;
#14497=CARTESIAN_POINT ( 'NONE',  ( -17.42442920454667998, 4.592095577738842138, 7.967605896327013326 ) ) ;
#14502=CARTESIAN_POINT ( 'NONE',  ( 2.418195492079564968, 11.72965300045306414, 4.174376928245445484 ) ) ;
#14503=ORIENTED_EDGE ( 'NONE', *, *, #22210, .F. ) ;
#14504=CARTESIAN_POINT ( 'NONE',  ( -1.969571242956765111, 11.64777130037908393, -4.396811160587570377 ) ) ;
#14511=CARTESIAN_POINT ( 'NONE',  ( 15.80625142131000160, 5.282396774718000287, -8.133049213409000444 ) ) ;
#14512=CARTESIAN_POINT ( 'NONE',  ( 18.69530137406649928, 9.024773782881792883, 5.230709212474926595 ) ) ;
#14516=CARTESIAN_POINT ( 'NONE',  ( 17.49421080085999947, -10.89330037972999854, 3.387123339711000103 ) ) ;
#14517=DIRECTION ( 'NONE',  ( -0.9999999999922942751, 3.925717498811976060E-06, 6.459656137320962354E-09 ) ) ;
#14521=CARTESIAN_POINT ( 'NONE',  ( 21.63524950958999682, -9.258690811328998294, -5.498005089659000255 ) ) ;
#14523=CARTESIAN_POINT ( 'NONE',  ( -24.17459695600129876, 8.825400305006976254, 4.719873724747784216 ) ) ;
#14525=CARTESIAN_POINT ( 'NONE',  ( -3.898965866421516324, 13.96122025683682288, 4.845918179761490308 ) ) ;
#14526=CARTESIAN_POINT ( 'NONE',  ( 4.940723035539999586, 12.51282731614000276, -0.1566769263144998925 ) ) ;
#14528=EDGE_LOOP ( 'NONE', ( #1646, #20530, #23566, #9768, #13877 ) ) ;
#14531=ORIENTED_EDGE ( 'NONE', *, *, #6857, .F. ) ;
#14533=CARTESIAN_POINT ( 'NONE',  ( 5.428958415689999484, 14.69816721964000195, 2.857937668952999832 ) ) ;
#14535=CARTESIAN_POINT ( 'NONE',  ( 19.45483333333332610, 6.898272746453336879, 6.189253307314870334 ) ) ;
#14537=EDGE_CURVE ( 'NONE', #7164, #1236, #21396, .T. ) ;
#14539=ORIENTED_EDGE ( 'NONE', *, *, #7041, .F. ) ;
#14544=CARTESIAN_POINT ( 'NONE',  ( -20.84844433051999957, -6.396441138360000167, -9.216716464522999530 ) ) ;
#14546=CARTESIAN_POINT ( 'NONE',  ( 14.66409083246537470, 6.614115962116787095, -7.929118690434196814 ) ) ;
#14547=DIRECTION ( 'NONE',  ( -1.000000000000000000, 0.000000000000000000, 0.000000000000000000 ) ) ;
#14548=CARTESIAN_POINT ( 'NONE',  ( 20.74819667979999949, 1.510347020690999909, 11.10979287247999991 ) ) ;
#14550=EDGE_CURVE ( 'NONE', #8738, #20461, #796, .T. ) ;
#14551=CARTESIAN_POINT ( 'NONE',  ( 13.98171503422127238, 7.305407177158877552, 5.378490655644252882 ) ) ;
#14556=CARTESIAN_POINT ( 'NONE',  ( -15.00576253787999903, -9.056359154562001024, 0.000000000000000000 ) ) ;
#14558=B_SPLINE_CURVE_WITH_KNOTS ( 'NONE', 3,
 ( #5055, #20054, #3691, #8800, #1532, #12886, #16162, #7087, #14477, #12551, #19936, #10618, #23564, #3580, #49, #20287, #22098, #3470, #1642, #3355, #20172, #10734, #16400, #9029, #14589 ),
 .UNSPECIFIED., .F., .F.,
 ( 4, 2, 2, 1, 2, 2, 2, 2, 1, 1, 2, 2, 2, 4 ),
 ( 0.000000000000000000, 0.2499999999999427125, 0.3749999999999121258, 0.4374999999998951949, 0.4687499999998844813, 0.4999999999998737676, 0.6249999999998363531, 0.6874999999998204769, 0.7187499999998154809, 0.7343749999998131495, 0.7421874999998120392, 0.7499999999998109290, 0.8749999999999055200, 1.000000000000000000 ),
 .UNSPECIFIED. ) ;
#14559=ADVANCED_FACE ( 'NONE', ( #2495 ), #8438, .T. ) ;
#14561=CARTESIAN_POINT ( 'NONE',  ( 21.72020603379665360, 2.415700825681953656, 8.988418979289773958 ) ) ;
#14562=CIRCLE ( 'NONE', #5305, 13.77250448648999637 ) ;
#14563=FACE_OUTER_BOUND ( 'NONE', #19814, .T. ) ;
#14564=CARTESIAN_POINT ( 'NONE',  ( -14.39083492636570583, 4.156485310037820291, 9.484860138480087244 ) ) ;
#14566=EDGE_CURVE ( 'NONE', #15625, #13107, #1863, .T. ) ;
#14568=VECTOR ( 'NONE', #21725, 1000.000000000000000 ) ;
#14569=CARTESIAN_POINT ( 'NONE',  ( -11.93821506584999881, 12.87565757039999959, -7.434806685507000523 ) ) ;
#14570=CARTESIAN_POINT ( 'NONE',  ( 13.49999999999999822, 5.804425006068715476, 8.246010899024623697 ) ) ;
#14571=CARTESIAN_POINT ( 'NONE',  ( -14.38789236265223437, -12.88903867673619885, -2.675117728967849384 ) ) ;
#14573=CARTESIAN_POINT ( 'NONE',  ( 20.47030772137050647, 5.028569603156692658, 9.244401094538714503 ) ) ;
#14574=FACE_OUTER_BOUND ( 'NONE', #7821, .T. ) ;
#14575=CARTESIAN_POINT ( 'NONE',  ( 15.97284269412691060, -9.008167718500386556, -5.113775645086368726 ) ) ;
#14579=VECTOR ( 'NONE', #7897, 1000.000000000000000 ) ;
#14585=CARTESIAN_POINT ( 'NONE',  ( 20.38436928271863025, 10.48308585629694711, 0.9317613066503177555 ) ) ;
#14587=ORIENTED_EDGE ( 'NONE', *, *, #10473, .F. ) ;
#14589=CARTESIAN_POINT ( 'NONE',  ( 4.829987487923999900, 14.79876397742000016, -3.766541047082999860 ) ) ;
#14590=CARTESIAN_POINT ( 'NONE',  ( -4.466956411286998829, 12.27369686073000032, -2.063459869057001406 ) ) ;
#14594=EDGE_CURVE ( 'NONE', #11381, #19819, #6088, .T. ) ;
#14595=ORIENTED_EDGE ( 'NONE', *, *, #22115, .F. ) ;
#14598=DIRECTION ( 'NONE',  ( 0.000000000000000000, -1.000000000000000000, 0.000000000000000000 ) ) ;
#14601=CARTESIAN_POINT ( 'NONE',  ( -15.83717920454666483, 8.841378262663962317, 2.376184731017836782 ) ) ;
#14602=CARTESIAN_POINT ( 'NONE',  ( -24.59729957373000175, 9.304297380551000529, -4.183949263271999897 ) ) ;
#14604=CARTESIAN_POINT ( 'NONE',  ( 18.33699999999999974, -9.141845273363999880, 1.095420050962999850E-14 ) ) ;
#14606=DIRECTION ( 'NONE',  ( -0.9996708941621513800, 0.02565352539213145919, 0.000000000000000000 ) ) ;
#14610=ORIENTED_EDGE ( 'NONE', *, *, #17551, .F. ) ;
#14612=CARTESIAN_POINT ( 'NONE',  ( -22.26176253788000281, -9.242562415387000740, 0.000000000000000000 ) ) ;
#14613=CARTESIAN_POINT ( 'NONE',  ( 5.302309017544000191, 13.73032573480000096, -4.450985556070999216 ) ) ;
#14617=DIRECTION ( 'NONE',  ( -1.000000000000000000, 0.000000000000000000, 0.000000000000000000 ) ) ;
#14620=CARTESIAN_POINT ( 'NONE',  ( -3.184315894841176053, 11.90921843639853606, -3.629752879533585386 ) ) ;
#14625=CARTESIAN_POINT ( 'NONE',  ( -14.25243324638999809, 13.93375672974000068, -0.8660254037843999608 ) ) ;
#14627=CARTESIAN_POINT ( 'NONE',  ( 15.28425158531000072, -8.882884205749999040, 4.999858360703999693 ) ) ;
#14628=CARTESIAN_POINT ( 'NONE',  ( 18.59693257352302354, 10.26249244534900029, 1.842170885552584902 ) ) ;
#14631=CARTESIAN_POINT ( 'NONE',  ( 24.25008227645999881, 0.000000000000000000, 0.000000000000000000 ) ) ;
#14632=CARTESIAN_POINT ( 'NONE',  ( 13.49999999999999645, -9.595521044434660141, 1.928683791516291324 ) ) ;
#14633=ORIENTED_EDGE ( 'NONE', *, *, #2236, .F. ) ;
#14635=CARTESIAN_POINT ( 'NONE',  ( 20.12460122230999815, 9.191763640279999592, -6.496768647051000656 ) ) ;
#14636=VECTOR ( 'NONE', #2672, 1000.000000000000000 ) ;
#14638=DIRECTION ( 'NONE',  ( 1.000000000000000000, 0.000000000000000000, 0.000000000000000000 ) ) ;
#14642=CARTESIAN_POINT ( 'NONE',  ( -12.24999999999999822, 13.59206128970241778, -6.344557540553090291 ) ) ;
#14644=ORIENTED_CLOSED_SHELL ( 'NONE', *, #8877, .F. );
#14645=CARTESIAN_POINT ( 'NONE',  ( -24.48285595303000051, -9.947371647070999856, -3.562228079131000147 ) ) ;
#14646=ORIENTED_EDGE ( 'NONE', *, *, #13824, .F. ) ;
#14647=LINE ( 'NONE', #8737, #12705 ) ;
#14651=CARTESIAN_POINT ( 'NONE',  ( 6.379286604629002433, 13.55943310907999688, 1.863575392949001763 ) ) ;
#14652=CARTESIAN_POINT ( 'NONE',  ( 11.07373617191544923, -0.5001676861130824880, -12.49996440465594993 ) ) ;
#14653=DIRECTION ( 'NONE',  ( -1.000000000000000000, 0.000000000000000000, 0.000000000000000000 ) ) ;
#14655=CARTESIAN_POINT ( 'NONE',  ( 18.38193924931000112, 10.76489784149000251, -0.6396482201651000343 ) ) ;
#14658=CARTESIAN_POINT ( 'NONE',  ( -15.00576253787999903, -9.056359154562001024, 0.000000000000000000 ) ) ;
#14659=AXIS2_PLACEMENT_3D ( 'NONE', #15365, #22756, #15491 ) ;
#14662=ORIENTED_EDGE ( 'NONE', *, *, #10699, .T. ) ;
#14663=CARTESIAN_POINT ( 'NONE',  ( -19.36326595524999661, -10.58611661219999966, 1.843048566446000125 ) ) ;
#14665=CARTESIAN_POINT ( 'NONE',  ( 14.76958591329545989, 9.026438462397976537, -5.017364683716268203 ) ) ;
#14667=CARTESIAN_POINT ( 'NONE',  ( -10.04281598263999875, 20.50000000000000000, -1.000000000000000000 ) ) ;
#14668=CARTESIAN_POINT ( 'NONE',  ( 18.82728777423999844, 0.006295662015650000005, 10.66412175315999988 ) ) ;
#14669=FACE_OUTER_BOUND ( 'NONE', #15134, .T. ) ;
#14670=CARTESIAN_POINT ( 'NONE',  ( 13.69915933970933963, 8.483254755539659797, -3.069216687506281183 ) ) ;
#14671=CARTESIAN_POINT ( 'NONE',  ( 4.517650654553999168, 12.53108973233999457, -1.707274550749000364 ) ) ;
#14672=CONICAL_SURFACE ( 'NONE', #10823, 9.157130689899000586, 0.02565634000431304615 ) ;
#14675=CARTESIAN_POINT ( 'NONE',  ( -14.60220935799346265, -1.520255290742261733, -8.953970405129554777 ) ) ;
#14676=CARTESIAN_POINT ( 'NONE',  ( -14.23150127962423994, -7.645023867421874009, 6.980454963417014547 ) ) ;
#14678=VECTOR ( 'NONE', #14606, 1000.000000000000000 ) ;
#14681=CARTESIAN_POINT ( 'NONE',  ( 11.18574820343480525, -11.70054794218647842, -4.734095432798069325 ) ) ;
#14682=CARTESIAN_POINT ( 'NONE',  ( 21.49345603379665093, 8.058846013972555511, 4.644683092982796246 ) ) ;
#14683=CARTESIAN_POINT ( 'NONE',  ( 13.54274790051000110, -0.4384800474203000564, 10.98015942592999927 ) ) ;
#14684=CARTESIAN_POINT ( 'NONE',  ( 23.99062354302999722, 6.216878364870000340, -12.50000000000000000 ) ) ;
#14687=ORIENTED_EDGE ( 'NONE', *, *, #5997, .F. ) ;
#14688=CARTESIAN_POINT ( 'NONE',  ( -9.487101138770000830, -6.342674860076999543, -13.83369712466000045 ) ) ;
#14689=CARTESIAN_POINT ( 'NONE',  ( 13.50000000000000178, 8.918778220045556537, -2.986288483409031524 ) ) ;
#14692=CARTESIAN_POINT ( 'NONE',  ( 23.76474137987780111, 10.57295235097301145, -0.8683397068570842814 ) ) ;
#14693=CARTESIAN_POINT ( 'NONE',  ( 24.37713355803436599, 9.330746210554012876, -8.838673490789293652 ) ) ;
#14694=CARTESIAN_POINT ( 'NONE',  ( 16.18775596657570048, -3.143559382843135630, -9.875345798663321517 ) ) ;
#14695=CARTESIAN_POINT ( 'NONE',  ( -18.95478082342999926, -4.545484222122999185, -10.15604107551000013 ) ) ;
#14697=VECTOR ( 'NONE', #20900, 1000.000000000000000 ) ;
#14698=CARTESIAN_POINT ( 'NONE',  ( -15.55485259867999837, 4.780789984251000213, 8.479691756156000793 ) ) ;
#14699=EDGE_CURVE ( 'NONE', #3590, #17463, #11526, .T. ) ;
#14701=ORIENTED_EDGE ( 'NONE', *, *, #19465, .F. ) ;
#14703=CARTESIAN_POINT ( 'NONE',  ( 20.55460958469728538, 8.198441454514611593, 6.607155824187043613 ) ) ;
#14704=CARTESIAN_POINT ( 'NONE',  ( -14.00000000000000000, -15.45000000000000107, 0.000000000000000000 ) ) ;
#14707=CARTESIAN_POINT ( 'NONE',  ( 4.834946199837999892, 12.42232141699000181, 0.1060585776307999689 ) ) ;
#14708=EDGE_LOOP ( 'NONE', ( #7976, #14361, #5626, #22642 ) ) ;
#14709=EDGE_CURVE ( 'NONE', #10709, #16663, #19708, .T. ) ;
#14710=CARTESIAN_POINT ( 'NONE',  ( 14.57325125730999993, -2.690795753208000018, 8.752124397991998705 ) ) ;
#14711=ORIENTED_EDGE ( 'NONE', *, *, #5047, .T. ) ;
#14712=CARTESIAN_POINT ( 'NONE',  ( -5.057059693511116727, 15.90694920458252071, 3.455692463001508230 ) ) ;
#14716=CARTESIAN_POINT ( 'NONE',  ( -20.31345166415999870, 6.452540530572000499, 8.416401568578999459 ) ) ;
#14717=CARTESIAN_POINT ( 'NONE',  ( 11.90008533511957367, -8.504566836174662470, -10.26973740115090017 ) ) ;
#14718=CARTESIAN_POINT ( 'NONE',  ( -5.273521783973994737, 14.65714449329999702, -3.721049535021002441 ) ) ;
#14719=CARTESIAN_POINT ( 'NONE',  ( -23.36664997781829456, -5.995105419842714944, 8.715914855933332817 ) ) ;
#14727=CARTESIAN_POINT ( 'NONE',  ( -18.99854661335000117, -6.966878364870000340, -12.06698729810999993 ) ) ;
#14728=CARTESIAN_POINT ( 'NONE',  ( 4.616100662420898004, 13.51152904214929684, -5.077026504744428514 ) ) ;
#14729=CARTESIAN_POINT ( 'NONE',  ( -24.23230866834131447, 0.5965514821640681697, -10.58710619923159335 ) ) ;
#14732=CARTESIAN_POINT ( 'NONE',  ( 4.797639067608940877, 12.42995552893798994, 0.8516731598688934701 ) ) ;
#14734=CARTESIAN_POINT ( 'NONE',  ( -0.6749559008190714193, 11.50211200430284464, -4.764868824692928939 ) ) ;
#14735=EDGE_CURVE ( 'NONE', #16006, #3092, #19824, .T. ) ;
#14736=DIRECTION ( 'NONE',  ( 0.9999999999999453770, -3.279696922991151128E-07, -4.019963350050187028E-08 ) ) ;
#14737=EDGE_CURVE ( 'NONE', #20461, #6021, #3781, .T. ) ;
#14739=ORIENTED_EDGE ( 'NONE', *, *, #3061, .F. ) ;
#14740=LINE ( 'NONE', #7467, #1063 ) ;
#14741=B_SPLINE_CURVE_WITH_KNOTS ( 'NONE', 3,
 ( #10713, #12645, #23774, #18104, #10945, #23891, #18222, #8901, #17982, #9011, #3213, #5377, #14689, #12418, #1510, #3452, #8651, #10597, #16268, #8777, #23660, #1384, #22081, #16015, #12528, #20154, #1741, #7070, #1623, #16382, #5148, #16138, #23541, #19917, #3332, #5489, #6953, #14570, #14454, #7297, #20034, #16500, #7176, #21848 ),
 .UNSPECIFIED., .F., .F.,
 ( 4, 1, 1, 1, 1, 1, 2, 2, 1, 1, 1, 1, 1, 2, 2, 1, 1, 1, 1, 2, 2, 2, 1, 1, 2, 2, 1, 1, 2, 2, 4 ),
 ( 0.000000000000000000, 0.1249999999999985567, 0.1874999999999978906, 0.2187499999999975575, 0.2343749999999973632, 0.2421874999999973355, 0.2460937499999973355, 0.2499999999999973355, 0.3124999999999971134, 0.3437499999999970024, 0.3593749999999969469, 0.3671874999999969469, 0.3710937499999969469, 0.3730468749999968914, 0.3749999999999968914, 0.4374999999999970579, 0.4687499999999971134, 0.4843749999999971689, 0.4921874999999972244, 0.4960937499999972244, 0.4999999999999972244, 0.6249999999999978906, 0.6874999999999982236, 0.7187499999999984457, 0.7343749999999985567, 0.7499999999999985567, 0.8124999999999988898, 0.8437499999999990008, 0.8593749999999992228, 0.8749999999999993339, 1.000000000000000000 ),
 .UNSPECIFIED. ) ;
#14742=CARTESIAN_POINT ( 'NONE',  ( 17.58768908531000008, -3.881224882977999613, -9.490963515925001204 ) ) ;
#14743=CARTESIAN_POINT ( 'NONE',  ( 18.81497143630078384, 6.186105294716906400, 8.399328565840326277 ) ) ;
#14746=FACE_OUTER_BOUND ( 'NONE', #23481, .T. ) ;
#14747=CARTESIAN_POINT ( 'NONE',  ( 13.50000000000000178, -7.996356175792731058, 6.080764513117456360 ) ) ;
#14750=CARTESIAN_POINT ( 'NONE',  ( 21.10410220312999741, -2.836328727688000040, 10.37276910986000011 ) ) ;
#14753=CARTESIAN_POINT ( 'NONE',  ( -11.04281598264000053, 1.359882291614000008E-14, 0.000000000000000000 ) ) ;
#14754=CARTESIAN_POINT ( 'NONE',  ( 24.49999999999999645, 4.566319020512484173, 9.204673959736052069 ) ) ;
#14755=CARTESIAN_POINT ( 'NONE',  ( 4.326177836376999153, 12.22448935855999430, 2.345174457005999802 ) ) ;
#14757=CARTESIAN_POINT ( 'NONE',  ( -20.30574230851999928, 6.911969653458998941, -8.632951638288000495 ) ) ;
#14759=ORIENTED_EDGE ( 'NONE', *, *, #5856, .F. ) ;
#14761=CARTESIAN_POINT ( 'NONE',  ( 4.820143762837000523, 14.15667339170999739, 4.018455007228999065 ) ) ;
#14762=CARTESIAN_POINT ( 'NONE',  ( 11.72559253309821514, -4.116598456382959625, -12.49995860919746171 ) ) ;
#14763=CARTESIAN_POINT ( 'NONE',  ( -14.00000000000000000, 10.59999999999999964, 0.000000000000000000 ) ) ;
#14765=CARTESIAN_POINT ( 'NONE',  ( 15.28425158531000072, -8.882884205749999040, 4.999858360703999693 ) ) ;
#14766=CIRCLE ( 'NONE', #14385, 3.850000000000000977 ) ;
#14768=ORIENTED_EDGE ( 'NONE', *, *, #5954, .F. ) ;
#14769=CARTESIAN_POINT ( 'NONE',  ( -18.73722805020999616, -7.945584595330000610, 4.815966472443999891 ) ) ;
#14770=DIRECTION ( 'NONE',  ( -0.9996708941621516020, 0.02565352539211874019, 3.461521573581829412E-14 ) ) ;
#14773=CARTESIAN_POINT ( 'NONE',  ( -10.05754950027480810, 16.19676296412049510, -1.000000000000009992 ) ) ;
#14775=CARTESIAN_POINT ( 'NONE',  ( 14.54050418697157632, 2.709612435072900727, -9.959934958062799382 ) ) ;
#14776=CARTESIAN_POINT ( 'NONE',  ( 3.000000000000000000, 20.00000000000000000, 0.000000000000000000 ) ) ;
#14777=CARTESIAN_POINT ( 'NONE',  ( 24.01511664711999927, 10.71773449166999903, -3.585769948605999957 ) ) ;
#14779=CARTESIAN_POINT ( 'NONE',  ( 13.72233838329553990, 8.705364101347321082, -2.397688811983387680 ) ) ;
#14780=CARTESIAN_POINT ( 'NONE',  ( 0.3670138381986997600, 11.65918066382002216, -4.834738583209002627 ) ) ;
#14782=CARTESIAN_POINT ( 'NONE',  ( 21.49165366772000141, -3.200527125370999926, -10.97220403775999920 ) ) ;
#14783=ORIENTED_EDGE ( 'NONE', *, *, #5645, .F. ) ;
#14784=AXIS2_PLACEMENT_3D ( 'NONE', #14320, #7044, #12265 ) ;
#14789=CARTESIAN_POINT ( 'NONE',  ( 21.87137270046332915, -2.416481638450508118, 8.992294409326092364 ) ) ;
#14790=CARTESIAN_POINT ( 'NONE',  ( 18.77582393802000382, 7.032165450859999112, 8.630870596427000052 ) ) ;
#14791=DIRECTION ( 'NONE',  ( -1.000000000000000000, 0.000000000000000000, 0.000000000000000000 ) ) ;
#14794=CARTESIAN_POINT ( 'NONE',  ( -10.00358756584999931, 4.021542441345999919, 14.31380562870000084 ) ) ;
#14797=ADVANCED_FACE ( 'NONE', ( #1292 ), #287, .F. ) ;
#14798=ORIENTED_EDGE ( 'NONE', *, *, #3900, .T. ) ;
#14799=CARTESIAN_POINT ( 'NONE',  ( -23.74465998031000069, 7.716878364870000340, 11.63397459621999985 ) ) ;
#14800=CARTESIAN_POINT ( 'NONE',  ( 20.05850351405853260, 9.867115815705442827, -3.636978922065039033 ) ) ;
#14802=CARTESIAN_POINT ( 'NONE',  ( 24.43449445986659896, 9.725059455069036574, -8.155702917191968382 ) ) ;
#14803=CARTESIAN_POINT ( 'NONE',  ( 15.93942490395575895, -9.558381615799778075, -3.992934203908755197 ) ) ;
#14804=CARTESIAN_POINT ( 'NONE',  ( -17.32881098813999898, -9.732670078718998141, -5.300370996713000160 ) ) ;
#14806=CARTESIAN_POINT ( 'NONE',  ( -16.16424364259000157, 4.823843515939000071, -8.474820356344999084 ) ) ;
#14809=ORIENTED_EDGE ( 'NONE', *, *, #14594, .F. ) ;
#14811=CARTESIAN_POINT ( 'NONE',  ( 22.56911982475166312, 2.085580828976256740, 10.36943491226754510 ) ) ;
#14814=CARTESIAN_POINT ( 'NONE',  ( 24.36165043081787118, -3.174800876238296876, 12.50000000000000178 ) ) ;
#14815=CARTESIAN_POINT ( 'NONE',  ( -14.25546138242000005, -6.466299263714999412, -12.35599677691000053 ) ) ;
#14816=CARTESIAN_POINT ( 'NONE',  ( -14.00000000000000000, -10.29545622790075754, 0.7917248717053737561 ) ) ;
#14817=CARTESIAN_POINT ( 'NONE',  ( 15.01200125731000057, -8.889299820566000321, -2.243156938537000045 ) ) ;
#14818=ORIENTED_EDGE ( 'NONE', *, *, #1856, .F. ) ;
#14823=CARTESIAN_POINT ( 'NONE',  ( -15.76159587121333061, 7.930222888495088718, 4.570839928504368821 ) ) ;
#14824=CARTESIAN_POINT ( 'NONE',  ( -3.922083573187000294, 12.31548052424001760, 2.678017928241000600 ) ) ;
#14825=CARTESIAN_POINT ( 'NONE',  ( -22.29709339959999781, -5.613794202598000105, 7.812648601633999768 ) ) ;
#14826=CARTESIAN_POINT ( 'NONE',  ( -14.13625157436999835, 5.599074946036999734, -7.913639695747000324 ) ) ;
#14827=CARTESIAN_POINT ( 'NONE',  ( 18.97945833333333354, 5.628133138040521288, -7.323704213949056019 ) ) ;
#14828=CARTESIAN_POINT ( 'NONE',  ( -19.66079187015698437, -8.028560904012943311, 6.742129426872167208 ) ) ;
#14829=DIRECTION ( 'NONE',  ( 0.000000000000000000, -1.000000000000000000, 0.000000000000000000 ) ) ;
#14836=CARTESIAN_POINT ( 'NONE',  ( -17.84603743917333674, 1.195142481609348328, -9.129246206417464649 ) ) ;
#14837=CARTESIAN_POINT ( 'NONE',  ( 19.01495727369000122, -0.2433744186648999774, -9.751344288430999541 ) ) ;
#14838=CARTESIAN_POINT ( 'NONE',  ( 13.56234160357046292, -2.191821534187185172, -8.802344811741308561 ) ) ;
#14839=CARTESIAN_POINT ( 'NONE',  ( -23.83066304303370941, 10.51063228770324542, -1.301520733571610133 ) ) ;
#14843=B_SPLINE_CURVE_WITH_KNOTS ( 'NONE', 3,
 ( #12008, #12127, #8734, #6662, #8860, #6547, #18058, #10184, #23621, #19637, #2803, #6784, #3171, #6909, #14302, #1219, #12250, #4987 ),
 .UNSPECIFIED., .F., .F.,
 ( 4, 2, 2, 2, 2, 2, 2, 2, 4 ),
 ( 0.000000000000000000, 0.1250000000000000555, 0.2500000000000000555, 0.3750000000000000000, 0.4999999999999999445, 0.6249999999999998890, 0.7500000000000000000, 0.8750000000000000000, 1.000000000000000000 ),
 .UNSPECIFIED. ) ;
#14844=CARTESIAN_POINT ( 'NONE',  ( 1.027876147065865720, 11.52789889760357056, 4.702132543716095014 ) ) ;
#14845=VERTEX_POINT ( 'NONE', #11388 ) ;
#14846=EDGE_CURVE ( 'NONE', #23190, #13740, #17306, .T. ) ;
#14847=CARTESIAN_POINT ( 'NONE',  ( -4.677864609647151894, 12.38500653705287213, -1.270735910758368448 ) ) ;
#14848=CARTESIAN_POINT ( 'NONE',  ( 24.37713355803437310, 12.31988888405492411, 3.661326509212557756 ) ) ;
#14850=VERTEX_POINT ( 'NONE', #1199 ) ;
#14851=ADVANCED_FACE ( 'NONE', ( #3024 ), #21057, .F. ) ;
#14852=ADVANCED_FACE ( 'NONE', ( #17433, #19495 ), #827, .T. ) ;
#14854=CARTESIAN_POINT ( 'NONE',  ( 14.51643908531000093, 10.16840836635999956, -0.3108424006793999994 ) ) ;
#14855=CARTESIAN_POINT ( 'NONE',  ( 18.39730916115231096, 9.079266745650221182, -5.115270949334341566 ) ) ;
#14858=CARTESIAN_POINT ( 'NONE',  ( 18.10358580085999947, 2.698449212464999913, -11.10147659952999888 ) ) ;
#14862=CARTESIAN_POINT ( 'NONE',  ( 21.98934771389999909, 2.052024005812999707, -10.58059816497999961 ) ) ;
#14863=EDGE_CURVE ( 'NONE', #22092, #14929, #20269, .T. ) ;
#14867=CARTESIAN_POINT ( 'NONE',  ( 24.50000000000000355, -6.535120425047818316, 8.327193666827611196 ) ) ;
#14868=CARTESIAN_POINT ( 'NONE',  ( 24.49999999999999645, 3.559007953318558570, 9.649945607071924059 ) ) ;
#14869=AXIS2_PLACEMENT_3D ( 'NONE', #5352, #14547, #1487 ) ;
#14870=CARTESIAN_POINT ( 'NONE',  ( -4.833494663361999066, 12.42176095785000456, -0.1505369627506999708 ) ) ;
#14872=CARTESIAN_POINT ( 'NONE',  ( -22.14367231210000142, 6.201338001754999496, -9.216948840397998666 ) ) ;
#14877=ORIENTED_EDGE ( 'NONE', *, *, #23927, .F. ) ;
#14879=CARTESIAN_POINT ( 'NONE',  ( 6.642147691535001286, 13.49920999050998915, -0.06642214614436001141 ) ) ;
#14882=CARTESIAN_POINT ( 'NONE',  ( -19.55887123173999953, -9.833822427806001798, 3.504477313184999776 ) ) ;
#14884=CARTESIAN_POINT ( 'NONE',  ( -19.04882659540000134, -6.818301851232999589, 6.682161380682999585 ) ) ;
#14885=CIRCLE ( 'NONE', #4059, 12.50000000000000178 ) ;
#14888=ORIENTED_EDGE ( 'NONE', *, *, #3604, .F. ) ;
#14889=CARTESIAN_POINT ( 'NONE',  ( -11.04281598264000053, 15.31903517202000131, -1.878299281600999793 ) ) ;
#14891=CARTESIAN_POINT ( 'NONE',  ( 14.77323574787787486, 9.091559497059186867, -4.898520349509332128 ) ) ;
#14892=CARTESIAN_POINT ( 'NONE',  ( -18.21805420454666802, -1.196138244234058678, -9.138792889823502463 ) ) ;
#14893=CARTESIAN_POINT ( 'NONE',  ( 21.44545916559000176, -11.00422963065999937, -2.246136312581000105 ) ) ;
#14895=EDGE_CURVE ( 'NONE', #5364, #2324, #15480, .T. ) ;
#14896=CARTESIAN_POINT ( 'NONE',  ( 14.23798725250559905, 0.5470205452132217427, 9.070214828626342651 ) ) ;
#14897=CARTESIAN_POINT ( 'NONE',  ( -0.5877938013789001381, 11.67164471879000764, -4.806037769057001974 ) ) ;
#14900=CARTESIAN_POINT ( 'NONE',  ( 11.22311500624865666, 9.824279701796063691, -7.983827916320604956 ) ) ;
#14904=ORIENTED_EDGE ( 'NONE', *, *, #6152, .F. ) ;
#14905=CARTESIAN_POINT ( 'NONE',  ( 24.36414987671881605, 9.252522660948818256, 8.974160653052738468 ) ) ;
#14907=CARTESIAN_POINT ( 'NONE',  ( 14.83973348638000189, 10.43777180253000125, 3.549999712421000098 ) ) ;
#14908=DIRECTION ( 'NONE',  ( 0.000000000000000000, 0.000000000000000000, 1.000000000000000000 ) ) ;
#14911=VERTEX_POINT ( 'NONE', #4843 ) ;
#14912=CARTESIAN_POINT ( 'NONE',  ( -11.42172863877000033, -11.83666328600000028, 9.565249431252999202 ) ) ;
#14915=ORIENTED_EDGE ( 'NONE', *, *, #10462, .F. ) ;
#14916=CARTESIAN_POINT ( 'NONE',  ( 19.98391666666666211, -7.737224675997203427, 5.060929617072193132 ) ) ;
#14917=CARTESIAN_POINT ( 'NONE',  ( 20.23499103147737799, 10.17266449058678646, 2.686287595386958493 ) ) ;
#14918=VECTOR ( 'NONE', #14117, 1000.000000000000114 ) ;
#14919=CARTESIAN_POINT ( 'NONE',  ( 6.236038179533940351, 13.70719429076894258, 1.534876996671144189 ) ) ;
#14920=CARTESIAN_POINT ( 'NONE',  ( 16.07974732740592927, -6.562937474929119830, -8.053821228520819275 ) ) ;
#14921=CARTESIAN_POINT ( 'NONE',  ( -17.83675921509000162, -8.097439812444001461, 7.586755343379000038 ) ) ;
#14923=CARTESIAN_POINT ( 'NONE',  ( -14.41758667332000066, 9.911104062797001291, 4.224474430483999399 ) ) ;
#14927=CARTESIAN_POINT ( 'NONE',  ( 20.63972973568440850, 5.922841969177226495, 8.703777380504034156 ) ) ;
#14928=CARTESIAN_POINT ( 'NONE',  ( -18.02253305375739245, -2.690258673799740041, 10.10105386629687807 ) ) ;
#14929=VERTEX_POINT ( 'NONE', #23228 ) ;
#14931=CARTESIAN_POINT ( 'NONE',  ( -4.771322057965996954, 13.13584649598000276, 5.062208158195999452 ) ) ;
#14932=AXIS2_PLACEMENT_3D ( 'NONE', #3278, #17440, #18831 ) ;
#14933=CARTESIAN_POINT ( 'NONE',  ( 17.84570833333332374, 1.195141376095346430, 9.129237760912879196 ) ) ;
#14934=CARTESIAN_POINT ( 'NONE',  ( 16.57406392130999961, -0.9113449805282999305, 9.675305505412000073 ) ) ;
#14936=CARTESIAN_POINT ( 'NONE',  ( -4.676970228494227833, 15.63772976374162837, 3.955111732555046000 ) ) ;
#14938=ORIENTED_EDGE ( 'NONE', *, *, #17321, .T. ) ;
#14940=CARTESIAN_POINT ( 'NONE',  ( -22.87210175995843642, 9.258583067823760615, -6.329161777784410158E-06 ) ) ;
#14941=CARTESIAN_POINT ( 'NONE',  ( -4.379988357423000522, 12.47718658113000778, 1.827485537232998336 ) ) ;
#14943=CARTESIAN_POINT ( 'NONE',  ( 12.00000000000000178, 0.4474594423088819051, -9.306393149668425124 ) ) ;
#14946=CARTESIAN_POINT ( 'NONE',  ( -19.84093775038680718, -2.572085328615516087, 10.16682444507051919 ) ) ;
#14948=AXIS2_PLACEMENT_3D ( 'NONE', #5807, #2055, #18648 ) ;
#14952=ORIENTED_EDGE ( 'NONE', *, *, #1252, .F. ) ;
#14953=CARTESIAN_POINT ( 'NONE',  ( 18.04870260588999997, 2.058813593266999753, 8.790077575217999595 ) ) ;
#14954=CARTESIAN_POINT ( 'NONE',  ( 14.74456678153594069, -5.921751136246636626, 6.913021773282147286 ) ) ;
#14956=CARTESIAN_POINT ( 'NONE',  ( -23.00059541739830138, -9.779468793944952054, 4.009870837034711144 ) ) ;
#14959=VECTOR ( 'NONE', #14736, 1000.000000000000114 ) ;
#14960=CARTESIAN_POINT ( 'NONE',  ( 2.791333439079350498, 11.81165397714371146, 3.935739769649145181 ) ) ;
#14962=CARTESIAN_POINT ( 'NONE',  ( -2.134135751890048560, 11.67542832177916168, -4.323373072577085807 ) ) ;
#14963=DIRECTION ( 'NONE',  ( 0.000000000000000000, -1.000000000000000000, 0.000000000000000000 ) ) ;
#14965=CARTESIAN_POINT ( 'NONE',  ( 4.834778359340923259, 12.44818675736157942, 0.2493437057047861172 ) ) ;
#14970=CARTESIAN_POINT ( 'NONE',  ( 16.05206408531000051, 5.563243567929000655, -8.565419716155998842 ) ) ;
#14973=CARTESIAN_POINT ( 'NONE',  ( 15.25983580085999947, 2.106191207965000256, 11.14826357266000123 ) ) ;
#14974=LINE ( 'NONE', #4091, #15067 ) ;
#14977=EDGE_CURVE ( 'NONE', #7629, #259, #10375, .T. ) ;
#14979=CARTESIAN_POINT ( 'NONE',  ( 19.94755212015000012, 3.776176937002000411, -10.59849602182999995 ) ) ;
#14983=CARTESIAN_POINT ( 'NONE',  ( 12.24709585780000154, -6.475684366039000217, -6.720579761511999983 ) ) ;
#14984=CARTESIAN_POINT ( 'NONE',  ( 24.50000000000000000, 7.523013873557660602, 6.698426195502327651 ) ) ;
#14985=CARTESIAN_POINT ( 'NONE',  ( 4.717414079990003728, 12.37669079585000098, 1.093762868586999559 ) ) ;
#14988=CARTESIAN_POINT ( 'NONE',  ( -23.27233823477999763, -8.296294695444000666, 7.433816105003999475 ) ) ;
#14993=CARTESIAN_POINT ( 'NONE',  ( 5.665862463139001548, 13.86305811703000757, 2.702659249994999069 ) ) ;
#14999=CARTESIAN_POINT ( 'NONE',  ( 13.44600174930999970, -1.304103625722999871, 10.57402029614000050 ) ) ;
#15002=CARTESIAN_POINT ( 'NONE',  ( -15.18934998397000058, -10.25623436264999988, -0.2727227130009000078 ) ) ;
#15003=LINE ( 'NONE', #11034, #20999 ) ;
#15005=CARTESIAN_POINT ( 'NONE',  ( -14.48875654244860378, -1.295999377397418328, 12.49999522859940448 ) ) ;
#15008=CARTESIAN_POINT ( 'NONE',  ( -19.99161065248000213, 7.877179509649999467, 7.955496492617000648 ) ) ;
#15010=CARTESIAN_POINT ( 'NONE',  ( 13.86823306426570745, -9.092836708730331452, 4.860699923063548589 ) ) ;
#15014=CARTESIAN_POINT ( 'NONE',  ( 14.33953349908450647, -2.586167250888467883, 8.677503207046257216 ) ) ;
#15015=CARTESIAN_POINT ( 'NONE',  ( 16.95684930358444120, 1.053055326748374654, 10.37866837094156658 ) ) ;
#15018=CARTESIAN_POINT ( 'NONE',  ( 11.70388046503181556, 12.85079422502293411, -2.741654745597553955 ) ) ;
#15025=CARTESIAN_POINT ( 'NONE',  ( 24.45564077607145137, 9.795255522623715905, 8.034119761694611839 ) ) ;
#15028=CARTESIAN_POINT ( 'NONE',  ( 15.38108617992000049, -6.523058388743000258, 8.906538625892999050 ) ) ;
#15029=DIRECTION ( 'NONE',  ( -1.000000000000000000, 0.000000000000000000, 0.000000000000000000 ) ) ;
#15031=EDGE_CURVE ( 'NONE', #8738, #3791, #2247, .T. ) ;
#15035=CARTESIAN_POINT ( 'NONE',  ( -11.61799971169000045, -12.10921122026999974, 9.785496380100999758 ) ) ;
#15037=CARTESIAN_POINT ( 'NONE',  ( 17.92512270046333711, 6.868744509127599152, 6.162759146932331511 ) ) ;
#15038=EDGE_LOOP ( 'NONE', ( #21339, #17615, #17938, #22655 ) ) ;
#15039=CARTESIAN_POINT ( 'NONE',  ( -14.44600786774907952, 9.403896164508505962, 8.711943152823643288 ) ) ;
#15040=CARTESIAN_POINT ( 'NONE',  ( 19.23489509943002318, -10.47072900379253468, 0.6798073259081474085 ) ) ;
#15042=CARTESIAN_POINT ( 'NONE',  ( 15.58016428004055243, -6.894168022670424278, 7.716933635784287482 ) ) ;
#15043=CARTESIAN_POINT ( 'NONE',  ( -18.77411750838999893, 2.263382236681999782, -10.88922404772999997 ) ) ;
#15047=VECTOR ( 'NONE', #10549, 1000.000000000000114 ) ;
#15048=CARTESIAN_POINT ( 'NONE',  ( -14.21445632535000136, 4.821896674351999756, 9.628268207709998805 ) ) ;
#15050=ORIENTED_EDGE ( 'NONE', *, *, #491, .F. ) ;
#15052=CARTESIAN_POINT ( 'NONE',  ( -24.50000000000000000, -5.823431203803898448, -8.822395769081024852 ) ) ;
#15053=CARTESIAN_POINT ( 'NONE',  ( -18.31192479224129954, 7.074229065390446713, 7.702880875266950866 ) ) ;
#15054=ORIENTED_EDGE ( 'NONE', *, *, #22236, .F. ) ;
#15055=CARTESIAN_POINT ( 'NONE',  ( -12.06624327026013077, -13.93375672973986745, 0.000000000000000000 ) ) ;
#15056=CARTESIAN_POINT ( 'NONE',  ( -5.152812823547000320, 16.37978035709998892, 3.507589799060998548 ) ) ;
#15057=CARTESIAN_POINT ( 'NONE',  ( -14.00000000000000000, -10.27687089286999900, -0.6428416445564000270 ) ) ;
#15059=CARTESIAN_POINT ( 'NONE',  ( 11.72137625731000021, -1.402369408125999861, -8.972525410429000203 ) ) ;
#15060=ORIENTED_EDGE ( 'NONE', *, *, #10326, .F. ) ;
#15061=DIRECTION ( 'NONE',  ( -1.000000000000000000, 0.000000000000000000, 0.000000000000000000 ) ) ;
#15065=CARTESIAN_POINT ( 'NONE',  ( -23.44771454634823726, -3.885502164501489997, -8.583207962873803609 ) ) ;
#15066=CARTESIAN_POINT ( 'NONE',  ( -4.183799302787003960, 12.40606742070998791, 2.243501369777998189 ) ) ;
#15067=VECTOR ( 'NONE', #4329, 1000.000000000000000 ) ;
#15068=CARTESIAN_POINT ( 'NONE',  ( 12.00000000000000000, 3.374757925648287138, -8.478241236122538993 ) ) ;
#15069=CARTESIAN_POINT ( 'NONE',  ( -14.47793699669672485, 9.918738539663852549, -7.820229401565270244 ) ) ;
#15070=CARTESIAN_POINT ( 'NONE',  ( -4.901394592536002293, 15.57359934946000379, -3.198976673040998087 ) ) ;
#15075=CARTESIAN_POINT ( 'NONE',  ( 23.51229047600000044, 8.801584319611000851, 5.566787828605999522 ) ) ;
#15076=CARTESIAN_POINT ( 'NONE',  ( 3.192791986568791707, 13.14721640538022918, -5.956854817651988654 ) ) ;
#15078=CARTESIAN_POINT ( 'NONE',  ( -21.50111841624438824, -1.002880873098122017, 10.61775532178399395 ) ) ;
#15081=ORIENTED_EDGE ( 'NONE', *, *, #2376, .T. ) ;
#15082=CARTESIAN_POINT ( 'NONE',  ( -18.29840813844436198, 10.40894792496784937, 1.972660505488252225 ) ) ;
#15085=CARTESIAN_POINT ( 'NONE',  ( -14.00000000000000000, 8.507292963980999545, 3.029321241734000303 ) ) ;
#15087=CARTESIAN_POINT ( 'NONE',  ( 16.92956408530999823, -4.671063266616000575, 9.108730853067999789 ) ) ;
#15089=CARTESIAN_POINT ( 'NONE',  ( -19.55803988934999893, -9.263500284663999551, 5.614856615822000130 ) ) ;
#15090=CARTESIAN_POINT ( 'NONE',  ( -19.54076253787999562, 9.172736192578000214, 0.000000000000000000 ) ) ;
#15091=CARTESIAN_POINT ( 'NONE',  ( 15.93739037305999950, -10.16690263577000053, 3.715714698119999770 ) ) ;
#15092=CARTESIAN_POINT ( 'NONE',  ( 13.49999999999999822, -8.302679662493304136, -4.371739577444137659 ) ) ;
#15095=CARTESIAN_POINT ( 'NONE',  ( 25.01064428847000087, 5.914600320551000934, 7.816648658713001296 ) ) ;
#15096=CARTESIAN_POINT ( 'NONE',  ( 23.99478584076000232, 13.93375672974000068, 0.6736217020456000126 ) ) ;
#15098=CARTESIAN_POINT ( 'NONE',  ( 11.47745461310999993, -6.461451563261999986, -6.705806860117999868 ) ) ;
#15099=CARTESIAN_POINT ( 'NONE',  ( -4.900699999999999612, 1.284663064832999817E-14, 0.000000000000000000 ) ) ;
#15101=CARTESIAN_POINT ( 'NONE',  ( -4.780243194648996941, 12.47971992104001515, 0.1257369525371998809 ) ) ;
#15102=CARTESIAN_POINT ( 'NONE',  ( 17.71428936713000013, 9.125865291226999076, 0.000000000000000000 ) ) ;
#15104=CARTESIAN_POINT ( 'NONE',  ( -24.44193005524000029, -0.7742905126174000063, -11.14459677524999925 ) ) ;
#15106=CARTESIAN_POINT ( 'NONE',  ( 19.05233531832000082, -1.887707665395999879, 10.26617185442000135 ) ) ;
#15108=CARTESIAN_POINT ( 'NONE',  ( -23.74465998031000069, 6.216878364870000340, -12.50000000000000000 ) ) ;
#15111=CARTESIAN_POINT ( 'NONE',  ( 16.65612270046333876, -7.950280935925901460, 4.582400664091437648 ) ) ;
#15112=CARTESIAN_POINT ( 'NONE',  ( -12.25000000000000000, 6.613190111079999767, -13.46349570337000046 ) ) ;
#15114=CARTESIAN_POINT ( 'NONE',  ( -13.36117685223999985, -10.17969989951000009, -0.7718705306884999784 ) ) ;
#15116=CARTESIAN_POINT ( 'NONE',  ( -14.44600785535404164, -2.842816319682948123, 12.49998455206137216 ) ) ;
#15117=ADVANCED_FACE ( 'NONE', ( #301, #17145 ), #13155, .F. ) ;
#15120=B_SPLINE_CURVE_WITH_KNOTS ( 'NONE', 3,
 ( #19349, #2628, #15569, #11835, #6130, #2500, #20796, #13884, #11960, #17527, #20919, #679, #2381, #12084, #10022, #2757, #13522, #8085 ),
 .UNSPECIFIED., .F., .F.,
 ( 4, 2, 2, 2, 2, 2, 2, 2, 4 ),
 ( 0.000000000000000000, 0.1250000000000000833, 0.2500000000000001665, 0.3750000000000001665, 0.5000000000000002220, 0.6250000000000002220, 0.7500000000000001110, 0.8750000000000001110, 1.000000000000000000 ),
 .UNSPECIFIED. ) ;
#15123=CARTESIAN_POINT ( 'NONE',  ( 14.36117453097103969, -3.509108449906709115, -9.716323635631455957 ) ) ;
#15126=CARTESIAN_POINT ( 'NONE',  ( 11.10357421856130777, 0.9986522863256600546, 12.49997040257240677 ) ) ;
#15127=CARTESIAN_POINT ( 'NONE',  ( -6.780563428402626158, 15.32813791308405449, -1.804059136873557012 ) ) ;
#15128=CARTESIAN_POINT ( 'NONE',  ( -6.723317613688290173, 15.34808456536819321, 1.731702247723928112 ) ) ;
#15129=EDGE_CURVE ( 'NONE', #1991, #8639, #7260, .T. ) ;
#15131=ORIENTED_EDGE ( 'NONE', *, *, #5622, .F. ) ;
#15132=CARTESIAN_POINT ( 'NONE',  ( -14.50606933757998718, 1.515976823860569755, -8.914235622657752600 ) ) ;
#15134=EDGE_LOOP ( 'NONE', ( #3300, #16755, #13806, #19873 ) ) ;
#15135=CARTESIAN_POINT ( 'NONE',  ( -15.99424577250664647, 2.377239741907454906, -8.845303993649501706 ) ) ;
#15137=CARTESIAN_POINT ( 'NONE',  ( 24.28455689590255062, 8.829963675777257492, 9.706054284564595847 ) ) ;
#15139=ORIENTED_EDGE ( 'NONE', *, *, #20951, .F. ) ;
#15140=CARTESIAN_POINT ( 'NONE',  ( 15.70815867464999904, -10.50977832323999905, 3.408686822334999533 ) ) ;
#15146=CARTESIAN_POINT ( 'NONE',  ( -13.99999999999999822, -9.377543214584244780, -3.820245374186972853 ) ) ;
#15148=CARTESIAN_POINT ( 'NONE',  ( -11.71982221168999949, -6.976145074222000808, 13.91841713096999911 ) ) ;
#15150=CARTESIAN_POINT ( 'NONE',  ( -12.25000000000000000, -15.45000000000000107, 0.000000000000000000 ) ) ;
#15151=EDGE_CURVE ( 'NONE', #13107, #5409, #20662, .T. ) ;
#15153=CARTESIAN_POINT ( 'NONE',  ( -19.77404557170999766, 5.276082107202000770, -8.045024713292999508 ) ) ;
#15154=EDGE_CURVE ( 'NONE', #1842, #6975, #2773, .T. ) ;
#15155=CARTESIAN_POINT ( 'NONE',  ( 19.78341666666665688, -2.704778927495326002, 8.835500971703069695 ) ) ;
#15156=CARTESIAN_POINT ( 'NONE',  ( 6.157060429383564681, 14.08832693936469838, 0.3628293340486281604 ) ) ;
#15157=CARTESIAN_POINT ( 'NONE',  ( 15.67870979658231612, -9.071254133873747350, 4.986216261053892040 ) ) ;
#15158=CARTESIAN_POINT ( 'NONE',  ( -13.71554468751000044, -9.276193085472000277, -4.453008734943000313 ) ) ;
#15161=CARTESIAN_POINT ( 'NONE',  ( -15.18934998397000058, -10.25623436264999988, -0.2727227130009000078 ) ) ;
#15164=ORIENTED_EDGE ( 'NONE', *, *, #1140, .T. ) ;
#15168=CARTESIAN_POINT ( 'NONE',  ( -19.06434331229947077, -2.167475688756183683, -10.25766573832537532 ) ) ;
#15169=VERTEX_POINT ( 'NONE', #19698 ) ;
#15173=CARTESIAN_POINT ( 'NONE',  ( 16.46437642130999990, 2.740937500800999960, 9.320585551182000827 ) ) ;
#15176=CARTESIAN_POINT ( 'NONE',  ( -5.951915486294003799, 16.41431975584002245, -1.007191989855000358 ) ) ;
#15177=CARTESIAN_POINT ( 'NONE',  ( 24.35625626386761056, -12.44383109334005866, 3.446652305529492200 ) ) ;
#15178=B_SPLINE_SURFACE_WITH_KNOTS ( 'NONE', 3, 3, ( 
 ( #6822, #23536, #17861, #21958, #1620, #8771, #19798, #3207, #6950, #21731, #9121, #5029, #18218, #17977, #21613, #10590, #21844, #21486, #1379, #5371, #5145, #3556, #10941, #12525, #20029, #23657, #10476, #12287, #12760, #8646, #23405, #23770, #8897, #3329, #18328 ),
 ( #14090, #4898, #16265, #7065, #14451, #3448, #5256, #12640, #23285, #19676, #6698, #10833, #3089, #1257, #9008, #16378, #7172, #11178, #9589, #18441, #23884, #15028, #13330, #20264, #14907, #13216, #11533, #7291, #20729, #3788, #4134, #18563, #3667, #20610, #4019 ),
 ( #20501, #2195, #1849, #14790, #9351, #3905, #7656, #2081, #16725, #18912, #22300, #18675, #22426, #18787, #16974, #9471, #375, #11415, #11298, #2320, #15140, #1967, #7773, #22537, #7525, #250, #11055, #135, #5716, #5943, #16494, #13103, #14683, #22076, #5832 ),
 ( #16847, #5484, #24, #5599, #12864, #9238, #16616, #7409, #22185, #12980, #20380, #19272, #7891, #607, #22893, #4628, #17092, #17209, #9944, #4266, #977, #12017, #19143, #6189, #13575, #17330, #2554, #12135, #15383, #19398, #4379, #8009, #20969, #8257, #15260 ) ),
 .UNSPECIFIED., .F., .F., .F.,
 ( 4, 4 ),
 ( 4, 1, 1, 1, 1, 1, 1, 1, 1, 1, 1, 1, 1, 1, 1, 1, 1, 1, 1, 1, 1, 1, 1, 1, 1, 1, 1, 1, 1, 1, 1, 1, 4 ),
 ( -0.6000240009601000013, 1.600024000959999970 ),
 ( -0.01645136390613000099, 0.01028210244132999988, 0.03701556878879000423, 0.06374903513624000095, 0.09048250148370000356, 0.1172159678312000020, 0.1439494341785999831, 0.1706829005261000232, 0.1974163668735000043, 0.2241498332209999889, 0.2508832995683999978, 0.2776167659159000101, 0.3043502322632999912, 0.3310836986108000035, 0.3578171649583000158, 0.3845506313056999970, 0.4112840976532000092, 0.4380175640006000459, 0.4647510303481000027, 0.4914844966954999839, 0.5182179630430000516, 0.5449514293905000084, 0.5716848957378999341, 0.5984183620854000019, 0.6251518284328000385, 0.6518852947802999953, 0.6786187611276999210, 0.7053522274751999888, 0.7320856938227000565, 0.7588191601701000932, 0.7855526265175999390, 0.8122860928649999757, 0.8390195592125000434 ),
 .UNSPECIFIED. ) ;
#15179=EDGE_LOOP ( 'NONE', ( #335, #12826, #18535, #7269, #5135, #5107 ) ) ;
#15180=CARTESIAN_POINT ( 'NONE',  ( -6.838539683285000059, 15.31903379280000088, 1.878299112549000061 ) ) ;
#15182=CARTESIAN_POINT ( 'NONE',  ( 3.683742661130003704, 12.24911308434999313, 3.113368964028000896 ) ) ;
#15184=CARTESIAN_POINT ( 'NONE',  ( 12.00000000000000355, 3.681377102019148584, -8.330751794720166359 ) ) ;
#15186=CARTESIAN_POINT ( 'NONE',  ( -3.634800904028002932, 14.60524886664999045, -4.947590794463004649 ) ) ;
#15188=CARTESIAN_POINT ( 'NONE',  ( 5.287285710763609536, 13.80050360415835264, -4.264351677957034958 ) ) ;
#15192=CARTESIAN_POINT ( 'NONE',  ( -18.03499577250666164, -4.599986451907970952, -7.981296679855804044 ) ) ;
#15193=CARTESIAN_POINT ( 'NONE',  ( 22.49347407775999841, -5.087491083399999781, -8.435107541370999940 ) ) ;
#15194=CARTESIAN_POINT ( 'NONE',  ( -0.06326846155994279852, 12.80354232408877380, -6.663658787853194099 ) ) ;
#15195=CARTESIAN_POINT ( 'NONE',  ( -23.68078907432000335, -9.459496811531000304, -9.754788243598999975E-09 ) ) ;
#15196=CARTESIAN_POINT ( 'NONE',  ( -22.14375141673819414, 9.048573216601598190, -5.684411342799975841 ) ) ;
#15199=CARTESIAN_POINT ( 'NONE',  ( 12.50897733419000168, -6.466910458125999739, 12.35564390364999987 ) ) ;
#15200=ORIENTED_EDGE ( 'NONE', *, *, #16612, .T. ) ;
#15201=CARTESIAN_POINT ( 'NONE',  ( -19.07992278086221205, -8.501993143676337183, -6.120330979234422486 ) ) ;
#15207=CARTESIAN_POINT ( 'NONE',  ( 14.21381424931000126, -3.754242569768000415, -9.992333729823998922 ) ) ;
#15208=CARTESIAN_POINT ( 'NONE',  ( -15.56314304594000042, -8.450047992442000222, -7.564511025612000061 ) ) ;
#15209=CARTESIAN_POINT ( 'NONE',  ( -10.04701370329000021, 16.31160201364000173, 0.9999999999983000265 ) ) ;
#15210=CARTESIAN_POINT ( 'NONE',  ( 14.85358580085999947, 11.33114005906999999, -0.2613888308919999903 ) ) ;
#15212=FACE_OUTER_BOUND ( 'NONE', #10325, .T. ) ;
#15213=CARTESIAN_POINT ( 'NONE',  ( 25.30572612538999877, -3.463782304174999993, 8.743710282844000758 ) ) ;
#15218=CARTESIAN_POINT ( 'NONE',  ( 4.837505978036000798, 12.42333062333001514, -0.02305947804070000370 ) ) ;
#15219=CARTESIAN_POINT ( 'NONE',  ( 11.00000000000000000, 10.59999999999999964, 0.000000000000000000 ) ) ;
#15220=CARTESIAN_POINT ( 'NONE',  ( -22.60400005165999815, 0.1503115455820999702, -11.12042372740999951 ) ) ;
#15221=ORIENTED_EDGE ( 'NONE', *, *, #9318, .F. ) ;
#15223=ORIENTED_EDGE ( 'NONE', *, *, #5008, .T. ) ;
#15224=EDGE_CURVE ( 'NONE', #18376, #9517, #13791, .T. ) ;
#15225=CARTESIAN_POINT ( 'NONE',  ( -24.16119556694614090, 4.108075931972949846, -12.49973851150938309 ) ) ;
#15228=CARTESIAN_POINT ( 'NONE',  ( 16.20262270046332631, 4.576539695569029398, 7.940112068752367414 ) ) ;
#15230=CARTESIAN_POINT ( 'NONE',  ( 13.88475174931000033, -10.63832449705000016, -0.7632376485559000390 ) ) ;
#15232=CARTESIAN_POINT ( 'NONE',  ( -14.57995894006000093, 5.497579849475999758, -8.642519878353001062 ) ) ;
#15233=CARTESIAN_POINT ( 'NONE',  ( 14.57325125730999993, -2.690795753208000018, 8.752124397991998705 ) ) ;
#15234=CARTESIAN_POINT ( 'NONE',  ( -14.32799115069592588, 5.161629268601040543, 12.49976764739585455 ) ) ;
#15235=VERTEX_POINT ( 'NONE', #11948 ) ;
#15236=EDGE_CURVE ( 'NONE', #20281, #1220, #16881, .T. ) ;
#15239=CARTESIAN_POINT ( 'NONE',  ( 14.26932110114051966, -6.379006366603656275, -8.140519857586468788 ) ) ;
#15240=CONICAL_SURFACE ( 'NONE', #9079, 9.787173237795000702, 0.7982263333994560339 ) ;
#15242=CARTESIAN_POINT ( 'NONE',  ( 3.182410876788997367, 13.14747453192001103, -5.653946747832996778 ) ) ;
#15244=CARTESIAN_POINT ( 'NONE',  ( 12.06371966926070805, 5.117452910143472700, 12.50009924165165742 ) ) ;
#15245=CARTESIAN_POINT ( 'NONE',  ( 18.37858639674107408, 10.40198410867141376, 1.159838069824709939 ) ) ;
#15253=EDGE_CURVE ( 'NONE', #17, #14047, #14562, .T. ) ;
#15254=CARTESIAN_POINT ( 'NONE',  ( -5.735278047652040634, 16.24235446318282072, -2.150590259619544753 ) ) ;
#15257=CARTESIAN_POINT ( 'NONE',  ( -6.250000000000000000, 15.73203524433000311, -1.185075242810999852 ) ) ;
#15259=VECTOR ( 'NONE', #7756, 1000.000000000000227 ) ;
#15260=CARTESIAN_POINT ( 'NONE',  ( 13.50891859955000029, 5.685114405159000128, 8.584150509224999226 ) ) ;
#15261=PLANE ( 'NONE',  #23347 ) ;
#15264=ORIENTED_EDGE ( 'NONE', *, *, #1069, .T. ) ;
#15265=CARTESIAN_POINT ( 'NONE',  ( -14.00000000000000178, 5.758787634741540096, -7.178423725779616404 ) ) ;
#15266=CARTESIAN_POINT ( 'NONE',  ( -11.41435471169000060, -15.33547020656999926, -2.685570560817000185 ) ) ;
#15271=CARTESIAN_POINT ( 'NONE',  ( -22.75980177062999843, -4.975256557067000429, 8.932912903997999976 ) ) ;
#15272=CARTESIAN_POINT ( 'NONE',  ( -14.42499013958002507, 12.50426282926201793, 3.341925919227497488 ) ) ;
#15273=CARTESIAN_POINT ( 'NONE',  ( 6.191435500673191150, 13.91538564218064522, 0.8033750926635572220 ) ) ;
#15274=CARTESIAN_POINT ( 'NONE',  ( 15.75535489895502828, -10.05762403353078405, 2.456177552663034280 ) ) ;
#15275=CARTESIAN_POINT ( 'NONE',  ( -19.24802401720000233, -4.548766302313999255, -10.16337245253999910 ) ) ;
#15277=CARTESIAN_POINT ( 'NONE',  ( -17.70843032205999990, -8.525337246235000777, 7.569901604118999927 ) ) ;
#15282=CARTESIAN_POINT ( 'NONE',  ( -18.97752579075431356, 0.9511254547103566992, -10.58491024144955794 ) ) ;
#15285=CARTESIAN_POINT ( 'NONE',  ( -4.015026692432003053, 15.25594080015998344, 4.668998453457999354 ) ) ;
#15287=CARTESIAN_POINT ( 'NONE',  ( -13.99999999999999822, -9.925668012745248348, 2.740213007417764413 ) ) ;
#15289=CARTESIAN_POINT ( 'NONE',  ( 12.40593892130999976, 9.405156509668998410, -1.966610333673999955 ) ) ;
#15291=VECTOR ( 'NONE', #9433, 1000.000000000000000 ) ;
#15292=CARTESIAN_POINT ( 'NONE',  ( -6.335698864392003138, 16.42991352047999243, -1.007191989855000358 ) ) ;
#15293=CARTESIAN_POINT ( 'NONE',  ( 23.99478584078000054, 7.550251870568999379, 11.73017644755000077 ) ) ;
#15294=VERTEX_POINT ( 'NONE', #21387 ) ;
#15296=DIRECTION ( 'NONE',  ( 0.000000000000000000, -6.254561278618000321E-11, -1.000000000000000000 ) ) ;
#15297=CARTESIAN_POINT ( 'NONE',  ( 12.04708237232646262, 8.300001991022620373, 10.62407327353252917 ) ) ;
#15298=CARTESIAN_POINT ( 'NONE',  ( 4.724321909639998651, 12.53663613935000853, -0.02272734326504999985 ) ) ;
#15300=CARTESIAN_POINT ( 'NONE',  ( 18.32366523450733808, 7.502789789981919810, -7.229229197467324397 ) ) ;
#15301=CARTESIAN_POINT ( 'NONE',  ( 11.99999999999999822, 0.3765524563881427200, -9.313981971731278620 ) ) ;
#15302=CARTESIAN_POINT ( 'NONE',  ( 19.52828936713000019, 9.172416106433001204, 0.000000000000000000 ) ) ;
#15303=DIRECTION ( 'NONE',  ( 1.000000000000000000, -5.653314293126999632E-09, 4.083276933743999944E-09 ) ) ;
#15309=CARTESIAN_POINT ( 'NONE',  ( 21.52721940996000072, 6.681649352278999920, 7.201632472380000038 ) ) ;
#15310=CARTESIAN_POINT ( 'NONE',  ( 2.441032952700726177, 13.00514025596468670, -6.261105887786398760 ) ) ;
#15313=B_SPLINE_CURVE_WITH_KNOTS ( 'NONE', 3,
 ( #4717, #10278, #20528, #16315, #20408 ),
 .UNSPECIFIED., .F., .F.,
 ( 4, 1, 4 ),
 ( 0.000000000000000000, 0.3333333333333000081, 0.4999999972379591262 ),
 .UNSPECIFIED. ) ;
#15314=VECTOR ( 'NONE', #10542, 1000.000000000000114 ) ;
#15318=ADVANCED_FACE ( 'NONE', ( #14471 ), #8788, .F. ) ;
#15321=CARTESIAN_POINT ( 'NONE',  ( -4.850000000102999920, 12.44999864901999942, -1.732907964652000048E-09 ) ) ;
#15322=CARTESIAN_POINT ( 'NONE',  ( 23.99062354302999722, -7.716878364870000340, 11.63397459621999985 ) ) ;
#15325=ORIENTED_EDGE ( 'NONE', *, *, #6857, .T. ) ;
#15328=CARTESIAN_POINT ( 'NONE',  ( -18.73259798496000172, -8.620928137991000995, 3.072238420002000314 ) ) ;
#15329=EDGE_CURVE ( 'NONE', #3196, #23059, #5620, .T. ) ;
#15331=CARTESIAN_POINT ( 'NONE',  ( 13.44600174930999970, -1.304103625722999871, 10.57402029614000050 ) ) ;
#15332=CARTESIAN_POINT ( 'NONE',  ( -13.53183956624999951, -0.9914182199946000029, -11.24149240260000049 ) ) ;
#15334=CARTESIAN_POINT ( 'NONE',  ( 19.45869494525999954, 0.9204530265265999933, 10.34116613746999924 ) ) ;
#15337=CARTESIAN_POINT ( 'NONE',  ( 21.55245587747999991, -7.890825992760999164, 6.521045315185999947 ) ) ;
#15338=CARTESIAN_POINT ( 'NONE',  ( 11.01624327026000039, -12.44999999999999929, 0.000000000000000000 ) ) ;
#15340=DIRECTION ( 'NONE',  ( -6.791358400560965595E-08, 0.9999999999999975575, 5.471897964325976456E-09 ) ) ;
#15343=CARTESIAN_POINT ( 'NONE',  ( 4.776862951938002588, 12.47838658620001162, -0.1510428563734999008 ) ) ;
#15345=CARTESIAN_POINT ( 'NONE',  ( -21.62195572587000214, 2.576950381532999934, 10.79137310468999900 ) ) ;
#15346=ORIENTED_EDGE ( 'NONE', *, *, #820, .F. ) ;
#15348=DIRECTION ( 'NONE',  ( 0.000000000000000000, 1.000000000000000000, 0.000000000000000000 ) ) ;
#15350=DIRECTION ( 'NONE',  ( 0.000000000000000000, 1.000000000000000000, 0.000000000000000000 ) ) ;
#15351=CARTESIAN_POINT ( 'NONE',  ( -3.792323924634558363, 12.19803457140297098, 2.925688007707359262 ) ) ;
#15355=CARTESIAN_POINT ( 'NONE',  ( 16.73662674931000183, 9.294473935295998857, 5.382749556855999984 ) ) ;
#15356=CARTESIAN_POINT ( 'NONE',  ( -18.27706328473999875, 10.02730951802000092, -4.225925492466999778 ) ) ;
#15357=CARTESIAN_POINT ( 'NONE',  ( 13.47637625730999922, -3.210294990792000203, -8.544406387913998202 ) ) ;
#15358=CARTESIAN_POINT ( 'NONE',  ( 24.28455689590275668, 12.82067141883539918, -2.793945715430803389 ) ) ;
#15362=CARTESIAN_POINT ( 'NONE',  ( 14.20013902425123575, -8.115563385662030171, -6.363435485192806773 ) ) ;
#15365=CARTESIAN_POINT ( 'NONE',  ( 5.625000000000000000, 21.50000000000000000, 1.676175670483999962E-09 ) ) ;
#15366=EDGE_CURVE ( 'NONE', #12621, #19254, #13002, .T. ) ;
#15368=CARTESIAN_POINT ( 'NONE',  ( 11.29022434642157791, 2.380282113839690794, 12.49997383652757144 ) ) ;
#15369=DIRECTION ( 'NONE',  ( -1.000000000000000000, 0.000000000000000000, 0.000000000000000000 ) ) ;
#15371=CARTESIAN_POINT ( 'NONE',  ( -21.32287077250664709, 5.665269408240008353, -7.371613913343743718 ) ) ;
#15376=ORIENTED_EDGE ( 'NONE', *, *, #10608, .F. ) ;
#15377=B_SPLINE_CURVE_WITH_KNOTS ( 'NONE', 3,
 ( #7455, #18260, #20083, #5768, #16424, #23813, #14954, #1901, #12806, #13154, #5423, #20547, #10985, #12912, #18489, #20194, #16665, #1780, #18612, #20428, #3837, #16775, #71, #1662, #5302, #184, #12692, #7344, #3603, #2131, #9169, #14838, #9520, #5531 ),
 .UNSPECIFIED., .F., .F.,
 ( 4, 2, 2, 2, 2, 2, 2, 2, 2, 2, 2, 2, 2, 2, 2, 2, 4 ),
 ( 0.000000000000000000, 0.06249999999999997224, 0.1249999999999999445, 0.1874999999999999167, 0.2499999999999998890, 0.3124999999999998890, 0.3749999999999998335, 0.4374999999999998335, 0.4999999999999998890, 0.5624999999999998890, 0.6249999999999997780, 0.6874999999999997780, 0.7499999999999998890, 0.8125000000000000000, 0.8750000000000000000, 0.9375000000000000000, 1.000000000000000000 ),
 .UNSPECIFIED. ) ;
#15380=CARTESIAN_POINT ( 'NONE',  ( -2.711598292089676399, 11.79220046658777044, 3.994969842139935334 ) ) ;
#15381=DIRECTION ( 'NONE',  ( 0.000000000000000000, 0.3197346865517833869, -0.9475071135435515490 ) ) ;
#15383=CARTESIAN_POINT ( 'NONE',  ( 14.41117308877000092, -6.232064677282999732, -9.080323572665999876 ) ) ;
#15384=CARTESIAN_POINT ( 'NONE',  ( -6.382276157104002756, 15.08198816355999128, -3.360859746888000377 ) ) ;
#15388=CARTESIAN_POINT ( 'NONE',  ( -14.00000000000000711, -1.908289287512767052, -9.413725350966782202 ) ) ;
#15389=VECTOR ( 'NONE', #7690, 1000.000000000000227 ) ;
#15391=CARTESIAN_POINT ( 'NONE',  ( -14.44097978627332601, -9.338505494777370686, -8.825220280763023339 ) ) ;
#15392=VERTEX_POINT ( 'NONE', #11078 ) ;
#15395=CARTESIAN_POINT ( 'NONE',  ( 15.25733488771729363, 3.913752835213978098, 9.572631007212564214 ) ) ;
#15397=CARTESIAN_POINT ( 'NONE',  ( -18.70603407209999958, 11.04749776926000138, -1.268528793046000080 ) ) ;
#15400=CARTESIAN_POINT ( 'NONE',  ( -21.15342916351980662, -9.631976845097828033, -4.232284332473250643 ) ) ;
#15401=CARTESIAN_POINT ( 'NONE',  ( -13.36117685223999985, -10.17969989951000009, -0.7718705306884999784 ) ) ;
#15404=EDGE_LOOP ( 'NONE', ( #22389, #23318, #15221, #10779, #6858 ) ) ;
#15406=CARTESIAN_POINT ( 'NONE',  ( -12.00000000000000000, -7.000000000000000000, 0.000000000000000000 ) ) ;
#15407=AXIS2_PLACEMENT_3D ( 'NONE', #22722, #19220, #22606 ) ;
#15409=CARTESIAN_POINT ( 'NONE',  ( 6.082094348699005337, 14.07676700545000159, -0.0001361385119140001254 ) ) ;
#15410=ADVANCED_FACE ( 'NONE', ( #16158 ), #19209, .F. ) ;
#15413=CARTESIAN_POINT ( 'NONE',  ( -20.40997087121332498, -9.195041791531188835, -1.203755103560655515 ) ) ;
#15414=CARTESIAN_POINT ( 'NONE',  ( 11.96718892131000089, -1.481964887125999830, -9.481920936164000224 ) ) ;
#15415=ORIENTED_EDGE ( 'NONE', *, *, #1985, .F. ) ;
#15416=CARTESIAN_POINT ( 'NONE',  ( -6.046766738174004452, 15.84711126475002274, -1.061654000538000409 ) ) ;
#15420=ORIENTED_EDGE ( 'NONE', *, *, #21994, .T. ) ;
#15424=DIRECTION ( 'NONE',  ( 0.000000000000000000, 0.8075558440518585401, 0.5897911144953695839 ) ) ;
#15425=AXIS2_PLACEMENT_3D ( 'NONE', #18953, #11577, #17136 ) ;
#15426=CARTESIAN_POINT ( 'NONE',  ( 18.32130157512671431, 7.445732629929010749, -7.287811148872539668 ) ) ;
#15427=CARTESIAN_POINT ( 'NONE',  ( 12.00000000000000000, -6.392339033789701475, -7.402648988114485462 ) ) ;
#15429=CARTESIAN_POINT ( 'NONE',  ( 18.81024770046333217, -7.320231837943222075, -5.625464605131847762 ) ) ;
#15430=CARTESIAN_POINT ( 'NONE',  ( -3.336044988794002020, 13.59222169570000815, -5.136926126623002631 ) ) ;
#15436=ORIENTED_EDGE ( 'NONE', *, *, #4475, .F. ) ;
#15437=CARTESIAN_POINT ( 'NONE',  ( 24.39041767111999803, -3.750290925976000000, 10.88138972583000097 ) ) ;
#15438=CARTESIAN_POINT ( 'NONE',  ( -3.913786546566217606, 13.31583390095716091, -5.570166324937983582 ) ) ;
#15441=CARTESIAN_POINT ( 'NONE',  ( -20.93881454081395432, -9.385637307247952421, -4.751717301100214286 ) ) ;
#15445=CARTESIAN_POINT ( 'NONE',  ( 12.52688711657000020, -7.716878364870000340, 11.63397459621999985 ) ) ;
#15446=ORIENTED_EDGE ( 'NONE', *, *, #3187, .F. ) ;
#15447=CARTESIAN_POINT ( 'NONE',  ( -17.20986988650785676, -7.119360151369234835, -7.611991465795363787 ) ) ;
#15448=CARTESIAN_POINT ( 'NONE',  ( -11.99999999434999864, 6.999999994347000154, 4.083276180409999442E-09 ) ) ;
#15452=CARTESIAN_POINT ( 'NONE',  ( -7.834000000000000519, 1.320585629393000037E-14, 0.000000000000000000 ) ) ;
#15453=CARTESIAN_POINT ( 'NONE',  ( 18.27225174930999785, 9.757448129154999705, -4.584997352848999341 ) ) ;
#15454=CARTESIAN_POINT ( 'NONE',  ( -14.11822151763998967, 4.169118407994018227, -8.067165099063066336 ) ) ;
#15456=CARTESIAN_POINT ( 'NONE',  ( -14.54749130609000041, 5.065910023622000047, 10.11535946923000040 ) ) ;
#15459=CARTESIAN_POINT ( 'NONE',  ( 16.68171080085999947, 11.38129333810999988, 0.2944024164967999901 ) ) ;
#15461=DIRECTION ( 'NONE',  ( 1.000000000000000000, 0.000000000000000000, 0.000000000000000000 ) ) ;
#15462=CARTESIAN_POINT ( 'NONE',  ( 20.31311216239999951, -2.731102875616999714, -9.830470219947999411 ) ) ;
#15465=CARTESIAN_POINT ( 'NONE',  ( 11.89062890675000084, 5.534444999978999746, -7.067249179718999130 ) ) ;
#15468=CARTESIAN_POINT ( 'NONE',  ( -4.671193161643005354, 12.51559483494999192, 0.7204251727433007568 ) ) ;
#15470=CARTESIAN_POINT ( 'NONE',  ( -20.45236390540999949, 6.914456025393000083, -8.636057584528000319 ) ) ;
#15471=VERTEX_POINT ( 'NONE', #1637 ) ;
#15476=CARTESIAN_POINT ( 'NONE',  ( 14.99328936713000004, -9.056039068417000237, 0.000000000000000000 ) ) ;
#15478=CARTESIAN_POINT ( 'NONE',  ( -3.476879115686000166, 13.24153924759999867, 5.444655603229995755 ) ) ;
#15480=LINE ( 'NONE', #21308, #8382 ) ;
#15481=CARTESIAN_POINT ( 'NONE',  ( -19.08958467661999947, -10.87501988123999830, 0.7812661330421999395 ) ) ;
#15482=CARTESIAN_POINT ( 'NONE',  ( 12.70856375730999943, -1.114725866925000197, 9.038927914362998806 ) ) ;
#15485=FACE_OUTER_BOUND ( 'NONE', #11435, .T. ) ;
#15487=CARTESIAN_POINT ( 'NONE',  ( 13.84634332888274244, -8.698285480931694735, 5.523431346751156212 ) ) ;
#15490=CARTESIAN_POINT ( 'NONE',  ( -3.088892724819999103, 14.26228888334000366, -5.340567897133000841 ) ) ;
#15491=DIRECTION ( 'NONE',  ( -3.122502256758250246E-14, 1.000000000000000000, 0.000000000000000000 ) ) ;
#15493=CARTESIAN_POINT ( 'NONE',  ( 11.43887872963242103, -3.075720902669945023, 12.49994001780760478 ) ) ;
#15494=CARTESIAN_POINT ( 'NONE',  ( 17.06835809520467251, -2.939044901913968388, 10.00778562106659031 ) ) ;
#15496=CARTESIAN_POINT ( 'NONE',  ( -21.05832910583999862, 9.211679941677999750, 0.000000000000000000 ) ) ;
#15498=ORIENTED_EDGE ( 'NONE', *, *, #4777, .F. ) ;
#15499=CARTESIAN_POINT ( 'NONE',  ( 11.18574820343724951, -9.950120879830603116, 7.765924039743827834 ) ) ;
#15500=VERTEX_POINT ( 'NONE', #13263 ) ;
#15502=CARTESIAN_POINT ( 'NONE',  ( 0.4218749374566191923, 11.48962318055099452, 4.794906470640148299 ) ) ;
#15504=DIRECTION ( 'NONE',  ( 0.000000000000000000, 0.000000000000000000, -1.000000000000000000 ) ) ;
#15505=CARTESIAN_POINT ( 'NONE',  ( -24.50000000000000000, 1.524685264937999788E-14, 0.000000000000000000 ) ) ;
#15506=CARTESIAN_POINT ( 'NONE',  ( -6.445315760836000329, 15.10728987923999966, -3.240892097991999066 ) ) ;
#15507=CARTESIAN_POINT ( 'NONE',  ( -6.838539683285000059, 15.31903379280000088, 1.878299112549000061 ) ) ;
#15508=VERTEX_POINT ( 'NONE', #22699 ) ;
#15509=VERTEX_POINT ( 'NONE', #6109 ) ;
#15510=CARTESIAN_POINT ( 'NONE',  ( -13.99999999999999645, 1.096942893147169196, -9.373824115781612676 ) ) ;
#15513=ORIENTED_EDGE ( 'NONE', *, *, #22509, .T. ) ;
#15514=CARTESIAN_POINT ( 'NONE',  ( -19.94541230731999804, -0.1261951200563999897, -9.624618949942000512 ) ) ;
#15516=CARTESIAN_POINT ( 'NONE',  ( 6.161504479767497600, 14.06289331633568374, 0.4242934236927147218 ) ) ;
#15517=CARTESIAN_POINT ( 'NONE',  ( 15.68994637415852367, -9.253307702421135872, 4.643068743934705367 ) ) ;
#15518=CARTESIAN_POINT ( 'NONE',  ( -14.04282959941999920, -10.81806137319999905, 1.946765347141999891 ) ) ;
#15520=CARTESIAN_POINT ( 'NONE',  ( -20.81887252879722894, 0.02655197213427299210, -10.51206043786136846 ) ) ;
#15521=CARTESIAN_POINT ( 'NONE',  ( -16.69277858220999988, 10.68419017778999880, -3.897213304429000491 ) ) ;
#15522=AXIS2_PLACEMENT_3D ( 'NONE', #23293, #23413, #4908 ) ;
#15523=B_SPLINE_CURVE_WITH_KNOTS ( 'NONE', 3,
 ( #10324, #19652, #6437, #985 ),
 .UNSPECIFIED., .F., .F.,
 ( 4, 4 ),
 ( 0.000000000000000000, 1.000000000000000000 ),
 .UNSPECIFIED. ) ;
#15525=ORIENTED_EDGE ( 'NONE', *, *, #14735, .T. ) ;
#15527=CARTESIAN_POINT ( 'NONE',  ( -15.59164245049265496, -7.009879148460222531, -7.667866936169112080 ) ) ;
#15530=CARTESIAN_POINT ( 'NONE',  ( 5.805692032784003587, 13.82232033692000428, -2.386350607328999729 ) ) ;
#15534=CARTESIAN_POINT ( 'NONE',  ( 18.02643908530999894, 9.290813243320000581, -4.365746228316999655 ) ) ;
#15537=CARTESIAN_POINT ( 'NONE',  ( 24.24531177150999994, 0.000000000000000000, 0.000000000000000000 ) ) ;
#15538=CARTESIAN_POINT ( 'NONE',  ( 24.50000000000000000, -11.33659675998026728, 5.364438426793228132 ) ) ;
#15541=CARTESIAN_POINT ( 'NONE',  ( 11.90008533512019717, 8.504566836169448862, 10.26973740115608535 ) ) ;
#15545=CARTESIAN_POINT ( 'NONE',  ( 18.32319020317524760, 7.491395659936667784, -7.241007325533137085 ) ) ;
#15546=CARTESIAN_POINT ( 'NONE',  ( 12.00000000000000711, -7.523096633965199231, -6.369279415753941187 ) ) ;
#15548=DIRECTION ( 'NONE',  ( 0.000000000000000000, 1.000000000000000000, 0.000000000000000000 ) ) ;
#15549=CARTESIAN_POINT ( 'NONE',  ( 20.08785956010000007, 11.04335702312000045, 1.829420851330999964 ) ) ;
#15551=CARTESIAN_POINT ( 'NONE',  ( -3.932855452960560605, 13.92334204325285363, -4.847046887875868570 ) ) ;
#15552=DIRECTION ( 'NONE',  ( -1.000000000000000000, 0.000000000000000000, 0.000000000000000000 ) ) ;
#15555=CARTESIAN_POINT ( 'NONE',  ( 21.96628300751999774, 0.8142437358098000288, 10.33950846541999979 ) ) ;
#15556=CARTESIAN_POINT ( 'NONE',  ( -2.908727297478219231, 13.08990433425206312, -6.081832042887836742 ) ) ;
#15558=CARTESIAN_POINT ( 'NONE',  ( -19.70710128986670284, -0.2415848317640648391, 10.48256611230249291 ) ) ;
#15559=CARTESIAN_POINT ( 'NONE',  ( -12.50000000000000000, 1.377727649040999975E-14, 0.000000000000000000 ) ) ;
#15564=CARTESIAN_POINT ( 'NONE',  ( -16.90284627698810027, 3.185908784686084960, -9.919433582464312948 ) ) ;
#15567=DIRECTION ( 'NONE',  ( 1.000000000000000000, 0.000000000000000000, 0.000000000000000000 ) ) ;
#15569=CARTESIAN_POINT ( 'NONE',  ( 16.88287270046333433, -8.867611548585280445, -2.382974050612994610 ) ) ;
#15570=CARTESIAN_POINT ( 'NONE',  ( 15.74943924931000083, -10.38900229657999930, -2.621660623529000311 ) ) ;
#15571=CARTESIAN_POINT ( 'NONE',  ( -22.13189778338000124, 11.16819092355999921, -0.3469374994123999856 ) ) ;
#15573=CARTESIAN_POINT ( 'NONE',  ( -14.88272252886000047, -2.429795583095000211, 9.959192131528999070 ) ) ;
#15575=CARTESIAN_POINT ( 'NONE',  ( 13.77119494526000132, 8.252143983288998896, 6.036643158187999347 ) ) ;
#15576=CARTESIAN_POINT ( 'NONE',  ( -14.25623308043999948, -13.93375672974000068, -0.4324171310913000332 ) ) ;
#15578=CARTESIAN_POINT ( 'NONE',  ( 21.29261314321999876, 7.944215266713999135, 5.566623593713999618 ) ) ;
#15582=CARTESIAN_POINT ( 'NONE',  ( -2.717159071278044902, 14.05084818344029962, 5.491236865063197747 ) ) ;
#15584=CARTESIAN_POINT ( 'NONE',  ( 0.8118633353224987692, 11.52213133294999459, 4.737706653456997152 ) ) ;
#15588=FACE_OUTER_BOUND ( 'NONE', #10356, .T. ) ;
#15590=CARTESIAN_POINT ( 'NONE',  ( 15.29562270046331740, -4.564817758524311486, -7.919774334405468075 ) ) ;
#15591=EDGE_CURVE ( 'NONE', #15625, #20267, #9514, .T. ) ;
#15593=CARTESIAN_POINT ( 'NONE',  ( -4.353590520638998207, 13.53542079822999256, 4.749304138607999271 ) ) ;
#15598=CARTESIAN_POINT ( 'NONE',  ( -6.046837210729000489, 16.30334039894000142, -1.000000000000000000 ) ) ;
#15599=CARTESIAN_POINT ( 'NONE',  ( 14.24418875730999900, 6.821019272440999259, 6.095525253705999624 ) ) ;
#15603=CARTESIAN_POINT ( 'NONE',  ( 19.94084516911093630, 7.608551632648391738, -7.249783728510496239 ) ) ;
#15606=CARTESIAN_POINT ( 'NONE',  ( 1.406122888814909988, 13.78777984639410548, -5.962141027037247021 ) ) ;
#15607=CARTESIAN_POINT ( 'NONE',  ( 4.921628875838995221, 13.75323042666000362, -4.185280411400999157 ) ) ;
#15608=DIRECTION ( 'NONE',  ( 0.000000000000000000, 0.000000000000000000, -1.000000000000000000 ) ) ;
#15609=CARTESIAN_POINT ( 'NONE',  ( 14.65997133257774543, -8.964114299601121161, 1.438260584116868079 ) ) ;
#15610=CARTESIAN_POINT ( 'NONE',  ( 16.87321770986947556, 3.972702165366156279, 9.639322115070482866 ) ) ;
#15617=CARTESIAN_POINT ( 'NONE',  ( 11.66614181941011985, -8.864734480512577619, 9.645689288213576518 ) ) ;
#15618=ORIENTED_EDGE ( 'NONE', *, *, #6996, .T. ) ;
#15621=CARTESIAN_POINT ( 'NONE',  ( -2.964817197442055186, 13.10038421424571276, 6.059153498010348748 ) ) ;
#15622=CARTESIAN_POINT ( 'NONE',  ( -4.900699999999999612, 1.284663064832999817E-14, 0.000000000000000000 ) ) ;
#15625=VERTEX_POINT ( 'NONE', #296 ) ;
#15626=CARTESIAN_POINT ( 'NONE',  ( -14.00000000000000711, -7.717499669629955150, -6.307697564917725153 ) ) ;
#15627=CONICAL_SURFACE ( 'NONE', #11398, 9.152445778720998959, 0.02565634000431304615 ) ;
#15628=CARTESIAN_POINT ( 'NONE',  ( 13.21250000000000036, 0.000000000000000000, 0.000000000000000000 ) ) ;
#15631=CARTESIAN_POINT ( 'NONE',  ( -20.97361272096999940, 4.049795877874999839, 8.762865524082998903 ) ) ;
#15633=CARTESIAN_POINT ( 'NONE',  ( 6.168359549731804670, 14.02575663701962760, 0.5147778748295055440 ) ) ;
#15634=CARTESIAN_POINT ( 'NONE',  ( 15.14759469764988786, 7.222759206179429015, 7.395737098632818807 ) ) ;
#15635=CARTESIAN_POINT ( 'NONE',  ( -13.86216628438999976, -9.279585093157001197, -4.454637058083000589 ) ) ;
#15636=CARTESIAN_POINT ( 'NONE',  ( 11.49999999537000051, 6.999999995366000149, 1.987950376480999949E-09 ) ) ;
#15637=CARTESIAN_POINT ( 'NONE',  ( -21.61666142697704629, -3.977296262259868431, 9.886869024158263741 ) ) ;
#15638=CARTESIAN_POINT ( 'NONE',  ( -15.67712684235999987, -11.34047394370000106, -0.3014134449561000073 ) ) ;
#15643=CARTESIAN_POINT ( 'NONE',  ( -16.19936510130885665, -3.025408273704439210, 9.955618328560920105 ) ) ;
#15644=EDGE_LOOP ( 'NONE', ( #5969, #17686 ) ) ;
#15646=CARTESIAN_POINT ( 'NONE',  ( 6.131636900325998951, 14.49487543762001351, -0.1732800415016998163 ) ) ;
#15649=CARTESIAN_POINT ( 'NONE',  ( 14.92875142131000210, -6.069959421551999412, 7.533852356441999909 ) ) ;
#15652=B_SPLINE_CURVE_WITH_KNOTS ( 'NONE', 3,
 ( #16074, #6762, #23473, #14155, #10770, #12465, #3503, #10883, #18036, #23601, #18270, #14393, #1669, #1909, #9765, #22598, #9414, #2256 ),
 .UNSPECIFIED., .F., .F.,
 ( 4, 2, 2, 2, 2, 2, 2, 2, 4 ),
 ( 0.000000000000000000, 0.09877299861065136355, 0.1975459972213027271, 0.2963189958319540351, 0.3950919944426053987, 0.4938649930532567067, 0.5926379916639080703, 0.6914109902745593228, 0.7901839888852105753 ),
 .UNSPECIFIED. ) ;
#15658=CARTESIAN_POINT ( 'NONE',  ( 24.02947265600820614, 7.126507592064388774, 7.874003420745752990 ) ) ;
#15659=CIRCLE ( 'NONE', #976, 12.44999999999999929 ) ;
#15660=CARTESIAN_POINT ( 'NONE',  ( -14.00000000000000000, -4.353401700033900035, 9.017588339353036275 ) ) ;
#15661=CARTESIAN_POINT ( 'NONE',  ( 18.05830141818303147, -1.129169376018525961, -10.34964973624757789 ) ) ;
#15662=DIRECTION ( 'NONE',  ( -1.000000000000000000, 0.000000000000000000, 0.000000000000000000 ) ) ;
#15663=CARTESIAN_POINT ( 'NONE',  ( -14.38789256606429490, -8.761241120844353247, 9.824672794992769909 ) ) ;
#15664=CARTESIAN_POINT ( 'NONE',  ( 22.84106400460000330, -10.84379783138999898, -3.067933783016000060 ) ) ;
#15666=CARTESIAN_POINT ( 'NONE',  ( -4.055068951189445770, 13.80018247765906025, -4.864706622278940351 ) ) ;
#15667=CARTESIAN_POINT ( 'NONE',  ( -24.09039453749000259, 1.716648116605999814E-14, 0.000000000000000000 ) ) ;
#15670=ORIENTED_EDGE ( 'NONE', *, *, #1552, .F. ) ;
#15671=CARTESIAN_POINT ( 'NONE',  ( 20.42027553904000214, -7.757497012334000352, 6.819440105516999751 ) ) ;
#15672=CARTESIAN_POINT ( 'NONE',  ( 24.21477607719004155, 7.477202524421422858, 7.546204228164135053 ) ) ;
#15674=CARTESIAN_POINT ( 'NONE',  ( -19.49289028970277116, -7.253846718909587210, 7.562220539910094352 ) ) ;
#15676=CARTESIAN_POINT ( 'NONE',  ( 4.903088169044051092, 14.37364044011246911, 3.818206020033084069 ) ) ;
#15678=CARTESIAN_POINT ( 'NONE',  ( 4.620886678299001460, 12.32869312146999263, -1.717839858747998161 ) ) ;
#15679=EDGE_LOOP ( 'NONE', ( #9474, #18937, #6211, #15525, #12156 ) ) ;
#15680=CARTESIAN_POINT ( 'NONE',  ( -14.97697090817717935, 6.668094886919918807, -7.940777754376553865 ) ) ;
#15687=CARTESIAN_POINT ( 'NONE',  ( 17.39475174931000012, -10.15246533026000186, 3.558175289345999914 ) ) ;
#15688=CARTESIAN_POINT ( 'NONE',  ( -23.68577204849000140, -2.454364077398999644, 10.41095670075000079 ) ) ;
#15689=CARTESIAN_POINT ( 'NONE',  ( -19.55472053216000106, -2.419448610677000122, -10.09555165608999872 ) ) ;
#15690=CARTESIAN_POINT ( 'NONE',  ( -6.107093651952999913, 16.13547971460000596, 0.9717940814902004121 ) ) ;
#15691=CARTESIAN_POINT ( 'NONE',  ( 14.24562451745999958, 2.264453579998999988, 9.429937331667000322 ) ) ;
#15693=AXIS2_PLACEMENT_3D ( 'NONE', #15099, #20455, #13060 ) ;
#15694=CARTESIAN_POINT ( 'NONE',  ( -18.99854661335000117, 13.93375672974000068, 0.000000000000000000 ) ) ;
#15696=CARTESIAN_POINT ( 'NONE',  ( -23.74465998031000069, -7.716878364870000340, -11.63397459621999985 ) ) ;
#15697=ORIENTED_EDGE ( 'NONE', *, *, #22063, .F. ) ;
#15700=CARTESIAN_POINT ( 'NONE',  ( -4.720332369741998768, 12.53505228420999984, -0.1483533514531999165 ) ) ;
#15702=CARTESIAN_POINT ( 'NONE',  ( -20.09773186494999919, 7.373291466226999269, 8.234872552958998781 ) ) ;
#15704=ORIENTED_EDGE ( 'NONE', *, *, #4777, .T. ) ;
#15705=DIRECTION ( 'NONE',  ( 0.000000000000000000, 0.000000000000000000, -1.000000000000000000 ) ) ;
#15707=ADVANCED_FACE ( 'NONE', ( #21379 ), #21544, .F. ) ;
#15708=CARTESIAN_POINT ( 'NONE',  ( -3.624149612674999243, 14.44537212523001202, 4.955916638659999762 ) ) ;
#15710=CARTESIAN_POINT ( 'NONE',  ( 12.00000000000000000, 0.000000000000000000, 0.000000000000000000 ) ) ;
#15712=CARTESIAN_POINT ( 'NONE',  ( -12.03266363877000167, 15.14665849299999856, -1.476125921680999875 ) ) ;
#15713=CARTESIAN_POINT ( 'NONE',  ( 12.00000000000000000, -8.391897884961000642, -3.194141202603999918 ) ) ;
#15714=CARTESIAN_POINT ( 'NONE',  ( 12.59887625730999972, 2.316137192978999781, 8.804988873405999783 ) ) ;
#15722=CARTESIAN_POINT ( 'NONE',  ( -2.281730950380269185, 13.94578545768103872, -5.684389550665945201 ) ) ;
#15723=EDGE_LOOP ( 'NONE', ( #4114, #17358, #14783, #12811 ) ) ;
#15724=AXIS2_PLACEMENT_3D ( 'NONE', #2140, #18620, #7231 ) ;
#15725=CARTESIAN_POINT ( 'NONE',  ( 4.901867555465002191, 14.36018495061998657, -3.565049704023001365 ) ) ;
#15726=FACE_OUTER_BOUND ( 'NONE', #18006, .T. ) ;
#15727=ADVANCED_FACE ( 'NONE', ( #21503 ), #23057, .F. ) ;
#15730=B_SPLINE_CURVE_WITH_KNOTS ( 'NONE', 3,
 ( #12685, #23584, #22116, #1894, #23693, #20073, #3488, #21656, #10634, #8934, #23929, #12452, #12799, #21883, #9284, #6988, #1774, #16658, #3372, #5294, #7338, #9044, #1422, #8822, #21771, #5523, #16538, #16416, #62, #14719, #5183, #7101, #12902, #23806, #10868, #22001, #12565, #3248, #18021, #19835, #20302, #7214, #18362, #19953, #14491, #14377, #18253, #10750, #3704, #5414, #20186, #18145, #3596, #1548, #10979, #16302, #11097, #6446, #11225, #4281, #15637, #2827, #22789, #5635, #9962, #6324, #10089, #17475, #20985, #15400, #17349, #9395, #625, #16767, #9844, #753, #869, #6204, #15520, #18604, #19161, #4396, #4517, #2010, #8273, #175, #17225, #23029, #8155, #11787, #13832, #12032, #8026, #7567, #13589, #10207, #21233, #22908, #4645, #19415, #17601, #7448, #14946, #2705, #13709, #22341, #21104, #14828, #2573, #11908, #6078 ),
 .UNSPECIFIED., .F., .F.,
 ( 4, 2, 2, 2, 2, 2, 1, 2, 2, 2, 2, 2, 2, 2, 2, 2, 2, 2, 2, 2, 2, 2, 2, 2, 2, 2, 2, 2, 1, 2, 2, 2, 2, 2, 2, 2, 2, 2, 2, 2, 2, 2, 2, 2, 2, 2, 2, 2, 2, 2, 1, 2, 2, 2, 2, 2, 4 ),
 ( 0.000000000000000000, 0.01562500000000000000, 0.03125000000000000000, 0.04687500000000000694, 0.06250000000000001388, 0.07812500000000002776, 0.09375000000000004163, 0.1093750000000000555, 0.1250000000000000555, 0.1406250000000000555, 0.1562500000000000555, 0.1718750000000000555, 0.1875000000000000555, 0.2031250000000000555, 0.2187500000000000555, 0.2343750000000000555, 0.2500000000000000555, 0.2656250000000000555, 0.2812500000000000555, 0.2968750000000000555, 0.3125000000000000555, 0.3281250000000000555, 0.3437500000000000555, 0.3593750000000000555, 0.3750000000000000555, 0.4062500000000000555, 0.4375000000000000555, 0.4687500000000000555, 0.5000000000000001110, 0.5312500000000001110, 0.5625000000000001110, 0.5937500000000001110, 0.6250000000000001110, 0.6406250000000001110, 0.6562500000000001110, 0.6718750000000001110, 0.6875000000000001110, 0.7031250000000001110, 0.7187500000000001110, 0.7343750000000001110, 0.7500000000000001110, 0.7656250000000001110, 0.7812500000000001110, 0.7968750000000001110, 0.8125000000000001110, 0.8281250000000001110, 0.8437500000000001110, 0.8593750000000001110, 0.8750000000000001110, 0.8906250000000001110, 0.9062500000000001110, 0.9218750000000001110, 0.9375000000000001110, 0.9531250000000001110, 0.9687500000000001110, 0.9843750000000001110, 1.000000000000000000 ),
 .UNSPECIFIED. ) ;
#15731=CARTESIAN_POINT ( 'NONE',  ( 15.06119984603782491, 3.964601025465794404, 9.748577488744984976 ) ) ;
#15734=CARTESIAN_POINT ( 'NONE',  ( -14.25699038479000080, -13.93375672974000068, 0.1440191439639999793 ) ) ;
#15736=CARTESIAN_POINT ( 'NONE',  ( -24.17970357210941756, -8.771272208539420134, 9.807700027330906067 ) ) ;
#15738=CARTESIAN_POINT ( 'NONE',  ( -24.50000000000000711, -8.967281873253046598, -5.478788448042904768 ) ) ;
#15740=EDGE_LOOP ( 'NONE', ( #23260, #22320, #19705, #15850 ) ) ;
#15743=EDGE_CURVE ( 'NONE', #14425, #3901, #11867, .T. ) ;
#15744=CARTESIAN_POINT ( 'NONE',  ( 2.606584289605573979, 13.03356560933178976, 6.201593128633253293 ) ) ;
#15745=VECTOR ( 'NONE', #13275, 1000.000000000000000 ) ;
#15746=CARTESIAN_POINT ( 'NONE',  ( 6.144426515170381187, 14.17071861772576646, -0.1469360130798122999 ) ) ;
#15747=CARTESIAN_POINT ( 'NONE',  ( -20.28383807595834298, -8.298568892495806537, 4.095387357305202869 ) ) ;
#15748=CARTESIAN_POINT ( 'NONE',  ( 24.37173283531060264, -3.055078579629052271, -12.50000000000000000 ) ) ;
#15749=AXIS2_PLACEMENT_3D ( 'NONE', #22603, #4206, #11600 ) ;
#15750=ORIENTED_EDGE ( 'NONE', *, *, #23836, .T. ) ;
#15755=CARTESIAN_POINT ( 'NONE',  ( -22.66095672860999954, -10.66205312073000044, -1.334338195151000273 ) ) ;
#15757=CARTESIAN_POINT ( 'NONE',  ( 20.79345833333331939, 5.656740788837752554, -7.360929357356189584 ) ) ;
#15758=CARTESIAN_POINT ( 'NONE',  ( 14.97266585189538368, 10.13449242591069144, 2.012324330117317039 ) ) ;
#15759=CARTESIAN_POINT ( 'NONE',  ( -17.47543258502999919, -9.736197399936997954, -5.302291535354000551 ) ) ;
#15760=EDGE_CURVE ( 'NONE', #8569, #17905, #10589, .T. ) ;
#15762=CARTESIAN_POINT ( 'NONE',  ( -22.86732996308985122, 4.662680996433341996, 8.088179580956165182 ) ) ;
#15763=EDGE_CURVE ( 'NONE', #1014, #13308, #17755, .T. ) ;
#15764=CARTESIAN_POINT ( 'NONE',  ( -1.406371714024999164, 11.64204510379998680, -4.531569040216001376 ) ) ;
#15766=CARTESIAN_POINT ( 'NONE',  ( 0.000000000000000000, 22.00000000000000000, 0.000000000000000000 ) ) ;
#15769=B_SPLINE_CURVE_WITH_KNOTS ( 'NONE', 3,
 ( #5596, #7769, #1965, #15137, #22534, #9349, #18908, #5940, #14905, #15025, #7522, #7653 ),
 .UNSPECIFIED., .F., .F.,
 ( 4, 1, 1, 1, 1, 2, 2, 4 ),
 ( 0.000000000000000000, 0.2500000000000041633, 0.3750000000000059952, 0.4375000000000063838, 0.4687500000000064948, 0.4843750000000064393, 0.5000000000000064393, 1.000000000000000000 ),
 .UNSPECIFIED. ) ;
#15771=CARTESIAN_POINT ( 'NONE',  ( -15.96785171052174412, -9.249139021331371779, 4.747086489963850298 ) ) ;
#15774=CARTESIAN_POINT ( 'NONE',  ( 5.066445834236000145, 14.82876933804001318, -3.462109428241999520 ) ) ;
#15777=EDGE_CURVE ( 'NONE', #5775, #8671, #20404, .T. ) ;
#15779=CARTESIAN_POINT ( 'NONE',  ( 14.38031392131000175, 9.076879665875999592, 3.306787424407999776 ) ) ;
#15781=CARTESIAN_POINT ( 'NONE',  ( 23.99062354302999722, 7.716878364870000340, -11.63397459621999985 ) ) ;
#15784=FILL_AREA_STYLE ('',( #19434 ) ) ;
#15785=ORIENTED_EDGE ( 'NONE', *, *, #17552, .F. ) ;
#15789=CARTESIAN_POINT ( 'NONE',  ( 16.43228481845074640, 5.324967529146916512, -8.918705523749617115 ) ) ;
#15792=CARTESIAN_POINT ( 'NONE',  ( -14.41332696916413170, -9.018101604870846444, 9.380024591087758878 ) ) ;
#15793=CARTESIAN_POINT ( 'NONE',  ( 21.88640382367999848, 10.36782067078999958, -4.349542176122999315 ) ) ;
#15794=CARTESIAN_POINT ( 'NONE',  ( -4.820913537080000033, 13.20111002679000123, 5.836439296936000609 ) ) ;
#15795=VECTOR ( 'NONE', #2159, 1000.000000000000000 ) ;
#15796=CARTESIAN_POINT ( 'NONE',  ( -4.267402886712965859, 13.63170725869960087, -4.942444299606017388 ) ) ;
#15798=ORIENTED_EDGE ( 'NONE', *, *, #14323, .F. ) ;
#15799=CARTESIAN_POINT ( 'NONE',  ( 22.98509940575999977, -5.647570509607000133, -9.363978333943000720 ) ) ;
#15800=CARTESIAN_POINT ( 'NONE',  ( 23.93104224056287777, 10.41832666982863564, -2.042517780468533051 ) ) ;
#15801=CARTESIAN_POINT ( 'NONE',  ( 6.243179582884000212, 1.148189900220999940E-14, 0.000000000000000000 ) ) ;
#15803=DIRECTION ( 'NONE',  ( 1.000000000000000000, 0.000000000000000000, 0.000000000000000000 ) ) ;
#15804=CARTESIAN_POINT ( 'NONE',  ( -12.25000000000000000, -15.43375672973998824, 0.000000000000000000 ) ) ;
#15805=ORIENTED_EDGE ( 'NONE', *, *, #20442, .F. ) ;
#15814=CARTESIAN_POINT ( 'NONE',  ( -10.04281598263999875, 16.40330333354999937, -1.000000000000000000 ) ) ;
#15816=FACE_OUTER_BOUND ( 'NONE', #3261, .T. ) ;
#15817=CARTESIAN_POINT ( 'NONE',  ( -14.47288607055999243, -6.205759095609786336, -6.641949884944085447 ) ) ;
#15818=CARTESIAN_POINT ( 'NONE',  ( -13.80102035161000096, -0.9449678463817999807, -10.71550788283000166 ) ) ;
#15819=CARTESIAN_POINT ( 'NONE',  ( -6.306081500775003512, 16.13779117371002059, 0.9717814567668997539 ) ) ;
#15820=CARTESIAN_POINT ( 'NONE',  ( 18.64619494525999954, 2.446936341558000105, -10.06727026104000089 ) ) ;
#15822=CARTESIAN_POINT ( 'NONE',  ( -24.50000000000000000, -8.081477262649000792, -6.807253044743999837 ) ) ;
#15823=TOROIDAL_SURFACE ( 'NONE', #5401, 16.43375672870000059, 1.000000000000000000 ) ;
#15825=EDGE_LOOP ( 'NONE', ( #15081, #14335 ) ) ;
#15831=CARTESIAN_POINT ( 'NONE',  ( -14.52843611649297806, 0.8125160302300082904, -9.009207629665930028 ) ) ;
#15832=CARTESIAN_POINT ( 'NONE',  ( -19.59647822760999958, -9.324997552198999173, 5.908885382590000290 ) ) ;
#15835=CARTESIAN_POINT ( 'NONE',  ( 3.161491510400058047, 11.90317520361505821, -3.649523268417677713 ) ) ;
#15836=CARTESIAN_POINT ( 'NONE',  ( 4.901795610954997606, 14.36014350025000219, 3.565170190326997446 ) ) ;
#15839=EDGE_CURVE ( 'NONE', #19206, #3147, #7224, .T. ) ;
#15841=CARTESIAN_POINT ( 'NONE',  ( -16.08338753829999845, -2.146827734392999787, 11.15102392286999944 ) ) ;
#15842=CARTESIAN_POINT ( 'NONE',  ( 11.31918875731000007, -8.923818741964000267, -0.1967739533420000131 ) ) ;
#15843=CARTESIAN_POINT ( 'NONE',  ( 24.43449445986659896, 2.200516184495611594, 12.50000000000000000 ) ) ;
#15844=ORIENTED_EDGE ( 'NONE', *, *, #16060, .F. ) ;
#15845=CARTESIAN_POINT ( 'NONE',  ( 5.302309868036999774, 13.73032359673999814, 4.450989051274000019 ) ) ;
#15850=ORIENTED_EDGE ( 'NONE', *, *, #18678, .T. ) ;
#15852=CARTESIAN_POINT ( 'NONE',  ( -24.43506354683006165, 11.72249354572300106, -4.696109227427953670 ) ) ;
#15854=EDGE_CURVE ( 'NONE', #14047, #2155, #20615, .T. ) ;
#15855=CARTESIAN_POINT ( 'NONE',  ( -23.71390419459027754, -9.377614579209383905, 1.734352417475094388 ) ) ;
#15856=CARTESIAN_POINT ( 'NONE',  ( 16.62232292872420558, 9.925332452011865314, 3.188991502716413073 ) ) ;
#15858=CARTESIAN_POINT ( 'NONE',  ( -21.66299577250665820, -4.646874200087295570, -8.062647617244037335 ) ) ;
#15859=CARTESIAN_POINT ( 'NONE',  ( -24.41904027020013146, -9.801083277811052596, 8.024000954858145462 ) ) ;
#15861=CARTESIAN_POINT ( 'NONE',  ( -24.50000000000000000, -9.826472200743234353, -3.257612521534738015 ) ) ;
#15862=CARTESIAN_POINT ( 'NONE',  ( 11.06619116164413619, -11.07450388079853809, 5.818393174557106029 ) ) ;
#15865=DIRECTION ( 'NONE',  ( -1.000000000000000000, 0.000000000000000000, 0.000000000000000000 ) ) ;
#15866=CARTESIAN_POINT ( 'NONE',  ( -2.918874744973449786, 13.09137196612760157, 6.078593498656847949 ) ) ;
#15867=CARTESIAN_POINT ( 'NONE',  ( 12.51792910804999970, 13.93375672974000068, 0.7216190549664999176 ) ) ;
#15869=EDGE_CURVE ( 'NONE', #7389, #837, #21092, .T. ) ;
#15870=CARTESIAN_POINT ( 'NONE',  ( -6.042815837158999948, 16.37762238964999995, -0.9999999878869999526 ) ) ;
#15872=CARTESIAN_POINT ( 'NONE',  ( -12.41173981160000039, 6.613190111079999767, -13.46349570337000046 ) ) ;
#15874=DIRECTION ( 'NONE',  ( 0.000000000000000000, 1.000000000000000000, 0.000000000000000000 ) ) ;
#15875=ORIENTED_EDGE ( 'NONE', *, *, #21380, .F. ) ;
#15876=CARTESIAN_POINT ( 'NONE',  ( -21.56023462137999758, 10.17996857714999948, -0.5018336655562000148 ) ) ;
#15878=CARTESIAN_POINT ( 'NONE',  ( 15.06027663792326265, 9.078858026381649182, 4.937948093896874724 ) ) ;
#15881=EDGE_CURVE ( 'NONE', #11881, #8871, #9970, .T. ) ;
#15883=CARTESIAN_POINT ( 'NONE',  ( 4.148757769666998385, 12.31837238841998783, -2.295775157709002201 ) ) ;
#15885=CARTESIAN_POINT ( 'NONE',  ( -14.25521440656999950, -2.679375877985999743, 10.98274110836000084 ) ) ;
#15889=CARTESIAN_POINT ( 'NONE',  ( -15.15755484276677656, 7.261073034381060332, -7.630493215577654809 ) ) ;
#15892=CARTESIAN_POINT ( 'NONE',  ( 6.461460758271004856, 13.53984578379000325, -1.553565135251000484 ) ) ;
#15893=CARTESIAN_POINT ( 'NONE',  ( 12.00000000000000000, -3.698948358382036172, -8.182095219967926880 ) ) ;
#15895=CARTESIAN_POINT ( 'NONE',  ( 15.17456408531000100, -6.393444021559000490, 7.935320769223000781 ) ) ;
#15896=ADVANCED_FACE ( 'NONE', ( #17714 ), #1110, .F. ) ;
#15905=CARTESIAN_POINT ( 'NONE',  ( 16.39583361425184549, 4.159787878704626074, -9.519236833959350719 ) ) ;
#15906=CARTESIAN_POINT ( 'NONE',  ( -16.27887281610000159, 9.774068015792000352, 5.162340849467000226 ) ) ;
#15907=CARTESIAN_POINT ( 'NONE',  ( -14.47826291725376358, -11.73192043637804893, 4.679722760534371417 ) ) ;
#15908=EDGE_CURVE ( 'NONE', #3069, #2709, #19811, .T. ) ;
#15913=CARTESIAN_POINT ( 'NONE',  ( -24.11803009774280326, -4.367939700960269178, 12.49970390894446659 ) ) ;
#15914=CARTESIAN_POINT ( 'NONE',  ( 22.21209567152000020, 0.8567587614818000796, 10.88017005124000036 ) ) ;
#15918=CYLINDRICAL_SURFACE ( 'NONE', #11842, 10.59999999999999964 ) ;
#15920=CARTESIAN_POINT ( 'NONE',  ( 4.913254300577998279, 12.43880135910001172, 0.1079351427945999670 ) ) ;
#15921=ORIENTED_EDGE ( 'NONE', *, *, #4312, .F. ) ;
#15922=CARTESIAN_POINT ( 'NONE',  ( -15.45146194107333493, -8.546491615899846295, -6.146800611315578422 ) ) ;
#15924=CARTESIAN_POINT ( 'NONE',  ( 17.97356375731000000, 4.354347264933000616, 8.156255255558999551 ) ) ;
#15928=ORIENTED_EDGE ( 'NONE', *, *, #13055, .T. ) ;
#15930=CARTESIAN_POINT ( 'NONE',  ( -12.40106293735999898, 6.430159825535999296, -13.55186498671000095 ) ) ;
#15931=CARTESIAN_POINT ( 'NONE',  ( -14.41377531173998960, -4.730461704047363547, -7.760299280567290126 ) ) ;
#15932=CARTESIAN_POINT ( 'NONE',  ( -18.87927905085999924, 10.04277392903999910, -4.232445057647000297 ) ) ;
#15934=ADVANCED_FACE ( 'NONE', ( #6676, #14068 ), #18072, .T. ) ;
#15935=CARTESIAN_POINT ( 'NONE',  ( 18.44306994526000310, -4.644512059083999667, -9.254651726414000024 ) ) ;
#15938=CARTESIAN_POINT ( 'NONE',  ( 15.46483333333333121, 7.923568558109999493, -4.567004612312420164 ) ) ;
#15939=EDGE_LOOP ( 'NONE', ( #14798, #17858 ) ) ;
#15940=CARTESIAN_POINT ( 'NONE',  ( -17.00872087121333109, -7.283262656812431679, 5.597053662224771742 ) ) ;
#15941=CARTESIAN_POINT ( 'NONE',  ( -0.2992355516767008505, 13.69531868001229569, 6.118419485397218693 ) ) ;
#15942=B_SPLINE_CURVE_WITH_KNOTS ( 'NONE', 3,
 ( #20236, #3755, #11143, #18529, #15940, #1310, #23811, #23459, #22007, #5421, #10639, #14497, #18151, #4951, #6750, #9050, #3139, #10523 ),
 .UNSPECIFIED., .F., .F.,
 ( 4, 2, 2, 2, 2, 2, 2, 2, 4 ),
 ( 0.000000000000000000, 0.1250000000000000278, 0.2500000000000000555, 0.3750000000000001110, 0.5000000000000000000, 0.6250000000000000000, 0.7500000000000000000, 0.8750000000000001110, 1.000000000000000000 ),
 .UNSPECIFIED. ) ;
#15944=CIRCLE ( 'NONE', #17909, 4.649999999999999467 ) ;
#15946=CARTESIAN_POINT ( 'NONE',  ( -14.40214030274523083, 4.602063563387535083, -7.815556307968948069 ) ) ;
#15947=CARTESIAN_POINT ( 'NONE',  ( -19.63171012731000076, -10.46828650075000056, 1.869663484996999969 ) ) ;
#15948=CARTESIAN_POINT ( 'NONE',  ( -3.938174484868301128, 12.12902309718726102, 2.809906632184955289 ) ) ;
#15949=EDGE_LOOP ( 'NONE', ( #6945, #7664, #8684, #3085 ) ) ;
#15950=DIRECTION ( 'NONE',  ( 1.000000000000000000, 0.000000000000000000, 0.000000000000000000 ) ) ;
#15951=CARTESIAN_POINT ( 'NONE',  ( 3.092048582739372442, 11.88530494256604086, -3.707092650763546882 ) ) ;
#15953=CARTESIAN_POINT ( 'NONE',  ( 12.00000000000000000, 5.273090321616999532, -7.267806174758000282 ) ) ;
#15956=CIRCLE ( 'NONE', #5532, 2.000000000000000000 ) ;
#15957=CARTESIAN_POINT ( 'NONE',  ( 17.45156392131000089, -0.08049851871593999286, -9.740865876825999692 ) ) ;
#15959=ORIENTED_EDGE ( 'NONE', *, *, #7583, .T. ) ;
#15960=CARTESIAN_POINT ( 'NONE',  ( -22.21032711986755004, -6.106567764693699552, 6.962914243618090637 ) ) ;
#15962=CARTESIAN_POINT ( 'NONE',  ( -14.97387077250666820, -5.565142630449472883, 7.241325911418540429 ) ) ;
#15963=CARTESIAN_POINT ( 'NONE',  ( 4.027454389662117329, 14.47011947778932850, -4.614682357420342385 ) ) ;
#15966=CARTESIAN_POINT ( 'NONE',  ( 8.837430739852999650, 1.116419486464999937E-14, 0.000000000000000000 ) ) ;
#15967=CARTESIAN_POINT ( 'NONE',  ( 6.124879597941472298, 14.37505545965193399, 0.1297071231249629641 ) ) ;
#15969=CARTESIAN_POINT ( 'NONE',  ( -4.105614703109887742, 13.75508681659879784, 4.877901297121352897 ) ) ;
#15970=CARTESIAN_POINT ( 'NONE',  ( -4.351728331912002368, 12.23318868280000338, 2.300835253139998038 ) ) ;
#15980=CARTESIAN_POINT ( 'NONE',  ( -3.018886224429293552, 13.11113671311871265, 6.035875662628554572 ) ) ;
#15982=CARTESIAN_POINT ( 'NONE',  ( -5.737494891779999939, 16.36109002579999228, -2.188889223574999487 ) ) ;
#15984=CARTESIAN_POINT ( 'NONE',  ( -16.81976253787999909, -9.102909969768001375, 0.000000000000000000 ) ) ;
#15989=CARTESIAN_POINT ( 'NONE',  ( -14.00000000000000000, -10.59999999999999964, 0.000000000000000000 ) ) ;
#15991=CARTESIAN_POINT ( 'NONE',  ( -19.91908895889000064, 10.46467446202999874, 2.086251744724999746 ) ) ;
#15993=CARTESIAN_POINT ( 'NONE',  ( 15.23439172698186006, 4.645476851500599302, 9.236356228214244624 ) ) ;
#15996=DIRECTION ( 'NONE',  ( 0.000000000000000000, 0.000000000000000000, -1.000000000000000000 ) ) ;
#15997=CARTESIAN_POINT ( 'NONE',  ( -4.089491575493999775, 12.29838637034998428, -2.375562731294997842 ) ) ;
#15999=CARTESIAN_POINT ( 'NONE',  ( -16.48964823424000059, 10.66299948276999920, 3.938515806081000825 ) ) ;
#16000=ADVANCED_FACE ( 'NONE', ( #21820 ), #18415, .T. ) ;
#16003=AXIS2_PLACEMENT_3D ( 'NONE', #16359, #21935, #14428 ) ;
#16005=CARTESIAN_POINT ( 'NONE',  ( -14.89710227813126231, 10.31717450065112196, 0.9898032812542618686 ) ) ;
#16006=VERTEX_POINT ( 'NONE', #14658 ) ;
#16008=CARTESIAN_POINT ( 'NONE',  ( 11.06626444616536453, -10.95085460510079578, -6.032555207299142630 ) ) ;
#16009=CARTESIAN_POINT ( 'NONE',  ( 12.00000000000000533, -8.178800721840129739, -3.754006756144630419 ) ) ;
#16010=CARTESIAN_POINT ( 'NONE',  ( 24.36414987671881605, 3.145589772713091481, -12.50000000000000178 ) ) ;
#16012=CARTESIAN_POINT ( 'NONE',  ( 15.39393908531000044, -10.10652924631000005, 1.349470982713999900 ) ) ;
#16013=ORIENTED_EDGE ( 'NONE', *, *, #18856, .F. ) ;
#16014=CARTESIAN_POINT ( 'NONE',  ( -10.41825149291999963, 4.409629518443999530, -13.83169641490000146 ) ) ;
#16015=CARTESIAN_POINT ( 'NONE',  ( 13.49999999999999822, 9.585208429812723807, 0.5427004933114440988 ) ) ;
#16018=CARTESIAN_POINT ( 'NONE',  ( -23.54411375508000148, 0.8581424843098000022, -9.685395125838999419 ) ) ;
#16019=FACE_OUTER_BOUND ( 'NONE', #10533, .T. ) ;
#16020=CARTESIAN_POINT ( 'NONE',  ( 22.76464544783179278, -9.731360964096962718, 4.172095693800953242 ) ) ;
#16022=CARTESIAN_POINT ( 'NONE',  ( 16.27409532413455651, -0.09483548955922246892, -10.36544530239856776 ) ) ;
#16024=CARTESIAN_POINT ( 'NONE',  ( -19.16948585659999793, -11.07481571228000128, 1.129444447747999902 ) ) ;
#16026=CONICAL_SURFACE ( 'NONE', #5967, 13.20532192316000142, 0.7853981633972997312 ) ;
#16027=CARTESIAN_POINT ( 'NONE',  ( -3.821786116376766795, 14.05616651468782408, -4.851985683239589342 ) ) ;
#16028=ADVANCED_FACE ( 'NONE', ( #18304 ), #19691, .F. ) ;
#16030=ORIENTED_EDGE ( 'NONE', *, *, #19016, .T. ) ;
#16031=B_SPLINE_CURVE_WITH_KNOTS ( 'NONE', 3,
 ( #19633, #14297, #2798, #17933 ),
 .UNSPECIFIED., .F., .F.,
 ( 4, 4 ),
 ( 0.000000000000000000, 1.000000000000000000 ),
 .UNSPECIFIED. ) ;
#16033=CARTESIAN_POINT ( 'NONE',  ( 11.55284350193159781, 9.059841367859290173, -9.307687628695044069 ) ) ;
#16035=CARTESIAN_POINT ( 'NONE',  ( 24.10128254254044222, 9.799474070031209294, 4.098014295304180266 ) ) ;
#16038=ORIENTED_EDGE ( 'NONE', *, *, #10534, .T. ) ;
#16040=CARTESIAN_POINT ( 'NONE',  ( -24.37124162822864903, -12.10385983559206657, -4.035505227296023456 ) ) ;
#16041=CARTESIAN_POINT ( 'NONE',  ( 4.344185795461002364, 12.29657164613998965, -2.399808224106998455 ) ) ;
#16043=CARTESIAN_POINT ( 'NONE',  ( -14.55830234973948301, 8.677646559420217898, 5.656680062773181916 ) ) ;
#16044=ADVANCED_FACE ( 'NONE', ( #7265 ), #6095, .F. ) ;
#16045=CARTESIAN_POINT ( 'NONE',  ( 17.86387625731000028, 7.066414026761999700, 5.957971218261000956 ) ) ;
#16047=CIRCLE ( 'NONE', #10661, 12.50000000000000178 ) ;
#16050=CARTESIAN_POINT ( 'NONE',  ( -14.32799115069066964, -5.161629268668690429, -12.49976764740148738 ) ) ;
#16052=CARTESIAN_POINT ( 'NONE',  ( -19.20402730749667342, 3.634917981653388530, 8.480016702260009254 ) ) ;
#16053=CARTESIAN_POINT ( 'NONE',  ( -4.488270148404611248, 15.47262777994140492, -4.168027791541332405 ) ) ;
#16054=CARTESIAN_POINT ( 'NONE',  ( -22.34908598416999936, 4.767165090499999813, 8.950667383615998673 ) ) ;
#16055=CARTESIAN_POINT ( 'NONE',  ( -17.92967774839999962, -8.030155173115000267, -6.508010117819000406 ) ) ;
#16057=CARTESIAN_POINT ( 'NONE',  ( 16.61494494526000310, -5.066514564376999097, -8.972071948347000614 ) ) ;
#16059=CARTESIAN_POINT ( 'NONE',  ( 20.23031853028999905, -9.645356037285999662, -0.7083642361915000185 ) ) ;
#16060=EDGE_CURVE ( 'NONE', #11527, #13583, #9417, .T. ) ;
#16063=EDGE_CURVE ( 'NONE', #5788, #20521, #8474, .T. ) ;
#16064=CARTESIAN_POINT ( 'NONE',  ( 0.1602288781992032007, 13.69217011570514408, 6.122907753317686996 ) ) ;
#16066=AXIS2_PLACEMENT_3D ( 'NONE', #6139, #22965, #6259 ) ;
#16067=CARTESIAN_POINT ( 'NONE',  ( -19.62224577250664836, 2.401608896698385287, -8.935982437824780078 ) ) ;
#16068=CARTESIAN_POINT ( 'NONE',  ( -23.41895983166000050, -8.299257554761000577, 7.436471366131000238 ) ) ;
#16069=CARTESIAN_POINT ( 'NONE',  ( -1.999833674025762731, 11.65281303458884388, 4.383429770535894221 ) ) ;
#16070=ORIENTED_EDGE ( 'NONE', *, *, #5954, .T. ) ;
#16071=PLANE ( 'NONE',  #22288 ) ;
#16072=CARTESIAN_POINT ( 'NONE',  ( 3.908839010041529338, 12.11978010317259624, -2.848422584409191494 ) ) ;
#16073=EDGE_CURVE ( 'NONE', #18848, #9480, #2649, .T. ) ;
#16074=CARTESIAN_POINT ( 'NONE',  ( 24.00016455292000117, -6.692834685703999753, -6.438753808737999407 ) ) ;
#16075=EDGE_CURVE ( 'NONE', #13265, #93, #17461, .T. ) ;
#16076=CARTESIAN_POINT ( 'NONE',  ( 11.75726969619406859, -1.905973412920116905, -8.794923108305912507 ) ) ;
#16079=CARTESIAN_POINT ( 'NONE',  ( -6.106641414993810635, 16.02162000603732039, -1.041475911028451495 ) ) ;
#16080=CARTESIAN_POINT ( 'NONE',  ( 17.89031392131000331, 9.735558222862998434, -0.5785200253907000212 ) ) ;
#16081=CARTESIAN_POINT ( 'NONE',  ( 18.73721358075558996, 8.207010595434798716, 6.444024777827928929 ) ) ;
#16083=CARTESIAN_POINT ( 'NONE',  ( -22.15362306480054855, -7.387026419981959080, 5.677192137557457663 ) ) ;
#16085=CARTESIAN_POINT ( 'NONE',  ( -12.30391327053333583, 6.613167033160651798, -13.46344878000693335 ) ) ;
#16086=CARTESIAN_POINT ( 'NONE',  ( -1.534377289436119618, 13.80481766533376664, -5.932914363609297581 ) ) ;
#16090=CARTESIAN_POINT ( 'NONE',  ( 16.10729166666666146, -1.189047888634119143, 9.084626563006764854 ) ) ;
#16092=CARTESIAN_POINT ( 'NONE',  ( 14.94969105441765933, 7.308427648130778387, 7.574777027619624903 ) ) ;
#16093=CARTESIAN_POINT ( 'NONE',  ( -4.054781151688798602, 13.80041719377518561, 4.864580294094072777 ) ) ;
#16094=CARTESIAN_POINT ( 'NONE',  ( -12.25000000000000178, 11.90766680615234030, -9.280428257930019242 ) ) ;
#16095=DIRECTION ( 'NONE',  ( 1.000000000000000000, 0.000000000000000000, 0.000000000000000000 ) ) ;
#16103=CARTESIAN_POINT ( 'NONE',  ( 6.073936677003999307, 14.07872263210999364, 0.3711081957835999368 ) ) ;
#16104=CARTESIAN_POINT ( 'NONE',  ( 11.22311500625219338, -2.002057944114464139, -12.49998975379739186 ) ) ;
#16108=AXIS2_PLACEMENT_3D ( 'NONE', #6610, #23307, #10124 ) ;
#16112=CARTESIAN_POINT ( 'NONE',  ( 0.000000000000000000, 22.00000000000000000, 0.000000000000000000 ) ) ;
#16114=ORIENTED_EDGE ( 'NONE', *, *, #6152, .T. ) ;
#16115=CARTESIAN_POINT ( 'NONE',  ( -18.98973358726000171, -8.519062351032999914, 5.466345576189000077 ) ) ;
#16116=CIRCLE ( 'NONE', #3748, 12.50000000000000000 ) ;
#16118=CARTESIAN_POINT ( 'NONE',  ( 14.88765803210585936, 10.27488610670529567, -1.076485988655981219 ) ) ;
#16121=CARTESIAN_POINT ( 'NONE',  ( 13.59412034164153127, 6.790033948132051300, -5.939210046344768124 ) ) ;
#16122=CARTESIAN_POINT ( 'NONE',  ( -4.143293793513998402, 12.24260701129999163, -2.395728961457999961 ) ) ;
#16123=EDGE_LOOP ( 'NONE', ( #8485, #6438 ) ) ;
#16124=CARTESIAN_POINT ( 'NONE',  ( -21.61930420454665480, 5.669944305763950254, -7.377697031876467193 ) ) ;
#16125=ORIENTED_EDGE ( 'NONE', *, *, #23855, .F. ) ;
#16126=CARTESIAN_POINT ( 'NONE',  ( -14.25243324638999809, -7.716878364870000340, -11.63397459621999985 ) ) ;
#16131=CARTESIAN_POINT ( 'NONE',  ( 17.05208333333332149, 2.384110632780776395, -8.871840809039129638 ) ) ;
#16133=CARTESIAN_POINT ( 'NONE',  ( 12.00000000000000000, -3.587209763994826162, -8.231553737011857663 ) ) ;
#16134=CARTESIAN_POINT ( 'NONE',  ( 24.50000000000000000, 1.022558425347698252, -12.50000000000000000 ) ) ;
#16138=CARTESIAN_POINT ( 'NONE',  ( 13.49999999999999822, 7.972579677993858027, 5.894026230626296048 ) ) ;
#16139=SURFACE_SIDE_STYLE ('',( #1385 ) ) ;
#16142=CARTESIAN_POINT ( 'NONE',  ( -22.85864681265000087, 6.094397095768999684, 7.552485123145999957 ) ) ;
#16144=CARTESIAN_POINT ( 'NONE',  ( 21.11742861857828402, -10.38876745042508887, -1.818149675393893272 ) ) ;
#16146=CARTESIAN_POINT ( 'NONE',  ( 16.73436614837550351, 10.39850575958874046, 0.1513134148926907341 ) ) ;
#16148=STYLED_ITEM ( 'NONE', ( #6593 ), #872 ) ;
#16149=CARTESIAN_POINT ( 'NONE',  ( -18.48849577250666343, -7.991465547029055649, 4.605847420430258410 ) ) ;
#16151=CARTESIAN_POINT ( 'NONE',  ( -15.96111329461999695, 9.155832847151000209, -3.339520933045000195 ) ) ;
#16155=CARTESIAN_POINT ( 'NONE',  ( 23.62661714482716135, -8.104942212434002258, 4.670640012506109606 ) ) ;
#16156=CARTESIAN_POINT ( 'NONE',  ( 20.91190086703999995, -8.572222040414001043, 7.535479936335000239 ) ) ;
#16157=CARTESIAN_POINT ( 'NONE',  ( 23.42032133463317578, -4.048152030985803229, -9.797826222544841812 ) ) ;
#16158=FACE_OUTER_BOUND ( 'NONE', #2041, .T. ) ;
#16159=ORIENTED_EDGE ( 'NONE', *, *, #18437, .F. ) ;
#16162=CARTESIAN_POINT ( 'NONE',  ( 4.946118329716994388, 14.26837597718816397, -3.850108340392321526 ) ) ;
#16163=B_SPLINE_CURVE_WITH_KNOTS ( 'NONE', 3,
 ( #13735, #10489, #8424, #2732, #15663, #21133, #15792, #1021, #13985, #21010, #11813, #21377, #1157, #4544, #17875, #11938, #6477, #19323, #4794, #12177, #10114, #8299, #2972, #15907, #10363, #21857, #9020, #16391, #9135, #10953, #12538, #12877 ),
 .UNSPECIFIED., .F., .F.,
 ( 4, 2, 2, 2, 2, 2, 2, 2, 2, 2, 2, 2, 2, 2, 2, 4 ),
 ( 0.000000000000000000, 0.1250000000000008882, 0.1875000000000012212, 0.2187500000000014988, 0.2500000000000017764, 0.3125000000000019429, 0.3437500000000021649, 0.3750000000000023870, 0.5000000000000026645, 0.5625000000000026645, 0.5937500000000025535, 0.6250000000000024425, 0.6875000000000019984, 0.7187500000000017764, 0.7500000000000015543, 1.000000000000000000 ),
 .UNSPECIFIED. ) ;
#16165=CARTESIAN_POINT ( 'NONE',  ( -2.134826703869001197, 11.69852116739000358, -4.295920201858003828 ) ) ;
#16166=ORIENTED_EDGE ( 'NONE', *, *, #2419, .F. ) ;
#16167=CARTESIAN_POINT ( 'NONE',  ( 16.21856375731000099, 2.595497835609000159, 8.825947828509001170 ) ) ;
#16173=EDGE_CURVE ( 'NONE', #3985, #14395, #9064, .T. ) ;
#16176=CIRCLE ( 'NONE', #18139, 10.59999999999999964 ) ;
#16177=CARTESIAN_POINT ( 'NONE',  ( -4.103062808073617340, 15.05306268770272204, -4.547585820430672499 ) ) ;
#16178=CARTESIAN_POINT ( 'NONE',  ( -22.67025935411000148, 10.14480762656000046, -0.3150725993096000210 ) ) ;
#16179=CARTESIAN_POINT ( 'NONE',  ( -19.62077096955999878, 4.445609397689999298, -8.787304043923001018 ) ) ;
#16180=CARTESIAN_POINT ( 'NONE',  ( 18.52595833333332109, -7.314397928097276846, -5.620981225341208365 ) ) ;
#16181=CARTESIAN_POINT ( 'NONE',  ( 0.000000000000000000, 21.50000000000000000, 0.000000000000000000 ) ) ;
#16187=ORIENTED_EDGE ( 'NONE', *, *, #5844, .T. ) ;
#16189=CARTESIAN_POINT ( 'NONE',  ( 3.700975972481636678, 14.35177231820836319, 4.880830331095896035 ) ) ;
#16191=AXIS2_PLACEMENT_3D ( 'NONE', #16226, #12717, #10904 ) ;
#16192=CARTESIAN_POINT ( 'NONE',  ( -4.750000000000000000, 20.10000000000000142, 0.000000000000000000 ) ) ;
#16196=CARTESIAN_POINT ( 'NONE',  ( -3.558068219325319692, 12.01240764178410281, 3.274221823266413534 ) ) ;
#16198=CARTESIAN_POINT ( 'NONE',  ( -6.042815982636000172, 21.50000000000000000, -1.000000000000000000 ) ) ;
#16201=CARTESIAN_POINT ( 'NONE',  ( -21.05832910583999862, 9.211679941677999750, 0.000000000000000000 ) ) ;
#16202=CARTESIAN_POINT ( 'NONE',  ( -21.31697087121332856, 9.218317199134103745, 1.206801847291242513 ) ) ;
#16205=EDGE_CURVE ( 'NONE', #21708, #17401, #368, .T. ) ;
#16206=CARTESIAN_POINT ( 'NONE',  ( -5.529771451991000397, -1.199084044040999915E-14, 0.000000000000000000 ) ) ;
#16208=CARTESIAN_POINT ( 'NONE',  ( 13.17375142130999954, -7.436937191241000278, 6.115943375764999246 ) ) ;
#16209=CARTESIAN_POINT ( 'NONE',  ( 18.72046758034523961, 8.553234081428245261, 5.969153472710740260 ) ) ;
#16214=CARTESIAN_POINT ( 'NONE',  ( -24.50000000000000000, 10.82531754731000007, -6.250000000000000000 ) ) ;
#16217=B_SPLINE_CURVE_WITH_KNOTS ( 'NONE', 3,
 ( #23895, #7302, #7539, #14802, #22197, #1980, #14693, #22085, #12874, #3678, #20274, #11069 ),
 .UNSPECIFIED., .F., .F.,
 ( 4, 1, 1, 1, 1, 2, 2, 4 ),
 ( 0.000000000000000000, 0.2499999999999986122, 0.3749999999999980571, 0.4374999999999979461, 0.4687499999999978351, 0.4843749999999980016, 0.4999999999999981126, 1.000000000000000000 ),
 .UNSPECIFIED. ) ;
#16219=AXIS2_PLACEMENT_3D ( 'NONE', #8633, #20014, #15996 ) ;
#16222=CARTESIAN_POINT ( 'NONE',  ( 16.44741666666666546, -8.856630573480710922, 2.380283675663321663 ) ) ;
#16223=ADVANCED_FACE ( 'NONE', ( #7808 ), #2258, .F. ) ;
#16226=CARTESIAN_POINT ( 'NONE',  ( -24.50000000000000000, 1.524685264937999788E-14, 0.000000000000000000 ) ) ;
#16231=CARTESIAN_POINT ( 'NONE',  ( -11.04281598264000053, 16.43285860070444215, 0.1718092760798936858 ) ) ;
#16233=B_SPLINE_CURVE_WITH_KNOTS ( 'NONE', 3,
 ( #10192, #4626, #8256, #851, #8503, #22891, #17458, #15980, #15621, #1104, #21211, #15866, #12383, #10315, #21086, #6307, #1227, #12015, #4496, #23130, #17582, #2930, #14186, #17832, #8618, #3056, #19397, #8377, #23256, #13940, #21583, #19769, #10444, #14062, #21334, #9943, #23010, #15744, #4749, #13690, #11887, #12134, #19271, #19522, #17706, #21455, #2685, #6428, #4870, #13812, #1595, #18299, #21928, #20123, #1819, #5228, #8868, #10560, #10679 ),
 .UNSPECIFIED., .F., .F.,
 ( 4, 2, 2, 1, 1, 1, 1, 1, 2, 2, 2, 2, 2, 1, 1, 1, 2, 2, 2, 2, 2, 2, 1, 1, 2, 2, 2, 2, 1, 1, 1, 1, 1, 2, 2, 2, 4 ),
 ( 0.000000000000000000, 0.1250000000000092704, 0.1875000000000140721, 0.2187500000000165701, 0.2343750000000176248, 0.2421875000000181799, 0.2460937500000183187, 0.2480468750000185407, 0.2490234375000186240, 0.2500000000000187628, 0.3750000000000224265, 0.4375000000000242029, 0.4687500000000250910, 0.4843750000000255351, 0.4921875000000258127, 0.4960937500000259237, 0.4980468750000259237, 0.5000000000000259792, 0.5625000000000269784, 0.6250000000000278666, 0.6875000000000289768, 0.7187500000000294209, 0.7343750000000297540, 0.7421875000000298650, 0.7460937500000298650, 0.7500000000000299760, 0.8125000000000306422, 0.8437500000000309752, 0.8593750000000310862, 0.8671875000000311973, 0.8710937500000313083, 0.8730468750000311973, 0.8740234375000311973, 0.8745117187500313083, 0.8750000000000314193, 0.9375000000000157652, 1.000000000000000000 ),
 .UNSPECIFIED. ) ;
#16237=CARTESIAN_POINT ( 'NONE',  ( 5.259117788274003225, 14.75723778743001802, 3.160412202088998423 ) ) ;
#16238=CARTESIAN_POINT ( 'NONE',  ( 11.06619116163201078, 0.4983756421073917697, -12.49999828234741805 ) ) ;
#16239=CARTESIAN_POINT ( 'NONE',  ( 19.32833333333333670, 8.869419113210506467, 2.676869261568202596 ) ) ;
#16242=EDGE_LOOP ( 'NONE', ( #11714, #19765, #11251, #4879, #3053 ) ) ;
#16243=CARTESIAN_POINT ( 'NONE',  ( -18.43943555148999991, -2.412201287215999912, -10.06532802039999908 ) ) ;
#16244=CIRCLE ( 'NONE', #20128, 11.50000000000000000 ) ;
#16247=ORIENTED_EDGE ( 'NONE', *, *, #18378, .T. ) ;
#16248=CARTESIAN_POINT ( 'NONE',  ( -19.57635548768000078, 1.980828427502000055, 10.47560186498999890 ) ) ;
#16250=CARTESIAN_POINT ( 'NONE',  ( 14.54019110570222750, 2.698302716369401999, -9.963003989504706226 ) ) ;
#16252=CARTESIAN_POINT ( 'NONE',  ( 20.41802811994999800, 7.805777114999000510, 8.035878495494999996 ) ) ;
#16253=CARTESIAN_POINT ( 'NONE',  ( 24.24531177150999994, 0.000000000000000000, 0.000000000000000000 ) ) ;
#16254=CARTESIAN_POINT ( 'NONE',  ( 13.57120437455812656, 6.313184194241564740, -6.461219362146199963 ) ) ;
#16255=CARTESIAN_POINT ( 'NONE',  ( -3.536243307738002439, 12.19150164470999442, -3.169402752236001763 ) ) ;
#16256=VERTEX_POINT ( 'NONE', #15180 ) ;
#16259=CARTESIAN_POINT ( 'NONE',  ( -6.043485951305999748, 16.34784564573999788, 1.000000003648999991 ) ) ;
#16262=DIRECTION ( 'NONE',  ( 0.000000000000000000, 1.000000000000000000, 0.000000000000000000 ) ) ;
#16263=CARTESIAN_POINT ( 'NONE',  ( 11.72559253310116389, -12.88358093001479432, -2.684900464184909907 ) ) ;
#16265=CARTESIAN_POINT ( 'NONE',  ( 18.80965323898000108, 0.6517886434522999206, 11.11406264393000143 ) ) ;
#16266=ORIENTED_EDGE ( 'NONE', *, *, #1684, .F. ) ;
#16267=CARTESIAN_POINT ( 'NONE',  ( -11.72719613877000100, 5.763420833702999957, 14.08487056595000020 ) ) ;
#16268=CARTESIAN_POINT ( 'NONE',  ( 13.50000000000000000, 9.165557434110747081, -2.271160277613796907 ) ) ;
#16271=CARTESIAN_POINT ( 'NONE',  ( 20.73503899750121704, -4.285134948126297694, 9.623718970242478576 ) ) ;
#16273=CARTESIAN_POINT ( 'NONE',  ( 15.93025666723834100, -9.681699128342794225, -3.681818963616494855 ) ) ;
#16274=CARTESIAN_POINT ( 'NONE',  ( -19.28992806661999992, -9.239313293073999844, 5.311636531851000598 ) ) ;
#16277=CARTESIAN_POINT ( 'NONE',  ( -12.30476703115999904, 8.600742661000001732, -2.211712587549000020 ) ) ;
#16280=CARTESIAN_POINT ( 'NONE',  ( -24.16119556692343551, -4.108075932065574420, 12.49973851152546089 ) ) ;
#16281=CARTESIAN_POINT ( 'NONE',  ( 11.92450592357671368, 13.18099206878371632, -2.169941377000860872 ) ) ;
#16282=CARTESIAN_POINT ( 'NONE',  ( 22.34213275544827937, 8.806011279328485486, 5.853390237427837484 ) ) ;
#16285=EDGE_CURVE ( 'NONE', #4621, #18634, #1558, .T. ) ;
#16286=CARTESIAN_POINT ( 'NONE',  ( 24.18393254356834632, -8.381833107684220963, -10.48223919692640393 ) ) ;
#16288=CARTESIAN_POINT ( 'NONE',  ( 3.823771652646001051, 12.06071475417000194, -3.000030641231999695 ) ) ;
#16289=ORIENTED_EDGE ( 'NONE', *, *, #14699, .T. ) ;
#16294=CARTESIAN_POINT ( 'NONE',  ( -14.49454818139149737, -1.035381146742340386, -12.50000698752768180 ) ) ;
#16295=B_SPLINE_CURVE_WITH_KNOTS ( 'NONE', 3,
 ( #9335, #14773, #9453, #16707, #118, #1830, #16827, #5580, #7154, #18204, #231, #1605, #9217, #23864, #22406, #1711, #20358, #5815, #7, #3429, #22169, #3766, #7506, #18309, #10813, #8990, #7390, #16361, #23750, #21938, #20132, #14889 ),
 .UNSPECIFIED., .F., .F.,
 ( 4, 2, 2, 2, 2, 2, 2, 2, 1, 2, 2, 2, 1, 1, 1, 2, 2, 4 ),
 ( 0.000000000000000000, 0.2500000000000005551, 0.3750000000000008327, 0.4374999999999986122, 0.4687499999999996114, 0.5000000000000005551, 0.6250000000000122125, 0.6875000000000178746, 0.7187500000000202061, 0.7343750000000223155, 0.7500000000000243139, 0.8125000000000297540, 0.8437500000000324185, 0.8593750000000328626, 0.8671875000000330846, 0.8710937500000331957, 0.8750000000000334177, 1.000000000000000000 ),
 .UNSPECIFIED. ) ;
#16298=CARTESIAN_POINT ( 'NONE',  ( -15.04355420454667325, -9.057328963212048833, 1.185474641176787802 ) ) ;
#16299=CARTESIAN_POINT ( 'NONE',  ( -22.02791261424000169, -5.912491595945999379, 8.228415427290999062 ) ) ;
#16300=CARTESIAN_POINT ( 'NONE',  ( -13.66394044103999938, 9.112107522246999380, -2.343211941154000222 ) ) ;
#16301=CARTESIAN_POINT ( 'NONE',  ( -6.143111768200996359, 14.96860033859000971, -3.824985432946004682 ) ) ;
#16302=CARTESIAN_POINT ( 'NONE',  ( -22.02842343893881250, 9.533828963910684351, 5.524295927557433927 ) ) ;
#16307=CARTESIAN_POINT ( 'NONE',  ( 24.00016455292000117, -9.066063387507998783, 2.014468017461000127 ) ) ;
#16313=CARTESIAN_POINT ( 'NONE',  ( 4.467732293902829888, 12.30836910800113060, 1.873439991674330285 ) ) ;
#16314=ORIENTED_EDGE ( 'NONE', *, *, #10313, .T. ) ;
#16315=CARTESIAN_POINT ( 'NONE',  ( -23.75856372112291481, -13.93375672973999890, 0.09623563749425553815 ) ) ;
#16316=CARTESIAN_POINT ( 'NONE',  ( 4.431702799432089002, 12.29558746875803976, -1.954764367055115803 ) ) ;
#16317=CARTESIAN_POINT ( 'NONE',  ( -17.72676253787999912, 9.126185377371999863, 0.000000000000000000 ) ) ;
#16319=CARTESIAN_POINT ( 'NONE',  ( -21.05242920454665878, 4.638983325918172085, 8.048956833715248393 ) ) ;
#16323=CARTESIAN_POINT ( 'NONE',  ( -16.10172087121332396, 7.264650085109141564, -5.582749836826320866 ) ) ;
#16324=CARTESIAN_POINT ( 'NONE',  ( 16.02562642131000104, 9.437180554902999674, -2.258696805882000280 ) ) ;
#16325=CARTESIAN_POINT ( 'NONE',  ( 18.80165828517651150, 6.582155627870158732, 8.096495908088112259 ) ) ;
#16330=CARTESIAN_POINT ( 'NONE',  ( 13.49999999999999822, -9.119346161239230142, 3.853256094986214908 ) ) ;
#16335=CARTESIAN_POINT ( 'NONE',  ( 23.31148506108999996, -6.143795288837999635, -9.535093121894000490 ) ) ;
#16337=CARTESIAN_POINT ( 'NONE',  ( 24.50000000000000000, -2.116736914405999759, 10.36413001332999961 ) ) ;
#16338=CARTESIAN_POINT ( 'NONE',  ( -4.085530525064275054, 13.77267084576624079, 4.872318283361749991 ) ) ;
#16339=CARTESIAN_POINT ( 'NONE',  ( -4.943683218093997134, 12.51395247683998058, -0.06195390666880997571 ) ) ;
#16341=CARTESIAN_POINT ( 'NONE',  ( 12.50000000000000000, 13.93375672974000068, 0.000000000000000000 ) ) ;
#16349=CARTESIAN_POINT ( 'NONE',  ( 6.132698908501003743, 14.49462454531001754, 0.1095711543429000179 ) ) ;
#16350=CARTESIAN_POINT ( 'NONE',  ( 12.28022044528181311, -5.662962823250645705, -12.50000000000071942 ) ) ;
#16351=AXIS2_PLACEMENT_3D ( 'NONE', #10449, #23377, #18069 ) ;
#16352=CARTESIAN_POINT ( 'NONE',  ( 19.66566666666665952, 1.030022276571363804, 9.215888979280039806 ) ) ;
#16353=CARTESIAN_POINT ( 'NONE',  ( -5.539688061797002128, 16.26872474856999773, -2.643098357780001351 ) ) ;
#16356=ORIENTED_EDGE ( 'NONE', *, *, #10862, .T. ) ;
#16357=CARTESIAN_POINT ( 'NONE',  ( -18.60180781823000018, -9.793299576559000741, 0.7034231180304000297 ) ) ;
#16359=CARTESIAN_POINT ( 'NONE',  ( 11.00000000000000000, 0.000000000000000000, 0.000000000000000000 ) ) ;
#16361=CARTESIAN_POINT ( 'NONE',  ( -10.83632914535144920, 15.36350589476169937, -1.682004463026524066 ) ) ;
#16363=CARTESIAN_POINT ( 'NONE',  ( 14.80091196040006984, 9.530334370396518651, -3.997581378746529968 ) ) ;
#16365=CARTESIAN_POINT ( 'NONE',  ( 23.35477952741999985, -0.2659429092311000331, -11.28040236504000049 ) ) ;
#16367=CARTESIAN_POINT ( 'NONE',  ( 13.80060059804144501, 9.025283489161427752, -0.03376589920026255159 ) ) ;
#16368=CARTESIAN_POINT ( 'NONE',  ( -4.660137320655001858, 12.58447456225998984, -1.233398502364998484 ) ) ;
#16369=CARTESIAN_POINT ( 'NONE',  ( -22.26176253788000281, -9.242562415387000740, 0.000000000000000000 ) ) ;
#16371=ORIENTED_EDGE ( 'NONE', *, *, #4832, .T. ) ;
#16372=DIRECTION ( 'NONE',  ( 1.000000000000000000, 0.000000000000000000, 0.000000000000000000 ) ) ;
#16376=CARTESIAN_POINT ( 'NONE',  ( 17.12766666666665571, 4.588260261546838414, -7.960951565941960517 ) ) ;
#16377=CARTESIAN_POINT ( 'NONE',  ( 24.50000000000000000, 0.000000000000000000, 0.000000000000000000 ) ) ;
#16378=CARTESIAN_POINT ( 'NONE',  ( 16.46379156698999680, 10.47191086351999978, -3.587674625133999928 ) ) ;
#16381=CARTESIAN_POINT ( 'NONE',  ( -10.10541006585000012, 9.582871899720000641, 11.36777908496999956 ) ) ;
#16382=CARTESIAN_POINT ( 'NONE',  ( 13.50000000000000000, 8.796014925232748638, 4.387719908057123419 ) ) ;
#16384=ORIENTED_EDGE ( 'NONE', *, *, #11500, .T. ) ;
#16385=CARTESIAN_POINT ( 'NONE',  ( 20.49972230760754854, 4.054746914731249596, 9.712109459497844099 ) ) ;
#16386=CARTESIAN_POINT ( 'NONE',  ( -24.50000000000000000, -10.30000000000000071, 0.000000000000000000 ) ) ;
#16387=CARTESIAN_POINT ( 'NONE',  ( 16.06122657628786143, -7.038767995605364369, -7.618814742105207038 ) ) ;
#16388=DIRECTION ( 'NONE',  ( 0.000000000000000000, 1.000000000000000000, 0.000000000000000000 ) ) ;
#16391=CARTESIAN_POINT ( 'NONE',  ( -14.44600769525627904, -12.24671445775785728, 3.788037462221160112 ) ) ;
#16394=ORIENTED_EDGE ( 'NONE', *, *, #12889, .F. ) ;
#16395=CARTESIAN_POINT ( 'NONE',  ( 20.35599589905567086, 10.52498947291094744, -0.1069429831477965442 ) ) ;
#16399=CARTESIAN_POINT ( 'NONE',  ( 20.43528936713000377, -9.195691514035999603, 0.000000000000000000 ) ) ;
#16400=CARTESIAN_POINT ( 'NONE',  ( 4.835835251289409165, 14.67308180627193082, -3.769935304963333511 ) ) ;
#16401=CARTESIAN_POINT ( 'NONE',  ( -4.910842247424000107, 12.43786476712998912, -0.3318925675130997011 ) ) ;
#16403=CARTESIAN_POINT ( 'NONE',  ( -15.00576253787999903, -9.056359154562001024, 0.000000000000000000 ) ) ;
#16406=CARTESIAN_POINT ( 'NONE',  ( -3.644446339697000159, 14.33206891720999998, 4.922772686299000000 ) ) ;
#16409=ORIENTED_EDGE ( 'NONE', *, *, #7395, .F. ) ;
#16410=CARTESIAN_POINT ( 'NONE',  ( 22.24928936712999672, -9.242242329243000043, 0.000000000000000000 ) ) ;
#16411=AXIS2_PLACEMENT_3D ( 'NONE', #3224, #10606, #16388 ) ;
#16412=CARTESIAN_POINT ( 'NONE',  ( -20.74321913448999766, 9.448588360516998463, 3.561785475570999893 ) ) ;
#16413=ORIENTED_CLOSED_SHELL ( 'NONE', *, #13106, .F. );
#16414=CARTESIAN_POINT ( 'NONE',  ( -16.77694609798000158, -7.614211477670999706, 6.119569497340999753 ) ) ;
#16415=CARTESIAN_POINT ( 'NONE',  ( -4.770933648794001058, 13.03075770454000448, -5.112134952572002788 ) ) ;
#16416=CARTESIAN_POINT ( 'NONE',  ( -23.44385535506140172, -3.478864065003184791, 9.993471346658315824 ) ) ;
#16419=CARTESIAN_POINT ( 'NONE',  ( -6.579472545193000954, 15.16114063110001986, 2.985323136169000691 ) ) ;
#16421=EDGE_LOOP ( 'NONE', ( #21482, #12166, #10880, #7118 ) ) ;
#16422=CARTESIAN_POINT ( 'NONE',  ( 23.40350286971751004, 6.148604348410775522, 7.026089829741110293 ) ) ;
#16424=CARTESIAN_POINT ( 'NONE',  ( 14.83790034821742587, -7.812907433739113117, 4.674760609328123095 ) ) ;
#16425=CARTESIAN_POINT ( 'NONE',  ( 5.826617149234366799, 14.45297212092532213, -1.888469283984045566 ) ) ;
#16428=CARTESIAN_POINT ( 'NONE',  ( 2.218588997953582442, 11.69175043203580877, 4.278498257537161287 ) ) ;
#16430=CARTESIAN_POINT ( 'NONE',  ( -2.776765130543696447, 11.80852668188584964, -3.944772877159900215 ) ) ;
#16431=CARTESIAN_POINT ( 'NONE',  ( -10.19258028079843825, 15.86589456477620708, 1.102853906025392350 ) ) ;
#16434=DIRECTION ( 'NONE',  ( 0.000000000000000000, 0.000000000000000000, -1.000000000000000000 ) ) ;
#16435=CARTESIAN_POINT ( 'NONE',  ( -14.25622733613999849, 13.93375672974000068, -0.4335075757610999947 ) ) ;
#16436=CARTESIAN_POINT ( 'NONE',  ( 15.39393908531000044, -10.10652924631000005, 1.349470982713999900 ) ) ;
#16437=CARTESIAN_POINT ( 'NONE',  ( 18.66008262533330964, 9.600337245201069791, 4.090230547807212069 ) ) ;
#16439=EDGE_CURVE ( 'NONE', #20267, #5409, #23139, .T. ) ;
#16442=CARTESIAN_POINT ( 'NONE',  ( 4.750000000000000000, 17.00000000000000000, 0.000000000000000000 ) ) ;
#16443=CARTESIAN_POINT ( 'NONE',  ( 13.49999999999999822, -9.438739345711907092, -1.583349858395037835 ) ) ;
#16444=AXIS2_PLACEMENT_3D ( 'NONE', #22609, #22726, #15461 ) ;
#16446=DIRECTION ( 'NONE',  ( 0.000000000000000000, 0.9995313430878892680, -0.03061199413497965940 ) ) ;
#16447=CARTESIAN_POINT ( 'NONE',  ( 23.84263236754999937, 10.83869278701999939, -3.393613122837999985 ) ) ;
#16448=CARTESIAN_POINT ( 'NONE',  ( 8.124934037954998800, 12.44999999999999929, 0.000000000000000000 ) ) ;
#16449=FACE_BOUND ( 'NONE', #12689, .T. ) ;
#16450=DIRECTION ( 'NONE',  ( 0.000000000000000000, -1.000000000000000000, 0.000000000000000000 ) ) ;
#16451=CARTESIAN_POINT ( 'NONE',  ( -1.986170008003000698, 11.69253133399998745, 4.555489092804997142 ) ) ;
#16454=CARTESIAN_POINT ( 'NONE',  ( -22.64492594945000192, -10.12459746114000048, -4.604741694910000405 ) ) ;
#16455=ORIENTED_EDGE ( 'NONE', *, *, #4339, .T. ) ;
#16459=CARTESIAN_POINT ( 'NONE',  ( 5.316076279024001039, 13.97452196382998579, 3.340701199846999092 ) ) ;
#16460=AXIS2_PLACEMENT_3D ( 'NONE', #5381, #7185, #12769 ) ;
#16461=CARTESIAN_POINT ( 'NONE',  ( 12.52688711657000020, -6.216878364870000340, -12.50000000000000000 ) ) ;
#16466=CARTESIAN_POINT ( 'NONE',  ( 12.21300158531000157, -1.561560366126000021, -9.991316461899998558 ) ) ;
#16467=VERTEX_POINT ( 'NONE', #17495 ) ;
#16468=DIRECTION ( 'NONE',  ( 0.000000000000000000, 1.000000000000000000, 0.000000000000000000 ) ) ;
#16470=FACE_OUTER_BOUND ( 'NONE', #2141, .T. ) ;
#16471=EDGE_CURVE ( 'NONE', #13328, #12183, #18029, .T. ) ;
#16473=LINE ( 'NONE', #1949, #22738 ) ;
#16475=CARTESIAN_POINT ( 'NONE',  ( 14.84742989479702402, 10.04995572500151368, -2.448758008351840765 ) ) ;
#16477=DIRECTION ( 'NONE',  ( -1.000000000000000000, 0.000000000000000000, 0.000000000000000000 ) ) ;
#16478=CARTESIAN_POINT ( 'NONE',  ( 24.23558897616999985, 6.589873019469000504, 9.188931193771999517 ) ) ;
#16480=CARTESIAN_POINT ( 'NONE',  ( 13.85469833500055614, 8.899865800911998193, 1.702839090396268018 ) ) ;
#16485=ADVANCED_FACE ( 'NONE', ( #772 ), #3066, .T. ) ;
#16487=FACE_OUTER_BOUND ( 'NONE', #16802, .T. ) ;
#16488=LINE ( 'NONE', #18433, #11926 ) ;
#16491=CARTESIAN_POINT ( 'NONE',  ( 16.90091666666665304, -2.383329820012265010, -8.867965379002798798 ) ) ;
#16494=CARTESIAN_POINT ( 'NONE',  ( 13.90364969620000046, -10.56859681273999918, 3.047681783393999755 ) ) ;
#16495=CARTESIAN_POINT ( 'NONE',  ( -14.78159224757403756, 10.16956135232626579, -2.008721191966370778 ) ) ;
#16497=ORIENTED_EDGE ( 'NONE', *, *, #22482, .F. ) ;
#16498=CIRCLE ( 'NONE', #1033, 11.50000000000000000 ) ;
#16499=CARTESIAN_POINT ( 'NONE',  ( -12.14186006585000044, 2.782277322838000000, -14.15314130824000038 ) ) ;
#16500=CARTESIAN_POINT ( 'NONE',  ( 13.49999999999999822, 4.107543256433543455, 9.382311906318680172 ) ) ;
#16502=EDGE_CURVE ( 'NONE', #22006, #1172, #16176, .T. ) ;
#16503=ORIENTED_EDGE ( 'NONE', *, *, #17664, .T. ) ;
#16504=EDGE_CURVE ( 'NONE', #379, #3740, #3810, .T. ) ;
#16505=CARTESIAN_POINT ( 'NONE',  ( 22.61757251664768020, -6.462774339621367048, 8.380718989448364908 ) ) ;
#16508=CARTESIAN_POINT ( 'NONE',  ( 16.00077574048890838, -8.450110195753781639, -5.996695405704878468 ) ) ;
#16509=CARTESIAN_POINT ( 'NONE',  ( -13.56892309062000201, -9.272801077787999446, -4.451380411803999237 ) ) ;
#16512=CARTESIAN_POINT ( 'NONE',  ( -18.64256589945999920, -8.356153348075000764, -6.118136038720999537 ) ) ;
#16519=CARTESIAN_POINT ( 'NONE',  ( 21.23557079259970948, -10.49101315042518578, 1.100340162171684399 ) ) ;
#16522=EDGE_LOOP ( 'NONE', ( #9027, #2536, #4465, #19577, #20641 ) ) ;
#16523=DIRECTION ( 'NONE',  ( 0.000000000000000000, -1.000000000000000000, 0.000000000000000000 ) ) ;
#16524=CARTESIAN_POINT ( 'NONE',  ( -14.25851234391999967, -6.965719916941000456, -12.06765612833000034 ) ) ;
#16525=CARTESIAN_POINT ( 'NONE',  ( 4.782053000032003176, 12.48037919467000378, -0.1093042574499999697 ) ) ;
#16527=CARTESIAN_POINT ( 'NONE',  ( 14.46356375731000021, 0.7465905146449000052, 9.123040730097999429 ) ) ;
#16529=B_SPLINE_CURVE_WITH_KNOTS ( 'NONE', 3,
 ( #1715, #18768, #2178, #5698, #9338, #20248, #1834, #356, #13084, #14892, #23867, #7637, #18545, #1952, #22283, #10927, #3654, #16710 ),
 .UNSPECIFIED., .F., .F.,
 ( 4, 2, 2, 2, 2, 2, 2, 2, 4 ),
 ( 0.000000000000000000, 0.1250000000000000000, 0.2500000000000000000, 0.3750000000000000000, 0.5000000000000000000, 0.6250000000000000000, 0.7500000000000000000, 0.8750000000000000000, 1.000000000000000000 ),
 .UNSPECIFIED. ) ;
#16530=CARTESIAN_POINT ( 'NONE',  ( -5.140663980495288499, 15.95621494436533183, 3.330719948904278471 ) ) ;
#16531=CARTESIAN_POINT ( 'NONE',  ( -14.49999964368427641, -0.5192523986907622291, -12.50000205182226942 ) ) ;
#16533=TOROIDAL_SURFACE ( 'NONE', #18097, 10.69999999999999929, 0.8000000000000000444 ) ;
#16534=CARTESIAN_POINT ( 'NONE',  ( 22.55162270046334072, -4.658593254882972268, -8.082476209181939097 ) ) ;
#16535=CARTESIAN_POINT ( 'NONE',  ( -25.29471151901000070, -3.100331240559000001, -8.843271378586997855 ) ) ;
#16536=CARTESIAN_POINT ( 'NONE',  ( 12.04708237236350321, -8.300001990989077427, -10.62407327360604903 ) ) ;
#16538=CARTESIAN_POINT ( 'NONE',  ( -23.46959048080880450, -2.571725778583679123, 10.26703556566396358 ) ) ;
#16540=CARTESIAN_POINT ( 'NONE',  ( -6.895677774260998483, 15.29532879160001002, 2.228068349403999893 ) ) ;
#16543=CARTESIAN_POINT ( 'NONE',  ( 3.546651244991242180, 14.29878692723004008, 4.995327959777049465 ) ) ;
#16544=CARTESIAN_POINT ( 'NONE',  ( 5.125153960889105242, 13.67047962957576779, -4.635569058280919030 ) ) ;
#16546=CARTESIAN_POINT ( 'NONE',  ( -24.39296691846460519, -5.087329382176355885, -9.307667590984573636 ) ) ;
#16550=CARTESIAN_POINT ( 'NONE',  ( 4.341046485804971766, 12.26343790180346538, 2.152316017657149860 ) ) ;
#16552=CONICAL_SURFACE ( 'NONE', #17332, 9.161549281532000322, 0.02565634000431304615 ) ;
#16554=CARTESIAN_POINT ( 'NONE',  ( -3.593739972392233639, 12.02247931475103471, -3.238798760568094348 ) ) ;
#16558=CARTESIAN_POINT ( 'NONE',  ( 16.80728936713000365, -9.102589883624000677, 0.000000000000000000 ) ) ;
#16560=CARTESIAN_POINT ( 'NONE',  ( 17.80706408530999951, 3.725969113535000155, -9.559170675091001712 ) ) ;
#16561=CARTESIAN_POINT ( 'NONE',  ( 18.71397797831778576, 8.679856506646080661, 5.781186714009264094 ) ) ;
#16563=DIRECTION ( 'NONE',  ( -1.000000000000000000, 0.000000000000000000, 0.000000000000000000 ) ) ;
#16564=DIRECTION ( 'NONE',  ( 0.000000000000000000, 1.000000000000000000, 0.000000000000000000 ) ) ;
#16565=CARTESIAN_POINT ( 'NONE',  ( 13.50000000000000355, -7.263987176282556746, 7.058588360321458310 ) ) ;
#16567=ORIENTED_EDGE ( 'NONE', *, *, #6981, .F. ) ;
#16569=CARTESIAN_POINT ( 'NONE',  ( 23.22869142897999950, -10.53159633789999994, 2.444661321055999981 ) ) ;
#16572=CARTESIAN_POINT ( 'NONE',  ( -24.25991043033701544, 10.09239344780629288, 0.3498110921733544876 ) ) ;
#16575=CARTESIAN_POINT ( 'NONE',  ( -4.784077338775003518, 12.40247651101999615, 0.7311471882772000441 ) ) ;
#16578=ORIENTED_EDGE ( 'NONE', *, *, #2299, .T. ) ;
#16581=ORIENTED_EDGE ( 'NONE', *, *, #18300, .F. ) ;
#16582=ADVANCED_FACE ( 'NONE', ( #12649 ), #20606, .F. ) ;
#16583=CARTESIAN_POINT ( 'NONE',  ( 6.273481336118004847, 13.70231772578000573, -0.06242386448472003746 ) ) ;
#16584=CARTESIAN_POINT ( 'NONE',  ( 11.59051697471118558, 3.660525265870015144, -12.49991113090446149 ) ) ;
#16587=CARTESIAN_POINT ( 'NONE',  ( 18.16256424931000168, 7.359336859262000097, -7.874515470102998904 ) ) ;
#16590=CARTESIAN_POINT ( 'NONE',  ( -15.55485259867999837, 4.780789984251000213, 8.479691756156000793 ) ) ;
#16595=EDGE_CURVE ( 'NONE', #3987, #19046, #16473, .T. ) ;
#16596=CARTESIAN_POINT ( 'NONE',  ( -22.73347842219999748, -8.487330385069000727, -7.414930595396000079 ) ) ;
#16598=CARTESIAN_POINT ( 'NONE',  ( 14.42291159610915408, -1.391709837791132109, -10.22364117141589368 ) ) ;
#16600=LINE ( 'NONE', #20593, #9487 ) ;
#16601=CARTESIAN_POINT ( 'NONE',  ( 22.40011934649999858, 7.222069075570000329, 8.635347600991998718 ) ) ;
#16603=CARTESIAN_POINT ( 'NONE',  ( 13.80184222826903806, 9.025291706593257857, 0.005214362689862574347 ) ) ;
#16604=CARTESIAN_POINT ( 'NONE',  ( -3.195009042999999771, 12.10691817796999636, -3.616280525526001988 ) ) ;
#16608=CARTESIAN_POINT ( 'NONE',  ( 24.50000000000000355, -10.16681666949672191, 1.404953793027732933 ) ) ;
#16611=ORIENTED_EDGE ( 'NONE', *, *, #16285, .F. ) ;
#16612=EDGE_CURVE ( 'NONE', #19046, #11394, #16295, .T. ) ;
#16613=CARTESIAN_POINT ( 'NONE',  ( 11.47028936713000036, -8.379193606113998882, -3.189305674207999708 ) ) ;
#16614=CARTESIAN_POINT ( 'NONE',  ( -6.249993692867000128, 16.07374114947999999, -3.420978559755999626 ) ) ;
#16615=DIRECTION ( 'NONE',  ( 0.000000000000000000, 0.8075558440518585401, 0.5897911144953695839 ) ) ;
#16616=CARTESIAN_POINT ( 'NONE',  ( 18.38109284136999833, 6.121338008679999554, -9.285840504967000086 ) ) ;
#16619=ORIENTED_EDGE ( 'NONE', *, *, #5666, .F. ) ;
#16620=CARTESIAN_POINT ( 'NONE',  ( -10.51270006584999805, 9.971762425829000520, -11.02822693349000005 ) ) ;
#16622=CARTESIAN_POINT ( 'NONE',  ( -14.48092005499817425, -11.66846015894605770, -4.789644024572045744 ) ) ;
#16623=VERTEX_POINT ( 'NONE', #22279 ) ;
#16625=CARTESIAN_POINT ( 'NONE',  ( -12.26714646669999986, 6.430159825535999296, -13.55186498671000095 ) ) ;
#16626=CARTESIAN_POINT ( 'NONE',  ( 20.81320603379664647, -2.409608536984290783, -8.965749368246138218 ) ) ;
#16627=CYLINDRICAL_SURFACE ( 'NONE', #16460, 4.750000000000000000 ) ;
#16628=CARTESIAN_POINT ( 'NONE',  ( 16.01310729382478826, -8.177487985005738480, -6.358481180217821382 ) ) ;
#16629=CARTESIAN_POINT ( 'NONE',  ( -14.29157635075000066, 5.124190584818000715, 9.732655983376998776 ) ) ;
#16632=CARTESIAN_POINT ( 'NONE',  ( -18.84569624743000205, -10.33415972889999956, 0.7423446255362999846 ) ) ;
#16633=ADVANCED_FACE ( 'NONE', ( #7271 ), #17310, .F. ) ;
#16635=ORIENTED_EDGE ( 'NONE', *, *, #13375, .T. ) ;
#16637=CARTESIAN_POINT ( 'NONE',  ( 19.56154115649750835, -9.843004022036630829, -3.930645473631872555 ) ) ;
#16639=EDGE_LOOP ( 'NONE', ( #17745, #23074, #22194, #20231 ) ) ;
#16640=EDGE_CURVE ( 'NONE', #9734, #386, #6476, .T. ) ;
#16644=CARTESIAN_POINT ( 'NONE',  ( -0.5922303555482001380, 11.50778550622999852, -4.771349591085003006 ) ) ;
#16645=CARTESIAN_POINT ( 'NONE',  ( 12.48918875731000000, 5.414613097170000167, 7.315858880121999697 ) ) ;
#16647=CARTESIAN_POINT ( 'NONE',  ( -4.645659211928634846, 15.61175543958523981, 3.991716869351718433 ) ) ;
#16650=VERTEX_POINT ( 'NONE', #19120 ) ;
#16652=FACE_OUTER_BOUND ( 'NONE', #1096, .T. ) ;
#16654=CARTESIAN_POINT ( 'NONE',  ( 2.290777621496001171, 11.89229473561999839, 4.253142527875998447 ) ) ;
#16656=CARTESIAN_POINT ( 'NONE',  ( -22.77885345450999921, 8.335141950908999675, 4.829927459581000448 ) ) ;
#16657=CARTESIAN_POINT ( 'NONE',  ( -13.93312122640000084, 8.641212754535999352, -2.222119620850000032 ) ) ;
#16658=CARTESIAN_POINT ( 'NONE',  ( -23.82988224127242205, 8.924282944053008038, 5.705145624228507906 ) ) ;
#16660=CARTESIAN_POINT ( 'NONE',  ( 16.03170833333333078, 1.189047888634058303, 9.082686945706512915 ) ) ;
#16663=VERTEX_POINT ( 'NONE', #14402 ) ;
#16665=CARTESIAN_POINT ( 'NONE',  ( 14.27789894812851301, 7.165480330777101337, 5.593028109329393871 ) ) ;
#16666=CARTESIAN_POINT ( 'NONE',  ( -23.64322841789023144, 9.153672998692304219, 5.321353405662923031 ) ) ;
#16669=CARTESIAN_POINT ( 'NONE',  ( 3.368441454496569509, 11.95864406845431382, 3.464918207308566700 ) ) ;
#16670=ORIENTED_EDGE ( 'NONE', *, *, #14566, .F. ) ;
#16671=CARTESIAN_POINT ( 'NONE',  ( -3.391218646352913701, 11.96540231941397714, -3.439755270211452221 ) ) ;
#16672=LINE ( 'NONE', #9651, #2214 ) ;
#16675=ADVANCED_FACE ( 'NONE', ( #1799 ), #9186, .T. ) ;
#16677=CARTESIAN_POINT ( 'NONE',  ( 12.54206408531000072, 8.432320343758000547, -5.597842903599000053 ) ) ;
#16678=CARTESIAN_POINT ( 'NONE',  ( 18.16027265446844297, 2.522309870967282652, -10.13363737170168477 ) ) ;
#16679=CARTESIAN_POINT ( 'NONE',  ( -23.99212502906159017, 5.142273543674439118, 12.50000000000264144 ) ) ;
#16681=CARTESIAN_POINT ( 'NONE',  ( 23.99062354302999722, -7.716878364870000340, -11.63397459621999985 ) ) ;
#16684=CARTESIAN_POINT ( 'NONE',  ( -24.50000000000293454, 10.95355345391266511, 6.027888894412471998 ) ) ;
#16685=CARTESIAN_POINT ( 'NONE',  ( 23.48853416324000065, 0.4636106205751999720, -11.33838736911999945 ) ) ;
#16686=CARTESIAN_POINT ( 'NONE',  ( -24.32816120980435670, 9.615500567526682474, -3.310132273745861387 ) ) ;
#16687=ORIENTED_EDGE ( 'NONE', *, *, #22403, .T. ) ;
#16688=CARTESIAN_POINT ( 'NONE',  ( 13.63946275288138565, -8.561423039799775481, 5.801876326834510600 ) ) ;
#16690=CARTESIAN_POINT ( 'NONE',  ( -4.479356662876004869, 12.28735091408998592, 1.840098238078000881 ) ) ;
#16693=CARTESIAN_POINT ( 'NONE',  ( -20.97408049164000232, -11.05085136034000115, 0.7637451293671000396 ) ) ;
#16694=VERTEX_POINT ( 'NONE', #5209 ) ;
#16698=CARTESIAN_POINT ( 'NONE',  ( 6.181149466256997016, 13.72396362260998970, 1.092410950252000301 ) ) ;
#16699=CARTESIAN_POINT ( 'NONE',  ( 16.31599770046333120, 1.190002857594358643, 9.089982371172002473 ) ) ;
#16700=DIRECTION ( 'NONE',  ( 0.000000000000000000, 1.000000000000000000, 0.000000000000000000 ) ) ;
#16701=DIRECTION ( 'NONE',  ( 0.000000000000000000, 1.000000000000000000, 0.000000000000000000 ) ) ;
#16702=CARTESIAN_POINT ( 'NONE',  ( 14.18737658531000001, 3.962519675866999602, -9.360324180111000203 ) ) ;
#16703=CARTESIAN_POINT ( 'NONE',  ( -14.33607051085999906, 5.206569482801000071, -8.184903637703000001 ) ) ;
#16704=CARTESIAN_POINT ( 'NONE',  ( -14.00000000000000000, 8.507292963980999545, 3.029321241734000303 ) ) ;
#16705=CARTESIAN_POINT ( 'NONE',  ( -14.44633172591991865, 2.842506014205136822, 12.49999152949037651 ) ) ;
#16706=VERTEX_POINT ( 'NONE', #12592 ) ;
#16707=CARTESIAN_POINT ( 'NONE',  ( -10.16281054619604873, 15.91872981196863002, -1.078691087397217752 ) ) ;
#16709=CARTESIAN_POINT ( 'NONE',  ( 14.76997825937266740, 9.033527493718441548, -5.004583818473492762 ) ) ;
#16710=CARTESIAN_POINT ( 'NONE',  ( -18.63376253787999914, -9.149460784975000038, 0.000000000000000000 ) ) ;
#16711=CARTESIAN_POINT ( 'NONE',  ( 21.48238453167000017, -7.521219210359999963, -8.342195645638000201 ) ) ;
#16712=EDGE_CURVE ( 'NONE', #2832, #12632, #13281, .T. ) ;
#16714=CARTESIAN_POINT ( 'NONE',  ( 14.13908848849179023, 3.495271894151044556, 8.348058256251976061 ) ) ;
#16715=CARTESIAN_POINT ( 'NONE',  ( -6.591948041516452861, 15.40797180132708988, -1.571325980949459078 ) ) ;
#16717=CARTESIAN_POINT ( 'NONE',  ( 20.52539899991999661, 5.356978891688999767, 10.06605121447999984 ) ) ;
#16718=VERTEX_POINT ( 'NONE', #21035 ) ;
#16719=AXIS2_PLACEMENT_3D ( 'NONE', #23262, #19888, #1480 ) ;
#16721=ORIENTED_EDGE ( 'NONE', *, *, #20523, .F. ) ;
#16722=CARTESIAN_POINT ( 'NONE',  ( -15.65412077250664957, 9.072997304709783606, -1.187525622282732396 ) ) ;
#16723=DIRECTION ( 'NONE',  ( 0.000000000000000000, 0.000000000000000000, -1.000000000000000000 ) ) ;
#16725=CARTESIAN_POINT ( 'NONE',  ( 17.87356944879000054, -6.873864763588999338, -8.725743989736999495 ) ) ;
#16726=CARTESIAN_POINT ( 'NONE',  ( -6.046835300290999804, 16.30334124114000360, 1.000000020649999932 ) ) ;
#16728=EDGE_LOOP ( 'NONE', ( #6299, #1887, #482 ) ) ;
#16730=CARTESIAN_POINT ( 'NONE',  ( -10.20723256584999916, 13.42721542333999984, 6.384960544076999867 ) ) ;
#16734=CARTESIAN_POINT ( 'NONE',  ( -14.48633706258206111, 10.11155074087842642, 7.486293916575140095 ) ) ;
#16735=DIRECTION ( 'NONE',  ( -0.000000000000000000, 1.000000000000000000, 0.000000000000000000 ) ) ;
#16737=CARTESIAN_POINT ( 'NONE',  ( 6.239308309756287585, 13.68455386514935412, 1.647755693301848456 ) ) ;
#16738=CARTESIAN_POINT ( 'NONE',  ( 15.90272818354428175, -9.982911839440134827, -2.763178835720944360 ) ) ;
#16739=CARTESIAN_POINT ( 'NONE',  ( -18.01742253012000106, -2.120327895178999889, 10.89685495860999964 ) ) ;
#16742=CARTESIAN_POINT ( 'NONE',  ( -15.63636876114000351, -8.424167882059999002, 6.770715351507000435 ) ) ;
#16744=EDGE_LOOP ( 'NONE', ( #12431, #21537, #16721, #15921 ) ) ;
#16746=CARTESIAN_POINT ( 'NONE',  ( 19.78852822580074999, -4.133238257719290765, -9.662078402654971754 ) ) ;
#16747=CARTESIAN_POINT ( 'NONE',  ( -18.10935057530256387, 0.4203439791810718029, 10.44572940319434196 ) ) ;
#16748=ORIENTED_EDGE ( 'NONE', *, *, #10903, .F. ) ;
#16749=CARTESIAN_POINT ( 'NONE',  ( -4.012824720309999371, 13.17021387432998658, 4.696499411533000767 ) ) ;
#16750=EDGE_CURVE ( 'NONE', #2766, #7012, #21189, .T. ) ;
#16752=CARTESIAN_POINT ( 'NONE',  ( -13.99999999999999645, -9.053648303160509059, 5.060582752402400075 ) ) ;
#16753=CARTESIAN_POINT ( 'NONE',  ( 14.02481375730999957, 9.137735611494999688, -0.2793723515763000265 ) ) ;
#16755=ORIENTED_EDGE ( 'NONE', *, *, #19284, .F. ) ;
#16758=CARTESIAN_POINT ( 'NONE',  ( 18.75008227645999881, 0.000000000000000000, 0.000000000000000000 ) ) ;
#16760=ORIENTED_EDGE ( 'NONE', *, *, #20605, .F. ) ;
#16761=CARTESIAN_POINT ( 'NONE',  ( 22.77837270046333629, 2.422573927148270023, -9.014964020370104691 ) ) ;
#16762=CARTESIAN_POINT ( 'NONE',  ( 4.699418951522004839, 12.59868348402000748, 0.6614101461372995372 ) ) ;
#16763=CARTESIAN_POINT ( 'NONE',  ( 12.00000000000000000, 5.273090321616999532, -7.267806174758000282 ) ) ;
#16764=EDGE_CURVE ( 'NONE', #7987, #2252, #4450, .T. ) ;
#16767=CARTESIAN_POINT ( 'NONE',  ( -20.99901840903234529, -6.127583174698123081, -8.547554176268754134 ) ) ;
#16768=CARTESIAN_POINT ( 'NONE',  ( 5.314999799853000972, 13.91584611406999983, 3.802386931276000137 ) ) ;
#16774=CARTESIAN_POINT ( 'NONE',  ( 21.72047034351999883, 0.7717287101376000269, 9.798846879612002070 ) ) ;
#16775=CARTESIAN_POINT ( 'NONE',  ( 14.02900943697788527, 8.904994502184068850, -1.790900335187071590 ) ) ;
#16776=CARTESIAN_POINT ( 'NONE',  ( -23.18803004254179001, -5.362570460539083150, 9.113462231227742905 ) ) ;
#16778=EDGE_CURVE ( 'NONE', #11958, #23264, #22934, .T. ) ;
#16780=CIRCLE ( 'NONE', #21837, 16.43375672870000415 ) ;
#16782=CARTESIAN_POINT ( 'NONE',  ( 1.004037071924726687, 11.52581781820473239, 4.707233457423458667 ) ) ;
#16784=CARTESIAN_POINT ( 'NONE',  ( -3.741193895918689005, 12.06686126286441407, -3.070321243407096112 ) ) ;
#16785=DIRECTION ( 'NONE',  ( 0.4593435542646316372, -0.8882586893217174762, 0.000000000000000000 ) ) ;
#16788=( BOUNDED_SURFACE ( )  B_SPLINE_SURFACE ( 3, 3, ( 
 ( #10906, #7025, #16339, #19760, #3287, #10669, #9080, #18290, #14412, #6783, #21804, #10792, #23495, #1587, #16451, #12602, #5105, #1342, #3522, #12486, #19988, #8969, #23730, #23841, #5332, #6908, #22040, #8733, #17936, #14175, #4986, #14526 ),
 ( #12832, #21918, #20113, #12372, #11014, #14301, #18398, #8609, #21693, #15970, #23365, #18057, #3169, #100, #213, #23965, #6024, #4098, #3743, #11376, #13061, #22151, #11259, #7485, #14755, #18748, #3982, #18871, #2277, #9670, #17051, #18638 ),
 ( #13410, #14870, #16805, #448, #2044, #16575, #20811, #22257, #16690, #5562, #7735, #11133, #1929, #22616, #12939, #4221, #9434, #7851, #5673, #20457, #11494, #3868, #7607, #20336, #11614, #13179, #5905, #14985, #22382, #5796, #15218, #20568 ),
 ( #1809, #7371, #2158, #15101, #9197, #18519, #9550, #9316, #16928, #331, #22496, #13291, #20690, #23090, #6267, #9784, #2643, #15584, #4584, #11977, #21047, #22854, #10039, #22732, #8101, #6147, #694, #17423, #21172, #13650, #817, #15343 ),
 ( #13771, #15700, #13536, #19363, #7971, #15468, #2769, #8218, #4460, #17540, #19230, #20931, #11850, #22971, #6514, #10155, #6388, #8334, #935, #18984, #2395, #17170, #565, #4337, #11729, #19103, #2515, #9905, #17293, #18948, #15298, #7692 ),
 ( #2006, #18828, #9627, #171, #2355, #7810, #5752, #5871, #14941, #15066, #14824, #20892, #9746, #18599, #2234, #3944, #13015, #2117, #22337, #5632, #17011, #410, #17132, #527, #7930, #22689, #9508, #20416, #16762, #3824, #6099, #9390 ),
 ( #7443, #11688, #13142, #7562, #11221, #22577, #20535, #11339, #13491, #18709, #4298, #16883, #19062, #291, #22460, #2476, #13256, #20649, #4058, #16654, #11453, #20767, #15182, #58, #22217, #5983, #13366, #4176, #11571, #2595, #21258, #6471 ) ),
 .UNSPECIFIED., .F., .F., .T. ) 
 B_SPLINE_SURFACE_WITH_KNOTS ( ( 4, 3, 4 ),
 ( 4, 1, 1, 1, 1, 1, 1, 1, 1, 1, 1, 1, 1, 1, 1, 1, 1, 1, 1, 1, 1, 1, 1, 1, 1, 1, 1, 1, 1, 4 ),
 ( 0.000000000000000000, 1.000000000000000000, 2.000000000000000000 ),
 ( -0.0001618831681000999832, 0.000000000000000000, 0.008762561342867999925, 0.01824509674601000261, 0.02863315657921999824, 0.04005085953976000174, 0.05263615618096000037, 0.06652419853735000443, 0.08184912555068998841, 0.09881173633437000114, 0.1176787978263000023, 0.1387116773469999897, 0.1621789585680999957, 0.1887288111371999977, 0.2191170703197999892, 0.2517299998975999764, 0.2825862214344000423, 0.3099915928082999650, 0.3345416994503000452, 0.3566258367156999731, 0.3765620894444000055, 0.3945985271376999948, 0.4110154862469999615, 0.4260441420834000237, 0.4400513890198000100, 0.4540949684832999989, 0.4686848077695999759, 0.4831735293021999778, 0.4971812856050999985, 0.5099256701170999939 ),
 .UNSPECIFIED. ) 
 GEOMETRIC_REPRESENTATION_ITEM ( )  RATIONAL_B_SPLINE_SURFACE ( (
 ( 1.293520787057000021, 1.293520787057000021, 1.293520787057000021, 1.293520787057000021, 1.293520787057000021, 1.293520787057000021, 1.293520787057000021, 1.293520787057000021, 1.293520787057000021, 1.293520787057000021, 1.293520787057000021, 1.293520787057000021, 1.293520787057000021, 1.293520787057000021, 1.293520787057000021, 1.293520787057000021, 1.293520787057000021, 1.293520787057000021, 1.293520787057000021, 1.293520787057000021, 1.293520787057000021, 1.293520787057000021, 1.293520787057000021, 1.293520787057000021, 1.293520787057000021, 1.293520787057000021, 1.293520787057000021, 1.293520787057000021, 1.293520787057000021, 1.293520787057000021, 1.293520787057000021, 1.293520787057000021),
 ( 0.9021597376475999353, 0.9021597376475999353, 0.9021597376475999353, 0.9021597376475999353, 0.9021597376475999353, 0.9021597376475999353, 0.9021597376475999353, 0.9021597376475999353, 0.9021597376475999353, 0.9021597376475999353, 0.9021597376475999353, 0.9021597376475999353, 0.9021597376475999353, 0.9021597376475999353, 0.9021597376475999353, 0.9021597376475999353, 0.9021597376475999353, 0.9021597376475999353, 0.9021597376475999353, 0.9021597376475999353, 0.9021597376475999353, 0.9021597376475999353, 0.9021597376475999353, 0.9021597376475999353, 0.9021597376475999353, 0.9021597376475999353, 0.9021597376475999353, 0.9021597376475999353, 0.9021597376475999353, 0.9021597376475999353, 0.9021597376475999353, 0.9021597376475999353),
 ( 0.9021597376475999353, 0.9021597376475999353, 0.9021597376475999353, 0.9021597376475999353, 0.9021597376475999353, 0.9021597376475999353, 0.9021597376475999353, 0.9021597376475999353, 0.9021597376475999353, 0.9021597376475999353, 0.9021597376475999353, 0.9021597376475999353, 0.9021597376475999353, 0.9021597376475999353, 0.9021597376475999353, 0.9021597376475999353, 0.9021597376475999353, 0.9021597376475999353, 0.9021597376475999353, 0.9021597376475999353, 0.9021597376475999353, 0.9021597376475999353, 0.9021597376475999353, 0.9021597376475999353, 0.9021597376475999353, 0.9021597376475999353, 0.9021597376475999353, 0.9021597376475999353, 0.9021597376475999353, 0.9021597376475999353, 0.9021597376475999353, 0.9021597376475999353),
 ( 1.293520787057000021, 1.293520787057000021, 1.293520787057000021, 1.293520787057000021, 1.293520787057000021, 1.293520787057000021, 1.293520787057000021, 1.293520787057000021, 1.293520787057000021, 1.293520787057000021, 1.293520787057000021, 1.293520787057000021, 1.293520787057000021, 1.293520787057000021, 1.293520787057000021, 1.293520787057000021, 1.293520787057000021, 1.293520787057000021, 1.293520787057000021, 1.293520787057000021, 1.293520787057000021, 1.293520787057000021, 1.293520787057000021, 1.293520787057000021, 1.293520787057000021, 1.293520787057000021, 1.293520787057000021, 1.293520787057000021, 1.293520787057000021, 1.293520787057000021, 1.293520787057000021, 1.293520787057000021),
 ( 0.9021597376475999353, 0.9021597376475999353, 0.9021597376475999353, 0.9021597376475999353, 0.9021597376475999353, 0.9021597376475999353, 0.9021597376475999353, 0.9021597376475999353, 0.9021597376475999353, 0.9021597376475999353, 0.9021597376475999353, 0.9021597376475999353, 0.9021597376475999353, 0.9021597376475999353, 0.9021597376475999353, 0.9021597376475999353, 0.9021597376475999353, 0.9021597376475999353, 0.9021597376475999353, 0.9021597376475999353, 0.9021597376475999353, 0.9021597376475999353, 0.9021597376475999353, 0.9021597376475999353, 0.9021597376475999353, 0.9021597376475999353, 0.9021597376475999353, 0.9021597376475999353, 0.9021597376475999353, 0.9021597376475999353, 0.9021597376475999353, 0.9021597376475999353),
 ( 0.9021597376475999353, 0.9021597376475999353, 0.9021597376475999353, 0.9021597376475999353, 0.9021597376475999353, 0.9021597376475999353, 0.9021597376475999353, 0.9021597376475999353, 0.9021597376475999353, 0.9021597376475999353, 0.9021597376475999353, 0.9021597376475999353, 0.9021597376475999353, 0.9021597376475999353, 0.9021597376475999353, 0.9021597376475999353, 0.9021597376475999353, 0.9021597376475999353, 0.9021597376475999353, 0.9021597376475999353, 0.9021597376475999353, 0.9021597376475999353, 0.9021597376475999353, 0.9021597376475999353, 0.9021597376475999353, 0.9021597376475999353, 0.9021597376475999353, 0.9021597376475999353, 0.9021597376475999353, 0.9021597376475999353, 0.9021597376475999353, 0.9021597376475999353),
 ( 1.293520787057000021, 1.293520787057000021, 1.293520787057000021, 1.293520787057000021, 1.293520787057000021, 1.293520787057000021, 1.293520787057000021, 1.293520787057000021, 1.293520787057000021, 1.293520787057000021, 1.293520787057000021, 1.293520787057000021, 1.293520787057000021, 1.293520787057000021, 1.293520787057000021, 1.293520787057000021, 1.293520787057000021, 1.293520787057000021, 1.293520787057000021, 1.293520787057000021, 1.293520787057000021, 1.293520787057000021, 1.293520787057000021, 1.293520787057000021, 1.293520787057000021, 1.293520787057000021, 1.293520787057000021, 1.293520787057000021, 1.293520787057000021, 1.293520787057000021, 1.293520787057000021, 1.293520787057000021) ) ) 
 REPRESENTATION_ITEM ( '' )  SURFACE ( )  );
#16789=DIRECTION ( 'NONE',  ( 0.000000000000000000, -0.4408793407386908947, 0.8975663802247817458 ) ) ;
#16790=CARTESIAN_POINT ( 'NONE',  ( 18.24581408530999838, 9.747919580236001025, 3.236577786812999680 ) ) ;
#16791=CARTESIAN_POINT ( 'NONE',  ( 18.06410204184560797, -0.9209652123333776919, -10.37059875417824095 ) ) ;
#16795=ADVANCED_FACE ( 'NONE', ( #11839 ), #11177, .T. ) ;
#16796=CARTESIAN_POINT ( 'NONE',  ( 17.56239037306000128, -5.826923919702999832, 9.176156247568000524 ) ) ;
#16800=CARTESIAN_POINT ( 'NONE',  ( 22.52049502035999851, 9.667974779076999425, 4.796159037922000046 ) ) ;
#16802=EDGE_LOOP ( 'NONE', ( #7927, #13505, #22650, #6910, #21920, #18697 ) ) ;
#16803=CARTESIAN_POINT ( 'NONE',  ( 11.33972984855999933, -8.487386343340000749, -2.878673876759000105 ) ) ;
#16804=CARTESIAN_POINT ( 'NONE',  ( -10.04281598263999875, 20.50000000000000000, 1.000000000000000000 ) ) ;
#16805=CARTESIAN_POINT ( 'NONE',  ( -4.836297190787002265, 12.42285795213999755, -0.06016108829675999997 ) ) ;
#16807=CARTESIAN_POINT ( 'NONE',  ( -24.31577140724999708, -6.742003853025999582, -8.902789307808999908 ) ) ;
#16809=ADVANCED_FACE ( 'NONE', ( #2147 ), #9539, .T. ) ;
#16811=FACE_OUTER_BOUND ( 'NONE', #18597, .T. ) ;
#16815=CARTESIAN_POINT ( 'NONE',  ( 6.470427684094998355, 13.53774001610998745, 1.516859935180999930 ) ) ;
#16818=CARTESIAN_POINT ( 'NONE',  ( 18.85240113949000218, -1.886779804701000041, 10.26112574610000117 ) ) ;
#16819=CARTESIAN_POINT ( 'NONE',  ( 23.99062354302999722, -13.93375672974000068, -0.8660254037843999608 ) ) ;
#16822=CARTESIAN_POINT ( 'NONE',  ( -13.15804650426999878, -7.258886979407000339, -7.170289537978000283 ) ) ;
#16825=CARTESIAN_POINT ( 'NONE',  ( -14.41332695378558171, 3.614289100492464435, 12.49991738134775865 ) ) ;
#16827=CARTESIAN_POINT ( 'NONE',  ( -10.26401792859842388, 15.76285626141247320, -1.163543192562826123 ) ) ;
#16829=CARTESIAN_POINT ( 'NONE',  ( 14.19210620200586526, -8.290201769613112504, -6.132491119281651137 ) ) ;
#16831=DIRECTION ( 'NONE',  ( 0.000000000000000000, -1.000000000000000000, 0.000000000000000000 ) ) ;
#16832=CARTESIAN_POINT ( 'NONE',  ( 21.84947845760000007, 5.758980354816999991, -9.655132153217000024 ) ) ;
#16834=CARTESIAN_POINT ( 'NONE',  ( 14.00631938592161596, 6.815600421199946801, 5.980478541323148711 ) ) ;
#16837=CARTESIAN_POINT ( 'NONE',  ( -6.611979220525382672, 15.39629419157375700, 1.595713814164479771 ) ) ;
#16839=CARTESIAN_POINT ( 'NONE',  ( 22.65115926907999722, -6.384260084937999125, 9.518811574639000739 ) ) ;
#16840=ORIENTED_EDGE ( 'NONE', *, *, #8066, .T. ) ;
#16843=ORIENTED_EDGE ( 'NONE', *, *, #15881, .T. ) ;
#16844=CARTESIAN_POINT ( 'NONE',  ( -16.22099577250664382, -4.576542577818303315, -7.940621211161685622 ) ) ;
#16845=LINE ( 'NONE', #18673, #6162 ) ;
#16847=CARTESIAN_POINT ( 'NONE',  ( 19.28334733059999806, -5.605041994797999472, 8.812776241869000771 ) ) ;
#16848=CARTESIAN_POINT ( 'NONE',  ( -23.74465998031000069, -7.716878364870000340, 11.63397459621999985 ) ) ;
#16851=ORIENTED_EDGE ( 'NONE', *, *, #12648, .F. ) ;
#16852=ORIENTED_EDGE ( 'NONE', *, *, #9193, .T. ) ;
#16855=CARTESIAN_POINT ( 'NONE',  ( -24.50000000000292033, -10.56908696369845480, -6.693804389271431177 ) ) ;
#16856=ORIENTED_EDGE ( 'NONE', *, *, #21675, .T. ) ;
#16857=CARTESIAN_POINT ( 'NONE',  ( -24.50000000000000000, 10.82531754731000007, 6.250000000000000000 ) ) ;
#16858=CARTESIAN_POINT ( 'NONE',  ( 19.14665134072065200, -9.780573450044347084, 3.801355032053034044 ) ) ;
#16860=CARTESIAN_POINT ( 'NONE',  ( 12.50000000000000000, -13.93375672974000068, 0.1442505881487999853 ) ) ;
#16861=CARTESIAN_POINT ( 'NONE',  ( 15.88567173426467782, -10.12137449307697246, -2.193410681915878069 ) ) ;
#16862=CARTESIAN_POINT ( 'NONE',  ( -15.16085120776000039, 1.689811185772999824, -10.89268608759000045 ) ) ;
#16864=CARTESIAN_POINT ( 'NONE',  ( -17.05828119693000033, -8.427367219174998425, -6.829844779585000580 ) ) ;
#16866=ORIENTED_EDGE ( 'NONE', *, *, #6395, .T. ) ;
#16868=CARTESIAN_POINT ( 'NONE',  ( -24.50000000000000000, -7.041797653771503462, -7.920532110923238278 ) ) ;
#16875=CARTESIAN_POINT ( 'NONE',  ( 13.58606375731000071, 0.1873974521201000054, -9.128548663592997769 ) ) ;
#16877=CARTESIAN_POINT ( 'NONE',  ( -4.526039284669313822, 15.50981481425817421, 4.129000272277018269 ) ) ;
#16878=CARTESIAN_POINT ( 'NONE',  ( 24.36414987671881960, -12.39811243366166416, 3.525839346946420427 ) ) ;
#16880=CARTESIAN_POINT ( 'NONE',  ( -14.25699038479000080, 13.93375672974000068, 0.000000000000000000 ) ) ;
#16881=CIRCLE ( 'NONE', #14190, 12.50000000000000178 ) ;
#16883=CARTESIAN_POINT ( 'NONE',  ( -3.633248405346000354, 12.23316262990001491, 3.176949996004001964 ) ) ;
#16885=CARTESIAN_POINT ( 'NONE',  ( -20.69122654991999966, 0.9355733309527999308, 9.531175163259002048 ) ) ;
#16887=CARTESIAN_POINT ( 'NONE',  ( 13.50000000000000000, 10.65000000000000036, 0.000000000000000000 ) ) ;
#16889=B_SPLINE_CURVE_WITH_KNOTS ( 'NONE', 3,
 ( #19042, #2452, #6809, #23391 ),
 .UNSPECIFIED., .F., .F.,
 ( 4, 4 ),
 ( 0.000000000000000000, 1.000000000000000000 ),
 .UNSPECIFIED. ) ;
#16895=ORIENTED_EDGE ( 'NONE', *, *, #6829, .T. ) ;
#16896=CARTESIAN_POINT ( 'NONE',  ( 23.89879234312000023, -3.396759081369000288, 9.855968912026000339 ) ) ;
#16898=CARTESIAN_POINT ( 'NONE',  ( -23.56048242866723541, -7.487011069796704277, -5.627623744119698124 ) ) ;
#16899=CARTESIAN_POINT ( 'NONE',  ( -22.19730416677924012, 7.811814599075145082, -7.288801720585950328 ) ) ;
#16902=CARTESIAN_POINT ( 'NONE',  ( 23.99062354302999722, -6.216878364870000340, -12.50000000000000000 ) ) ;
#16903=ORIENTED_EDGE ( 'NONE', *, *, #21197, .T. ) ;
#16904=EDGE_CURVE ( 'NONE', #10277, #17895, #7038, .T. ) ;
#16905=CARTESIAN_POINT ( 'NONE',  ( -18.66125422242449616, 5.045625058748018255, -9.162508174574998776 ) ) ;
#16906=CARTESIAN_POINT ( 'NONE',  ( 24.36881528991173340, 12.37037615450637240, 3.573879991655171562 ) ) ;
#16907=CIRCLE ( 'NONE', #23095, 14.43375672974000778 ) ;
#16910=ORIENTED_EDGE ( 'NONE', *, *, #17195, .F. ) ;
#16913=CARTESIAN_POINT ( 'NONE',  ( 11.56500142131000075, -9.431037050546001055, -0.2079650321152999859 ) ) ;
#16917=CARTESIAN_POINT ( 'NONE',  ( 12.82233580085999947, 8.050892032625998951, -7.895715898540999866 ) ) ;
#16918=CARTESIAN_POINT ( 'NONE',  ( -12.25000000000000000, 6.489681479813073750, -13.21205004727046095 ) ) ;
#16919=AXIS2_PLACEMENT_3D ( 'NONE', #4721, #19372, #4470 ) ;
#16920=( GEOMETRIC_REPRESENTATION_CONTEXT ( 3 ) GLOBAL_UNCERTAINTY_ASSIGNED_CONTEXT ( ( #7238 ) ) GLOBAL_UNIT_ASSIGNED_CONTEXT ( ( #12292, #6828, #21618 ) ) REPRESENTATION_CONTEXT ( 'NONE', 'WORKASPACE' ) );
#16921=PLANE ( 'NONE',  #11049 ) ;
#16922=CARTESIAN_POINT ( 'NONE',  ( 25.03442155319000051, -3.648015224982000149, 9.208730145795000155 ) ) ;
#16925=ORIENTED_EDGE ( 'NONE', *, *, #2779, .F. ) ;
#16926=CARTESIAN_POINT ( 'NONE',  ( 11.75290414220000024, 1.735136046860999981, -9.156654427831000476 ) ) ;
#16927=CARTESIAN_POINT ( 'NONE',  ( 24.50000000000000355, 2.870590891033125036, 9.920898659907861017 ) ) ;
#16928=CARTESIAN_POINT ( 'NONE',  ( -4.424063187269999808, 12.34346680701001375, 1.825612035066000560 ) ) ;
#16931=CARTESIAN_POINT ( 'NONE',  ( -22.29029390899000163, 6.203558690370000406, -9.220249974902001711 ) ) ;
#16932=ORIENTED_EDGE ( 'NONE', *, *, #4833, .F. ) ;
#16935=CARTESIAN_POINT ( 'NONE',  ( -24.48376588671094467, 1.022231981141815904, -12.50007328824528408 ) ) ;
#16936=EDGE_CURVE ( 'NONE', #5409, #20267, #14271, .T. ) ;
#16939=CARTESIAN_POINT ( 'NONE',  ( 15.93808103379664942, 9.080284284670666395, 1.188479485729086127 ) ) ;
#16940=ADVANCED_FACE ( 'NONE', ( #12451 ), #7819, .F. ) ;
#16942=CARTESIAN_POINT ( 'NONE',  ( -12.24999999999999822, 13.59206128970241778, -6.344557540553090291 ) ) ;
#16943=DIRECTION ( 'NONE',  ( -1.000000000000000000, 0.000000000000000000, 0.000000000000000000 ) ) ;
#16944=B_SPLINE_CURVE_WITH_KNOTS ( 'NONE', 3,
 ( #13459, #22546, #16983, #9952, #20863, #743, #5841, #7782, #8146, #5725, #18921, #19033, #16855, #11778 ),
 .UNSPECIFIED., .F., .F.,
 ( 4, 2, 2, 2, 2, 2, 4 ),
 ( 0.000000000000000000, 0.2500000000000001665, 0.3750000000000001665, 0.5000000000000002220, 0.6250000000000002220, 0.7500000000000001110, 1.000000000000000000 ),
 .UNSPECIFIED. ) ;
#16945=CARTESIAN_POINT ( 'NONE',  ( -12.95491615630000126, -0.8957832334074999903, -10.15856198502000041 ) ) ;
#16949=ORIENTED_EDGE ( 'NONE', *, *, #11697, .T. ) ;
#16955=CARTESIAN_POINT ( 'NONE',  ( 14.19115849146925434, -8.310449043169278127, -6.104973310725267055 ) ) ;
#16957=LINE ( 'NONE', #3770, #15259 ) ;
#16958=CARTESIAN_POINT ( 'NONE',  ( 22.58366630947000075, 0.6838113323537999833, 11.24159121164000119 ) ) ;
#16960=CARTESIAN_POINT ( 'NONE',  ( 11.59051697470635922, -3.660525265868878275, 12.49991113089975947 ) ) ;
#16961=CARTESIAN_POINT ( 'NONE',  ( 18.62948117788694802, 5.836193035541882068, 8.699610836940262715 ) ) ;
#16962=CIRCLE ( 'NONE', #9245, 9.974367097859005327 ) ;
#16964=CARTESIAN_POINT ( 'NONE',  ( 24.15736593521747011, -13.39690473052857378, -1.795880342563474397 ) ) ;
#16965=ORIENTED_EDGE ( 'NONE', *, *, #14566, .T. ) ;
#16966=CARTESIAN_POINT ( 'NONE',  ( -19.24432910583999856, 9.165129126472001175, 0.000000000000000000 ) ) ;
#16969=CARTESIAN_POINT ( 'NONE',  ( 18.62128936713000371, -9.149140698829999252, 0.000000000000000000 ) ) ;
#16970=CARTESIAN_POINT ( 'NONE',  ( -11.00000000000000000, 1.359357947053999856E-14, 0.000000000000000000 ) ) ;
#16971=CARTESIAN_POINT ( 'NONE',  ( -21.96532910583999865, -9.234955349282000014, 0.000000000000000000 ) ) ;
#16972=ORIENTED_EDGE ( 'NONE', *, *, #15743, .F. ) ;
#16973=AXIS2_PLACEMENT_3D ( 'NONE', #13435, #22876, #19007 ) ;
#16974=CARTESIAN_POINT ( 'NONE',  ( 16.79086406172000068, 10.59994276663999990, 3.220549048678999604 ) ) ;
#16977=EDGE_LOOP ( 'NONE', ( #10035, #10586, #5947, #23066, #16384 ) ) ;
#16979=CARTESIAN_POINT ( 'NONE',  ( -14.00000000000000178, -7.401164869303885396, -6.642430693032337352 ) ) ;
#16980=CARTESIAN_POINT ( 'NONE',  ( -9.479727211694999767, 6.392817954487000520, -14.19584414485000146 ) ) ;
#16983=CARTESIAN_POINT ( 'NONE',  ( -23.97728971651672580, -8.249343195707872667, -10.71120260264468982 ) ) ;
#16985=CARTESIAN_POINT ( 'NONE',  ( -20.80224598535999903, -1.543422969988999860, 9.524520383917000288 ) ) ;
#16986=CARTESIAN_POINT ( 'NONE',  ( -14.40719396494353433, 12.69649082866680523, 3.008800086016248709 ) ) ;
#16987=CARTESIAN_POINT ( 'NONE',  ( 19.05840758201121687, -8.181074449885935351, 6.563687483177104376 ) ) ;
#16988=CARTESIAN_POINT ( 'NONE',  ( 6.205361592948507976, 13.85340785436878441, 0.9861407796932231129 ) ) ;
#16989=CARTESIAN_POINT ( 'NONE',  ( 15.76648294310377807, -10.14853226314255608, 2.049597006397073429 ) ) ;
#16990=CARTESIAN_POINT ( 'NONE',  ( -14.25753463260000053, -1.547198325978000000, 10.88880281900999947 ) ) ;
#16993=CARTESIAN_POINT ( 'NONE',  ( -12.54865546036000090, 9.084388929069001861, -2.336084003038000123 ) ) ;
#16997=CARTESIAN_POINT ( 'NONE',  ( 19.10756701789335210, -3.879051868053418950, 9.750401366061593578 ) ) ;
#16999=ORIENTED_EDGE ( 'NONE', *, *, #6717, .T. ) ;
#17000=CARTESIAN_POINT ( 'NONE',  ( 17.42999999999999972, 9.118569865760999704, 0.000000000000000000 ) ) ;
#17001=CARTESIAN_POINT ( 'NONE',  ( -4.770941035428000632, 13.03080120692000143, 5.112121747560996354 ) ) ;
#17004=CARTESIAN_POINT ( 'NONE',  ( 17.23218892130999791, -6.764005061571999988, -7.001918906472000437 ) ) ;
#17005=ORIENTED_EDGE ( 'NONE', *, *, #1552, .T. ) ;
#17006=CARTESIAN_POINT ( 'NONE',  ( -6.132854427276997811, 15.85506591466998394, -1.061654000538000409 ) ) ;
#17008=ORIENTED_EDGE ( 'NONE', *, *, #7616, .T. ) ;
#17010=CARTESIAN_POINT ( 'NONE',  ( 21.24695833333333184, 7.370235643207817766, 5.663892701536951790 ) ) ;
#17011=CARTESIAN_POINT ( 'NONE',  ( 2.811787122143001749, 11.98948095905999267, 3.831734478701003255 ) ) ;
#17012=CARTESIAN_POINT ( 'NONE',  ( -10.04701370329000021, 16.31160201364000173, 0.9999999999983000265 ) ) ;
#17013=CONICAL_SURFACE ( 'NONE', #7348, 14.24955550637000101, 0.7853981633972997312 ) ;
#17014=CARTESIAN_POINT ( 'NONE',  ( 12.00000000000000178, -2.051339698423416458, -9.248432771917977746 ) ) ;
#17015=CARTESIAN_POINT ( 'NONE',  ( 18.99920603379665351, -2.397423959588824705, -8.920410146158499032 ) ) ;
#17016=CARTESIAN_POINT ( 'NONE',  ( -6.046837210729000489, 16.30334039894000142, -1.000000000000000000 ) ) ;
#17017=DIRECTION ( 'NONE',  ( 1.000000000000000000, 0.000000000000000000, 0.000000000000000000 ) ) ;
#17019=DIRECTION ( 'NONE',  ( 0.000000000000000000, -1.000000000000000000, 2.763497949612999920E-10 ) ) ;
#17020=EDGE_CURVE ( 'NONE', #20353, #20749, #3323, .T. ) ;
#17023=CARTESIAN_POINT ( 'NONE',  ( 22.54603580819999920, -9.726366907112000249, -3.646778938341999954 ) ) ;
#17024=CARTESIAN_POINT ( 'NONE',  ( 3.181525383082363323, 13.14482206580053081, -5.962137341915427768 ) ) ;
#17025=B_SPLINE_CURVE_WITH_KNOTS ( 'NONE', 3,
 ( #326, #15096, #22492, #4094, #11490 ),
 .UNSPECIFIED., .F., .F.,
 ( 4, 1, 4 ),
 ( 0.000000000000000000, 0.3333333333333000081, 0.4999999999411116058 ),
 .UNSPECIFIED. ) ;
#17027=CARTESIAN_POINT ( 'NONE',  ( -21.34046016612140662, -6.456723609324719781, 8.482265010774550973 ) ) ;
#17029=DIRECTION ( 'NONE',  ( -1.000000000000000000, 0.000000000000000000, 0.000000000000000000 ) ) ;
#17031=CARTESIAN_POINT ( 'NONE',  ( -19.35893705290999733, -9.828989445528000246, 3.502754984265999738 ) ) ;
#17033=CARTESIAN_POINT ( 'NONE',  ( 5.302302355349000074, 1.583778078195999810E-14, 0.000000000000000000 ) ) ;
#17035=ORIENTED_EDGE ( 'NONE', *, *, #10608, .T. ) ;
#17037=LINE ( 'NONE', #16558, #20792 ) ;
#17038=CARTESIAN_POINT ( 'NONE',  ( 18.16256424931000168, 7.359336859262000097, -7.874515470102998904 ) ) ;
#17039=CARTESIAN_POINT ( 'NONE',  ( -18.00070722157999725, -1.604546417804000091, 11.29584027591999984 ) ) ;
#17041=CARTESIAN_POINT ( 'NONE',  ( 12.68691913419000095, 3.375578516944000018, -10.11458711995999948 ) ) ;
#17042=CARTESIAN_POINT ( 'NONE',  ( -12.30441696485953784, 6.530730161421050894, -13.29560061155498474 ) ) ;
#17043=FACE_OUTER_BOUND ( 'NONE', #9174, .T. ) ;
#17044=CARTESIAN_POINT ( 'NONE',  ( 25.18769339062000157, 0.3376592128354999889, 9.800598048666000039 ) ) ;
#17045=ADVANCED_FACE ( 'NONE', ( #5291 ), #12797, .F. ) ;
#17047=ORIENTED_EDGE ( 'NONE', *, *, #21792, .T. ) ;
#17048=CARTESIAN_POINT ( 'NONE',  ( 12.14717598830999989, 5.538504084190000398, -7.072432456372999887 ) ) ;
#17050=AXIS2_PLACEMENT_3D ( 'NONE', #89, #20445, #16564 ) ;
#17051=CARTESIAN_POINT ( 'NONE',  ( 4.915898507422000741, 12.43979313904999806, -0.02346798552494998302 ) ) ;
#17053=CARTESIAN_POINT ( 'NONE',  ( -20.78653299696999923, -5.135752357527000100, -9.808972968573000273 ) ) ;
#17062=CARTESIAN_POINT ( 'NONE',  ( 12.23943924931000105, -8.418214415862998123, -6.478404025908999664 ) ) ;
#17063=CARTESIAN_POINT ( 'NONE',  ( -15.83949910911000281, -2.044365629921999883, 10.61848174243000109 ) ) ;
#17064=CARTESIAN_POINT ( 'NONE',  ( 16.32825125730999716, -0.8629760640228999469, 9.162002845358001579 ) ) ;
#17066=CARTESIAN_POINT ( 'NONE',  ( -14.40719416829650612, 3.742543968275074295, 12.49988362781941476 ) ) ;
#17070=CARTESIAN_POINT ( 'NONE',  ( 13.76737141588828095, -6.929425286909939530, 7.636379834157821733 ) ) ;
#17075=CARTESIAN_POINT ( 'NONE',  ( 11.48696334737260649, -3.271224437879229008, 12.49992143329651384 ) ) ;
#17077=CARTESIAN_POINT ( 'NONE',  ( 18.51797238626636499, 8.753726328939421819, 5.912621535854910348 ) ) ;
#17079=CARTESIAN_POINT ( 'NONE',  ( -6.081455072267000439, 16.30616274740000193, 0.9999994084348999834 ) ) ;
#17080=B_SPLINE_CURVE_WITH_KNOTS ( 'NONE', 3,
 ( #9274, #20061, #20531, #13138, #54 ),
 .UNSPECIFIED., .F., .F.,
 ( 4, 1, 4 ),
 ( 0.000000000000000000, 0.5000000000000000000, 1.000000000000000000 ),
 .UNSPECIFIED. ) ;
#17083=CARTESIAN_POINT ( 'NONE',  ( 12.52688711657000020, -13.93375672974000068, 0.8660254037843999608 ) ) ;
#17084=ORIENTED_EDGE ( 'NONE', *, *, #1692, .F. ) ;
#17087=CARTESIAN_POINT ( 'NONE',  ( 11.74999999482999868, 0.000000000000000000, 0.000000000000000000 ) ) ;
#17089=ADVANCED_FACE ( 'NONE', ( #18143 ), #17592, .F. ) ;
#17090=CARTESIAN_POINT ( 'NONE',  ( -12.24999999459000044, 1.554281285377000029E-14, 1.045589212608000028E-14 ) ) ;
#17092=CARTESIAN_POINT ( 'NONE',  ( 16.57658386292000330, 6.394698053106999680, -9.039278891232999769 ) ) ;
#17093=CARTESIAN_POINT ( 'NONE',  ( -6.203295285168947792, 15.80526711864483858, 1.136188345634133512 ) ) ;
#17097=CARTESIAN_POINT ( 'NONE',  ( -14.00000000000000355, -8.100261608394585977, -5.884167551250959249 ) ) ;
#17098=VECTOR ( 'NONE', #19889, 1000.000000000000000 ) ;
#17099=CARTESIAN_POINT ( 'NONE',  ( -11.21070971169000074, -8.063269234037999666, -13.31813143584999892 ) ) ;
#17103=CARTESIAN_POINT ( 'NONE',  ( -21.83044639899999950, -2.479786445640999482, -9.353611583463001367 ) ) ;
#17104=DIRECTION ( 'NONE',  ( -1.000000000000000000, 0.000000000000000000, 0.000000000000000000 ) ) ;
#17105=CARTESIAN_POINT ( 'NONE',  ( 6.200714323271902195, 13.87387049108663994, 0.9230690017325009489 ) ) ;
#17106=CARTESIAN_POINT ( 'NONE',  ( 15.24483978148135854, 4.315420778289077219, 9.396116420522842461 ) ) ;
#17111=AXIS2_PLACEMENT_3D ( 'NONE', #19681, #12764, #5261 ) ;
#17112=CARTESIAN_POINT ( 'NONE',  ( -13.80819562941000100, -8.705043851576000691, 6.319240472362000816 ) ) ;
#17116=DIRECTION ( 'NONE',  ( 1.167437459203999868E-09, -4.746895044359150089E-20, 1.000000000000000000 ) ) ;
#17122=CARTESIAN_POINT ( 'NONE',  ( 18.14804166666665708, -7.306463158791289381, 5.615200829187670273 ) ) ;
#17123=CARTESIAN_POINT ( 'NONE',  ( 18.46518908530999781, 4.839936825908999651, 9.065913725881001639 ) ) ;
#17124=EDGE_LOOP ( 'NONE', ( #16866, #13483, #14539, #21793 ) ) ;
#17126=CARTESIAN_POINT ( 'NONE',  ( -6.309791894495001330, 15.63766035666998455, -1.260321238843998604 ) ) ;
#17127=CARTESIAN_POINT ( 'NONE',  ( 23.99062354302999722, 6.216878364870000340, 12.50000000000000000 ) ) ;
#17129=ORIENTED_EDGE ( 'NONE', *, *, #1103, .T. ) ;
#17130=DIRECTION ( 'NONE',  ( 0.000000000000000000, -1.000000000000000000, 0.000000000000000000 ) ) ;
#17131=DIRECTION ( 'NONE',  ( -1.000000000000000000, 0.000000000000000000, 0.000000000000000000 ) ) ;
#17132=CARTESIAN_POINT ( 'NONE',  ( 3.630035897976001902, 12.22073688872999853, 3.060979205723000085 ) ) ;
#17133=CARTESIAN_POINT ( 'NONE',  ( -14.00000000000000000, -7.736145084527675131, 6.778938498890537900 ) ) ;
#17134=CARTESIAN_POINT ( 'NONE',  ( -23.42120019438000256, -1.240814169192000049, -9.570677478896000068 ) ) ;
#17135=CARTESIAN_POINT ( 'NONE',  ( -14.25243324638999809, 13.93375672974000068, 0.8660254037843999608 ) ) ;
#17136=DIRECTION ( 'NONE',  ( 0.000000000000000000, 0.000000000000000000, 1.000000000000000000 ) ) ;
#17138=CARTESIAN_POINT ( 'NONE',  ( 5.243024108832019969, 13.88130074418577742, -4.105508865373297844 ) ) ;
#17143=CARTESIAN_POINT ( 'NONE',  ( 3.209708669317350438, 13.15082032542322032, -5.948897312515923019 ) ) ;
#17145=FACE_OUTER_BOUND ( 'NONE', #2692, .T. ) ;
#17146=CARTESIAN_POINT ( 'NONE',  ( -21.23335466603941768, -8.967721452004571603, 5.512103568260062758 ) ) ;
#17148=AXIS2_PLACEMENT_3D ( 'NONE', #9597, #2206, #13582 ) ;
#17149=CARTESIAN_POINT ( 'NONE',  ( 19.52828936713000019, 9.172416106433001204, 0.000000000000000000 ) ) ;
#17151=CARTESIAN_POINT ( 'NONE',  ( -17.79600586831931253, -3.696083808623826794, 9.922044588331354831 ) ) ;
#17155=EDGE_CURVE ( 'NONE', #17699, #2459, #4155, .T. ) ;
#17156=ORIENTED_EDGE ( 'NONE', *, *, #18997, .T. ) ;
#17158=CARTESIAN_POINT ( 'NONE',  ( 12.21300158531000157, -1.561560366126000021, -9.991316461899998558 ) ) ;
#17161=CARTESIAN_POINT ( 'NONE',  ( 19.59411161192999984, -3.684212632671000520, 9.107267109273999850 ) ) ;
#17163=DIRECTION ( 'NONE',  ( 1.000000000000000000, 0.000000000000000000, 0.000000000000000000 ) ) ;
#17164=CARTESIAN_POINT ( 'NONE',  ( 21.46966224536999945, 3.294543478880000098, 9.128948853653000128 ) ) ;
#17165=CARTESIAN_POINT ( 'NONE',  ( 15.90028936713000185, 9.079314476020000413, 0.000000000000000000 ) ) ;
#17167=VECTOR ( 'NONE', #12503, 1000.000000000000000 ) ;
#17170=CARTESIAN_POINT ( 'NONE',  ( 3.263617933816000516, 12.03395420755000167, 3.428733546877001714 ) ) ;
#17172=CARTESIAN_POINT ( 'NONE',  ( -23.45988572945000072, 3.477105412697999665, 10.58835565412000079 ) ) ;
#17176=CARTESIAN_POINT ( 'NONE',  ( 15.03108103379664939, -9.057008877067680430, -1.185432741998447614 ) ) ;
#17177=CARTESIAN_POINT ( 'NONE',  ( -11.04281598264000053, 15.43375672938999976, 4.619452968294999437E-14 ) ) ;
#17178=CARTESIAN_POINT ( 'NONE',  ( -7.034000000000000696, 1.310788454998999989E-14, 0.000000000000000000 ) ) ;
#17180=CARTESIAN_POINT ( 'NONE',  ( 16.18818924931000325, 2.089945795291999975, -10.52064088945999920 ) ) ;
#17181=EDGE_CURVE ( 'NONE', #12251, #12959, #11457, .T. ) ;
#17182=B_SPLINE_CURVE_WITH_KNOTS ( 'NONE', 3,
 ( #13648, #3866, #11256, #211 ),
 .UNSPECIFIED., .F., .F.,
 ( 4, 4 ),
 ( 0.000000000000000000, 1.000000000000000000 ),
 .UNSPECIFIED. ) ;
#17183=AXIS2_PLACEMENT_3D ( 'NONE', #9977, #22684, #22803 ) ;
#17184=CARTESIAN_POINT ( 'NONE',  ( -13.97056789615000127, 4.578996057282999743, 9.143398144881999201 ) ) ;
#17185=CARTESIAN_POINT ( 'NONE',  ( 15.45075125730999943, 1.788522226178000052, -9.003565944673999510 ) ) ;
#17189=CARTESIAN_POINT ( 'NONE',  ( 13.84875374132612791, -8.743024429450152013, 5.452792944436931855 ) ) ;
#17190=CONICAL_SURFACE ( 'NONE', #11013, 9.157130689899000586, 0.02565634000431304615 ) ;
#17191=ORIENTED_EDGE ( 'NONE', *, *, #9059, .T. ) ;
#17192=CARTESIAN_POINT ( 'NONE',  ( 3.874219016647000746, 14.52284758957000932, -4.808120738072998890 ) ) ;
#17195=EDGE_CURVE ( 'NONE', #11527, #3987, #7330, .T. ) ;
#17196=CARTESIAN_POINT ( 'NONE',  ( 14.40637819618423343, -4.518304899556225607, 7.830849211221313944 ) ) ;
#17197=CARTESIAN_POINT ( 'NONE',  ( 17.96042842816580176, 2.416909556611977816, -10.17044595465547729 ) ) ;
#17200=CARTESIAN_POINT ( 'NONE',  ( 24.43449445986660962, -11.92557563953692856, -4.344297082815015365 ) ) ;
#17201=VERTEX_POINT ( 'NONE', #9870 ) ;
#17203=VERTEX_POINT ( 'NONE', #416 ) ;
#17204=DIRECTION ( 'NONE',  ( 0.000000000000000000, 0.000000000000000000, 1.000000000000000000 ) ) ;
#17205=CARTESIAN_POINT ( 'NONE',  ( -4.694832530803901172, 12.39124191863946045, 1.229044316482024835 ) ) ;
#17209=CARTESIAN_POINT ( 'NONE',  ( 16.39613296506999873, -0.1032919116580000157, -11.06709702821000008 ) ) ;
#17211=ADVANCED_FACE ( 'NONE', ( #7814, #22581 ), #4180, .F. ) ;
#17213=VERTEX_POINT ( 'NONE', #532 ) ;
#17214=ORIENTED_EDGE ( 'NONE', *, *, #23877, .T. ) ;
#17215=CARTESIAN_POINT ( 'NONE',  ( -14.00000000000000178, 1.091918795757769178, -9.374698143281760210 ) ) ;
#17219=CARTESIAN_POINT ( 'NONE',  ( -21.90296809259000099, 3.348283013937999986, -9.636535320535001503 ) ) ;
#17220=DIRECTION ( 'NONE',  ( -1.000000000000000000, 0.000000000000000000, 0.000000000000000000 ) ) ;
#17221=CARTESIAN_POINT ( 'NONE',  ( 6.146734651151617435, 14.15406834883495790, 0.1968692019807686822 ) ) ;
#17222=CARTESIAN_POINT ( 'NONE',  ( 15.70271885188221184, -9.447517964781408040, 4.243853946881596784 ) ) ;
#17224=ADVANCED_FACE ( 'NONE', ( #23054 ), #7846, .F. ) ;
#17225=CARTESIAN_POINT ( 'NONE',  ( -20.51005101983020396, 9.225122117455688553, -5.023185617052088325 ) ) ;
#17227=CARTESIAN_POINT ( 'NONE',  ( -18.68332398068000089, -2.538655790982999871, -10.59268337770999935 ) ) ;
#17229=ORIENTED_EDGE ( 'NONE', *, *, #9786, .T. ) ;
#17231=CARTESIAN_POINT ( 'NONE',  ( -5.372805085453999929, 16.07374366015000078, -2.940844016990000309 ) ) ;
#17235=CARTESIAN_POINT ( 'NONE',  ( -20.25880420454665298, -7.349778174321106583, -5.648488567666000826 ) ) ;
#17237=AXIS2_PLACEMENT_3D ( 'NONE', #147, #1745, #2093 ) ;
#17238=CARTESIAN_POINT ( 'NONE',  ( 15.14812642130999976, -9.595485766438999420, 1.281252696419999948 ) ) ;
#17239=ADVANCED_FACE ( 'NONE', ( #20711 ), #13797, .F. ) ;
#17240=ORIENTED_EDGE ( 'NONE', *, *, #4312, .T. ) ;
#17242=CARTESIAN_POINT ( 'NONE',  ( -6.042020549532005624, 15.62678062179001515, -1.260321238843998604 ) ) ;
#17243=FACE_OUTER_BOUND ( 'NONE', #16744, .T. ) ;
#17245=CARTESIAN_POINT ( 'NONE',  ( 0.000000000000000000, 21.50000000000000000, 0.000000000000000000 ) ) ;
#17246=ORIENTED_EDGE ( 'NONE', *, *, #602, .F. ) ;
#17250=CARTESIAN_POINT ( 'NONE',  ( 24.35303310461301152, -3.983639806630030034, 9.847948561538306222 ) ) ;
#17251=DIRECTION ( 'NONE',  ( 0.000000000000000000, -1.000000000000000000, 0.000000000000000000 ) ) ;
#17252=CARTESIAN_POINT ( 'NONE',  ( 18.37439921296329004, 8.632675712573684379, -5.842281130979909420 ) ) ;
#17253=CARTESIAN_POINT ( 'NONE',  ( -5.833999999999999631, -1.199084044040999915E-14, 0.000000000000000000 ) ) ;
#17254=CARTESIAN_POINT ( 'NONE',  ( -14.37382047448982014, 8.632461983038428599, -10.04764370666018714 ) ) ;
#17255=CARTESIAN_POINT ( 'NONE',  ( -4.008978351765000170, 13.27365510235000379, -4.673626722282001822 ) ) ;
#17263=CARTESIAN_POINT ( 'NONE',  ( 19.40145914081000100, 9.444312231696999405, -2.482237776557999709 ) ) ;
#17264=CARTESIAN_POINT ( 'NONE',  ( -1.842050125101387659, 12.91841030608713048, -6.438214839482312435 ) ) ;
#17265=AXIS2_PLACEMENT_3D ( 'NONE', #23008, #19019, #6425 ) ;
#17266=CARTESIAN_POINT ( 'NONE',  ( -11.00000000000000000, 1.359357947053999856E-14, 0.000000000000000000 ) ) ;
#17267=VECTOR ( 'NONE', #22694, 1000.000000000000000 ) ;
#17268=CARTESIAN_POINT ( 'NONE',  ( -20.77815629069096559, -5.457173657242292641, -8.988420674274129496 ) ) ;
#17272=CARTESIAN_POINT ( 'NONE',  ( -17.46107102157156987, -10.41957730825670936, 0.5355958063994551432 ) ) ;
#17279=CARTESIAN_POINT ( 'NONE',  ( 5.302302355349000074, 1.583778078195999810E-14, 0.000000000000000000 ) ) ;
#17280=CARTESIAN_POINT ( 'NONE',  ( 16.84631424931000154, 6.637278256850999369, 8.448060240267999177 ) ) ;
#17281=CARTESIAN_POINT ( 'NONE',  ( -14.20688765586999303, 1.535651113041606619, -8.952319352988645562 ) ) ;
#17282=DIRECTION ( 'NONE',  ( -1.000000000000000000, 0.000000000000000000, 0.000000000000000000 ) ) ;
#17283=CARTESIAN_POINT ( 'NONE',  ( 22.83420833333331501, 9.257252502730580090, -1.211898466613929637 ) ) ;
#17284=CARTESIAN_POINT ( 'NONE',  ( 19.25556994526000310, 7.389816571954000324, 7.286178097052999902 ) ) ;
#17287=CARTESIAN_POINT ( 'NONE',  ( 23.59425147122999888, -6.506847782497000132, 7.278924568632000103 ) ) ;
#17293=CARTESIAN_POINT ( 'NONE',  ( 4.683509707950999079, 12.52043781250001153, 0.6549564855534005803 ) ) ;
#17295=CARTESIAN_POINT ( 'NONE',  ( -23.12571663788999743, -8.293331836127999068, 7.431160843878000577 ) ) ;
#17298=DIRECTION ( 'NONE',  ( 0.000000000000000000, -1.000000000000000000, 0.000000000000000000 ) ) ;
#17299=EDGE_LOOP ( 'NONE', ( #16038, #4907, #5552, #21090 ) ) ;
#17300=CARTESIAN_POINT ( 'NONE',  ( -24.41513307468559901, 2.047838742109346466, -12.49997210311845564 ) ) ;
#17302=CARTESIAN_POINT ( 'NONE',  ( 4.683882115557001846, 14.25929394625999080, 3.864918841593002696 ) ) ;
#17304=CARTESIAN_POINT ( 'NONE',  ( 12.05662674931000033, -10.44547366770999908, -0.2303471896619999904 ) ) ;
#17305=CARTESIAN_POINT ( 'NONE',  ( -19.22500490859999900, -8.822855456895000614, 5.347747867906999630 ) ) ;
#17306=CIRCLE ( 'NONE', #23104, 9.030549305585997999 ) ;
#17307=CARTESIAN_POINT ( 'NONE',  ( 14.13450125731000107, 8.592455601080001060, 3.130286720869000394 ) ) ;
#17310=CYLINDRICAL_SURFACE ( 'NONE', #19279, 10.59999999999999964 ) ;
#17312=CARTESIAN_POINT ( 'NONE',  ( 14.13913242659573299, -9.311690260717602641, -4.516683420423269979 ) ) ;
#17313=ORIENTED_EDGE ( 'NONE', *, *, #1692, .T. ) ;
#17314=CARTESIAN_POINT ( 'NONE',  ( -1.989847688386000124, 13.98044646450001061, -5.851777455581000709 ) ) ;
#17315=CARTESIAN_POINT ( 'NONE',  ( -24.16119556692216364, 12.87912905767985450, -2.692171137914732171 ) ) ;
#17317=CARTESIAN_POINT ( 'NONE',  ( 12.40357033524261254, -5.939957768490999435, 12.49999999999918820 ) ) ;
#17318=CARTESIAN_POINT ( 'NONE',  ( 17.29137567844483669, -9.236652306994301398, 5.172519770036458908 ) ) ;
#17321=EDGE_CURVE ( 'NONE', #15235, #4168, #22013, .T. ) ;
#17323=CARTESIAN_POINT ( 'NONE',  ( 2.399426801160061462, 11.81735415996129568, -4.146195241240062224 ) ) ;
#17324=VERTEX_POINT ( 'NONE', #10060 ) ;
#17326=DIRECTION ( 'NONE',  ( -1.000000000000000000, 0.000000000000000000, 0.000000000000000000 ) ) ;
#17327=CARTESIAN_POINT ( 'NONE',  ( -0.9971822219135534349, 11.51405072702774746, 4.736263398427000837 ) ) ;
#17330=CARTESIAN_POINT ( 'NONE',  ( 14.95252578230999951, 10.54459643182000228, -3.229425179476999919 ) ) ;
#17331=CARTESIAN_POINT ( 'NONE',  ( -20.78894092153334228, 5.513289374754998029, 7.448743673073256133 ) ) ;
#17332=AXIS2_PLACEMENT_3D ( 'NONE', #2420, #9810, #7021 ) ;
#17334=EDGE_CURVE ( 'NONE', #17770, #5775, #19435, .T. ) ;
#17335=ORIENTED_EDGE ( 'NONE', *, *, #50, .T. ) ;
#17336=EDGE_LOOP ( 'NONE', ( #20390, #269, #22739, #18353 ) ) ;
#17337=CARTESIAN_POINT ( 'NONE',  ( -13.99999999999999822, 3.110363060826788484, -8.795536003872138409 ) ) ;
#17340=CARTESIAN_POINT ( 'NONE',  ( -14.33281118273068167, -8.249344442822355461, -10.71171629589809449 ) ) ;
#17342=FACE_OUTER_BOUND ( 'NONE', #18284, .T. ) ;
#17344=CARTESIAN_POINT ( 'NONE',  ( 15.88870756930322159, -10.09910537503753503, -2.295021277106512603 ) ) ;
#17345=B_SPLINE_CURVE_WITH_KNOTS ( 'NONE', 3,
 ( #20146, #4014, #3553, #12977 ),
 .UNSPECIFIED., .F., .F.,
 ( 4, 4 ),
 ( 0.000000000000000000, 1.000000000000000000 ),
 .UNSPECIFIED. ) ;
#17347=CARTESIAN_POINT ( 'NONE',  ( -16.03012606477000190, -7.866000996152999747, 7.756133801015000273 ) ) ;
#17349=CARTESIAN_POINT ( 'NONE',  ( -21.12769403777191357, -9.214013686813418147, -5.077623156764633272 ) ) ;
#17353=ORIENTED_EDGE ( 'NONE', *, *, #11135, .F. ) ;
#17356=CARTESIAN_POINT ( 'NONE',  ( -16.95178362136691774, 7.756708774288529895, -7.108411929819117070 ) ) ;
#17358=ORIENTED_EDGE ( 'NONE', *, *, #19654, .T. ) ;
#17359=DIRECTION ( 'NONE',  ( 0.000000000000000000, 1.000000000000000000, 0.000000000000000000 ) ) ;
#17360=CARTESIAN_POINT ( 'NONE',  ( 5.826396675508998868, 13.70895565241001179, -3.199610063967998741 ) ) ;
#17363=CARTESIAN_POINT ( 'NONE',  ( -24.50000000000000355, -0.1211919172565497221, -10.51440256396106854 ) ) ;
#17365=CARTESIAN_POINT ( 'NONE',  ( 11.85750142130999940, -4.891210171397999851, -8.253706317253998392 ) ) ;
#17366=ORIENTED_EDGE ( 'NONE', *, *, #4216, .T. ) ;
#17367=CARTESIAN_POINT ( 'NONE',  ( 18.25370603379667145, -2.693211065087175893, 8.797714532981757429 ) ) ;
#17368=PLANE ( 'NONE',  #1831 ) ;
#17369=CARTESIAN_POINT ( 'NONE',  ( 24.07420734439604004, -13.66464621573615190, 1.332138486891153217 ) ) ;
#17370=CIRCLE ( 'NONE', #12731, 13.93375672974000068 ) ;
#17371=ORIENTED_EDGE ( 'NONE', *, *, #22099, .T. ) ;
#17373=CARTESIAN_POINT ( 'NONE',  ( 21.13358333333333050, 8.973854058736122852, 2.411525931920532440 ) ) ;
#17374=CARTESIAN_POINT ( 'NONE',  ( 23.82357055235148380, 10.53309116123875633, 1.283855905984082835 ) ) ;
#17375=CARTESIAN_POINT ( 'NONE',  ( -14.00000000000000000, -8.319952449050001420, 6.066771132503999020 ) ) ;
#17376=VECTOR ( 'NONE', #19477, 1000.000000000000114 ) ;
#17377=CARTESIAN_POINT ( 'NONE',  ( 17.66135951571182616, -10.36152372384453280, -0.9047222416689953972 ) ) ;
#17379=ADVANCED_FACE ( 'NONE', ( #3164 ), #10546, .T. ) ;
#17380=DIRECTION ( 'NONE',  ( -1.000000000000000000, 0.000000000000000000, 0.000000000000000000 ) ) ;
#17381=FACE_OUTER_BOUND ( 'NONE', #18782, .T. ) ;
#17382=CARTESIAN_POINT ( 'NONE',  ( 21.73978222679999917, 10.36410918087999988, -4.347985533771000277 ) ) ;
#17383=DIRECTION ( 'NONE',  ( 1.000000000000000000, 0.000000000000000000, 0.000000000000000000 ) ) ;
#17384=CIRCLE ( 'NONE', #6949, 0.09999999999999939493 ) ;
#17389=ORIENTED_EDGE ( 'NONE', *, *, #21571, .T. ) ;
#17391=CARTESIAN_POINT ( 'NONE',  ( 23.06000586213199455, 7.405742005601795519, 5.691048056048777504 ) ) ;
#17392=CARTESIAN_POINT ( 'NONE',  ( 21.24584100372000250, -3.048715644316999818, -10.45155468166000112 ) ) ;
#17393=CARTESIAN_POINT ( 'NONE',  ( -1.017692192065588586, 12.83700921921063909, -6.598984237050126822 ) ) ;
#17396=CARTESIAN_POINT ( 'NONE',  ( -20.18907604024003177, 10.46691963189587327, -0.7924825188483891614 ) ) ;
#17401=VERTEX_POINT ( 'NONE', #12598 ) ;
#17402=CARTESIAN_POINT ( 'NONE',  ( -17.23778112373701887, -7.827069389925411791, -6.885115441211981491 ) ) ;
#17403=EDGE_CURVE ( 'NONE', #1857, #23530, #9054, .T. ) ;
#17407=EDGE_LOOP ( 'NONE', ( #15513, #1987, #22481, #18894, #1309 ) ) ;
#17410=CARTESIAN_POINT ( 'NONE',  ( 11.81081408531000143, -9.938255359128000066, -0.2191561108886999898 ) ) ;
#17411=CARTESIAN_POINT ( 'NONE',  ( -24.54069805790000203, -5.308769442286998874, -9.260118962789000818 ) ) ;
#17412=CARTESIAN_POINT ( 'NONE',  ( -16.30463496464999906, -10.28730417320999990, -0.2735448704119000096 ) ) ;
#17413=CARTESIAN_POINT ( 'NONE',  ( 19.20620833333333621, 9.164150872317845753, -1.199711491691351162 ) ) ;
#17414=CARTESIAN_POINT ( 'NONE',  ( 16.47999951746000136, -9.167179358941000444, 3.350482958538000045 ) ) ;
#17417=CARTESIAN_POINT ( 'NONE',  ( 19.60491575378000206, -4.129469127383999627, 9.308132072280001168 ) ) ;
#17423=CARTESIAN_POINT ( 'NONE',  ( 4.661177797444999271, 12.43313903173000234, 1.085618546728999378 ) ) ;
#17425=CARTESIAN_POINT ( 'NONE',  ( -19.28277208493999950, -10.43152901666999810, -0.1440240251737999744 ) ) ;
#17426=DIRECTION ( 'NONE',  ( -1.000000000000000000, 0.000000000000000000, 0.000000000000000000 ) ) ;
#17427=ORIENTED_EDGE ( 'NONE', *, *, #8821, .F. ) ;
#17428=CARTESIAN_POINT ( 'NONE',  ( -24.36724102301519324, 2.559142463805198719, -12.49991998443061725 ) ) ;
#17433=FACE_BOUND ( 'NONE', #23315, .T. ) ;
#17434=CARTESIAN_POINT ( 'NONE',  ( -18.11469101799999848, 6.086102628551000038, 9.654141096248000764 ) ) ;
#17435=CARTESIAN_POINT ( 'NONE',  ( 15.77981375731000036, 8.935760978467000015, -2.138706884349000248 ) ) ;
#17436=DIRECTION ( 'NONE',  ( -0.6979779633368832226, -0.7161192377642821016, 2.278080596574945599E-09 ) ) ;
#17438=CARTESIAN_POINT ( 'NONE',  ( 20.73762270046331579, -4.635149380793306406, -8.041800740487824228 ) ) ;
#17440=DIRECTION ( 'NONE',  ( 0.000000000000000000, 0.000000000000000000, -1.000000000000000000 ) ) ;
#17441=CARTESIAN_POINT ( 'NONE',  ( 2.374403550057654577, 13.96633455033458659, -5.646771293307399908 ) ) ;
#17444=CARTESIAN_POINT ( 'NONE',  ( 0.5251751504343997734, 13.80000824378999091, -6.149280467907001224 ) ) ;
#17445=CARTESIAN_POINT ( 'NONE',  ( 19.60998953592000049, -11.09065046613000050, -1.415985076781999918 ) ) ;
#17447=CARTESIAN_POINT ( 'NONE',  ( 11.45478115325733448, -3.141659414319388777, 12.49993290927351453 ) ) ;
#17448=CARTESIAN_POINT ( 'NONE',  ( 14.05762072145689245, -6.813077977408399377, -7.800977375048761431 ) ) ;
#17449=CARTESIAN_POINT ( 'NONE',  ( -14.25623329758000146, -13.93375672974000068, 0.4323758512254999853 ) ) ;
#17452=VERTEX_POINT ( 'NONE', #3041 ) ;
#17453=DIRECTION ( 'NONE',  ( 1.000000000000000000, 0.000000000000000000, 0.000000000000000000 ) ) ;
#17454=CARTESIAN_POINT ( 'NONE',  ( 11.36701043060094563, -9.445581393775620782, 8.639701956158534202 ) ) ;
#17458=CARTESIAN_POINT ( 'NONE',  ( -3.128506986885329688, 13.13341830447926917, 5.987348177181893938 ) ) ;
#17459=CARTESIAN_POINT ( 'NONE',  ( 6.145347424894735511, 14.16395735418471702, -0.1681360381669483595 ) ) ;
#17461=B_SPLINE_CURVE_WITH_KNOTS ( 'NONE', 3,
 ( #15713, #21432, #6643, #14038 ),
 .UNSPECIFIED., .F., .F.,
 ( 4, 4 ),
 ( 0.000000000000000000, 1.000000000000000000 ),
 .UNSPECIFIED. ) ;
#17463=VERTEX_POINT ( 'NONE', #14049 ) ;
#17465=CARTESIAN_POINT ( 'NONE',  ( -13.99999999999999822, -5.054693537803610859, -8.380144158881588368 ) ) ;
#17466=CYLINDRICAL_SURFACE ( 'NONE', #10154, 7.000000000000000000 ) ;
#17467=DIRECTION ( 'NONE',  ( -1.000000000000000000, 0.000000000000000000, 0.000000000000000000 ) ) ;
#17471=DIRECTION ( 'NONE',  ( 0.000000000000000000, 1.000000000000000000, 0.000000000000000000 ) ) ;
#17472=CARTESIAN_POINT ( 'NONE',  ( 15.14846033456440644, 7.199530315733793984, 7.418362551489144252 ) ) ;
#17473=CARTESIAN_POINT ( 'NONE',  ( -14.40415622949000074, -1.547762950494000034, 10.89277918470000017 ) ) ;
#17475=CARTESIAN_POINT ( 'NONE',  ( -21.23063454076328327, -10.41326765124834708, -1.537861545000790864 ) ) ;
#17476=CARTESIAN_POINT ( 'NONE',  ( -15.27086614641999951, -1.548365329537000123, -11.22688807791999999 ) ) ;
#17481=CARTESIAN_POINT ( 'NONE',  ( -17.06754031676047134, 4.332830716336383503, -9.488203514064112554 ) ) ;
#17483=VERTEX_POINT ( 'NONE', #12243 ) ;
#17485=CARTESIAN_POINT ( 'NONE',  ( 6.533539489258001431, 13.52322660849999991, -1.215173520708999977 ) ) ;
#17486=CARTESIAN_POINT ( 'NONE',  ( 11.99999999999999822, -3.638042036673571733, -8.209236114036826848 ) ) ;
#17489=CARTESIAN_POINT ( 'NONE',  ( 18.79425158531000051, -6.072333155528000681, 7.996935486658999892 ) ) ;
#17490=EDGE_LOOP ( 'NONE', ( #1135, #16314, #23744, #22794, #8850 ) ) ;
#17495=CARTESIAN_POINT ( 'NONE',  ( -14.25243324638999809, -6.216878364870000340, 12.50000000000000000 ) ) ;
#17496=B_SPLINE_CURVE_WITH_KNOTS ( 'NONE', 3,
 ( #15445, #19079, #21023, #15199, #18726 ),
 .UNSPECIFIED., .F., .F.,
 ( 4, 1, 4 ),
 ( 0.000000000000000000, 0.5000000000000000000, 1.000000000000000000 ),
 .UNSPECIFIED. ) ;
#17497=CARTESIAN_POINT ( 'NONE',  ( 12.28779254560826395, 7.992768853863905676, 11.15614400023877906 ) ) ;
#17498=CARTESIAN_POINT ( 'NONE',  ( -23.16929462096833703, 9.265295224643226746, 1.607743681355135241E-05 ) ) ;
#17500=DIRECTION ( 'NONE',  ( 0.000000000000000000, -1.000000000000000000, 0.000000000000000000 ) ) ;
#17501=CARTESIAN_POINT ( 'NONE',  ( 18.39137590704549297, 8.967538887471349085, -5.308501318233523669 ) ) ;
#17502=CARTESIAN_POINT ( 'NONE',  ( 11.99999999999999645, -6.864517642019856147, -7.017967020444166870 ) ) ;
#17503=CARTESIAN_POINT ( 'NONE',  ( -14.50000017458758705, 10.95512910623404856, -6.025157725042314283 ) ) ;
#17504=CARTESIAN_POINT ( 'NONE',  ( 19.17012474526000076, -11.07867377307000112, -1.414454806264999975 ) ) ;
#17505=DIRECTION ( 'NONE',  ( 0.000000000000000000, -1.000000000000000000, 0.000000000000000000 ) ) ;
#17506=CARTESIAN_POINT ( 'NONE',  ( -3.738560243459424282, 14.17257416838673301, -4.872431394003077898 ) ) ;
#17507=DIRECTION ( 'NONE',  ( -1.000000000000000000, 0.000000000000000000, 0.000000000000000000 ) ) ;
#17511=CARTESIAN_POINT ( 'NONE',  ( 22.40534660507999831, -6.082126118738999665, 9.068436681591000692 ) ) ;
#17512=CARTESIAN_POINT ( 'NONE',  ( 23.19333426533477649, -9.788860759441813997, -4.063454424824834987 ) ) ;
#17516=TOROIDAL_SURFACE ( 'NONE', #22529, 14.44999999999999929, 3.850000000000000089 ) ;
#17517=CARTESIAN_POINT ( 'NONE',  ( -4.788527363615000532, 12.45561528826001485, -1.254325367001999147 ) ) ;
#17518=ORIENTED_EDGE ( 'NONE', *, *, #11166, .T. ) ;
#17519=ADVANCED_FACE ( 'NONE', ( #15726 ), #21208, .F. ) ;
#17520=LINE ( 'NONE', #8441, #6618 ) ;
#17525=ADVANCED_FACE ( 'NONE', ( #23213, #8456, #3136 ), #928, .F. ) ;
#17526=ORIENTED_EDGE ( 'NONE', *, *, #6046, .T. ) ;
#17527=CARTESIAN_POINT ( 'NONE',  ( 17.29858103379666545, 1.193049601325067988, -9.115197396075636505 ) ) ;
#17528=CARTESIAN_POINT ( 'NONE',  ( 15.53006424931000140, -9.332187211223001100, 5.252733788881000621 ) ) ;
#17529=CARTESIAN_POINT ( 'NONE',  ( -24.48870547333000047, 5.980820260656999565, -8.894311732265000714 ) ) ;
#17530=CARTESIAN_POINT ( 'NONE',  ( -18.13280809636999891, -10.33926822794999900, 0.2327566560484999880 ) ) ;
#17532=CARTESIAN_POINT ( 'NONE',  ( 15.26124951745999958, 1.362798856695000005, -9.630360975484999031 ) ) ;
#17533=FACE_BOUND ( 'NONE', #18198, .T. ) ;
#17534=FACE_OUTER_BOUND ( 'NONE', #14496, .T. ) ;
#17536=CARTESIAN_POINT ( 'NONE',  ( 6.162318803892000041, 13.65473356602000088, -2.204421525222999723 ) ) ;
#17537=ORIENTED_EDGE ( 'NONE', *, *, #10428, .T. ) ;
#17538=CARTESIAN_POINT ( 'NONE',  ( -0.7737468029517903245, 13.71960327777151356, 6.079035818031503169 ) ) ;
#17540=CARTESIAN_POINT ( 'NONE',  ( -4.175107824646003607, 12.32875441307999864, 2.224447038902001239 ) ) ;
#17541=CARTESIAN_POINT ( 'NONE',  ( -19.31991243917331857, 8.928523062339214889, -2.399343565118006172 ) ) ;
#17542=CARTESIAN_POINT ( 'NONE',  ( -14.46243031116633659, 2.866065099209276656, -8.600290833557869163 ) ) ;
#17543=CARTESIAN_POINT ( 'NONE',  ( -22.58353710275999759, 6.208000067599999561, -9.226852243910000695 ) ) ;
#17545=VERTEX_POINT ( 'NONE', #15822 ) ;
#17547=CARTESIAN_POINT ( 'NONE',  ( 4.750000000000000000, 20.10000000000000142, 0.000000000000000000 ) ) ;
#17548=CARTESIAN_POINT ( 'NONE',  ( 3.197564234074002254, 13.68604480655000621, 5.201785757272003430 ) ) ;
#17550=DIRECTION ( 'NONE',  ( -1.000000000000000000, 0.000000000000000000, 0.000000000000000000 ) ) ;
#17551=EDGE_CURVE ( 'NONE', #20493, #21674, #21534, .T. ) ;
#17552=EDGE_CURVE ( 'NONE', #12256, #2155, #7712, .T. ) ;
#17554=CARTESIAN_POINT ( 'NONE',  ( -18.52095171394000062, 10.52702611403999988, -4.436598560839000172 ) ) ;
#17555=CARTESIAN_POINT ( 'NONE',  ( 13.69575125731000043, 3.560502093102000387, -8.410767149301999979 ) ) ;
#17558=EDGE_LOOP ( 'NONE', ( #4743, #2563, #9467, #23607, #3115, #10736 ) ) ;
#17559=B_SPLINE_CURVE_WITH_KNOTS ( 'NONE', 3,
 ( #13307, #4113, #18887, #15358, #9685, #6039, #13427, #20947, #22748, #6167, #17679, #19621 ),
 .UNSPECIFIED., .F., .F.,
 ( 4, 1, 1, 1, 1, 2, 2, 4 ),
 ( 0.000000000000000000, 0.2499999999999964473, 0.3749999999999947820, 0.4374999999999936717, 0.4687499999999933387, 0.4843749999999933942, 0.4999999999999934497, 1.000000000000000000 ),
 .UNSPECIFIED. ) ;
#17560=CARTESIAN_POINT ( 'NONE',  ( -22.49384739520191800, 2.420755952246590237, 9.006231210083697647 ) ) ;
#17562=CARTESIAN_POINT ( 'NONE',  ( -12.41173981160000039, 6.613190111079999767, -13.46349570337000046 ) ) ;
#17563=CARTESIAN_POINT ( 'NONE',  ( 2.053618936107731052, 13.89760215911831942, -5.770478405391227916 ) ) ;
#17565=CARTESIAN_POINT ( 'NONE',  ( 4.566396831513001686, 14.20660692728000285, -4.011688757825002227 ) ) ;
#17570=ADVANCED_FACE ( 'NONE', ( #12333 ), #19837, .T. ) ;
#17571=CARTESIAN_POINT ( 'NONE',  ( 15.61874380413824781, -10.39027652322779183, 0.2460966605066790269 ) ) ;
#17573=DIRECTION ( 'NONE',  ( 1.000000000000000000, 0.000000000000000000, 0.000000000000000000 ) ) ;
#17574=CIRCLE ( 'NONE', #7117, 10.59999999999999964 ) ;
#17577=CARTESIAN_POINT ( 'NONE',  ( -24.50000000000000000, -5.567336242322655337, -8.985968813393915511 ) ) ;
#17580=CARTESIAN_POINT ( 'NONE',  ( -5.684582646178887977, 16.21817490744206580, -2.283151055710457733 ) ) ;
#17582=CARTESIAN_POINT ( 'NONE',  ( -0.6548632618487933987, 12.81818377440604273, 6.635320921360461810 ) ) ;
#17583=CIRCLE ( 'NONE', #17969, 12.50000000000000178 ) ;
#17584=CARTESIAN_POINT ( 'NONE',  ( 6.144969876179364299, 14.16671624030418108, -0.1596052567943958833 ) ) ;
#17586=CARTESIAN_POINT ( 'NONE',  ( 24.37713355803437665, -2.989142673506740788, -12.50000000000000355 ) ) ;
#17592=( BOUNDED_SURFACE ( )  B_SPLINE_SURFACE ( 3, 3, ( 
 ( #20420, #14376, #10632, #1547, #1421, #21770, #5182, #16301, #3486, #18252, #1654 ),
 ( #16415, #23805, #7213, #22000, #5413, #20185, #14718, #3595, #10978, #1773, #23926 ),
 ( #22114, #17255, #3947, #654, #7566, #8058, #11342, #15070, #22464, #20899, #5760 ),
 ( #2359, #15430, #22816, #15186, #7936, #18712, #11224, #6232, #5874, #13613, #174 ) ),
 .UNSPECIFIED., .F., .F., .T. ) 
 B_SPLINE_SURFACE_WITH_KNOTS ( ( 4, 4 ),
 ( 4, 1, 1, 1, 1, 1, 1, 1, 4 ),
 ( 0.000000000000000000, 1.000000000000000000 ),
 ( 0.6777550477067999513, 0.7077183713728000258, 0.7630935829821999805, 0.8160430438097999728, 0.8631236143084000112, 0.9059812851685999924, 0.9500234102994999930, 1.000000000000000000, 1.005511424025000045 ),
 .UNSPECIFIED. ) 
 GEOMETRIC_REPRESENTATION_ITEM ( )  RATIONAL_B_SPLINE_SURFACE ( (
 ( 1.339324717273000065, 1.339324717273000065, 1.339324717273000065, 1.339324717273000065, 1.339324717273000065, 1.339324717273000065, 1.339324717273000065, 1.339324717273000065, 1.339324717273000065, 1.339324717273000065, 1.339324717273000065),
 ( 0.8868917609088999843, 0.8868917609088999843, 0.8868917609088999843, 0.8868917609088999843, 0.8868917609088999843, 0.8868917609088999843, 0.8868917609088999843, 0.8868917609088999843, 0.8868917609088999843, 0.8868917609088999843, 0.8868917609088999843),
 ( 0.8868917609088999843, 0.8868917609088999843, 0.8868917609088999843, 0.8868917609088999843, 0.8868917609088999843, 0.8868917609088999843, 0.8868917609088999843, 0.8868917609088999843, 0.8868917609088999843, 0.8868917609088999843, 0.8868917609088999843),
 ( 1.339324717273000065, 1.339324717273000065, 1.339324717273000065, 1.339324717273000065, 1.339324717273000065, 1.339324717273000065, 1.339324717273000065, 1.339324717273000065, 1.339324717273000065, 1.339324717273000065, 1.339324717273000065) ) ) 
 REPRESENTATION_ITEM ( '' )  SURFACE ( )  );
#17593=EDGE_LOOP ( 'NONE', ( #16030, #16289, #6406, #13209 ) ) ;
#17594=CARTESIAN_POINT ( 'NONE',  ( -24.44714577827999946, -5.477234815341000207, -9.903190068764999410 ) ) ;
#17597=CARTESIAN_POINT ( 'NONE',  ( 15.04368363787946805, 9.348761382856489277, 4.437686386494108071 ) ) ;
#17599=CARTESIAN_POINT ( 'NONE',  ( -16.89940092177999986, 10.96253337826999896, -1.543077568198000016 ) ) ;
#17600=CARTESIAN_POINT ( 'NONE',  ( 4.834858920412084871, 12.45115190511012138, -0.1243179763900293527 ) ) ;
#17601=CARTESIAN_POINT ( 'NONE',  ( -19.91814312763024475, 0.2067535327646641552, 10.49027380322098324 ) ) ;
#17602=CARTESIAN_POINT ( 'NONE',  ( -0.5801434548614997633, 11.64265918162999114, -4.731509157062997240 ) ) ;
#17607=CARTESIAN_POINT ( 'NONE',  ( -17.00966196906368921, 6.126770844779409586, -8.438622901460794523 ) ) ;
#17611=CARTESIAN_POINT ( 'NONE',  ( 6.132481042133004046, 14.49467011299998909, -0.0001351461492217999522 ) ) ;
#17612=CARTESIAN_POINT ( 'NONE',  ( -4.633248246530266456, 13.46040479489061248, -5.211335153246753116 ) ) ;
#17613=CARTESIAN_POINT ( 'NONE',  ( 23.99062354302999722, 6.216878364870000340, -12.50000000000000000 ) ) ;
#17614=CARTESIAN_POINT ( 'NONE',  ( 18.35550158530999809, 7.854726640733000309, 6.622681824707000509 ) ) ;
#17615=ORIENTED_EDGE ( 'NONE', *, *, #21353, .T. ) ;
#17616=CARTESIAN_POINT ( 'NONE',  ( -10.04281598263999875, 1.347635823622999967E-14, 0.000000000000000000 ) ) ;
#17617=CARTESIAN_POINT ( 'NONE',  ( 4.849999930150000083, 12.54999993386000057, -7.274541077495999001E-07 ) ) ;
#17621=DIRECTION ( 'NONE',  ( 0.000000000000000000, 1.000000000000000000, 0.000000000000000000 ) ) ;
#17622=CARTESIAN_POINT ( 'NONE',  ( -7.834000000000000519, -10.59999999999999964, 0.000000000000000000 ) ) ;
#17623=AXIS2_PLACEMENT_3D ( 'NONE', #11722, #22489, #8210 ) ;
#17625=CARTESIAN_POINT ( 'NONE',  ( 17.66124585261385604, -10.36187385480047851, -0.9006329633823950687 ) ) ;
#17626=CARTESIAN_POINT ( 'NONE',  ( -23.76320767499999675, 6.967090338468000077, 12.06686491509000092 ) ) ;
#17627=CARTESIAN_POINT ( 'NONE',  ( 13.21250000000000036, 0.000000000000000000, 0.000000000000000000 ) ) ;
#17628=CARTESIAN_POINT ( 'NONE',  ( 21.33576293477999641, -7.518524484350999515, -8.339206206814999689 ) ) ;
#17630=CARTESIAN_POINT ( 'NONE',  ( 12.52688711657000020, 6.216878364870000340, -12.50000000000000000 ) ) ;
#17633=CARTESIAN_POINT ( 'NONE',  ( 19.69983353523999980, 6.514647315076000034, -8.669487664655999737 ) ) ;
#17636=EDGE_CURVE ( 'NONE', #17401, #7987, #929, .T. ) ;
#17639=CARTESIAN_POINT ( 'NONE',  ( 4.912321670294291565, 14.34861163470688084, 3.825009897921954227 ) ) ;
#17640=ORIENTED_EDGE ( 'NONE', *, *, #6076, .F. ) ;
#17641=CARTESIAN_POINT ( 'NONE',  ( -14.86532595926124500, 9.166658182833229418, -4.831506234239814290 ) ) ;
#17645=CARTESIAN_POINT ( 'NONE',  ( -14.38789255203824879, -4.127795921257689571, -12.49979377837149208 ) ) ;
#17648=DIRECTION ( 'NONE',  ( 1.000000000000000000, 0.000000000000000000, 0.000000000000000000 ) ) ;
#17649=CARTESIAN_POINT ( 'NONE',  ( -5.372805085453999929, 16.07374366015000078, -2.940844016990000309 ) ) ;
#17650=CARTESIAN_POINT ( 'NONE',  ( -24.38011137294000008, 0.4010730224961999713, -11.22689660418999935 ) ) ;
#17651=CARTESIAN_POINT ( 'NONE',  ( -19.75785088013000035, -8.381234170548999884, -6.136494560970000123 ) ) ;
#17652=CARTESIAN_POINT ( 'NONE',  ( -6.063697158388001718, 15.62880598230002249, 1.260709251179999324 ) ) ;
#17653=CARTESIAN_POINT ( 'NONE',  ( 19.72999951746000136, 0.8733432563274000637, 9.811130420370998806 ) ) ;
#17655=CIRCLE ( 'NONE', #2566, 13.75000000000000000 ) ;
#17656=B_SPLINE_CURVE_WITH_KNOTS ( 'NONE', 3,
 ( #15108, #9791, #13418, #6393, #15225, #19110, #4593, #572, #17428, #17300, #8223, #16935, #20696, #6156 ),
 .UNSPECIFIED., .F., .F.,
 ( 4, 2, 2, 2, 2, 2, 4 ),
 ( 0.000000000000000000, 0.2500000000000001110, 0.3750000000000001110, 0.5000000000000001110, 0.6250000000000000000, 0.7500000000000000000, 1.000000000000000000 ),
 .UNSPECIFIED. ) ;
#17657=AXIS2_PLACEMENT_3D ( 'NONE', #9992, #2853, #6837 ) ;
#17658=CARTESIAN_POINT ( 'NONE',  ( 20.76146583675999935, 3.250716185844000350, -9.124108739569999571 ) ) ;
#17660=ORIENTED_EDGE ( 'NONE', *, *, #7834, .T. ) ;
#17661=CARTESIAN_POINT ( 'NONE',  ( 1.413067587578629380, 13.78907544507517535, 5.959893886319711953 ) ) ;
#17663=CARTESIAN_POINT ( 'NONE',  ( -19.88678743917331815, -5.642442153596147314, -7.342323539242457286 ) ) ;
#17664=EDGE_CURVE ( 'NONE', #17201, #3390, #6990, .T. ) ;
#17669=CARTESIAN_POINT ( 'NONE',  ( 15.90028936713000185, 9.079314476020000413, 0.000000000000000000 ) ) ;
#17670=CARTESIAN_POINT ( 'NONE',  ( 2.331536102386086107, 11.71301274535795933, -4.220455149562390318 ) ) ;
#17671=CARTESIAN_POINT ( 'NONE',  ( 4.166162063823999340, 14.03319894470998364, 4.455060026797000639 ) ) ;
#17674=DIRECTION ( 'NONE',  ( 0.000000000000000000, -1.000000000000000000, 0.000000000000000000 ) ) ;
#17676=CARTESIAN_POINT ( 'NONE',  ( -11.51617721169000141, -15.07264118231999994, 3.899284990158000230 ) ) ;
#17677=CARTESIAN_POINT ( 'NONE',  ( -17.30216962611999776, -8.848728181206000798, -7.171245711509000920 ) ) ;
#17678=CARTESIAN_POINT ( 'NONE',  ( 13.06406392131000160, -4.637122060904999898, 8.435305548789999719 ) ) ;
#17679=CARTESIAN_POINT ( 'NONE',  ( 24.50000000000000000, 11.33659675998026728, -5.364438426793228132 ) ) ;
#17685=CARTESIAN_POINT ( 'NONE',  ( -1.730145359313365550, 13.83619868571590672, -5.879316393191865942 ) ) ;
#17686=ORIENTED_EDGE ( 'NONE', *, *, #1664, .T. ) ;
#17689=CARTESIAN_POINT ( 'NONE',  ( 24.50000000000000000, 0.000000000000000000, 0.000000000000000000 ) ) ;
#17690=DIRECTION ( 'NONE',  ( -1.000000000000000000, 0.000000000000000000, 0.000000000000000000 ) ) ;
#17693=CARTESIAN_POINT ( 'NONE',  ( 14.72667347117745429, 10.36589271863794259, 0.2970802226479983266 ) ) ;
#17695=CARTESIAN_POINT ( 'NONE',  ( -3.644446339697000159, 14.33206891720999998, 4.922772686299000000 ) ) ;
#17697=ADVANCED_FACE ( 'NONE', ( #17534 ), #8328, .T. ) ;
#17698=CARTESIAN_POINT ( 'NONE',  ( -24.46742986864117597, -10.18447769902851263, 7.359979596114137657 ) ) ;
#17699=VERTEX_POINT ( 'NONE', #13892 ) ;
#17701=ADVANCED_FACE ( 'NONE', ( #14494 ), #20070, .F. ) ;
#17702=CARTESIAN_POINT ( 'NONE',  ( -19.10482910584000038, 1.458613477275000161E-14, 0.000000000000000000 ) ) ;
#17703=ORIENTED_EDGE ( 'NONE', *, *, #15151, .T. ) ;
#17706=CARTESIAN_POINT ( 'NONE',  ( 3.696164193155713207, 13.26185372247518046, 5.697559243385613037 ) ) ;
#17708=CARTESIAN_POINT ( 'NONE',  ( 6.226966478309651443, 13.75515049843148674, -1.330623856768273106 ) ) ;
#17711=AXIS2_PLACEMENT_3D ( 'NONE', #2261, #18735, #2142 ) ;
#17712=EDGE_LOOP ( 'NONE', ( #16247, #14809, #15376, #2650 ) ) ;
#17714=FACE_OUTER_BOUND ( 'NONE', #7385, .T. ) ;
#17718=CARTESIAN_POINT ( 'NONE',  ( -24.10441230706999960, 7.126933907174000105, -8.778685816131000408 ) ) ;
#17721=CARTESIAN_POINT ( 'NONE',  ( 15.23247813278353746, 4.705309158913490108, 9.205882947448541742 ) ) ;
#17722=CARTESIAN_POINT ( 'NONE',  ( 11.77156519342000074, 1.080486702797000030E-14, 0.000000000000000000 ) ) ;
#17724=DIRECTION ( 'NONE',  ( 0.000000000000000000, 1.000000000000000000, 0.000000000000000000 ) ) ;
#17725=CARTESIAN_POINT ( 'NONE',  ( -3.895265127482998579, 12.15836816443999702, -2.782973809895999295 ) ) ;
#17732=CARTESIAN_POINT ( 'NONE',  ( -16.63345270903459294, 9.745656342660240057, 3.687025462406674503 ) ) ;
#17735=CARTESIAN_POINT ( 'NONE',  ( 6.372376369063001533, 13.56112563602000165, -1.886254648120999411 ) ) ;
#17736=CARTESIAN_POINT ( 'NONE',  ( 11.99999999999999822, 1.399482473622788659, -8.879313528662020616 ) ) ;
#17737=CARTESIAN_POINT ( 'NONE',  ( -19.95647087121332675, 1.202231731695357908, -9.183404087729607923 ) ) ;
#17738=CARTESIAN_POINT ( 'NONE',  ( 16.38112658530999610, 10.11489150981000051, 1.477102707085000022 ) ) ;
#17740=ORIENTED_EDGE ( 'NONE', *, *, #8687, .T. ) ;
#17742=AXIS2_PLACEMENT_3D ( 'NONE', #17702, #8134, #14058 ) ;
#17744=CARTESIAN_POINT ( 'NONE',  ( -20.44776253787999920, -9.196011600180998613, 0.000000000000000000 ) ) ;
#17745=ORIENTED_EDGE ( 'NONE', *, *, #10839, .F. ) ;
#17746=CARTESIAN_POINT ( 'NONE',  ( 11.83261479513476999, 13.04738324256021897, 2.401298039133532125 ) ) ;
#17748=CARTESIAN_POINT ( 'NONE',  ( -5.819905644321182514, 14.78666136312912549, -4.230997804075329327 ) ) ;
#17749=CARTESIAN_POINT ( 'NONE',  ( 16.21516467252304494, -2.163961224650327253, -10.13852251010399641 ) ) ;
#17750=B_SPLINE_CURVE_WITH_KNOTS ( 'NONE', 3,
 ( #23039, #6459, #3206, #10099, #10588, #13843, #17612, #1005 ),
 .UNSPECIFIED., .F., .F.,
 ( 4, 2, 2, 4 ),
 ( 0.000000000000000000, 0.2499999999999990563, 0.4999999999999981126, 1.000000000000000000 ),
 .UNSPECIFIED. ) ;
#17751=CARTESIAN_POINT ( 'NONE',  ( -23.74465998031000069, 7.716878364870000340, 11.63397459621999985 ) ) ;
#17752=DIRECTION ( 'NONE',  ( -1.000000000000000000, 0.000000000000000000, 0.000000000000000000 ) ) ;
#17754=CARTESIAN_POINT ( 'NONE',  ( -4.281325311130067313, 13.62243467556385212, -4.949493687103234230 ) ) ;
#17755=LINE ( 'NONE', #8663, #1041 ) ;
#17759=CARTESIAN_POINT ( 'NONE',  ( 23.37160127288000311, 7.821747501224999510, -7.657236109244999867 ) ) ;
#17760=CARTESIAN_POINT ( 'NONE',  ( -12.25000000000000000, 1.374666032043000015E-14, 0.000000000000000000 ) ) ;
#17763=CARTESIAN_POINT ( 'NONE',  ( -19.35893705290999733, -9.828989445528000246, 3.502754984265999738 ) ) ;
#17764=CARTESIAN_POINT ( 'NONE',  ( -24.50000000000292744, -10.95355345393464574, -6.027888894374386908 ) ) ;
#17765=CARTESIAN_POINT ( 'NONE',  ( -4.946046029160003243, 12.51485534603999383, -0.01135644941591000372 ) ) ;
#17766=ORIENTED_EDGE ( 'NONE', *, *, #23886, .F. ) ;
#17768=CARTESIAN_POINT ( 'NONE',  ( -16.40044400686480586, 9.230068319053810200, 4.808581141419865368 ) ) ;
#17769=CARTESIAN_POINT ( 'NONE',  ( 17.09606375731000227, -3.490954664894000192, -8.536518206589999380 ) ) ;
#17770=VERTEX_POINT ( 'NONE', #12801 ) ;
#17771=AXIS2_PLACEMENT_3D ( 'NONE', #19354, #2881, #22962 ) ;
#17778=CARTESIAN_POINT ( 'NONE',  ( -4.547121837679138245, 15.52640757196256338, -4.103591966345952358 ) ) ;
#17779=CARTESIAN_POINT ( 'NONE',  ( -22.45307115331999981, 4.633966765693999790, -10.17689589833000063 ) ) ;
#17780=EDGE_CURVE ( 'NONE', #3196, #1114, #3842, .T. ) ;
#17781=CARTESIAN_POINT ( 'NONE',  ( -19.96098122809999964, -10.36515734744000028, 0.7445752835680999882 ) ) ;
#17783=CARTESIAN_POINT ( 'NONE',  ( 18.23994494525999954, -9.523641201324000605, -4.050084129495000518 ) ) ;
#17784=CARTESIAN_POINT ( 'NONE',  ( 4.829987487923999900, 14.79876397742000016, -3.766541047082999860 ) ) ;
#17785=CARTESIAN_POINT ( 'NONE',  ( 20.58441673460000132, -2.591490884510000203, -9.327754992274998713 ) ) ;
#17787=CARTESIAN_POINT ( 'NONE',  ( 24.50000000000000000, 8.054858440593999802, 5.882793087032000656 ) ) ;
#17789=CARTESIAN_POINT ( 'NONE',  ( 23.65010203509851294, -1.257950004970036506, 9.261471990918924035 ) ) ;
#17790=CARTESIAN_POINT ( 'NONE',  ( 2.815613996704550370, 14.07709565253041362, 5.439481458778258727 ) ) ;
#17793=CIRCLE ( 'NONE', #11591, 7.000000000000000000 ) ;
#17795=CARTESIAN_POINT ( 'NONE',  ( -14.17283651172096981, 8.841951170099118684, -2.221021055535443267 ) ) ;
#17796=ADVANCED_FACE ( 'NONE', ( #7103 ), #20188, .T. ) ;
#17798=CARTESIAN_POINT ( 'NONE',  ( -4.630910936227792263, 12.36731740134543323, 1.448661297286960803 ) ) ;
#17799=ORIENTED_EDGE ( 'NONE', *, *, #10145, .T. ) ;
#17801=CARTESIAN_POINT ( 'NONE',  ( 1.541259979151140769, 11.58204529230899915, -4.568150535643495047 ) ) ;
#17803=CARTESIAN_POINT ( 'NONE',  ( -21.09022087121333300, 5.661420876518568512, 7.367019229478493969 ) ) ;
#17804=CARTESIAN_POINT ( 'NONE',  ( 11.50000000000000000, 0.000000000000000000, 0.000000000000000000 ) ) ;
#17807=CARTESIAN_POINT ( 'NONE',  ( 18.51187642130999933, -4.805399430337999434, 8.325799818148999165 ) ) ;
#17813=CARTESIAN_POINT ( 'NONE',  ( -15.12503743917333487, -1.186002250417325099, 9.059419983607615023 ) ) ;
#17814=CARTESIAN_POINT ( 'NONE',  ( -2.491868457724357722, 13.99434024406236787, -5.595226495223592167 ) ) ;
#17818=CARTESIAN_POINT ( 'NONE',  ( 24.49181240879000043, -4.016481066597000549, 10.13876987169999921 ) ) ;
#17821=CARTESIAN_POINT ( 'NONE',  ( 15.78600699156848819, -8.833878469997333838, -5.484853103214551773 ) ) ;
#17822=CARTESIAN_POINT ( 'NONE',  ( -3.839124943223277242, 14.03390693797235755, 4.849677718342541688 ) ) ;
#17823=CARTESIAN_POINT ( 'NONE',  ( -21.81416243917332665, -8.065940078106184075, -4.649062424942554728 ) ) ;
#17828=CARTESIAN_POINT ( 'NONE',  ( 11.18529249867181363, -11.69879683431631179, 4.737131156288532985 ) ) ;
#17829=ORIENTED_EDGE ( 'NONE', *, *, #14709, .F. ) ;
#17832=CARTESIAN_POINT ( 'NONE',  ( -0.4485994107868310210, 12.81051815475211519, 6.650126618851852633 ) ) ;
#17833=CARTESIAN_POINT ( 'NONE',  ( 6.233555060839315765, 13.72084049725845567, -1.474633800018174679 ) ) ;
#17834=CARTESIAN_POINT ( 'NONE',  ( -5.983874849942004026, 15.83682689383999076, -0.8929930702161996692 ) ) ;
#17836=DIRECTION ( 'NONE',  ( 0.000000000000000000, 0.000000000000000000, -1.000000000000000000 ) ) ;
#17838=CARTESIAN_POINT ( 'NONE',  ( -12.30391311677716359, 12.15793044322834504, -9.412942108898313620 ) ) ;
#17840=LINE ( 'NONE', #6678, #12893 ) ;
#17843=CARTESIAN_POINT ( 'NONE',  ( -23.68915714226000091, 10.30687545221999990, -3.135322633623999877 ) ) ;
#17844=EDGE_CURVE ( 'NONE', #4978, #16650, #15377, .T. ) ;
#17845=CARTESIAN_POINT ( 'NONE',  ( 20.30216666666665759, -8.032133636156673973, -4.629287041203744124 ) ) ;
#17846=CARTESIAN_POINT ( 'NONE',  ( 15.15146838647111238, 7.118369732183343679, 7.496456199561704281 ) ) ;
#17848=DIRECTION ( 'NONE',  ( -1.000000000000000000, 0.000000000000000000, 0.000000000000000000 ) ) ;
#17849=CARTESIAN_POINT ( 'NONE',  ( 13.59924040960673786, 6.893992233393349878, -5.816697367115062356 ) ) ;
#17850=CARTESIAN_POINT ( 'NONE',  ( -3.149587440023998486, 12.07849849174000312, -3.556593144048001864 ) ) ;
#17852=FACE_OUTER_BOUND ( 'NONE', #3818, .T. ) ;
#17856=DIRECTION ( 'NONE',  ( -1.000000000000000000, 0.000000000000000000, 0.000000000000000000 ) ) ;
#17857=CARTESIAN_POINT ( 'NONE',  ( -17.58844544603152116, -10.40508157927476951, -2.008783379089892573 ) ) ;
#17858=ORIENTED_EDGE ( 'NONE', *, *, #1393, .F. ) ;
#17859=CARTESIAN_POINT ( 'NONE',  ( 4.924532323579002835, 14.11581327235000316, -3.892461550489000111 ) ) ;
#17860=CARTESIAN_POINT ( 'NONE',  ( 12.00000000000000000, 2.690641297232414519, -8.571655010542230002 ) ) ;
#17861=CARTESIAN_POINT ( 'NONE',  ( 18.66303164209000087, 0.6515539281180999787, 11.11005403933000046 ) ) ;
#17862=CARTESIAN_POINT ( 'NONE',  ( 18.93037674931000325, -2.874963284959999754, 10.40852167983000065 ) ) ;
#17864=CARTESIAN_POINT ( 'NONE',  ( -10.52007399291999867, -1.707568499793000072, -14.41682586501999985 ) ) ;
#17867=EDGE_CURVE ( 'NONE', #12256, #3010, #13936, .T. ) ;
#17868=ORIENTED_EDGE ( 'NONE', *, *, #9343, .T. ) ;
#17869=EDGE_CURVE ( 'NONE', #4443, #10646, #21644, .T. ) ;
#17871=CARTESIAN_POINT ( 'NONE',  ( 22.32342665428159378, 3.749095308366488410, 9.883727313549222515 ) ) ;
#17872=CARTESIAN_POINT ( 'NONE',  ( -6.249999999916000526, 15.09564573669999987, 3.212813967733000098 ) ) ;
#17873=CARTESIAN_POINT ( 'NONE',  ( 16.33715996058963427, 2.151044717592483835, -10.15474803909974000 ) ) ;
#17874=CARTESIAN_POINT ( 'NONE',  ( -5.758336963890107185, 14.73197845513246662, 4.351221581719583398 ) ) ;
#17875=CARTESIAN_POINT ( 'NONE',  ( -14.48092000065305385, -9.982182315257093208, 7.710362946285843400 ) ) ;
#17880=CARTESIAN_POINT ( 'NONE',  ( 11.40904387244416185, 9.351110459849435230, -8.803306989966603879 ) ) ;
#17882=CARTESIAN_POINT ( 'NONE',  ( 22.65423997573916992, -1.018721363148856529, 10.53549965532916133 ) ) ;
#17885=( BOUNDED_CURVE ( )  B_SPLINE_CURVE ( 3, ( #17872, #5040, #10604, #19922 ),
 .UNSPECIFIED., .F., .T. ) 
 B_SPLINE_CURVE_WITH_KNOTS ( ( 4, 4 ),
 ( 0.000000000000000000, 1.000000000000000000 ),
 .UNSPECIFIED. ) 
 CURVE ( )  GEOMETRIC_REPRESENTATION_ITEM ( )  RATIONAL_B_SPLINE_CURVE ( ( 1.134253127167035746, 0.9460051651271520479, 0.9557263079415558860, 1.163416555610247594 ) ) 
 REPRESENTATION_ITEM ( '' )  );
#17886=CARTESIAN_POINT ( 'NONE',  ( 24.50000000000000355, -10.31403833462485053, -7.135561573215231768 ) ) ;
#17887=FACE_OUTER_BOUND ( 'NONE', #17407, .T. ) ;
#17889=CARTESIAN_POINT ( 'NONE',  ( -15.06070461986450049, 4.116752997674038461, -9.515275712647939699 ) ) ;
#17891=ORIENTED_EDGE ( 'NONE', *, *, #16173, .F. ) ;
#17895=VERTEX_POINT ( 'NONE', #4921 ) ;
#17897=CARTESIAN_POINT ( 'NONE',  ( 12.78787674931000140, 8.861872729009999006, -5.882981327196000088 ) ) ;
#17898=CARTESIAN_POINT ( 'NONE',  ( -22.72225193867999948, 4.421850665685999715, -9.710967849992998779 ) ) ;
#17899=CARTESIAN_POINT ( 'NONE',  ( -15.42606313537000062, 5.797595928499999829, -9.114297677153000876 ) ) ;
#17900=CARTESIAN_POINT ( 'NONE',  ( 22.34291666666665321, -2.419883552198663690, -9.003983045265712803 ) ) ;
#17901=CARTESIAN_POINT ( 'NONE',  ( 18.30812451746000136, -9.368717106552999496, 2.913269227472000011 ) ) ;
#17903=CARTESIAN_POINT ( 'NONE',  ( 13.65000000000000036, 1.057482511063999969E-14, 0.000000000000000000 ) ) ;
#17904=CARTESIAN_POINT ( 'NONE',  ( 24.46338342271116062, 9.116595994419974147, 4.069120185925712008 ) ) ;
#17905=VERTEX_POINT ( 'NONE', #12070 ) ;
#17906=CARTESIAN_POINT ( 'NONE',  ( 23.35066019142154659, 7.280967731064075465, 5.766833715589692488 ) ) ;
#17907=CARTESIAN_POINT ( 'NONE',  ( 0.1555892161840528309, 13.69209904246603493, 6.123026241355283616 ) ) ;
#17909=AXIS2_PLACEMENT_3D ( 'NONE', #10080, #4386, #19404 ) ;
#17911=CARTESIAN_POINT ( 'NONE',  ( 6.015441748752945017, 14.40198550462790017, -1.164718804201562818 ) ) ;
#17912=CARTESIAN_POINT ( 'NONE',  ( -21.91519891963999811, 2.578799165454999986, 10.79911247067000168 ) ) ;
#17913=CARTESIAN_POINT ( 'NONE',  ( -3.374921343011017871, 11.96071138814094859, 3.456569768525166175 ) ) ;
#17915=CARTESIAN_POINT ( 'NONE',  ( 15.74912270046332274, 7.929943201579005674, -4.570678727046721512 ) ) ;
#17916=CARTESIAN_POINT ( 'NONE',  ( 3.972980349958184831, 12.14025353368746174, -2.760264024277557571 ) ) ;
#17917=CARTESIAN_POINT ( 'NONE',  ( -10.62890643558121617, 15.45176336733469036, 1.489320882496812493 ) ) ;
#17918=CARTESIAN_POINT ( 'NONE',  ( 11.95587595596410679, 4.161512325801380641, -8.073311510776072453 ) ) ;
#17919=ORIENTED_EDGE ( 'NONE', *, *, #13696, .F. ) ;
#17921=CARTESIAN_POINT ( 'NONE',  ( -13.10414243475000085, 9.447148007457000674, -4.942668164112999918 ) ) ;
#17922=CARTESIAN_POINT ( 'NONE',  ( 16.68375142130999933, -4.435783964195000095, 8.649968580473998969 ) ) ;
#17923=CARTESIAN_POINT ( 'NONE',  ( 18.51005996110214014, 10.35102410635204606, -1.233439651704276274 ) ) ;
#17928=CARTESIAN_POINT ( 'NONE',  ( 3.187263766028701539, 14.18382903446076249, -5.230654009935672200 ) ) ;
#17929=ORIENTED_EDGE ( 'NONE', *, *, #11940, .T. ) ;
#17931=DIRECTION ( 'NONE',  ( 0.000000000000000000, 1.000000000000000000, 0.000000000000000000 ) ) ;
#17933=CARTESIAN_POINT ( 'NONE',  ( -12.50000000000000000, 6.992973968623999781, -5.709239639804999378 ) ) ;
#17934=CARTESIAN_POINT ( 'NONE',  ( 14.39214709631707834, 4.421562029032312324, -9.372419967397966900 ) ) ;
#17935=DIRECTION ( 'NONE',  ( -1.000000000000000000, 0.000000000000000000, 0.000000000000000000 ) ) ;
#17936=CARTESIAN_POINT ( 'NONE',  ( 4.902363039930995647, 12.49825868767001147, 0.6843989955805002134 ) ) ;
#17938=ORIENTED_EDGE ( 'NONE', *, *, #4899, .T. ) ;
#17939=DIRECTION ( 'NONE',  ( 0.000000000000000000, 0.000000000000000000, -1.000000000000000000 ) ) ;
#17943=EDGE_CURVE ( 'NONE', #19018, #12884, #12235, .T. ) ;
#17944=DIRECTION ( 'NONE',  ( 0.000000000000000000, 1.000000000000000000, 0.000000000000000000 ) ) ;
#17945=CARTESIAN_POINT ( 'NONE',  ( 11.10357421856130600, -0.9986522863917048909, -12.49997040256712388 ) ) ;
#17947=CARTESIAN_POINT ( 'NONE',  ( 6.179202422571329123, 13.97195698268568087, -0.6507670915169003756 ) ) ;
#17948=CARTESIAN_POINT ( 'NONE',  ( 13.49999999999999822, 0.5660735980287910918, 10.31195207906871403 ) ) ;
#17950=ORIENTED_EDGE ( 'NONE', *, *, #20523, .T. ) ;
#17955=ORIENTED_EDGE ( 'NONE', *, *, #1841, .T. ) ;
#17957=CARTESIAN_POINT ( 'NONE',  ( -24.03189061347999811, 0.9515185275740000170, -10.74041837823999934 ) ) ;
#17959=CARTESIAN_POINT ( 'NONE',  ( 15.06085725605862358, 9.069360526526905275, 4.955433154737670876 ) ) ;
#17961=DIRECTION ( 'NONE',  ( -1.000000000000000000, 0.000000000000000000, 0.000000000000000000 ) ) ;
#17964=CARTESIAN_POINT ( 'NONE',  ( -4.782017827913002783, 12.48036279474998977, -0.01094907448527000608 ) ) ;
#17966=CARTESIAN_POINT ( 'NONE',  ( -21.88384587121331393, -2.416565420321704849, -8.992606164485385634 ) ) ;
#17967=ORIENTED_EDGE ( 'NONE', *, *, #23738, .F. ) ;
#17969=AXIS2_PLACEMENT_3D ( 'NONE', #18010, #1294, #21760 ) ;
#17975=CARTESIAN_POINT ( 'NONE',  ( 12.06371966924003658, -13.38412994814091306, -1.818205398009610008 ) ) ;
#17977=CARTESIAN_POINT ( 'NONE',  ( 16.67807176579999862, 6.709682755504000617, 8.811495003121999403 ) ) ;
#17979=CARTESIAN_POINT ( 'NONE',  ( 18.82068924930999998, 1.189837805593999986, 10.72966125727000097 ) ) ;
#17981=CARTESIAN_POINT ( 'NONE',  ( -10.92736399291999838, -14.05489928066999994, 3.635995652016000168 ) ) ;
#17982=CARTESIAN_POINT ( 'NONE',  ( 13.49999999999999822, 8.021967196418742674, -4.687592336913057878 ) ) ;
#17983=DIRECTION ( 'NONE',  ( 0.000000000000000000, -1.000000000000000000, 0.000000000000000000 ) ) ;
#17987=CARTESIAN_POINT ( 'NONE',  ( 23.41176634503839082, 2.789004178826171465, -10.22545939124784375 ) ) ;
#17988=B_SPLINE_CURVE_WITH_KNOTS ( 'NONE', 3,
 ( #15057, #5974, #14816, #9380, #13134, #13245, #18817, #20639, #3933, #15287, #2224, #16752, #22680 ),
 .UNSPECIFIED., .F., .F.,
 ( 4, 1, 1, 1, 1, 1, 2, 2, 4 ),
 ( 0.000000000000000000, 0.2500000000000000000, 0.3750000000000000000, 0.4374999999999999445, 0.4687500000000000000, 0.4843750000000000555, 0.4921875000000000000, 0.4999999999999999445, 1.000000000000000000 ),
 .UNSPECIFIED. ) ;
#17989=DIRECTION ( 'NONE',  ( 0.000000000000000000, 1.000000000000000000, 0.000000000000000000 ) ) ;
#17990=CARTESIAN_POINT ( 'NONE',  ( 16.30560488073658831, 1.031953949068942000, -10.32206256363679309 ) ) ;
#17993=CARTESIAN_POINT ( 'NONE',  ( -3.921362958110083952, 13.93606275262591332, -4.846548280059000291 ) ) ;
#17996=CARTESIAN_POINT ( 'NONE',  ( 11.22285964976442862, 11.82554192014311312, -4.517540867263379667 ) ) ;
#17997=CARTESIAN_POINT ( 'NONE',  ( 23.78917532224939890, 8.220281951958336109, -6.706429737208729591 ) ) ;
#18004=EDGE_CURVE ( 'NONE', #17545, #1942, #7606, .T. ) ;
#18006=EDGE_LOOP ( 'NONE', ( #5092, #12569, #4972, #5854, #4343, #6548, #10544, #863, #22672, #22429, #3280 ) ) ;
#18007=CARTESIAN_POINT ( 'NONE',  ( 16.65731375730999986, -8.692770150473998925, 3.046645682941000022 ) ) ;
#18008=VERTEX_POINT ( 'NONE', #5857 ) ;
#18010=CARTESIAN_POINT ( 'NONE',  ( -24.50000000000000000, 1.524685264937999788E-14, 0.000000000000000000 ) ) ;
#18011=PRODUCT_CONTEXT ( 'NONE', #6007, 'mechanical' ) ;
#18013=ORIENTED_EDGE ( 'NONE', *, *, #19614, .F. ) ;
#18014=EDGE_CURVE ( 'NONE', #11394, #6063, #7326, .T. ) ;
#18017=CARTESIAN_POINT ( 'NONE',  ( -3.900110430061300981, 14.77499599200090152, -4.723055523159343849 ) ) ;
#18018=CARTESIAN_POINT ( 'NONE',  ( -22.99143272405000360, 4.209734565676999551, -9.245039801656998790 ) ) ;
#18019=CARTESIAN_POINT ( 'NONE',  ( -14.54251227031000049, -6.905310822002999949, -6.821119646334000031 ) ) ;
#18021=CARTESIAN_POINT ( 'NONE',  ( -23.00635821734891806, -10.16212841000448286, -2.913267094275154179 ) ) ;
#18024=CARTESIAN_POINT ( 'NONE',  ( 14.78458333333333385, -8.815166781429585541, -2.368879911036435804 ) ) ;
#18029=B_SPLINE_CURVE_WITH_KNOTS ( 'NONE', 3,
 ( #6224, #21004, #23176, #13363, #20764 ),
 .UNSPECIFIED., .F., .F.,
 ( 4, 1, 4 ),
 ( 0.000000000000000000, 0.5000000000000000000, 1.000000000000000000 ),
 .UNSPECIFIED. ) ;
#18030=LINE ( 'NONE', #5424, #5644 ) ;
#18032=CARTESIAN_POINT ( 'NONE',  ( -4.121623016841069465, 12.18874198761142047, 2.540134958274468779 ) ) ;
#18035=CARTESIAN_POINT ( 'NONE',  ( 2.690147716812516077, 11.78874550216520056, -4.003645878357374066 ) ) ;
#18036=CARTESIAN_POINT ( 'NONE',  ( 24.17967779705173115, 2.685270347960766024, -9.197338196224221107 ) ) ;
#18037=CARTESIAN_POINT ( 'NONE',  ( -20.86347087121333388, -1.205278475425912932, 9.206679495332496188 ) ) ;
#18039=DIRECTION ( 'NONE',  ( 1.000000000000000000, 0.000000000000000000, 0.000000000000000000 ) ) ;
#18042=CARTESIAN_POINT ( 'NONE',  ( 13.28343892131000104, -9.177482186369001482, 2.922696180057999804 ) ) ;
#18043=CARTESIAN_POINT ( 'NONE',  ( 18.44601586413295990, 9.834069045321928826, -3.450538262810350698 ) ) ;
#18047=DIRECTION ( 'NONE',  ( 1.000000000000000000, 0.000000000000000000, 0.000000000000000000 ) ) ;
#18048=CARTESIAN_POINT ( 'NONE',  ( 4.750000000000000000, 17.00000000000000000, 0.000000000000000000 ) ) ;
#18053=CARTESIAN_POINT ( 'NONE',  ( 15.91833333333333300, 4.572865580834726273, 7.933737425283369227 ) ) ;
#18054=CARTESIAN_POINT ( 'NONE',  ( -23.90159383812773086, -3.635517970721634295, 9.022299759201507285 ) ) ;
#18055=DIRECTION ( 'NONE',  ( 1.000000000000000000, 0.000000000000000000, 0.000000000000000000 ) ) ;
#18057=CARTESIAN_POINT ( 'NONE',  ( -3.735429536209002865, 12.03300774351999713, 3.212544806379001638 ) ) ;
#18058=CARTESIAN_POINT ( 'NONE',  ( 19.83062270046332642, 4.623427443748358456, 8.021463006140603369 ) ) ;
#18065=CARTESIAN_POINT ( 'NONE',  ( 6.132134859666997784, 14.49476015624998482, -0.03567915623813002618 ) ) ;
#18066=CARTESIAN_POINT ( 'NONE',  ( 12.40357033523132912, 5.939957768465679244, -12.49999999999918288 ) ) ;
#18067=CARTESIAN_POINT ( 'NONE',  ( 6.189458490575474592, 13.92434823838417479, -0.7784157444028274586 ) ) ;
#18069=DIRECTION ( 'NONE',  ( 0.000000000000000000, 1.000000000000000000, 0.000000000000000000 ) ) ;
#18071=ORIENTED_EDGE ( 'NONE', *, *, #11135, .T. ) ;
#18072=PLANE ( 'NONE',  #10051 ) ;
#18077=CARTESIAN_POINT ( 'NONE',  ( -24.20325734908000115, -5.220886106840999297, -9.439784460628999341 ) ) ;
#18078=AXIS2_PLACEMENT_3D ( 'NONE', #9091, #14653, #16700 ) ;
#18080=CARTESIAN_POINT ( 'NONE',  ( 14.54094227179021992, 2.725430164165235425, -9.955622680467328678 ) ) ;
#18081=CARTESIAN_POINT ( 'NONE',  ( -12.25000000000000000, 1.374666032043000015E-14, 0.000000000000000000 ) ) ;
#18082=CARTESIAN_POINT ( 'NONE',  ( 23.20815793052999965, -0.2658484307651000078, -11.27637876372000036 ) ) ;
#18083=ADVANCED_FACE ( 'NONE', ( #969 ), #18556, .F. ) ;
#18086=CARTESIAN_POINT ( 'NONE',  ( -0.5822634062851997916, 11.56436112468998623, -4.714933848958999363 ) ) ;
#18087=EDGE_LOOP ( 'NONE', ( #7956, #17353, #7685 ) ) ;
#18094=CARTESIAN_POINT ( 'NONE',  ( -12.25000000000000000, 1.374666032043000015E-14, 0.000000000000000000 ) ) ;
#18095=CARTESIAN_POINT ( 'NONE',  ( 17.35441666666665839, 8.879300184524714368, -2.386375964361124424 ) ) ;
#18097=AXIS2_PLACEMENT_3D ( 'NONE', #19853, #3026, #10888 ) ;
#18098=CARTESIAN_POINT ( 'NONE',  ( 21.38008103379665314, 9.219936730289768789, 1.206759948112953618 ) ) ;
#18099=CARTESIAN_POINT ( 'NONE',  ( 24.45564077607145492, 2.060124049349388642, -12.50000000000000355 ) ) ;
#18103=CARTESIAN_POINT ( 'NONE',  ( -9.894391138769998761, -12.85207681411000102, 8.150135934440999819 ) ) ;
#18104=CARTESIAN_POINT ( 'NONE',  ( 13.50000000000000178, 7.201649267261895915, -5.777227494228245774 ) ) ;
#18105=CARTESIAN_POINT ( 'NONE',  ( -14.25243324638999809, -13.93375672974000068, -0.8660254037843999608 ) ) ;
#18108=CARTESIAN_POINT ( 'NONE',  ( 22.58815793041088682, -5.572103469424654065, 8.998486307808107654 ) ) ;
#18109=CARTESIAN_POINT ( 'NONE',  ( -14.00000000000000178, 7.473072963007769687, 5.353906094287523842 ) ) ;
#18110=CARTESIAN_POINT ( 'NONE',  ( 17.54864771944206936, -9.976641182250055806, 3.124397047610406819 ) ) ;
#18111=AXIS2_PLACEMENT_3D ( 'NONE', #10506, #5171, #14480 ) ;
#18113=CARTESIAN_POINT ( 'NONE',  ( -18.75303743917333321, -1.198189225339903352, 9.152521614020351137 ) ) ;
#18114=EDGE_CURVE ( 'NONE', #2392, #17545, #7576, .T. ) ;
#18116=CARTESIAN_POINT ( 'NONE',  ( -13.32041877100999905, -7.827390682981001824, 5.681961735881999154 ) ) ;
#18119=CARTESIAN_POINT ( 'NONE',  ( -24.24003052284658466, -3.589673254547931514, 12.49985157730626284 ) ) ;
#18120=CARTESIAN_POINT ( 'NONE',  ( 23.42416300332000034, 1.450584581381999971, -11.39090740897000131 ) ) ;
#18121=CARTESIAN_POINT ( 'NONE',  ( 22.42725290643797109, 6.724562262194361040, 8.161878525604194579 ) ) ;
#18123=ORIENTED_EDGE ( 'NONE', *, *, #5383, .F. ) ;
#18124=FACE_OUTER_BOUND ( 'NONE', #23475, .T. ) ;
#18125=DIRECTION ( 'NONE',  ( -1.000000000000000000, 0.000000000000000000, 0.000000000000000000 ) ) ;
#18127=CONICAL_SURFACE ( 'NONE', #17742, 9.161549281532000322, 0.02565634000431304615 ) ;
#18128=CARTESIAN_POINT ( 'NONE',  ( -4.558962899038999872, 12.31676645013000915, -1.631911765495000166 ) ) ;
#18130=CARTESIAN_POINT ( 'NONE',  ( 15.99918875730999979, 7.956028365285000348, 4.607548929765999723 ) ) ;
#18131=ORIENTED_EDGE ( 'NONE', *, *, #3187, .T. ) ;
#18135=CARTESIAN_POINT ( 'NONE',  ( -23.74465998031000069, -13.93375672974000068, -0.8660254037843999608 ) ) ;
#18138=CARTESIAN_POINT ( 'NONE',  ( -19.06933321534334169, -0.5773117834577096152, 9.204639638764268383 ) ) ;
#18139=AXIS2_PLACEMENT_3D ( 'NONE', #19315, #22928, #2725 ) ;
#18140=CARTESIAN_POINT ( 'NONE',  ( -21.54615255932999673, -7.601428298414999674, -6.679749176401998945 ) ) ;
#18143=FACE_OUTER_BOUND ( 'NONE', #17490, .T. ) ;
#18145=CARTESIAN_POINT ( 'NONE',  ( -22.38871519940780175, 8.023834466003746613, -7.050152665355915005 ) ) ;
#18148=CARTESIAN_POINT ( 'NONE',  ( -6.248053578788996809, 15.23699721607000868, 1.996732876636001963 ) ) ;
#18150=EDGE_LOOP ( 'NONE', ( #18330, #194, #14116, #7492, #18243 ) ) ;
#18151=CARTESIAN_POINT ( 'NONE',  ( -17.46222087121334710, 5.604205574924105093, 7.292568942664221510 ) ) ;
#18155=CARTESIAN_POINT ( 'NONE',  ( -24.47329604352722754, -7.448162605973902117, -7.555104833657267704 ) ) ;
#18159=CARTESIAN_POINT ( 'NONE',  ( 3.761864348328608720, 12.07395163634499546, 3.036815456826709614 ) ) ;
#18161=CARTESIAN_POINT ( 'NONE',  ( 17.80791666666665662, 2.389422108709928327, 8.890634990046439867 ) ) ;
#18162=CARTESIAN_POINT ( 'NONE',  ( 2.541275575112173613, 11.75631033188225771, -4.097795235817846660 ) ) ;
#18163=CARTESIAN_POINT ( 'NONE',  ( -10.04701370329000021, 16.31160201364000173, 0.9999999999983000265 ) ) ;
#18164=CIRCLE ( 'NONE', #22388, 10.59999999999999964 ) ;
#18165=CARTESIAN_POINT ( 'NONE',  ( -20.52334587121333698, -8.958601747919349378, 2.407426987275048891 ) ) ;
#18167=FACE_OUTER_BOUND ( 'NONE', #2304, .T. ) ;
#18169=CARTESIAN_POINT ( 'NONE',  ( 15.03843892131000004, -8.433581200277000534, 4.746982932527000543 ) ) ;
#18170=CARTESIAN_POINT ( 'NONE',  ( 18.70320243966950358, 8.881428319331240218, 5.464808494914835002 ) ) ;
#18171=UNCERTAINTY_MEASURE_WITH_UNIT (LENGTH_MEASURE( 1.000000000000000082E-05 ), #5688, 'distance_accuracy_value', 'NONE');
#18174=CARTESIAN_POINT ( 'NONE',  ( 18.91608580085999947, 1.014672566925000075, 11.40123757166999852 ) ) ;
#18175=CARTESIAN_POINT ( 'NONE',  ( -23.74465998031000069, -13.93375672974000068, 0.8660254037843999608 ) ) ;
#18176=AXIS2_PLACEMENT_3D ( 'NONE', #15966, #17690, #17931 ) ;
#18180=CARTESIAN_POINT ( 'NONE',  ( 20.04180759019999769, -2.870714866723000025, -10.33318544762000002 ) ) ;
#18182=PLANE ( 'NONE',  #12340 ) ;
#18190=ORIENTED_EDGE ( 'NONE', *, *, #2527, .T. ) ;
#18194=CARTESIAN_POINT ( 'NONE',  ( 11.53663804754732602, 3.465671449080339972, -12.49990775415077238 ) ) ;
#18195=CARTESIAN_POINT ( 'NONE',  ( 6.225415451459330285, 13.76263273567627721, -1.301510523365907668 ) ) ;
#18197=CARTESIAN_POINT ( 'NONE',  ( -6.045497365604999729, 16.31815993523999708, -1.000000000000000000 ) ) ;
#18198=EDGE_LOOP ( 'NONE', ( #12607, #7551, #2439 ) ) ;
#18199=DIRECTION ( 'NONE',  ( 0.000000000000000000, 1.000000000000000000, 0.000000000000000000 ) ) ;
#18202=CYLINDRICAL_SURFACE ( 'NONE', #20573, 6.125000000000000000 ) ;
#18203=ORIENTED_EDGE ( 'NONE', *, *, #5972, .F. ) ;
#18204=CARTESIAN_POINT ( 'NONE',  ( -10.32558623928693464, 15.68963668235006459, -1.216814257780576503 ) ) ;
#18206=CARTESIAN_POINT ( 'NONE',  ( 14.76281341799735536, 8.902647515865099948, -5.236912464659464916 ) ) ;
#18208=CARTESIAN_POINT ( 'NONE',  ( 23.02461096755999748, -6.906568182436000569, -8.911400877533001363 ) ) ;
#18210=CARTESIAN_POINT ( 'NONE',  ( 14.38895978305333223, -4.028520541369379870, 8.094092768459281828 ) ) ;
#18212=CARTESIAN_POINT ( 'NONE',  ( -21.77047087121331614, 1.208325219156647146, -9.229954902935974204 ) ) ;
#18216=CARTESIAN_POINT ( 'NONE',  ( 11.78924557931885886, -12.98180138940026396, -2.514846131778560867 ) ) ;
#18218=CARTESIAN_POINT ( 'NONE',  ( 16.85852266364000229, 0.2855060302065000055, 11.07656398360000161 ) ) ;
#18220=ORIENTED_EDGE ( 'NONE', *, *, #2718, .F. ) ;
#18221=CARTESIAN_POINT ( 'NONE',  ( -8.985362565845999683, 11.16660274832999988, -9.816446337639002095 ) ) ;
#18222=CARTESIAN_POINT ( 'NONE',  ( 13.49999999999999467, 7.950735579686481813, -4.793967810291187348 ) ) ;
#18223=CARTESIAN_POINT ( 'NONE',  ( -14.25546672378000146, -6.466739220293000301, 12.35574276786000070 ) ) ;
#18225=CARTESIAN_POINT ( 'NONE',  ( 20.55855148008149413, 2.013822818936180425, 10.33642651244847599 ) ) ;
#18226=CARTESIAN_POINT ( 'NONE',  ( 12.50448119322000018, -13.93375672974000068, 0.4328388268750000267 ) ) ;
#18227=CARTESIAN_POINT ( 'NONE',  ( 15.97809595731088450, -8.909303387638358274, -5.284970025649013969 ) ) ;
#18228=CARTESIAN_POINT ( 'NONE',  ( -5.345626673175369881, 14.28230134421816722, 5.048067894539765454 ) ) ;
#18230=FACE_OUTER_BOUND ( 'NONE', #9853, .T. ) ;
#18233=CARTESIAN_POINT ( 'NONE',  ( 20.46948943370828999, 9.758937805927079268, 3.938997005426223996 ) ) ;
#18235=ORIENTED_EDGE ( 'NONE', *, *, #9109, .F. ) ;
#18238=B_SPLINE_CURVE_WITH_KNOTS ( 'NONE', 3,
 ( #14556, #5362, #21949, #12751, #3550, #10934, #20143, #12972, #23875, #18320, #7281, #1726, #22069, #5592, #14675, #5477, #20257, #19365, #15831, #10274, #23219, #21417, #19485, #15132, #2187, #12217, #9580, #17542, #22974, #15946, #23092, #14026, #21542, #19607, #17795, #1191, #18778 ),
 .UNSPECIFIED., .F., .F.,
 ( 4, 2, 2, 2, 2, 2, 2, 2, 2, 2, 1, 1, 2, 2, 1, 2, 2, 2, 2, 4 ),
 ( 0.000000000000000000, 0.1115186113371554461, 0.1672779170057331344, 0.2230372226743108366, 0.2787965283428885943, 0.3345558340114662688, 0.3903151396800439987, 0.4460744453486216732, 0.4739540981829105659, 0.4878939246000549290, 0.4948638378086272493, 0.4983487944129132985, 0.4992200335639848108, 0.5000912727150563786, 0.5018337510171992921, 0.5575930566857747461, 0.6133523623543503112, 0.6691116680229257652, 0.7806302793600768952, 0.8921488906972279143 ),
 .UNSPECIFIED. ) ;
#18239=CARTESIAN_POINT ( 'NONE',  ( -1.429747209652000084, 11.58582448925999131, -4.584039058762003016 ) ) ;
#18242=CARTESIAN_POINT ( 'NONE',  ( 0.000000000000000000, 17.00000000000000000, 0.000000000000000000 ) ) ;
#18243=ORIENTED_EDGE ( 'NONE', *, *, #18731, .F. ) ;
#18244=B_SPLINE_CURVE_WITH_KNOTS ( 'NONE', 3,
 ( #6634, #937, #19733, #4830, #12099, #17663, #6515, #12216, #8461, #21416, #16067, #19364, #19606, #6754, #23091, #17541, #8583, #14025 ),
 .UNSPECIFIED., .F., .F.,
 ( 4, 2, 2, 2, 2, 2, 2, 2, 4 ),
 ( 0.000000000000000000, 0.1249999999999998612, 0.2499999999999997224, 0.3749999999999996114, 0.4999999999999996669, 0.6249999999999997780, 0.7499999999999997780, 0.8749999999999998890, 1.000000000000000000 ),
 .UNSPECIFIED. ) ;
#18245=CARTESIAN_POINT ( 'NONE',  ( -5.182227472513371680, 15.97908023997939075, 3.265408057167412448 ) ) ;
#18246=CARTESIAN_POINT ( 'NONE',  ( -14.45529023501843824, 2.584742736972815536, -12.49997119545760782 ) ) ;
#18248=CARTESIAN_POINT ( 'NONE',  ( -15.38367920454667370, -2.373138586668962713, 8.830043457142039642 ) ) ;
#18249=CARTESIAN_POINT ( 'NONE',  ( -21.06439250443000333, 7.381144841870000306, -6.903346092959000480 ) ) ;
#18250=EDGE_CURVE ( 'NONE', #10960, #1186, #19911, .T. ) ;
#18251=CARTESIAN_POINT ( 'NONE',  ( 12.40357033524515451, -7.855338663056838477, -11.39415432492425850 ) ) ;
#18252=CARTESIAN_POINT ( 'NONE',  ( -6.370829674278999377, 15.09915248894001749, -3.226228642116999001 ) ) ;
#18253=CARTESIAN_POINT ( 'NONE',  ( -22.69753670837523885, -2.324815390030910756, -10.30365430221285905 ) ) ;
#18259=DIRECTION ( 'NONE',  ( 0.000000000000000000, -1.000000000000000000, 0.000000000000000000 ) ) ;
#18260=CARTESIAN_POINT ( 'NONE',  ( 14.96234510379274418, -9.055474543150360489, 0.9759141728302277441 ) ) ;
#18261=B_SPLINE_CURVE_WITH_KNOTS ( 'NONE', 3,
 ( #1928, #5303, #18371, #17911, #21666, #8943, #18264, #9170, #3380, #16425, #12694, #23814, #1782, #6997, #8831, #14386 ),
 .UNSPECIFIED., .F., .F.,
 ( 4, 2, 2, 1, 1, 1, 1, 2, 2, 4 ),
 ( 0.000000000000000000, 0.2500000000000089373, 0.3750000000000134892, 0.4375000000000157097, 0.4687500000000168199, 0.4843750000000172640, 0.4921875000000175415, 0.4960937500000173750, 0.5000000000000172085, 1.000000000000000000 ),
 .UNSPECIFIED. ) ;
#18264=CARTESIAN_POINT ( 'NONE',  ( 5.895600255881173091, 14.43378529329739202, -1.663721376250851591 ) ) ;
#18269=CARTESIAN_POINT ( 'NONE',  ( -3.028157117397000331, 11.86875440406517157, -3.760788192032637589 ) ) ;
#18270=CARTESIAN_POINT ( 'NONE',  ( 24.22902234330208771, 5.299939913159104954, -8.069587291013673891 ) ) ;
#18275=CARTESIAN_POINT ( 'NONE',  ( -14.25394822846000054, 13.93375672974000068, -0.7219352443379000173 ) ) ;
#18276=CARTESIAN_POINT ( 'NONE',  ( 17.36831408530999710, -9.345903658884999743, -4.204539402675000481 ) ) ;
#18277=CARTESIAN_POINT ( 'NONE',  ( 18.58914845423001694, 10.30955476201900112, 1.554838316117926222 ) ) ;
#18278=ADVANCED_FACE ( 'NONE', ( #23733 ), #17190, .F. ) ;
#18281=CARTESIAN_POINT ( 'NONE',  ( -12.51334610648000023, 6.705591387245999790, -5.997258770121999483 ) ) ;
#18282=CARTESIAN_POINT ( 'NONE',  ( 13.50000000000000178, -7.857961930001017059, 6.282614375059098144 ) ) ;
#18284=EDGE_LOOP ( 'NONE', ( #1723, #19589, #2955, #9501 ) ) ;
#18286=CARTESIAN_POINT ( 'NONE',  ( 19.51066028373000094, -9.186672159909999635, 5.505812582796999699 ) ) ;
#18288=CARTESIAN_POINT ( 'NONE',  ( 13.77884874240669433, -10.28178801782097374, 1.171900820996238490 ) ) ;
#18290=CARTESIAN_POINT ( 'NONE',  ( -4.720810408942003988, 12.43069267676998635, 1.485243188514001833 ) ) ;
#18292=CARTESIAN_POINT ( 'NONE',  ( -12.25000000000000000, 9.358908280841877314, -11.49204783487746617 ) ) ;
#18297=ADVANCED_FACE ( 'NONE', ( #14415 ), #3173, .T. ) ;
#18299=CARTESIAN_POINT ( 'NONE',  ( 4.151454423752853451, 13.37950420772049043, 5.414973749174229134 ) ) ;
#18300=EDGE_CURVE ( 'NONE', #3092, #11881, #9900, .T. ) ;
#18301=CONICAL_SURFACE ( 'NONE', #2036, 14.15464499511999996, 0.6126053401530057174 ) ;
#18302=CARTESIAN_POINT ( 'NONE',  ( -5.916823184047997231, 16.44723308294000930, -1.645665246264000237 ) ) ;
#18304=FACE_OUTER_BOUND ( 'NONE', #10672, .T. ) ;
#18308=ADVANCED_FACE ( 'NONE', ( #1049 ), #9981, .F. ) ;
#18309=CARTESIAN_POINT ( 'NONE',  ( -10.78142806654279084, 15.38209275545921173, -1.630562623988462079 ) ) ;
#18310=EDGE_CURVE ( 'NONE', #8938, #21190, #14245, .T. ) ;
#18312=CARTESIAN_POINT ( 'NONE',  ( 14.55590497721902388, 3.259501315177474989, -9.794662651058661851 ) ) ;
#18313=CYLINDRICAL_SURFACE ( 'NONE', #7149, 10.65000000000000036 ) ;
#18314=CARTESIAN_POINT ( 'NONE',  ( 22.03302542056999869, 10.37153216069000017, -4.351098818476000218 ) ) ;
#18316=CARTESIAN_POINT ( 'NONE',  ( 13.64892411898719615, 7.821303059129255608, -4.509097355506050953 ) ) ;
#18317=CARTESIAN_POINT ( 'NONE',  ( -6.250000000000000000, 15.73203524433000311, -1.185075242810999852 ) ) ;
#18320=CARTESIAN_POINT ( 'NONE',  ( -14.75505759937285610, -5.861744336721237403, -6.919050695072026080 ) ) ;
#18325=CARTESIAN_POINT ( 'NONE',  ( 11.09594815121266898, -10.32758188524896958, -7.112100880958000637 ) ) ;
#18326=CARTESIAN_POINT ( 'NONE',  ( 21.53124770046332515, 7.376069553053762107, 5.668376081327591187 ) ) ;
#18328=CARTESIAN_POINT ( 'NONE',  ( 13.06905380888999879, 5.678881668803000160, 8.574739485425999064 ) ) ;
#18329=CARTESIAN_POINT ( 'NONE',  ( -16.14924287180106788, 2.273826895442076168, 10.14427581049354288 ) ) ;
#18330=ORIENTED_EDGE ( 'NONE', *, *, #8184, .T. ) ;
#18331=CARTESIAN_POINT ( 'NONE',  ( -11.01443863877000062, -7.881785293157000716, -13.01837374353999977 ) ) ;
#18333=CARTESIAN_POINT ( 'NONE',  ( -14.25547010304999951, -7.466739166992000243, 11.77839252945000048 ) ) ;
#18334=ORIENTED_EDGE ( 'NONE', *, *, #4623, .F. ) ;
#18335=CARTESIAN_POINT ( 'NONE',  ( 22.70581627535820246, -8.684860224558871522, 6.045228987698447298 ) ) ;
#18336=DIRECTION ( 'NONE',  ( -1.000000000000000000, 0.000000000000000000, 0.000000000000000000 ) ) ;
#18337=CARTESIAN_POINT ( 'NONE',  ( 15.97136033905609231, -9.035590316731877181, -5.065116864595969659 ) ) ;
#18338=CARTESIAN_POINT ( 'NONE',  ( -17.36285270628999911, -10.99392015758999896, 1.404702108876000111 ) ) ;
#18340=CARTESIAN_POINT ( 'NONE',  ( -17.78928642635000301, 9.027876325972000515, -3.804579355723999967 ) ) ;
#18344=CARTESIAN_POINT ( 'NONE',  ( 19.61828792382229381, -8.805202494819290848, -5.729946969217829533 ) ) ;
#18348=FACE_OUTER_BOUND ( 'NONE', #21488, .T. ) ;
#18349=CARTESIAN_POINT ( 'NONE',  ( -4.778817678460002938, 12.40039738087000387, -0.7843833587508003413 ) ) ;
#18350=ORIENTED_EDGE ( 'NONE', *, *, #13086, .F. ) ;
#18351=CARTESIAN_POINT ( 'NONE',  ( 11.61168875731000050, -4.628380041800000733, -7.810153319783999848 ) ) ;
#18352=CIRCLE ( 'NONE', #9069, 10.59999999999999964 ) ;
#18353=ORIENTED_EDGE ( 'NONE', *, *, #22865, .T. ) ;
#18354=CARTESIAN_POINT ( 'NONE',  ( -5.091933128512972750, 15.92787516682906634, 3.404252275490784463 ) ) ;
#18357=CARTESIAN_POINT ( 'NONE',  ( 8.124934037954998800, 14.44999999999999929, 0.000000000000000000 ) ) ;
#18358=AXIS2_PLACEMENT_3D ( 'NONE', #6683, #5013, #12398 ) ;
#18359=CARTESIAN_POINT ( 'NONE',  ( -19.94028570965000213, -9.569631055272999731, 0.0004266524341263999969 ) ) ;
#18360=CARTESIAN_POINT ( 'NONE',  ( 12.28779254565060519, -7.992768853820558128, -11.15614400032192144 ) ) ;
#18362=CARTESIAN_POINT ( 'NONE',  ( -22.85194746286182976, -7.255022703790015903, -7.682962849886891377 ) ) ;
#18369=CARTESIAN_POINT ( 'NONE',  ( 4.423436775227599149, 14.62387349557263505, 4.241731953385504461 ) ) ;
#18371=CARTESIAN_POINT ( 'NONE',  ( 6.095484411338158104, 14.38176773113363360, -0.6831047453619784049 ) ) ;
#18375=CARTESIAN_POINT ( 'NONE',  ( 2.018676308209844894, 11.65591130541151088, 4.375244769163982639 ) ) ;
#18376=VERTEX_POINT ( 'NONE', #895 ) ;
#18377=CARTESIAN_POINT ( 'NONE',  ( -4.237782011582903685, 12.22811978868115190, -2.340022628918474457 ) ) ;
#18378=EDGE_CURVE ( 'NONE', #5746, #19819, #13983, .T. ) ;
#18379=CARTESIAN_POINT ( 'NONE',  ( -10.73781098442203330, 15.39563139958459104, 1.589574342470376100 ) ) ;
#18381=ORIENTED_EDGE ( 'NONE', *, *, #4648, .F. ) ;
#18383=CARTESIAN_POINT ( 'NONE',  ( -5.194121241700999647, 12.44999999995000017, 4.899969256345999539E-10 ) ) ;
#18384=CARTESIAN_POINT ( 'NONE',  ( 17.69737658530999980, -0.08473977435852000917, -10.25642497589999991 ) ) ;
#18385=CARTESIAN_POINT ( 'NONE',  ( 18.46827294453634849, 10.07514253733398490, -2.674013015929876946 ) ) ;
#18388=CARTESIAN_POINT ( 'NONE',  ( -12.50958960166000189, 6.524993957290000424, -6.187564705242000862 ) ) ;
#18389=CARTESIAN_POINT ( 'NONE',  ( 13.50000000000000000, -9.107210294142168650, 3.887247416875642791 ) ) ;
#18390=AXIS2_PLACEMENT_3D ( 'NONE', #9898, #21038, #13403 ) ;
#18393=CARTESIAN_POINT ( 'NONE',  ( 24.19673057186000165, 6.858943761402000128, 9.064940718355000371 ) ) ;
#18395=CARTESIAN_POINT ( 'NONE',  ( -24.07222078679921040, 5.017431004176742704, 8.537427716843492220 ) ) ;
#18397=LINE ( 'NONE', #16804, #18410 ) ;
#18398=CARTESIAN_POINT ( 'NONE',  ( -4.796084242829001809, 12.39410533642999468, 1.092145777077000890 ) ) ;
#18401=CARTESIAN_POINT ( 'NONE',  ( -20.80699594585999890, -9.665068862928000826, -5.402836533902000582 ) ) ;
#18408=EDGE_CURVE ( 'NONE', #14395, #15392, #21462, .T. ) ;
#18409=CARTESIAN_POINT ( 'NONE',  ( 12.12543434883977866, 5.255139125105725562, -12.50003690308978221 ) ) ;
#18410=VECTOR ( 'NONE', #13177, 1000.000000000000000 ) ;
#18413=CARTESIAN_POINT ( 'NONE',  ( 14.51643908531000093, 10.16840836635999956, -0.3108424006793999994 ) ) ;
#18415=CYLINDRICAL_SURFACE ( 'NONE', #14313, 15.43375672974000068 ) ;
#18417=EDGE_CURVE ( 'NONE', #7412, #13026, #13964, .T. ) ;
#18418=DIRECTION ( 'NONE',  ( 0.000000000000000000, 1.000000000000000000, 0.000000000000000000 ) ) ;
#18420=CARTESIAN_POINT ( 'NONE',  ( -21.19117780174000032, -10.95007088059999845, 2.483471832359000153 ) ) ;
#18422=CARTESIAN_POINT ( 'NONE',  ( 14.48754660397587024, 0.8598977260950438906, -10.31086185088971341 ) ) ;
#18423=CARTESIAN_POINT ( 'NONE',  ( 25.72500000000000142, 0.000000000000000000, 0.000000000000000000 ) ) ;
#18424=CARTESIAN_POINT ( 'NONE',  ( 22.54674094339000234, 7.224650810196000528, 8.638435146791000108 ) ) ;
#18425=ADVANCED_FACE ( 'NONE', ( #4673 ), #15240, .F. ) ;
#18427=CARTESIAN_POINT ( 'NONE',  ( 14.07840962283755459, 5.123541359228647174, 7.439753567503393228 ) ) ;
#18428=EDGE_CURVE ( 'NONE', #2392, #7244, #5598, .T. ) ;
#18429=CARTESIAN_POINT ( 'NONE',  ( -2.125825771822000831, 11.86025111954001510, -4.338660460033000099 ) ) ;
#18430=LINE ( 'NONE', #3198, #10649 ) ;
#18433=CARTESIAN_POINT ( 'NONE',  ( 23.99062354302999722, 7.716878364870000340, -11.63397459621999985 ) ) ;
#18434=VERTEX_POINT ( 'NONE', #19189 ) ;
#18435=CARTESIAN_POINT ( 'NONE',  ( -16.03203743917331536, 1.189048994148058869, -9.082695391211098368 ) ) ;
#18437=EDGE_CURVE ( 'NONE', #5630, #17905, #22693, .T. ) ;
#18440=ADVANCED_FACE ( 'NONE', ( #2479 ), #15627, .F. ) ;
#18441=CARTESIAN_POINT ( 'NONE',  ( 15.74198797560999807, -10.51823260210000122, -3.385534472279999818 ) ) ;
#18444=ORIENTED_EDGE ( 'NONE', *, *, #6981, .T. ) ;
#18446=CARTESIAN_POINT ( 'NONE',  ( -11.11626113876999966, -12.56137170044999962, -8.591422195069000622 ) ) ;
#18448=CARTESIAN_POINT ( 'NONE',  ( -14.47125382252186299, -11.86037473473667170, -4.457180938895510813 ) ) ;
#18450=CARTESIAN_POINT ( 'NONE',  ( -3.783910185920449809, 14.59334639074173445, -4.817427536659290688 ) ) ;
#18451=CARTESIAN_POINT ( 'NONE',  ( 19.85260141040004811, 5.075921885626229368, -9.207587878805371773 ) ) ;
#18453=CARTESIAN_POINT ( 'NONE',  ( 16.01328496030753001, -8.173510217667363520, -6.363600821709828104 ) ) ;
#18454=CARTESIAN_POINT ( 'NONE',  ( -16.42549441298000445, 9.777619552165999650, 5.164216230235000538 ) ) ;
#18456=CONICAL_SURFACE ( 'NONE', #4542, 13.23032192316000000, 1.093540295016705466 ) ;
#18457=CARTESIAN_POINT ( 'NONE',  ( -17.99241677431999875, 4.425129475628999387, -8.746809379632999537 ) ) ;
#18461=CARTESIAN_POINT ( 'NONE',  ( 19.93039514411395885, 0.9077646897284779026, -10.46986812490325391 ) ) ;
#18462=CIRCLE ( 'NONE', #656, 0.09999999855979024854 ) ;
#18465=DIRECTION ( 'NONE',  ( 0.000000000000000000, 1.000000000000000000, 0.000000000000000000 ) ) ;
#18466=FACE_OUTER_BOUND ( 'NONE', #14365, .T. ) ;
#18467=EDGE_CURVE ( 'NONE', #8416, #1912, #12560, .T. ) ;
#18468=CARTESIAN_POINT ( 'NONE',  ( 1.417387361724000705, 11.51821284730998229, -4.666326094144003456 ) ) ;
#18469=CARTESIAN_POINT ( 'NONE',  ( 13.47637625730999922, -3.210294990792000203, -8.544406387913998202 ) ) ;
#18474=CARTESIAN_POINT ( 'NONE',  ( 12.50000000000000000, -13.93375672974000068, 0.000000000000000000 ) ) ;
#18475=B_SPLINE_SURFACE_WITH_KNOTS ( 'NONE', 3, 3, ( 
 ( #14645, #12603, #16807, #10908, #12722, #21919, #18521, #20116, #1693, #2046, #9082, #9436, #16454, #5451, #20228, #14872, #3632, #5221, #9319, #215, #7610, #7373, #16693, #18401, #1812, #22259, #14757, #5564, #12941, #20460, #11262, #21806, #3411, #5799, #18750 ),
 ( #9673, #19232, #9553, #21049, #20570, #10041, #6026, #13181, #17172, #13538, #17295, #696, #4223, #22618, #567, #16931, #19106, #819, #13413, #15345, #8103, #20813, #22735, #2160, #17053, #451, #15470, #22856, #2647, #7853, #6149, #334, #4463, #3984, #17425 ),
 ( #11617, #7737, #11378, #15104, #22498, #9907, #18987, #5907, #4340, #13293, #14988, #20692, #4100, #9787, #15220, #2397, #11852, #11731, #2517, #22384, #11497, #7973, #6270, #18874, #13653, #2280, #20934, #23339, #3016, #15702, #1062, #8464, #15832, #1315, #10528 ),
 ( #4958, #6517, #6876, #8337, #10157, #13774, #21174, #6755, #3259, #8703, #16068, #23220, #4831, #4588, #14148, #17543, #10402, #1192, #23094, #17912, #21543, #21301, #21418, #13902, #6635, #6390, #12460, #23464, #12342, #2771, #4714, #22975, #19734, #15947, #19366 ) ),
 .UNSPECIFIED., .F., .F., .F.,
 ( 4, 4 ),
 ( 4, 1, 1, 1, 1, 1, 1, 1, 1, 1, 1, 1, 1, 1, 1, 1, 1, 1, 1, 1, 1, 1, 1, 1, 1, 1, 1, 1, 1, 1, 1, 1, 4 ),
 ( -0.6000240009599999702, 1.600024000959999970 ),
 ( 0.1610006166028000174, 0.1877334400934000114, 0.2144662635840000053, 0.2411990870745999993, 0.2679319105651999933, 0.2946647340557999595, 0.3213975575463999812, 0.3481303810370000029, 0.3748632045276000246, 0.4015960280181999908, 0.4283288515088000126, 0.4550616749994000343, 0.4817944984900000005, 0.5085273219806000222, 0.5352601454711999329, 0.5619929689617000346, 0.5887257924522999453, 0.6154586159428999670, 0.6421914394334999887, 0.6689242629241000104, 0.6956570864147000322, 0.7223899099052999428, 0.7491227333958999646, 0.7758555568864999863, 0.8025883803771000080, 0.8293212038677000297, 0.8560540273582999404, 0.8827868508488999622, 0.9095196743394999839, 0.9362524978301000056, 0.9629853213207000273, 0.9897181448113000490, 1.016450968301999991 ),
 .UNSPECIFIED. ) ;
#18476=ORIENTED_EDGE ( 'NONE', *, *, #18428, .T. ) ;
#18478=CARTESIAN_POINT ( 'NONE',  ( -22.61826676953999993, 4.526472954474000332, 8.498838343196000622 ) ) ;
#18479=CARTESIAN_POINT ( 'NONE',  ( 11.92450592358771999, -8.469720391588866804, -10.33010329016888029 ) ) ;
#18481=CARTESIAN_POINT ( 'NONE',  ( -18.13088126894000141, 9.136555860487012737, 0.000000000000000000 ) ) ;
#18483=CARTESIAN_POINT ( 'NONE',  ( 15.69158333333333211, 8.837836392473214175, 2.374972199734133760 ) ) ;
#18484=CARTESIAN_POINT ( 'NONE',  ( -6.058164523583997152, 16.51672836841997949, 0.9500184723446998269 ) ) ;
#18485=CARTESIAN_POINT ( 'NONE',  ( 12.00000000000000000, 7.500000000000000000, 0.000000000000000000 ) ) ;
#18487=CARTESIAN_POINT ( 'NONE',  ( -17.73266243917333185, 4.596313708240831630, -7.974420273544428284 ) ) ;
#18488=CARTESIAN_POINT ( 'NONE',  ( 3.446647972078433764, 14.26578946693170558, 5.064530567705452846 ) ) ;
#18489=CARTESIAN_POINT ( 'NONE',  ( 14.37123251481000530, 5.018772503670207108, 7.581327530252383262 ) ) ;
#18491=CARTESIAN_POINT ( 'NONE',  ( -21.66177666636737342, 4.758819052736769528, 9.550088228515980049 ) ) ;
#18493=CARTESIAN_POINT ( 'NONE',  ( 1.871649831644675466, 11.63140178027804161, 4.440172657072205098 ) ) ;
#18495=CONICAL_SURFACE ( 'NONE', #6102, 13.23032192316000000, 1.235249617460683957 ) ;
#18496=CARTESIAN_POINT ( 'NONE',  ( -0.4068995525957177506, 11.48930230209881387, -4.795673420918372898 ) ) ;
#18497=CARTESIAN_POINT ( 'NONE',  ( 23.99478584078000054, -6.383504859148000143, -12.40379814867000086 ) ) ;
#18502=CARTESIAN_POINT ( 'NONE',  ( -16.52332910583999848, -9.095302903661998783, 0.000000000000000000 ) ) ;
#18504=CARTESIAN_POINT ( 'NONE',  ( 12.65175158531000044, 9.909822556590000886, -2.072115565883000166 ) ) ;
#18505=CARTESIAN_POINT ( 'NONE',  ( 18.29206332576804073, 6.690873865058084569, -7.988726941084996369 ) ) ;
#18508=DIRECTION ( 'NONE',  ( 0.000000000000000000, -1.000000000000000000, 0.000000000000000000 ) ) ;
#18510=ORIENTED_EDGE ( 'NONE', *, *, #7923, .T. ) ;
#18511=CARTESIAN_POINT ( 'NONE',  ( -24.17970357211641286, 12.87935348060952379, 2.692294542479934716 ) ) ;
#18512=CARTESIAN_POINT ( 'NONE',  ( 21.89509224385000152, 8.147067418188999710, -7.836651225645998586 ) ) ;
#18513=EDGE_CURVE ( 'NONE', #22006, #1172, #2104, .T. ) ;
#18514=CARTESIAN_POINT ( 'NONE',  ( -24.36228659953834352, 8.887038971774549267, -5.014620418582080852 ) ) ;
#18515=EDGE_LOOP ( 'NONE', ( #4321, #11188, #16497, #16266, #10077 ) ) ;
#18516=CARTESIAN_POINT ( 'NONE',  ( 13.52795396126032479, -5.741355442642295692, 8.603735498112436986 ) ) ;
#18519=CARTESIAN_POINT ( 'NONE',  ( -4.727635250208997775, 12.45903567298001668, 0.7257861805102000519 ) ) ;
#18521=CARTESIAN_POINT ( 'NONE',  ( -23.64743322413000115, 11.09837689733000055, 1.069113796759999957 ) ) ;
#18523=DIRECTION ( 'NONE',  ( 0.000000000000000000, 1.000000000000000000, -6.254606381427991854E-11 ) ) ;
#18527=CARTESIAN_POINT ( 'NONE',  ( 5.504749613137996711, 13.91273307856000940, 3.018176302422998614 ) ) ;
#18529=CARTESIAN_POINT ( 'NONE',  ( -16.97092920454666753, -7.957437029153473951, 4.586234609216395697 ) ) ;
#18531=CARTESIAN_POINT ( 'NONE',  ( 15.72300158530999958, -5.453124986814999353, -8.625711720232999369 ) ) ;
#18533=EDGE_CURVE ( 'NONE', #12632, #11620, #9331, .T. ) ;
#18535=ORIENTED_EDGE ( 'NONE', *, *, #19795, .F. ) ;
#18540=ORIENTED_EDGE ( 'NONE', *, *, #8687, .F. ) ;
#18541=CARTESIAN_POINT ( 'NONE',  ( -19.64887718127000227, -4.424839147307999987, 10.27402513662999972 ) ) ;
#18543=CARTESIAN_POINT ( 'NONE',  ( 14.39581696055360815, -2.328303387492436372, -10.05895166234070714 ) ) ;
#18545=CARTESIAN_POINT ( 'NONE',  ( -18.36922087121333647, -5.618509400322853509, -7.311181514368041867 ) ) ;
#18546=CARTESIAN_POINT ( 'NONE',  ( 22.17964701745000156, 10.37524365059999809, -4.352655460828000145 ) ) ;
#18549=CARTESIAN_POINT ( 'NONE',  ( 13.70789982098004423, 8.571058519759501948, -2.817337828859955096 ) ) ;
#18550=CARTESIAN_POINT ( 'NONE',  ( -6.500384775316716990, 15.46782671400865539, -1.463283840608048614 ) ) ;
#18552=AXIS2_PLACEMENT_3D ( 'NONE', #16970, #11174, #4016 ) ;
#18553=CARTESIAN_POINT ( 'NONE',  ( 18.85055757573999813, 0.1142443464370000022, 10.79806225559999966 ) ) ;
#18556=TOROIDAL_SURFACE ( 'NONE', #5024, 10.69999999999999929, 0.8000000000000000444 ) ;
#18561=FACE_OUTER_BOUND ( 'NONE', #3396, .T. ) ;
#18562=CARTESIAN_POINT ( 'NONE',  ( 22.09812270046333182, -8.072307342008256725, 4.652732286360434344 ) ) ;
#18563=CARTESIAN_POINT ( 'NONE',  ( 13.57657720147000013, -6.781973559127000506, 8.648568256107001417 ) ) ;
#18565=EDGE_CURVE ( 'NONE', #6719, #11336, #10238, .T. ) ;
#18567=ORIENTED_EDGE ( 'NONE', *, *, #11923, .T. ) ;
#18569=CARTESIAN_POINT ( 'NONE',  ( -10.40350363876999928, 13.74367368368000086, 6.535443979581000207 ) ) ;
#18571=CARTESIAN_POINT ( 'NONE',  ( -14.49284522991462509, -10.30702784337245248, -7.147655011466097719 ) ) ;
#18573=CARTESIAN_POINT ( 'NONE',  ( -14.49999963946489423, 11.08494587601020065, 5.800314632267468795 ) ) ;
#18574=FACE_BOUND ( 'NONE', #7868, .T. ) ;
#18575=CARTESIAN_POINT ( 'NONE',  ( 6.242982157972016388, 13.64690610122263514, 1.860940423144956446 ) ) ;
#18576=CARTESIAN_POINT ( 'NONE',  ( 16.01456160276670104, -8.144906968459116214, -6.400242916633066770 ) ) ;
#18577=CARTESIAN_POINT ( 'NONE',  ( -18.55941247522000381, 11.04350775505000115, -1.268070264779000089 ) ) ;
#18579=EDGE_CURVE ( 'NONE', #8876, #2459, #2372, .T. ) ;
#18580=B_SPLINE_CURVE_WITH_KNOTS ( 'NONE', 3,
 ( #22980, #19111, #4467, #4230, #15351, #6157, #4105, #6394, #7858, #13542, #20697, #2523, #944, #6030, #19369, #2286, #8341, #9912 ),
 .UNSPECIFIED., .F., .F.,
 ( 4, 2, 2, 2, 2, 2, 2, 2, 4 ),
 ( 0.000000000000000000, 0.1250000000000000555, 0.2500000000000000555, 0.3750000000000000000, 0.4999999999999999445, 0.6249999999999998890, 0.7500000000000000000, 0.8750000000000000000, 1.000000000000000000 ),
 .UNSPECIFIED. ) ;
#18581=CARTESIAN_POINT ( 'NONE',  ( -19.08958467661999947, -10.87501988123999830, 0.7812661330421999395 ) ) ;
#18585=CARTESIAN_POINT ( 'NONE',  ( 21.71791831486828173, -0.02456864104712422336, -10.71023399046199209 ) ) ;
#18586=DIRECTION ( 'NONE',  ( -0.1671082301074949539, 0.9859385576344705804, 0.000000000000000000 ) ) ;
#18589=CARTESIAN_POINT ( 'NONE',  ( -4.823557208340003122, 13.17411124896998764, 5.974450474228996555 ) ) ;
#18590=LINE ( 'NONE', #5862, #13022 ) ;
#18591=ADVANCED_FACE ( 'NONE', ( #20161 ), #5043, .F. ) ;
#18592=CARTESIAN_POINT ( 'NONE',  ( 18.43875142131000189, -2.600393254974000090, 9.414598814742999977 ) ) ;
#18593=ADVANCED_FACE ( 'NONE', ( #8660 ), #19058, .F. ) ;
#18596=CARTESIAN_POINT ( 'NONE',  ( -14.47826287373678156, 1.813202974803316048, -12.50000251924343608 ) ) ;
#18597=EDGE_LOOP ( 'NONE', ( #2835, #1592, #13592, #19542 ) ) ;
#18598=CARTESIAN_POINT ( 'NONE',  ( -15.64822087121333460, 5.575597924126876492, 7.255343799257086168 ) ) ;
#18599=CARTESIAN_POINT ( 'NONE',  ( -2.587409587117002641, 11.93419056235999953, 3.993438532374998573 ) ) ;
#18601=DIRECTION ( 'NONE',  ( 1.000000000000000000, 0.000000000000000000, 0.000000000000000000 ) ) ;
#18604=CARTESIAN_POINT ( 'NONE',  ( -20.76740227730209654, 1.886003063178867123, -10.34259919642779657 ) ) ;
#18605=DIRECTION ( 'NONE',  ( 0.7071067811865474617, -0.7071067811865474617, 0.000000000000000000 ) ) ;
#18607=CARTESIAN_POINT ( 'NONE',  ( -5.966878999860996124, 15.10316773259998868, 2.678439550780997713 ) ) ;
#18609=ORIENTED_EDGE ( 'NONE', *, *, #10158, .T. ) ;
#18610=CARTESIAN_POINT ( 'NONE',  ( -17.43032910583999850, 9.118578311265999048, 0.000000000000000000 ) ) ;
#18611=CARTESIAN_POINT ( 'NONE',  ( 22.30022314420000029, -9.218578328389000376, -3.456323596348999772 ) ) ;
#18612=CARTESIAN_POINT ( 'NONE',  ( 14.18456538144702961, 8.569177250714071548, 3.026341649409048706 ) ) ;
#18613=CARTESIAN_POINT ( 'NONE',  ( -23.67000479291073489, 9.608364060292810649, 4.444627409576130006 ) ) ;
#18616=CARTESIAN_POINT ( 'NONE',  ( 2.176439727641916289, 11.68391463016446963, 4.299875751357343567 ) ) ;
#18618=CARTESIAN_POINT ( 'NONE',  ( -3.421692785168691575, 11.97394591298616007, -3.409861883590250109 ) ) ;
#18620=DIRECTION ( 'NONE',  ( -1.000000000000000000, 0.000000000000000000, 0.000000000000000000 ) ) ;
#18623=CARTESIAN_POINT ( 'NONE',  ( 11.63812642131000175, -9.225545160481999574, -2.612645831888999570 ) ) ;
#18624=CARTESIAN_POINT ( 'NONE',  ( 18.39061514238058237, 8.952924735988446514, -5.333109133230360399 ) ) ;
#18627=CARTESIAN_POINT ( 'NONE',  ( 16.27546080085999947, 2.142700662188999683, -11.17012464664999882 ) ) ;
#18628=CARTESIAN_POINT ( 'NONE',  ( 13.50000000000000000, -4.002954420673999536, -8.080569262580000967 ) ) ;
#18629=ORIENTED_EDGE ( 'NONE', *, *, #2886, .F. ) ;
#18631=CARTESIAN_POINT ( 'NONE',  ( 20.83279763092000181, -2.973987989840999990, 10.87602257598999955 ) ) ;
#18632=VECTOR ( 'NONE', #14372, 1000.000000000000000 ) ;
#18634=VERTEX_POINT ( 'NONE', #23388 ) ;
#18638=CARTESIAN_POINT ( 'NONE',  ( 4.911758408288000588, 12.43820144620001145, -0.1548390653590999422 ) ) ;
#18647=DIRECTION ( 'NONE',  ( 1.000000000000000000, 0.000000000000000000, 0.000000000000000000 ) ) ;
#18648=DIRECTION ( 'NONE',  ( 0.000000000000000000, 1.000000000000000000, 0.000000000000000000 ) ) ;
#18650=CARTESIAN_POINT ( 'NONE',  ( 13.77506424931000240, -10.16002631551000057, 3.235559929811000046 ) ) ;
#18651=CARTESIAN_POINT ( 'NONE',  ( -18.84569624743000205, -10.33415972889999956, 0.7423446255362999846 ) ) ;
#18654=CARTESIAN_POINT ( 'NONE',  ( -14.45561360439974585, 2.584657965300122928, 12.49996445837907544 ) ) ;
#18655=EDGE_LOOP ( 'NONE', ( #4808, #18235, #3694, #15164 ) ) ;
#18656=CARTESIAN_POINT ( 'NONE',  ( -20.16297738808999895, 10.98403905672000036, 2.189746316398999859 ) ) ;
#18658=CARTESIAN_POINT ( 'NONE',  ( 13.93008789665596225, -9.927308807215476705, 2.819245968838537397 ) ) ;
#18659=CYLINDRICAL_SURFACE ( 'NONE', #13329, 6.125000000000000000 ) ;
#18660=CARTESIAN_POINT ( 'NONE',  ( 23.13430719836999927, -10.85154302445999974, -3.070125849493000381 ) ) ;
#18662=CARTESIAN_POINT ( 'NONE',  ( 13.77521226315460723, 8.994996949847150702, -0.8114643769208054191 ) ) ;
#18663=CARTESIAN_POINT ( 'NONE',  ( -6.383654667732219679, 15.56864394822520659, -1.329852007301480565 ) ) ;
#18665=ADVANCED_FACE ( 'NONE', ( #10691 ), #16026, .T. ) ;
#18666=CARTESIAN_POINT ( 'NONE',  ( 24.00391580400000180, 9.718215813663000802, 6.146681693640999811 ) ) ;
#18668=AXIS2_PLACEMENT_3D ( 'NONE', #4760, #2940, #4346 ) ;
#18669=CARTESIAN_POINT ( 'NONE',  ( 11.92450592357671901, -13.18099206878370921, 2.169941377000833338 ) ) ;
#18673=CARTESIAN_POINT ( 'NONE',  ( -19.10482910584000038, 9.161549281532014533, 0.000000000000000000 ) ) ;
#18675=CARTESIAN_POINT ( 'NONE',  ( 17.33221675526000283, -6.256935606695999574, 9.160251492536000129 ) ) ;
#18676=CARTESIAN_POINT ( 'NONE',  ( -24.50000000000000000, -7.216878364870000340, 12.50000000000000000 ) ) ;
#18678=EDGE_CURVE ( 'NONE', #9388, #8104, #19529, .T. ) ;
#18680=ORIENTED_EDGE ( 'NONE', *, *, #10699, .F. ) ;
#18684=ORIENTED_EDGE ( 'NONE', *, *, #18884, .F. ) ;
#18685=CARTESIAN_POINT ( 'NONE',  ( 19.88366666666665949, -5.551639645582684857, 7.389795051981888463 ) ) ;
#18686=CARTESIAN_POINT ( 'NONE',  ( 20.47308103379664956, -9.196661322686781048, -1.203713204382315327 ) ) ;
#18688=CARTESIAN_POINT ( 'NONE',  ( 15.93519615271878465, -9.616653625581596643, -3.849179279724161962 ) ) ;
#18689=CARTESIAN_POINT ( 'NONE',  ( -19.31610745349000169, -11.07881103579000026, 1.129852276557000046 ) ) ;
#18691=CARTESIAN_POINT ( 'NONE',  ( -12.79254388956000099, 9.568035197138000214, -2.460455418527999871 ) ) ;
#18695=CARTESIAN_POINT ( 'NONE',  ( -24.50000000000001066, -7.686026772365445403, -7.276726432132435640 ) ) ;
#18696=CARTESIAN_POINT ( 'NONE',  ( -18.54343818302843516, 10.45866049467905512, 0.2745342069438318489 ) ) ;
#18697=ORIENTED_EDGE ( 'NONE', *, *, #7068, .F. ) ;
#18698=CARTESIAN_POINT ( 'NONE',  ( 24.34804274388863377, -3.330488627411554159, 12.49999999999999467 ) ) ;
#18700=CARTESIAN_POINT ( 'NONE',  ( 18.51344355829000321, -6.966878364870000340, -12.06698729810999993 ) ) ;
#18702=CARTESIAN_POINT ( 'NONE',  ( 15.12168875731000028, -7.425874990359000449, -5.381511109182000041 ) ) ;
#18704=CARTESIAN_POINT ( 'NONE',  ( -5.067526505253444391, 15.91328937823097789, 3.440358843088985097 ) ) ;
#18708=CARTESIAN_POINT ( 'NONE',  ( -14.25243324638999809, 7.716878364870000340, -11.63397459621999985 ) ) ;
#18709=CARTESIAN_POINT ( 'NONE',  ( -4.247598233711002536, 12.43461358834999153, 2.282855730625001467 ) ) ;
#18710=CARTESIAN_POINT ( 'NONE',  ( 11.99999999999999467, -3.013426419913816101, -9.057261035705595376 ) ) ;
#18711=CARTESIAN_POINT ( 'NONE',  ( -14.29262089642102218, 7.983102671798921079, -11.17286057040529990 ) ) ;
#18712=CARTESIAN_POINT ( 'NONE',  ( -4.357829670976999026, 15.67924589997999085, -4.374970551269004027 ) ) ;
#18713=CARTESIAN_POINT ( 'NONE',  ( -23.74228231688656976, 8.693394395448456762E-05, -9.522797051439189531 ) ) ;
#18720=CARTESIAN_POINT ( 'NONE',  ( 24.41412816595000024, -8.463997690975000765, -5.186418078094000350 ) ) ;
#18723=CARTESIAN_POINT ( 'NONE',  ( -22.51862066702934939, -3.086810711953226427, -10.23562687710141894 ) ) ;
#18726=CARTESIAN_POINT ( 'NONE',  ( 12.52688711657000020, -6.216878364870000340, 12.50000000000000000 ) ) ;
#18727=VERTEX_POINT ( 'NONE', #4883 ) ;
#18728=CARTESIAN_POINT ( 'NONE',  ( -3.409519937314366977, 11.97052822634232605, -3.421840553652563788 ) ) ;
#18729=EDGE_CURVE ( 'NONE', #12346, #1991, #21843, .T. ) ;
#18731=EDGE_CURVE ( 'NONE', #259, #44, #940, .T. ) ;
#18733=DIRECTION ( 'NONE',  ( -1.000000000000000000, 0.000000000000000000, 0.000000000000000000 ) ) ;
#18735=DIRECTION ( 'NONE',  ( 0.000000000000000000, 1.000000000000000000, 0.000000000000000000 ) ) ;
#18736=CARTESIAN_POINT ( 'NONE',  ( 18.02643908530999894, 9.290813243320000581, -4.365746228316999655 ) ) ;
#18737=DIRECTION ( 'NONE',  ( 0.000000000000000000, -0.5000000000000169864, 0.8660254037844288266 ) ) ;
#18738=CARTESIAN_POINT ( 'NONE',  ( 22.87199999999999989, 9.258222311379999070, 0.000000000000000000 ) ) ;
#18739=CARTESIAN_POINT ( 'NONE',  ( 16.88483580085999947, 8.492437095885001952, 7.591307468212999510 ) ) ;
#18740=CARTESIAN_POINT ( 'NONE',  ( 21.34228936713000024, 9.218966921638999779, 0.000000000000000000 ) ) ;
#18742=CARTESIAN_POINT ( 'NONE',  ( 19.15656207941999867, 1.952743198197999908, 9.858894681773000102 ) ) ;
#18743=CARTESIAN_POINT ( 'NONE',  ( 16.52299999999999969, -9.095294458157999529, 0.000000000000000000 ) ) ;
#18745=CARTESIAN_POINT ( 'NONE',  ( 12.00945122375999929, 1.736409555422999906, -9.163372685490999814 ) ) ;
#18748=CARTESIAN_POINT ( 'NONE',  ( 4.518219764248003756, 12.29191853473001217, 1.948622234166999201 ) ) ;
#18750=CARTESIAN_POINT ( 'NONE',  ( -19.13615048806000019, -10.42776677607999858, -0.1439720813952999889 ) ) ;
#18751=ORIENTED_EDGE ( 'NONE', *, *, #1103, .F. ) ;
#18755=CARTESIAN_POINT ( 'NONE',  ( 4.720426297672999816, 14.52234792950999243, 3.835364363128998644 ) ) ;
#18757=DIRECTION ( 'NONE',  ( 0.000000000000000000, 0.8660254037844288266, -0.5000000000000169864 ) ) ;
#18759=CARTESIAN_POINT ( 'NONE',  ( 12.45881424931000048, -1.641155845125999768, -10.50071198764000080 ) ) ;
#18760=CARTESIAN_POINT ( 'NONE',  ( -13.60506528143999994, -10.72046298714999857, -0.8128029906560000351 ) ) ;
#18761=CIRCLE ( 'NONE', #17623, 0.5000000000000004441 ) ;
#18762=DIRECTION ( 'NONE',  ( 0.000000000000000000, 1.000000000000000000, 0.000000000000000000 ) ) ;
#18763=CARTESIAN_POINT ( 'NONE',  ( -14.43045987140110498, 3.231330187236305385, 12.49999333232803700 ) ) ;
#18767=CARTESIAN_POINT ( 'NONE',  ( 13.84793461847943696, -8.727815944628217082, 5.476926543191370733 ) ) ;
#18768=CARTESIAN_POINT ( 'NONE',  ( -17.76455420454666978, 9.127155186021923328, -1.194614872368742198 ) ) ;
#18769=CARTESIAN_POINT ( 'NONE',  ( 18.76610545325000245, 2.168194506458000159, 10.20310581668000083 ) ) ;
#18771=CARTESIAN_POINT ( 'NONE',  ( 14.39816148159241749, -4.288529584651731064, 7.959032380803818363 ) ) ;
#18772=CARTESIAN_POINT ( 'NONE',  ( 18.82462156322305447, -0.8953968736580824039, 10.44005362496722178 ) ) ;
#18774=DIRECTION ( 'NONE',  ( 0.000000000000000000, -1.000000000000000000, 0.000000000000000000 ) ) ;
#18775=CONICAL_SURFACE ( 'NONE', #23027, 9.157130689899000586, 0.02565634000431304615 ) ;
#18776=CARTESIAN_POINT ( 'NONE',  ( 24.28255857085423841, -12.88093503250115290, -2.689566074712900434 ) ) ;
#18778=CARTESIAN_POINT ( 'NONE',  ( -14.09989322724901051, 9.032303263851988007, 3.309274488355915889E-05 ) ) ;
#18781=B_SPLINE_CURVE_WITH_KNOTS ( 'NONE', 3,
 ( #2480, #18711, #9869, #17254, #2122, #6231, #22339, #13612, #9392, #3946, #11341, #293, #7695, #15069, #12059, #19689, #779, #17503, #4913, #8179, #23053, #19190, #23184, #19569, #23299, #6714, #10235, #4674, #6600, #22935, #13860, #6352 ),
 .UNSPECIFIED., .F., .F.,
 ( 4, 2, 2, 2, 2, 2, 2, 2, 2, 2, 2, 2, 2, 2, 2, 4 ),
 ( 0.000000000000000000, 0.1249999999999996114, 0.1874999999999994171, 0.2187499999999992784, 0.2499999999999991118, 0.3124999999999990008, 0.3437499999999991118, 0.3749999999999992228, 0.4999999999999991118, 0.5624999999999991118, 0.5937499999999991118, 0.6249999999999991118, 0.6874999999999992228, 0.7187499999999992228, 0.7499999999999991118, 1.000000000000000000 ),
 .UNSPECIFIED. ) ;
#18782=EDGE_LOOP ( 'NONE', ( #11359, #23682, #7767, #8766 ) ) ;
#18785=CARTESIAN_POINT ( 'NONE',  ( -23.75392841908999841, -7.466663059413999548, -11.77843647018000084 ) ) ;
#18787=CARTESIAN_POINT ( 'NONE',  ( 16.97131495957000169, 6.714547727491000373, 8.817885161969000407 ) ) ;
#18788=FACE_OUTER_BOUND ( 'NONE', #1000, .T. ) ;
#18790=ORIENTED_EDGE ( 'NONE', *, *, #1343, .F. ) ;
#18792=CARTESIAN_POINT ( 'NONE',  ( -13.99999999999999467, 2.521425489992599189, -9.027018840861916971 ) ) ;
#18795=CARTESIAN_POINT ( 'NONE',  ( -14.44600786774907597, -9.403896164503946054, -8.711943152828570902 ) ) ;
#18796=ADVANCED_FACE ( 'NONE', ( #14075 ), #19782, .T. ) ;
#18798=CARTESIAN_POINT ( 'NONE',  ( 19.91708333333331993, -6.375401374836546786, 6.693310963685535242 ) ) ;
#18799=CARTESIAN_POINT ( 'NONE',  ( 19.76435765169019021, 2.069040484427104420, -10.29933159267119791 ) ) ;
#18801=CARTESIAN_POINT ( 'NONE',  ( 6.226186241163151003, 13.75890038697268025, 1.316088922015740570 ) ) ;
#18802=CARTESIAN_POINT ( 'NONE',  ( 15.68554067004900787, -9.183687389534485490, 4.778903167209843872 ) ) ;
#18803=B_SPLINE_CURVE_WITH_KNOTS ( 'NONE', 3,
 ( #23594, #18155, #5192, #16546, #12573, #23938, #7345, #14729, #4957, #5884, #11106, #5646, #11352, #11235, #2133, #22231, #14839, #13031, #3959, #7710, #18613, #16666, #13384, #425, #7577, #2018, #9407, #22353, #13270, #20430, #4191, #5771, #16776, #3839, #185, #20664, #20311, #14956, #18963, #13156, #2370, #9522, #72, #7947, #4074, #11468, #9292, #7825, #18723, #7457, #18844, #9759, #16899, #15196, #20784, #12913, #3716, #304, #18491, #2249, #15078, #9644, #17027, #22592, #17146, #1903, #542, #22474, #22124, #5998, #5533, #15441, #2615, #10006, #8436, #17268, #22707, #13874, #12190, #19077, #13744, #666, #19336, #21277, #19578, #21145, #6491, #10125, #8310, #13995, #17396, #11823, #790, #8190, #4558, #6241, #8072, #6117, #2863, #20908, #10373, #15558, #11950, #22827, #4313, #13624, #15674, #22946, #10247, #6362, #17763 ),
 .UNSPECIFIED., .F., .F.,
 ( 4, 2, 2, 2, 2, 2, 1, 2, 2, 2, 2, 2, 2, 2, 2, 2, 2, 2, 2, 2, 2, 2, 2, 2, 2, 2, 2, 2, 1, 2, 2, 2, 2, 2, 2, 2, 2, 2, 2, 2, 2, 2, 2, 2, 2, 2, 2, 2, 2, 2, 1, 2, 2, 2, 2, 2, 4 ),
 ( 0.000000000000000000, 0.01562500000000002776, 0.03125000000000005551, 0.04687500000000008327, 0.06250000000000011102, 0.07812500000000013878, 0.09375000000000016653, 0.1093750000000001943, 0.1250000000000002220, 0.1406250000000002498, 0.1562500000000002776, 0.1718750000000003053, 0.1875000000000003331, 0.2031250000000003608, 0.2187500000000003886, 0.2343750000000004163, 0.2500000000000003886, 0.2656250000000003886, 0.2812500000000004441, 0.2968750000000004441, 0.3125000000000004996, 0.3281250000000004996, 0.3437500000000005551, 0.3593750000000005551, 0.3750000000000006106, 0.4062500000000006106, 0.4375000000000006661, 0.4687500000000006661, 0.5000000000000006661, 0.5312500000000006661, 0.5625000000000007772, 0.5937500000000007772, 0.6250000000000008882, 0.6406250000000008882, 0.6562500000000008882, 0.6718750000000009992, 0.6875000000000009992, 0.7031250000000009992, 0.7187500000000009992, 0.7343750000000011102, 0.7500000000000011102, 0.7656250000000009992, 0.7812500000000008882, 0.7968750000000008882, 0.8125000000000007772, 0.8281250000000006661, 0.8437500000000005551, 0.8593750000000005551, 0.8750000000000004441, 0.8906250000000003331, 0.9062500000000002220, 0.9218750000000002220, 0.9375000000000001110, 0.9531250000000000000, 0.9687499999999998890, 0.9843750000000000000, 1.000000000000000000 ),
 .UNSPECIFIED. ) ;
#18804=CARTESIAN_POINT ( 'NONE',  ( -14.61886126265999941, 9.861861598182999344, 4.891081622639000592 ) ) ;
#18806=CARTESIAN_POINT ( 'NONE',  ( -14.17369824411999879, 9.412195986946999327, 4.011894131497999005 ) ) ;
#18807=ADVANCED_FACE ( 'NONE', ( #23520 ), #13731, .F. ) ;
#18809=ORIENTED_EDGE ( 'NONE', *, *, #17869, .T. ) ;
#18812=CARTESIAN_POINT ( 'NONE',  ( 19.24943393620590371, -8.016451796436484756, 6.770655802219995856 ) ) ;
#18813=CARTESIAN_POINT ( 'NONE',  ( -19.23797835538982426, -7.594763024543788710, -7.229160888945107999 ) ) ;
#18815=CARTESIAN_POINT ( 'NONE',  ( 23.99062354302999722, -6.216878364870000340, 12.50000000000000000 ) ) ;
#18816=CARTESIAN_POINT ( 'NONE',  ( -5.155802126857005341, 15.83900978869999854, 2.700290858290999907 ) ) ;
#18817=CARTESIAN_POINT ( 'NONE',  ( -13.99999999999999822, -9.953687737870106744, 2.637001505031396409 ) ) ;
#18818=CARTESIAN_POINT ( 'NONE',  ( 14.35387625730999872, 4.075369344914999914, 8.193037116081999471 ) ) ;
#18825=CARTESIAN_POINT ( 'NONE',  ( -16.66859587121331998, -7.950560622842369973, -4.582561865549370062 ) ) ;
#18828=CARTESIAN_POINT ( 'NONE',  ( -4.736842207410001393, 12.61338879614000241, -0.1498249729732001601 ) ) ;
#18830=CARTESIAN_POINT ( 'NONE',  ( 12.00000000000000533, -4.155383997292160458, -8.661442538515151668 ) ) ;
#18831=DIRECTION ( 'NONE',  ( 0.000000000000000000, -1.000000000000000000, 0.000000000000000000 ) ) ;
#18832=CARTESIAN_POINT ( 'NONE',  ( -6.080190197657000084, 16.30605817606999608, -1.000000000000000000 ) ) ;
#18834=AXIS2_PLACEMENT_3D ( 'NONE', #15622, #8378, #23131 ) ;
#18840=CARTESIAN_POINT ( 'NONE',  ( -17.27916243917333361, 7.964251406370663311, 4.590452739718227093 ) ) ;
#18841=CARTESIAN_POINT ( 'NONE',  ( 18.62845540657000143, -9.535387850010000221, -2.003629948511000070 ) ) ;
#18842=CARTESIAN_POINT ( 'NONE',  ( 0.7581189486232848829, 12.82322678404221250, -6.625575084922103564 ) ) ;
#18844=CARTESIAN_POINT ( 'NONE',  ( -22.35796241690466601, 2.784267768755626982, -10.31842131618721936 ) ) ;
#18848=VERTEX_POINT ( 'NONE', #14433 ) ;
#18851=CARTESIAN_POINT ( 'NONE',  ( -5.833999999999999631, 12.89775331292639926, 5.076162411588415241E-10 ) ) ;
#18852=CIRCLE ( 'NONE', #21956, 14.43375672973999890 ) ;
#18854=FACE_OUTER_BOUND ( 'NONE', #1100, .T. ) ;
#18856=EDGE_CURVE ( 'NONE', #8479, #23530, #16047, .T. ) ;
#18857=FACE_OUTER_BOUND ( 'NONE', #2846, .T. ) ;
#18858=CARTESIAN_POINT ( 'NONE',  ( 15.20100174931000048, 0.8726850093137999975, 10.66462197497000020 ) ) ;
#18859=CARTESIAN_POINT ( 'NONE',  ( -16.57879478578999866, 10.66533002439999933, 3.939376312692000504 ) ) ;
#18861=CARTESIAN_POINT ( 'NONE',  ( 13.83796080085999947, -10.41640823646999969, 4.395528184185000242 ) ) ;
#18863=AXIS2_PLACEMENT_3D ( 'NONE', #17266, #4189, #11351 ) ;
#18864=DIRECTION ( 'NONE',  ( 0.000000000000000000, 1.000000000000000000, 0.000000000000000000 ) ) ;
#18865=CARTESIAN_POINT ( 'NONE',  ( 22.08360318395000021, -4.195824812958000471, -9.353156391488001375 ) ) ;
#18867=CARTESIAN_POINT ( 'NONE',  ( 24.50000000000000000, -10.82531754731000007, 6.250000000000000000 ) ) ;
#18868=ORIENTED_EDGE ( 'NONE', *, *, #9672, .F. ) ;
#18869=CARTESIAN_POINT ( 'NONE',  ( 12.52254538689000007, 1.738956572546000112, -9.176809200813000444 ) ) ;
#18871=CARTESIAN_POINT ( 'NONE',  ( 4.793508155719999664, 12.39309388022998526, 1.113049502895999021 ) ) ;
#18874=CARTESIAN_POINT ( 'NONE',  ( -21.10023913963000197, -9.672014745719000217, -5.406718608085999911 ) ) ;
#18876=CARTESIAN_POINT ( 'NONE',  ( -19.35893705290999733, -9.828989445528000246, 3.502754984265999738 ) ) ;
#18882=CARTESIAN_POINT ( 'NONE',  ( 14.65256424931000190, 9.798150841947000700, -4.264230833847999946 ) ) ;
#18884=EDGE_CURVE ( 'NONE', #4798, #10616, #16529, .T. ) ;
#18885=CARTESIAN_POINT ( 'NONE',  ( -18.68332398068000089, -2.538655790982999871, -10.59268337770999935 ) ) ;
#18887=CARTESIAN_POINT ( 'NONE',  ( 24.18393254356861632, 13.26880198692879276, -2.017760803068382458 ) ) ;
#18889=ORIENTED_EDGE ( 'NONE', *, *, #7459, .T. ) ;
#18892=CARTESIAN_POINT ( 'NONE',  ( 14.33390021297796224, -4.407876064383785319, -9.345721391049526261 ) ) ;
#18893=AXIS2_PLACEMENT_3D ( 'NONE', #7928, #17130, #10228 ) ;
#18894=ORIENTED_EDGE ( 'NONE', *, *, #5556, .F. ) ;
#18895=CARTESIAN_POINT ( 'NONE',  ( -0.8198258211412998708, 12.74638329176999996, -6.440467097934996055 ) ) ;
#18897=EDGE_CURVE ( 'NONE', #14252, #15392, #16957, .T. ) ;
#18898=CARTESIAN_POINT ( 'NONE',  ( 11.66614181937426409, 3.921044720225134839, 12.49992990203553589 ) ) ;
#18899=CARTESIAN_POINT ( 'NONE',  ( 18.85240113949000218, -1.886779804701000041, 10.26112574610000117 ) ) ;
#18900=AXIS2_PLACEMENT_3D ( 'NONE', #23, #1731, #12863 ) ;
#18901=CARTESIAN_POINT ( 'NONE',  ( -6.046835300290999804, 16.30334124114000360, 1.000000020649999932 ) ) ;
#18905=ORIENTED_EDGE ( 'NONE', *, *, #5622, .T. ) ;
#18908=CARTESIAN_POINT ( 'NONE',  ( 24.35625626386759279, 9.206804001270699089, 9.053347694469197293 ) ) ;
#18910=EDGE_LOOP ( 'NONE', ( #16503, #144, #12983, #15798, #2298 ) ) ;
#18911=VECTOR ( 'NONE', #22486, 1000.000000000000000 ) ;
#18912=CARTESIAN_POINT ( 'NONE',  ( 17.69311855095000041, -10.67520284561000032, -3.052685539234999634 ) ) ;
#18917=CARTESIAN_POINT ( 'NONE',  ( -24.49594166687720076, 10.56920153269230411, -6.693539566634715499 ) ) ;
#18918=CARTESIAN_POINT ( 'NONE',  ( -10.70159721169000022, 15.56649841902000020, 0.2703010418137000714 ) ) ;
#18921=CARTESIAN_POINT ( 'NONE',  ( -24.43506354683044535, -9.928196662809744666, -7.803922592514855872 ) ) ;
#18923=CARTESIAN_POINT ( 'NONE',  ( -23.44526871306000260, 9.800235893351999295, -2.981156924137000175 ) ) ;
#18924=CARTESIAN_POINT ( 'NONE',  ( -14.50000018026810444, 10.69550487835361352, 6.474840093757361359 ) ) ;
#18925=CARTESIAN_POINT ( 'NONE',  ( -23.74465998031000069, 6.216878364870000340, 12.50000000000000000 ) ) ;
#18926=CARTESIAN_POINT ( 'NONE',  ( 15.32840305081342258, 1.511959382472310764, 10.25233748923334964 ) ) ;
#18927=CARTESIAN_POINT ( 'NONE',  ( -13.77576579251999966, -10.20643469992999997, -2.518766116505000152 ) ) ;
#18928=CIRCLE ( 'NONE', #13893, 6.125000000000000000 ) ;
#18930=AXIS2_PLACEMENT_3D ( 'NONE', #8577, #1426, #14261 ) ;
#18932=CARTESIAN_POINT ( 'NONE',  ( -15.39248033193999987, -8.001506135565000122, 6.430926145009000727 ) ) ;
#18936=CARTESIAN_POINT ( 'NONE',  ( -17.87783718451543535, -7.209909598057388180, 7.565398080760625810 ) ) ;
#18937=ORIENTED_EDGE ( 'NONE', *, *, #5842, .T. ) ;
#18939=CARTESIAN_POINT ( 'NONE',  ( -5.079296814832000351, 15.76344662027999988, 2.859901774060001678 ) ) ;
#18941=CARTESIAN_POINT ( 'NONE',  ( 15.36750142131000096, -7.843339156370999099, -5.684071587432000250 ) ) ;
#18943=CARTESIAN_POINT ( 'NONE',  ( 18.48762270046333356, -8.239590629339057060, 4.107793420616442148 ) ) ;
#18948=CARTESIAN_POINT ( 'NONE',  ( 4.722003391458004629, 12.53571431330998465, 0.2446935953583998513 ) ) ;
#18949=DIRECTION ( 'NONE',  ( 1.000000000000000000, 0.000000000000000000, 2.391262342458999903E-11 ) ) ;
#18950=VECTOR ( 'NONE', #11368, 999.9999999999998863 ) ;
#18951=CARTESIAN_POINT ( 'NONE',  ( -21.49415997476000229, 2.491858532101999923, -9.269619466602000202 ) ) ;
#18953=CARTESIAN_POINT ( 'NONE',  ( -12.25000000000000000, 1.374666032043000015E-14, 0.000000000000000000 ) ) ;
#18958=ORIENTED_EDGE ( 'NONE', *, *, #15031, .T. ) ;
#18959=CARTESIAN_POINT ( 'NONE',  ( 21.91372127707999695, -5.477858186341999058, 8.167686895493000421 ) ) ;
#18960=CARTESIAN_POINT ( 'NONE',  ( -2.791226855812472873, 13.06767197116077028, -6.129407314324748057 ) ) ;
#18961=CARTESIAN_POINT ( 'NONE',  ( -23.62063575149434058, -8.943480941775941773, -2.984471859962635421 ) ) ;
#18963=CARTESIAN_POINT ( 'NONE',  ( -22.94704266735730513, -10.35193671520849179, 2.143217020573386922 ) ) ;
#18967=CARTESIAN_POINT ( 'NONE',  ( -17.96347329169541496, 2.346826270286123339, 10.32639379259640400 ) ) ;
#18968=CARTESIAN_POINT ( 'NONE',  ( 23.99062354302999722, 13.93375672974000068, -0.8660254037843999608 ) ) ;
#18971=ADVANCED_FACE ( 'NONE', ( #11040 ), #18659, .T. ) ;
#18974=CARTESIAN_POINT ( 'NONE',  ( 15.85912674931000055, -8.678267488395999152, -6.289192543930000490 ) ) ;
#18976=CARTESIAN_POINT ( 'NONE',  ( 12.95822370638999921, 3.216216234831999810, -9.637132962990998308 ) ) ;
#18978=DIRECTION ( 'NONE',  ( 0.000000000000000000, 1.000000000000000000, 0.000000000000000000 ) ) ;
#18979=CARTESIAN_POINT ( 'NONE',  ( 21.82376044967999817, -7.488614721695999954, 6.188719846541999026 ) ) ;
#18982=DIRECTION ( 'NONE',  ( 1.000000000000000000, 0.000000000000000000, 0.000000000000000000 ) ) ;
#18984=CARTESIAN_POINT ( 'NONE',  ( 2.263485475614001707, 11.78661699911999960, 4.163976765251001133 ) ) ;
#18986=ADVANCED_FACE ( 'NONE', ( #10 ), #18313, .F. ) ;
#18987=CARTESIAN_POINT ( 'NONE',  ( -23.94067641790000067, 11.10629741394000014, 1.069876158558999979 ) ) ;
#18988=VERTEX_POINT ( 'NONE', #14667 ) ;
#18994=CARTESIAN_POINT ( 'NONE',  ( 0.9223941759128004847, 12.69701722427999790, 7.033009390352000345 ) ) ;
#18996=CARTESIAN_POINT ( 'NONE',  ( 14.87193924930999955, 10.04572779547000039, 3.659788831486999960 ) ) ;
#18997=EDGE_CURVE ( 'NONE', #19976, #9506, #14885, .T. ) ;
#18998=CARTESIAN_POINT ( 'NONE',  ( -15.59561067990999916, -1.941903525450000112, 10.08593956198000008 ) ) ;
#18999=CARTESIAN_POINT ( 'NONE',  ( 15.34106375730999972, -1.677480367812999917, -9.021981177529999840 ) ) ;
#19001=ORIENTED_EDGE ( 'NONE', *, *, #1722, .T. ) ;
#19004=CARTESIAN_POINT ( 'NONE',  ( 4.691448533132819065, 14.73702420321861695, -3.942640714737680518 ) ) ;
#19005=EDGE_LOOP ( 'NONE', ( #13552, #8913, #20375, #17191, #9598, #13324, #20818, #500 ) ) ;
#19007=DIRECTION ( 'NONE',  ( 0.000000000000000000, 0.5000000000000169864, -0.8660254037844288266 ) ) ;
#19009=CARTESIAN_POINT ( 'NONE',  ( 14.61207169101494685, -8.609499306320094192, 2.892750243897086904 ) ) ;
#19010=CARTESIAN_POINT ( 'NONE',  ( 18.12769161559589293, 7.594118990230957600, -7.191324035859334884 ) ) ;
#19013=EDGE_CURVE ( 'NONE', #5502, #9480, #16600, .T. ) ;
#19014=CARTESIAN_POINT ( 'NONE',  ( 24.50000000000000000, -10.82531754731000007, -6.250000000000000000 ) ) ;
#19015=EDGE_LOOP ( 'NONE', ( #20126, #10464, #1444, #8759 ) ) ;
#19016=EDGE_CURVE ( 'NONE', #6411, #3590, #2065, .T. ) ;
#19018=VERTEX_POINT ( 'NONE', #234 ) ;
#19019=DIRECTION ( 'NONE',  ( 0.000000000000000000, 0.000000000000000000, -1.000000000000000000 ) ) ;
#19021=CARTESIAN_POINT ( 'NONE',  ( -3.079591938543706497, 11.88219301979877862, 3.716998605068117634 ) ) ;
#19024=CARTESIAN_POINT ( 'NONE',  ( 6.175768678244707210, 13.98844511635596177, -0.6082058386448220277 ) ) ;
#19025=CARTESIAN_POINT ( 'NONE',  ( -7.128598361965003960, 15.40011789705998702, -1.088345829342000526 ) ) ;
#19029=ORIENTED_EDGE ( 'NONE', *, *, #5216, .T. ) ;
#19031=CARTESIAN_POINT ( 'NONE',  ( 5.699442596042000098, 1.578914512950999657E-14, -14.15464499511999996 ) ) ;
#19033=CARTESIAN_POINT ( 'NONE',  ( -24.48376588670980070, -10.31426502621016006, -7.135315508364757697 ) ) ;
#19035=CARTESIAN_POINT ( 'NONE',  ( -22.41706829942000212, -10.13657052992000196, -1.268620720673999891 ) ) ;
#19036=CARTESIAN_POINT ( 'NONE',  ( -14.45960647534970889, 9.597314625695767987, 8.376896358970226331 ) ) ;
#19037=CARTESIAN_POINT ( 'NONE',  ( 6.226910483035863919, 13.75536151932502449, 1.330040350533948423 ) ) ;
#19038=CARTESIAN_POINT ( 'NONE',  ( 15.58002254845384016, -6.890210661546990245, 7.720466256389740600 ) ) ;
#19039=B_SPLINE_CURVE_WITH_KNOTS ( 'NONE', 3,
 ( #18867, #2272, #9665, #14262, #6746, #8329, #19726, #14019, #10150, #12455, #6630, #6383 ),
 .UNSPECIFIED., .F., .F.,
 ( 4, 1, 1, 1, 1, 2, 2, 4 ),
 ( 0.000000000000000000, 0.2499999999999986122, 0.3749999999999980571, 0.4374999999999979461, 0.4687499999999978351, 0.4843749999999980016, 0.4999999999999981126, 1.000000000000000000 ),
 .UNSPECIFIED. ) ;
#19040=CARTESIAN_POINT ( 'NONE',  ( -19.79001396229000065, -7.801656982797999795, 6.945750858680000306 ) ) ;
#19042=CARTESIAN_POINT ( 'NONE',  ( -18.63376253787999914, -9.149460784975000038, 0.000000000000000000 ) ) ;
#19044=CARTESIAN_POINT ( 'NONE',  ( -12.95491615630000126, -0.8957832334074999903, -10.15856198502000041 ) ) ;
#19046=VERTEX_POINT ( 'NONE', #10059 ) ;
#19048=CARTESIAN_POINT ( 'NONE',  ( -19.15116083384464574, -5.105618582937671235, -9.150693563290923649 ) ) ;
#19053=CARTESIAN_POINT ( 'NONE',  ( -20.29659587121332365, -8.031911560230602376, -4.629449613728698232 ) ) ;
#19054=CARTESIAN_POINT ( 'NONE',  ( 14.70937642131000089, 0.7886220128679000130, 9.636901145054999063 ) ) ;
#19056=CARTESIAN_POINT ( 'NONE',  ( -6.232893174142998483, 15.85796039161002824, -1.061654000538000409 ) ) ;
#19057=FACE_OUTER_BOUND ( 'NONE', #132, .T. ) ;
#19058=B_SPLINE_SURFACE_WITH_KNOTS ( 'NONE', 3, 3, ( 
 ( #12653, #16274, #16024, #8785, #7187, #21742, #5156, #23780, #10720, #12537, #3568, #19924, #18338, #3342, #1518, #23666, #21856, #5267, #15906, #13232, #264, #7670, #22553, #5496, #5959, #9252, #13344, #12876, #20744, #16629, #20395, #3801, #2212, #11071, #16509 ),
 ( #3921, #11313, #18689, #20276, #14695, #15043, #4151, #7541, #22439, #2095, #9485, #7788, #11194, #14804, #23898, #39, #20625, #7421, #18454, #7305, #4035, #22087, #11548, #149, #3680, #16862, #5849, #11429, #18804, #9604, #16990, #391, #13118, #18927, #15158 ),
 ( #1864, #9134, #1982, #5732, #22199, #5612, #12994, #18577, #9365, #22315, #16739, #14921, #20516, #15759, #6443, #6322, #12149, #992, #11784, #4642, #12030, #17347, #10086, #13467, #20983, #4394, #2825, #19412, #13954, #19159, #17473, #4279, #15518, #623, #15635 ),
 ( #19040, #21230, #6202, #867, #15275, #9842, #22906, #15397, #13707, #2449, #8024, #22786, #749, #11905, #13587, #21348, #10205, #17599, #8153, #8394, #8271, #23150, #22667, #21100, #20869, #23026, #19289, #13831, #2570, #4515, #9960, #6570, #2702, #4763, #2337 ) ),
 .UNSPECIFIED., .F., .F., .F.,
 ( 4, 4 ),
 ( 4, 1, 1, 1, 1, 1, 1, 1, 1, 1, 1, 1, 1, 1, 1, 1, 1, 1, 1, 1, 1, 1, 1, 1, 1, 1, 1, 1, 1, 1, 1, 1, 4 ),
 ( -0.6000240009601000013, 1.600024000959999970 ),
 ( -0.01778791961293000115, 0.01111744975807999955, 0.04002281912908000477, 0.06892818850008999854, 0.09783355787108999335, 0.1267389272420999802, 0.1556442966131000027, 0.1845496659840999976, 0.2134550353551000201, 0.2423604047261000149, 0.2712657740971000098, 0.3001711434680999768, 0.3290765128390999994, 0.3579818822100999665, 0.3868872515810999890, 0.4157926209521000116, 0.4446979903232000098, 0.4736033596941999768, 0.5025087290651999439, 0.5314140984361999109, 0.5603194678071999890, 0.5892248371781999561, 0.6181302065492000342, 0.6470355759202000012, 0.6759409452911999683, 0.7048463146621999353, 0.7337516840332000134, 0.7626570534041999805, 0.7915624227752000586, 0.8204677921462000256, 0.8493731615171999927, 0.8782785308881999597, 0.9071839002592000378 ),
 .UNSPECIFIED. ) ;
#19059=ORIENTED_EDGE ( 'NONE', *, *, #3604, .T. ) ;
#19061=FACE_OUTER_BOUND ( 'NONE', #21593, .T. ) ;
#19062=CARTESIAN_POINT ( 'NONE',  ( -3.187683228664999646, 12.10419657022999651, 3.627759556269996910 ) ) ;
#19063=CARTESIAN_POINT ( 'NONE',  ( -14.00000000000000000, -2.869707268214888529, 9.513533945855728646 ) ) ;
#19064=CARTESIAN_POINT ( 'NONE',  ( 17.71169237777402827, -10.07440819872460658, -2.697916929237545780 ) ) ;
#19065=CARTESIAN_POINT ( 'NONE',  ( 18.75008227645999881, 0.000000000000000000, 0.000000000000000000 ) ) ;
#19066=CARTESIAN_POINT ( 'NONE',  ( 18.77245603379665795, -7.997832810931552849, -4.609517281848381387 ) ) ;
#19067=CARTESIAN_POINT ( 'NONE',  ( -6.147399691167000135, 16.31019195569000146, -0.9999999999994999555 ) ) ;
#19071=ORIENTED_EDGE ( 'NONE', *, *, #4700, .T. ) ;
#19074=CARTESIAN_POINT ( 'NONE',  ( 4.321647192813569127, 13.42637534801005117, -5.297716879388643108 ) ) ;
#19077=CARTESIAN_POINT ( 'NONE',  ( -20.61749804056798752, 0.1139427650053814606, -10.51009152996787144 ) ) ;
#19079=CARTESIAN_POINT ( 'NONE',  ( 12.50898179946000077, -7.466908609752000103, 11.77829470162000014 ) ) ;
#19080=ORIENTED_EDGE ( 'NONE', *, *, #17636, .F. ) ;
#19081=CARTESIAN_POINT ( 'NONE',  ( -18.71707669688263920, 3.197755709358065523, -9.964328844018272235 ) ) ;
#19084=CYLINDRICAL_SURFACE ( 'NONE', #13825, 4.750000000000000000 ) ;
#19088=CARTESIAN_POINT ( 'NONE',  ( 17.94318924931000225, -0.08898103000111000360, -10.77198407497000154 ) ) ;
#19090=CARTESIAN_POINT ( 'NONE',  ( -24.32811878836000119, 9.771184119221999254, -4.393942764655000666 ) ) ;
#19092=CARTESIAN_POINT ( 'NONE',  ( -19.08240939882999854, 4.922202718798000198, -9.729665371451000411 ) ) ;
#19094=CARTESIAN_POINT ( 'NONE',  ( 18.78114037306000128, 10.87330394281000068, 0.8145811978064999570 ) ) ;
#19097=CARTESIAN_POINT ( 'NONE',  ( 21.64671134753000104, -2.561010203381999695, 9.366262177596999194 ) ) ;
#19099=ORIENTED_EDGE ( 'NONE', *, *, #17334, .F. ) ;
#19101=CARTESIAN_POINT ( 'NONE',  ( -6.042815635770000249, 16.39253429789999927, 0.9999999720525000191 ) ) ;
#19103=CARTESIAN_POINT ( 'NONE',  ( 4.336915520410000724, 12.38777958348998709, 1.884790593294000782 ) ) ;
#19106=CARTESIAN_POINT ( 'NONE',  ( -22.12320936320999820, 10.23231788766999983, -4.323895602960999618 ) ) ;
#19108=DIRECTION ( 'NONE',  ( -0.8193292504149961575, 0.000000000000000000, -0.5733232765328829528 ) ) ;
#19110=CARTESIAN_POINT ( 'NONE',  ( -24.24003052286102999, 3.589673254490056031, -12.49985157729351215 ) ) ;
#19111=CARTESIAN_POINT ( 'NONE',  ( -4.749994070560452641, 12.54999978084880752, 0.6289937086464317817 ) ) ;
#19112=CARTESIAN_POINT ( 'NONE',  ( 4.878286811419003222, 14.94151125082000497, 3.715753592770002722 ) ) ;
#19114=CARTESIAN_POINT ( 'NONE',  ( 12.67818924931000168, 6.046592098211998945, -8.747551238178997934 ) ) ;
#19115=CARTESIAN_POINT ( 'NONE',  ( -16.65202050098999820, 5.360250747359000201, -9.417511137717001546 ) ) ;
#19116=CARTESIAN_POINT ( 'NONE',  ( 13.80543875730999837, 6.427790461817999734, -6.492639392963999612 ) ) ;
#19117=CARTESIAN_POINT ( 'NONE',  ( 18.94203808734637207, 2.038145998098363609, 10.23480975536132220 ) ) ;
#19118=ADVANCED_FACE ( 'NONE', ( #6044 ), #12907, .F. ) ;
#19120=CARTESIAN_POINT ( 'NONE',  ( 13.50000000000000000, -4.002954420673999536, -8.080569262580000967 ) ) ;
#19122=CARTESIAN_POINT ( 'NONE',  ( 14.00976417969420851, -10.32366805564640799, -0.007670053520953104033 ) ) ;
#19123=AXIS2_PLACEMENT_3D ( 'NONE', #16231, #1221, #1468 ) ;
#19125=CARTESIAN_POINT ( 'NONE',  ( 1.712095296464997585, 13.93444603479998811, -5.928653740531998118 ) ) ;
#19126=CARTESIAN_POINT ( 'NONE',  ( -24.11803009774155626, 13.00903097541294073, -2.467105211237874851 ) ) ;
#19128=CARTESIAN_POINT ( 'NONE',  ( 11.31235608929811498, -2.505169353225074058, 12.49996790083181963 ) ) ;
#19129=CARTESIAN_POINT ( 'NONE',  ( 17.40288447006501826, -10.49761850512724415, 1.364539225918563359 ) ) ;
#19130=CARTESIAN_POINT ( 'NONE',  ( -14.25699038479000080, -13.93375672974000068, 0.000000000000000000 ) ) ;
#19132=CARTESIAN_POINT ( 'NONE',  ( -6.250000000000000000, 1.301187224093999891E-14, 0.000000000000000000 ) ) ;
#19135=VERTEX_POINT ( 'NONE', #19630 ) ;
#19136=CARTESIAN_POINT ( 'NONE',  ( 0.6252065045458350401, 11.57481763370839545, -4.750366986350042176 ) ) ;
#19139=CARTESIAN_POINT ( 'NONE',  ( -1.987853604051396106, 11.65079879119223349, 4.388780662035608238 ) ) ;
#19143=CARTESIAN_POINT ( 'NONE',  ( 15.49387847584000077, -0.07844713208112001623, 11.04258953166000090 ) ) ;
#19149=CARTESIAN_POINT ( 'NONE',  ( -14.00000000000000178, -6.309619694642019994, -7.620818005153923380 ) ) ;
#19154=CARTESIAN_POINT ( 'NONE',  ( -19.43131210050000135, 9.425945272632999306, 1.879262601378000053 ) ) ;
#19157=CARTESIAN_POINT ( 'NONE',  ( 6.185782116123350605, 13.94105495766904390, 0.7320468670209526740 ) ) ;
#19158=CARTESIAN_POINT ( 'NONE',  ( 15.88509334382326443, -10.12552540729580564, -2.174043714885656620 ) ) ;
#19159=CARTESIAN_POINT ( 'NONE',  ( -14.58481954452000018, 5.127933381152999459, 9.739763264848999569 ) ) ;
#19161=CARTESIAN_POINT ( 'NONE',  ( -20.74166715155477192, 2.803544456025320208, -10.13304684785263454 ) ) ;
#19163=CARTESIAN_POINT ( 'NONE',  ( -23.80485347273356211, -1.053090434097245121, -9.586785637656749515 ) ) ;
#19166=ORIENTED_EDGE ( 'NONE', *, *, #14550, .F. ) ;
#19170=CARTESIAN_POINT ( 'NONE',  ( -15.44694658125069608, -2.463998168450752146, -10.08867902004827677 ) ) ;
#19174=CARTESIAN_POINT ( 'NONE',  ( 4.817436639547997501, 14.48250318153000471, -3.715459049975000205 ) ) ;
#19176=CARTESIAN_POINT ( 'NONE',  ( -19.57855420454666984, 9.173706001228294937, -1.200708359830031657 ) ) ;
#19177=CARTESIAN_POINT ( 'NONE',  ( 13.61250142131000196, -6.495520710102000272, -7.123429297049000297 ) ) ;
#19178=EDGE_LOOP ( 'NONE', ( #21727, #313, #7416 ) ) ;
#19180=CARTESIAN_POINT ( 'NONE',  ( 18.35395603379666341, -5.527903405087061905, 7.358200411944897823 ) ) ;
#19184=CARTESIAN_POINT ( 'NONE',  ( 24.24531177150999994, 0.000000000000000000, 0.000000000000000000 ) ) ;
#19185=DIRECTION ( 'NONE',  ( -0.9999999999999998890, -9.268909281637997623E-09, 3.975906136097999155E-09 ) ) ;
#19186=CARTESIAN_POINT ( 'NONE',  ( 23.85298513858829139, 10.35157075127159487, 2.356844212935751859 ) ) ;
#19188=CARTESIAN_POINT ( 'NONE',  ( 18.10698583361175551, 0.6240570753724111741, -10.40424229370149689 ) ) ;
#19189=CARTESIAN_POINT ( 'NONE',  ( 4.834782059083999606, 12.44497316928999808, -0.3759403457470999466 ) ) ;
#19190=CARTESIAN_POINT ( 'NONE',  ( -14.48875658296588398, 11.47331197282439774, -5.127631166282751174 ) ) ;
#19191=CARTESIAN_POINT ( 'NONE',  ( 22.29042311570000123, 0.6833233609315999546, 11.23355659561000053 ) ) ;
#19192=CARTESIAN_POINT ( 'NONE',  ( -12.25000000000000000, 13.93375672974000068, 0.000000000000000000 ) ) ;
#19193=CARTESIAN_POINT ( 'NONE',  ( -3.644450799678000230, 14.33206891749000000, -4.922778709793999674 ) ) ;
#19198=CARTESIAN_POINT ( 'NONE',  ( 22.79184847219999810, -10.23415548584000057, -3.837234280334999692 ) ) ;
#19199=CARTESIAN_POINT ( 'NONE',  ( -0.2273504397345396943, 12.80486570122317680, -6.661112331329158032 ) ) ;
#19201=CARTESIAN_POINT ( 'NONE',  ( -11.99999999434999864, 6.999999994347000154, 4.083276180409999442E-09 ) ) ;
#19203=CARTESIAN_POINT ( 'NONE',  ( -19.35893705290999733, -9.828989445528000246, 3.502754984265999738 ) ) ;
#19206=VERTEX_POINT ( 'NONE', #21687 ) ;
#19207=CARTESIAN_POINT ( 'NONE',  ( -17.04240246313371188, -1.782570974809130293, -10.26454133355910336 ) ) ;
#19209=CONICAL_SURFACE ( 'NONE', #10722, 7.249999994833000727, 0.7853981633972997312 ) ;
#19212=DIRECTION ( 'NONE',  ( 1.000000000000000000, 0.000000000000000000, 0.000000000000000000 ) ) ;
#19213=ORIENTED_EDGE ( 'NONE', *, *, #1811, .F. ) ;
#19214=B_SPLINE_CURVE_WITH_KNOTS ( 'NONE', 3,
 ( #1367, #4766, #4886, #16254, #12274, #16121, #3075, #17849, #6935, #14331, #5130, #19898, #23647, #7054, #14437, #21832, #9460, #3657, #7160, #18316, #5355, #9224, #11285, #3546, #12746, #7277, #1611, #1955, #5702, #14670, #5587, #12968, #18549, #14779, #9108, #5821, #18662, #8997, #4005, #20487, #23871, #16367, #3895, #20364, #3774, #20138, #23757, #7512, #2069, #16603, #9341, #16480, #12855, #11043, #14551, #16834, #10930, #20252, #21945, #18427, #22413, #22065, #238, #1718, #1837, #13, #7397, #5473, #22175, #11162, #16714, #13088, #125, #14896, #7641, #22286, #15014, #13204, #20596, #18210, #9811, #18771, #4251, #13316, #19258, #22997, #20839, #17196, #591, #11403, #7760, #6048, #21073, #2181, #9931, #19009, #15609, #20714, #22879 ),
 .UNSPECIFIED., .F., .F.,
 ( 4, 2, 2, 2, 1, 1, 2, 2, 1, 1, 1, 2, 2, 2, 2, 1, 1, 2, 1, 1, 1, 2, 2, 2, 2, 2, 1, 1, 1, 1, 1, 2, 2, 2, 2, 2, 2, 2, 1, 1, 1, 1, 1, 2, 2, 2, 2, 2, 2, 2, 2, 1, 1, 1, 1, 1, 2, 2, 2, 2, 2, 4 ),
 ( 0.000000000000000000, 0.03125000000005528911, 0.06250000000011057821, 0.07812500000013818113, 0.08203125000014512003, 0.08300781250014672985, 0.08325195312514714618, 0.08337402343764720170, 0.08349609375014727108, 0.08398437500014754864, 0.08593750000014858947, 0.09375000000015272505, 0.1250000000001691147, 0.1562500000001855460, 0.1640625000001895983, 0.1660156250001906530, 0.1665039062501909306, 0.1666259765626908473, 0.1667480468751907918, 0.1669921875001907086, 0.1679687500001903755, 0.1718750000001889877, 0.1875000000001834088, 0.2187500000001722789, 0.2343750000001667000, 0.2421875000001639244, 0.2460937500001625367, 0.2480468750001618428, 0.2490234375001615097, 0.2495117187501613432, 0.2497558593751612599, 0.2498779296876612321, 0.2500000000001612044, 0.3125000000001456057, 0.3750000000001300071, 0.4375000000001144085, 0.4687500000001066369, 0.4843750000001026956, 0.4921875000001008083, 0.4960937500000998090, 0.4980468750000993650, 0.4990234375000991429, 0.4995117187500989764, 0.4997558593750989209, 0.5000000000000988098, 0.5312500000000929257, 0.5625000000000869305, 0.6250000000000750511, 0.6875000000000631717, 0.7187500000000571765, 0.7343750000000541789, 0.7421875000000526246, 0.7460937500000519584, 0.7480468750000516254, 0.7490234375000514033, 0.7495117187500512923, 0.7497558593750511813, 0.7500000000000510703, 0.8125000000000383027, 0.8750000000000255351, 0.9375000000000127676, 1.000000000000000000 ),
 .UNSPECIFIED. ) ;
#19217=CARTESIAN_POINT ( 'NONE',  ( 16.62693924930999856, 10.62505432564000074, 1.551621659364999850 ) ) ;
#19218=CARTESIAN_POINT ( 'NONE',  ( -14.56155220878999046, -7.925308545561296825, -4.456233346637926473 ) ) ;
#19219=CARTESIAN_POINT ( 'NONE',  ( -18.20383756955000010, 6.087427736527000199, 9.656242520863001388 ) ) ;
#19220=DIRECTION ( 'NONE',  ( 0.000000000000000000, 1.000000000000000000, 0.000000000000000000 ) ) ;
#19221=CARTESIAN_POINT ( 'NONE',  ( 13.16181994525999954, 0.8615620839388999919, -9.360004375220999151 ) ) ;
#19224=CARTESIAN_POINT ( 'NONE',  ( 24.91638881842000330, 0.3555708854531000607, 10.32200993542000056 ) ) ;
#19227=CARTESIAN_POINT ( 'NONE',  ( -2.143920584830219411, 13.91597717198021478, 5.737536879300400905 ) ) ;
#19230=CARTESIAN_POINT ( 'NONE',  ( -3.916368311430999505, 12.23844822715000369, 2.656827315156998548 ) ) ;
#19232=CARTESIAN_POINT ( 'NONE',  ( -24.57378270132000253, -9.262129720473000205, -5.482658259817999813 ) ) ;
#19233=CONICAL_SURFACE ( 'NONE', #20027, 13.20532192316000142, 0.7853981633972997312 ) ;
#19234=DIRECTION ( 'NONE',  ( -1.167437209404000066E-09, -4.744820243581140101E-20, -1.000000000000000000 ) ) ;
#19237=CARTESIAN_POINT ( 'NONE',  ( 15.18224770046331606, -7.245781551128942510, -5.568249303537384343 ) ) ;
#19238=AXIS2_PLACEMENT_3D ( 'NONE', #10384, #21286, #1044 ) ;
#19239=CARTESIAN_POINT ( 'NONE',  ( 8.124934037954998800, 1.125145054518999965E-14, 0.000000000000000000 ) ) ;
#19243=CARTESIAN_POINT ( 'NONE',  ( -14.82384736926000102, 5.788590216149999357, -9.100136119003000346 ) ) ;
#19244=AXIS2_PLACEMENT_3D ( 'NONE', #17804, #17550, #17674 ) ;
#19246=CARTESIAN_POINT ( 'NONE',  ( 11.39231375731000107, -8.729484032481000355, -2.472142458034000345 ) ) ;
#19249=PLANE ( 'NONE',  #23155 ) ;
#19251=B_SPLINE_CURVE_WITH_KNOTS ( 'NONE', 3,
 ( #20392, #18686, #11067, #2092, #6407, #3797, #17438, #16626, #20273, #261, #11191, #13229, #9600, #4477, #11865, #4032, #11426, #710 ),
 .UNSPECIFIED., .F., .F.,
 ( 4, 2, 2, 2, 2, 2, 2, 2, 4 ),
 ( 0.000000000000000000, 0.1249999999999999722, 0.2500000000000000000, 0.3750000000000000000, 0.5000000000000001110, 0.6250000000000001110, 0.7500000000000000000, 0.8750000000000000000, 1.000000000000000000 ),
 .UNSPECIFIED. ) ;
#19253=CARTESIAN_POINT ( 'NONE',  ( 2.113792074058734816, 13.90978049634387936, -5.748768854935037531 ) ) ;
#19254=VERTEX_POINT ( 'NONE', #8851 ) ;
#19255=CARTESIAN_POINT ( 'NONE',  ( -4.023636228000000870, 13.98888312590999661, -4.533167282472001069 ) ) ;
#19258=CARTESIAN_POINT ( 'NONE',  ( 14.40516388438136985, -4.484488855952614372, 7.850264337849301555 ) ) ;
#19259=CARTESIAN_POINT ( 'NONE',  ( -6.651120061331225131, 15.37734650507915113, -1.642905757035629577 ) ) ;
#19260=DIRECTION ( 'NONE',  ( 0.000000000000000000, 0.000000000000000000, 1.000000000000000000 ) ) ;
#19261=CARTESIAN_POINT ( 'NONE',  ( -21.58741243917332753, -2.414574286862336550, -8.985197089948746552 ) ) ;
#19264=DIRECTION ( 'NONE',  ( 0.000000000000000000, -0.9999173538268769645, 0.01285634146465969990 ) ) ;
#19267=ADVANCED_FACE ( 'NONE', ( #21799 ), #19941, .F. ) ;
#19271=CARTESIAN_POINT ( 'NONE',  ( 3.217986197202229448, 13.15087042456258537, 5.950358584322657407 ) ) ;
#19272=CARTESIAN_POINT ( 'NONE',  ( 17.47883835214000214, -6.259200876991000584, 9.163567223394000649 ) ) ;
#19273=CARTESIAN_POINT ( 'NONE',  ( -20.92363501368665979, 8.282032949706003677, 4.165695112817996204 ) ) ;
#19274=CONICAL_SURFACE ( 'NONE', #21975, 9.152445778720998959, 0.02565634000431304615 ) ;
#19276=ORIENTED_EDGE ( 'NONE', *, *, #4448, .T. ) ;
#19277=ORIENTED_EDGE ( 'NONE', *, *, #18513, .T. ) ;
#19278=CARTESIAN_POINT ( 'NONE',  ( -14.00000000000000355, -4.688626905535442368, -8.566863040657263895 ) ) ;
#19279=AXIS2_PLACEMENT_3D ( 'NONE', #8121, #8236, #13309 ) ;
#19282=( BOUNDED_SURFACE ( )  B_SPLINE_SURFACE ( 3, 3, ( 
 ( #10128, #19822, #10376, #3118, #13876, #4807, #16041, #21279, #6728, #19339, #1289, #14243, #1168, #12192, #4689, #19582, #10619, #2988, #21639, #2747, #19459, #12438, #17517, #1037, #8439, #17765, #910 ),
 ( #3236, #15920, #23314, #14120, #8312, #15678, #4927, #1408, #12314, #8802, #10503, #22949, #23065, #6364, #4562, #11952, #6495, #12074, #6974, #1643, #14590, #1533, #5399, #22100, #16401, #14478, #10735 ),
 ( #1880, #14707, #21987, #11083, #5510, #23681, #9032, #16288, #23792, #14364, #18468, #23911, #3358, #12785, #21870, #5169, #21755, #23565, #7321, #20173, #9149, #18128, #12887, #18349, #20288, #12670, #12552 ),
 ( #3692, #7201, #16525, #20056, #19937, #9267, #7089, #8921, #5280, #1760, #3472, #10856, #16644, #18239, #16165, #3581, #10965, #2947, #17725, #16122, #19541, #23272, #996, #10695, #1244, #17964, #4767 ),
 ( #23392, #12275, #12033, #8634, #6810, #12513, #15883, #23523, #8397, #8524, #21234, #6686, #18086, #15764, #19899, #19416, #8885, #4887, #2828, #15997, #12401, #6936, #14332, #3076, #21473, #14203, #23153 ),
 ( #4646, #19787, #6574, #21600, #14079, #10463, #3315, #10578, #1368, #1491, #13957, #21721, #17602, #19662, #5132, #5016, #17850, #16255, #3195, #21351, #8758, #23648, #13833, #10208, #12152, #10335, #1125 ),
 ( #2070, #7278, #7513, #10931, #3437, #14671, #1612, #22287, #9342, #5703, #22066, #14780, #14897, #23759, #18429, #3658, #16604, #1719, #5356, #20253, #8998, #20015, #16368, #21833, #1956, #5474, #10821 ) ),
 .UNSPECIFIED., .F., .F., .T. ) 
 B_SPLINE_SURFACE_WITH_KNOTS ( ( 4, 3, 4 ),
 ( 4, 1, 1, 1, 1, 1, 1, 1, 1, 1, 1, 1, 1, 1, 1, 1, 1, 1, 1, 1, 1, 1, 1, 1, 4 ),
 ( 0.000000000000000000, 1.000000000000000000, 2.000000000000000000 ),
 ( 0.4898034299706000017, 0.4943545979319000083, 0.5111317270519999401, 0.5298150905820000478, 0.5506159615357999471, 0.5738885039238000862, 0.6000497485708999879, 0.6296087238595999835, 0.6631460577478999197, 0.6990545679290000036, 0.7337557558452000306, 0.7651098038429999804, 0.7931348371437000333, 0.8181853307084000493, 0.8407431172970000199, 0.8611305378076999917, 0.8795824795753000025, 0.8963530464747999638, 0.9117079150094000717, 0.9258708385234000193, 0.9397608587919999978, 0.9542041168318999844, 0.9687118367007999664, 0.9836094246282999221, 0.9997243908991000350 ),
 .UNSPECIFIED. ) 
 GEOMETRIC_REPRESENTATION_ITEM ( )  RATIONAL_B_SPLINE_SURFACE ( (
 ( 1.293342249838999924, 1.293342249838999924, 1.293342249838999924, 1.293342249838999924, 1.293342249838999924, 1.293342249838999924, 1.293342249838999924, 1.293342249838999924, 1.293342249838999924, 1.293342249838999924, 1.293342249838999924, 1.293342249838999924, 1.293342249838999924, 1.293342249838999924, 1.293342249838999924, 1.293342249838999924, 1.293342249838999924, 1.293342249838999924, 1.293342249838999924, 1.293342249838999924, 1.293342249838999924, 1.293342249838999924, 1.293342249838999924, 1.293342249838999924, 1.293342249838999924, 1.293342249838999924, 1.293342249838999924),
 ( 0.9022192500537999926, 0.9022192500537999926, 0.9022192500537999926, 0.9022192500537999926, 0.9022192500537999926, 0.9022192500537999926, 0.9022192500537999926, 0.9022192500537999926, 0.9022192500537999926, 0.9022192500537999926, 0.9022192500537999926, 0.9022192500537999926, 0.9022192500537999926, 0.9022192500537999926, 0.9022192500537999926, 0.9022192500537999926, 0.9022192500537999926, 0.9022192500537999926, 0.9022192500537999926, 0.9022192500537999926, 0.9022192500537999926, 0.9022192500537999926, 0.9022192500537999926, 0.9022192500537999926, 0.9022192500537999926, 0.9022192500537999926, 0.9022192500537999926),
 ( 0.9022192500537999926, 0.9022192500537999926, 0.9022192500537999926, 0.9022192500537999926, 0.9022192500537999926, 0.9022192500537999926, 0.9022192500537999926, 0.9022192500537999926, 0.9022192500537999926, 0.9022192500537999926, 0.9022192500537999926, 0.9022192500537999926, 0.9022192500537999926, 0.9022192500537999926, 0.9022192500537999926, 0.9022192500537999926, 0.9022192500537999926, 0.9022192500537999926, 0.9022192500537999926, 0.9022192500537999926, 0.9022192500537999926, 0.9022192500537999926, 0.9022192500537999926, 0.9022192500537999926, 0.9022192500537999926, 0.9022192500537999926, 0.9022192500537999926),
 ( 1.293342249838999924, 1.293342249838999924, 1.293342249838999924, 1.293342249838999924, 1.293342249838999924, 1.293342249838999924, 1.293342249838999924, 1.293342249838999924, 1.293342249838999924, 1.293342249838999924, 1.293342249838999924, 1.293342249838999924, 1.293342249838999924, 1.293342249838999924, 1.293342249838999924, 1.293342249838999924, 1.293342249838999924, 1.293342249838999924, 1.293342249838999924, 1.293342249838999924, 1.293342249838999924, 1.293342249838999924, 1.293342249838999924, 1.293342249838999924, 1.293342249838999924, 1.293342249838999924, 1.293342249838999924),
 ( 0.9022192500537999926, 0.9022192500537999926, 0.9022192500537999926, 0.9022192500537999926, 0.9022192500537999926, 0.9022192500537999926, 0.9022192500537999926, 0.9022192500537999926, 0.9022192500537999926, 0.9022192500537999926, 0.9022192500537999926, 0.9022192500537999926, 0.9022192500537999926, 0.9022192500537999926, 0.9022192500537999926, 0.9022192500537999926, 0.9022192500537999926, 0.9022192500537999926, 0.9022192500537999926, 0.9022192500537999926, 0.9022192500537999926, 0.9022192500537999926, 0.9022192500537999926, 0.9022192500537999926, 0.9022192500537999926, 0.9022192500537999926, 0.9022192500537999926),
 ( 0.9022192500537999926, 0.9022192500537999926, 0.9022192500537999926, 0.9022192500537999926, 0.9022192500537999926, 0.9022192500537999926, 0.9022192500537999926, 0.9022192500537999926, 0.9022192500537999926, 0.9022192500537999926, 0.9022192500537999926, 0.9022192500537999926, 0.9022192500537999926, 0.9022192500537999926, 0.9022192500537999926, 0.9022192500537999926, 0.9022192500537999926, 0.9022192500537999926, 0.9022192500537999926, 0.9022192500537999926, 0.9022192500537999926, 0.9022192500537999926, 0.9022192500537999926, 0.9022192500537999926, 0.9022192500537999926, 0.9022192500537999926, 0.9022192500537999926),
 ( 1.293342249838999924, 1.293342249838999924, 1.293342249838999924, 1.293342249838999924, 1.293342249838999924, 1.293342249838999924, 1.293342249838999924, 1.293342249838999924, 1.293342249838999924, 1.293342249838999924, 1.293342249838999924, 1.293342249838999924, 1.293342249838999924, 1.293342249838999924, 1.293342249838999924, 1.293342249838999924, 1.293342249838999924, 1.293342249838999924, 1.293342249838999924, 1.293342249838999924, 1.293342249838999924, 1.293342249838999924, 1.293342249838999924, 1.293342249838999924, 1.293342249838999924, 1.293342249838999924, 1.293342249838999924) ) ) 
 REPRESENTATION_ITEM ( '' )  SURFACE ( )  );
#19284=EDGE_CURVE ( 'NONE', #9908, #10857, #14125, .T. ) ;
#19287=CARTESIAN_POINT ( 'NONE',  ( 15.81878663761505166, -10.36539687577051261, 0.1259574713066463070 ) ) ;
#19288=CONICAL_SURFACE ( 'NONE', #14260, 13.97499999999999964, 1.402900403544236729 ) ;
#19289=CARTESIAN_POINT ( 'NONE',  ( -15.27343108650000048, 7.751837191927000603, -7.841115722439000457 ) ) ;
#19291=CARTESIAN_POINT ( 'NONE',  ( 8.124934037954998800, -14.44999999999999929, 0.000000000000000000 ) ) ;
#19298=CARTESIAN_POINT ( 'NONE',  ( -15.33118988585713360, 1.667259466958864955, -10.39754702251702767 ) ) ;
#19299=VECTOR ( 'NONE', #11484, 1000.000000000000000 ) ;
#19302=DIRECTION ( 'NONE',  ( 0.000000000000000000, -1.000000000000000000, 0.000000000000000000 ) ) ;
#19303=CARTESIAN_POINT ( 'NONE',  ( 6.274105421348001421, 13.70217340327999445, -0.0001422782095605998798 ) ) ;
#19306=CARTESIAN_POINT ( 'NONE',  ( 17.42999999999999972, 9.118569865760999704, 0.000000000000000000 ) ) ;
#19307=CARTESIAN_POINT ( 'NONE',  ( 12.84468892131000040, 2.447276857699999919, 9.303608529293999396 ) ) ;
#19309=DIRECTION ( 'NONE',  ( -1.000000000000000000, 0.000000000000000000, 0.000000000000000000 ) ) ;
#19310=FACE_BOUND ( 'NONE', #4046, .T. ) ;
#19315=CARTESIAN_POINT ( 'NONE',  ( -14.00000000000000000, 1.396097351027999937E-14, 0.000000000000000000 ) ) ;
#19316=CARTESIAN_POINT ( 'NONE',  ( 14.99328936713000004, -9.056039068417000237, 0.000000000000000000 ) ) ;
#19318=CARTESIAN_POINT ( 'NONE',  ( -23.50032910583999879, -5.270462733209999584, -7.631233524726999562 ) ) ;
#19320=CARTESIAN_POINT ( 'NONE',  ( 18.42637794657805372, 9.567720008368787887, -4.137431501767250275 ) ) ;
#19321=AXIS2_PLACEMENT_3D ( 'NONE', #8884, #10577, #8757 ) ;
#19322=CARTESIAN_POINT ( 'NONE',  ( 12.00000000000000000, -7.836133899445423268, -6.030681244544030761 ) ) ;
#19323=CARTESIAN_POINT ( 'NONE',  ( -14.50000017458758883, -10.95512910623405567, 6.025157725042295631 ) ) ;
#19324=CARTESIAN_POINT ( 'NONE',  ( 24.49298667129999885, -10.14947584299000027, 2.979949436719000033 ) ) ;
#19331=CARTESIAN_POINT ( 'NONE',  ( 22.59859753864000353, -10.40165104099999915, 3.339338359392999944 ) ) ;
#19332=CARTESIAN_POINT ( 'NONE',  ( -2.860127424524721462, 13.08059937058052924, -6.101802095341746224 ) ) ;
#19333=CARTESIAN_POINT ( 'NONE',  ( 24.50000000000000000, 0.000000000000000000, 0.000000000000000000 ) ) ;
#19334=AXIS2_PLACEMENT_3D ( 'NONE', #17087, #11530, #485 ) ;
#19336=CARTESIAN_POINT ( 'NONE',  ( -20.51039254048601279, 3.918938775750210102, -9.746684010221523309 ) ) ;
#19337=CARTESIAN_POINT ( 'NONE',  ( 4.835696606763119298, 14.67450102544439794, 3.769838936156646447 ) ) ;
#19339=CARTESIAN_POINT ( 'NONE',  ( 2.436990620365000471, 11.77112358195999775, -4.345572479020002987 ) ) ;
#19341=CARTESIAN_POINT ( 'NONE',  ( -19.02410030640447758, -7.225764994020523524, -7.707796388380748986 ) ) ;
#19342=DIRECTION ( 'NONE',  ( -1.000000000000000000, 0.000000000000000000, 0.000000000000000000 ) ) ;
#19343=VECTOR ( 'NONE', #6107, 999.9999999999998863 ) ;
#19349=CARTESIAN_POINT ( 'NONE',  ( 16.80728936713000365, -9.102589883624000677, 0.000000000000000000 ) ) ;
#19351=CARTESIAN_POINT ( 'NONE',  ( 18.60131424931000055, 8.248882947719001990, 6.955037127929000640 ) ) ;
#19352=CARTESIAN_POINT ( 'NONE',  ( -20.20485756376000097, 10.40668476090000105, 3.922866990116000263 ) ) ;
#19353=CARTESIAN_POINT ( 'NONE',  ( -17.66049696303999994, -8.440406808323999144, -6.840409896643000920 ) ) ;
#19354=CARTESIAN_POINT ( 'NONE',  ( 0.000000000000000000, 20.10000000000000142, 0.000000000000000000 ) ) ;
#19355=CARTESIAN_POINT ( 'NONE',  ( 18.03681994525999954, -9.876911530946999918, 3.071220598218000308 ) ) ;
#19359=CARTESIAN_POINT ( 'NONE',  ( 24.39431354042982747, 9.829649394705615606, 2.587219325858395311E-05 ) ) ;
#19361=CARTESIAN_POINT ( 'NONE',  ( 0.005043638803689440113, 13.69078929351160134, 6.125306092024061400 ) ) ;
#19363=CARTESIAN_POINT ( 'NONE',  ( -4.723653023056002986, 12.53637152982000913, 0.1248203372519999244 ) ) ;
#19364=CARTESIAN_POINT ( 'NONE',  ( -19.54666243917331769, 4.619757582330495715, -8.015095742238548482 ) ) ;
#19365=CARTESIAN_POINT ( 'NONE',  ( -14.53474671855800793, 0.6128746787797743067, -9.025483422738085793 ) ) ;
#19366=CARTESIAN_POINT ( 'NONE',  ( -19.57601527871000258, -10.43905349783999981, -0.1441279127309000041 ) ) ;
#19367=CARTESIAN_POINT ( 'NONE',  ( 23.99062354302999722, 7.716878364870000340, 11.63397459621999985 ) ) ;
#19369=CARTESIAN_POINT ( 'NONE',  ( 4.143372994309425295, 12.32180263635245687, 2.404628968344424855 ) ) ;
#19372=DIRECTION ( 'NONE',  ( 0.000000000000000000, -1.000000000000000000, 0.000000000000000000 ) ) ;
#19374=DIRECTION ( 'NONE',  ( 0.000000000000000000, 1.000000000000000000, 0.000000000000000000 ) ) ;
#19375=CARTESIAN_POINT ( 'NONE',  ( 18.08325125730999972, 1.019414021290000028, 9.192347282599000025 ) ) ;
#19376=CARTESIAN_POINT ( 'NONE',  ( 24.15736593520906794, 5.143174366503609818, 12.50000000000000355 ) ) ;
#19377=ORIENTED_EDGE ( 'NONE', *, *, #7181, .T. ) ;
#19378=CARTESIAN_POINT ( 'NONE',  ( -22.28593252662366808, -4.096005354656629294, 8.307274234526197176 ) ) ;
#19381=CARTESIAN_POINT ( 'NONE',  ( 3.348931919835092863, 14.23418124123950612, -5.129098008807517317 ) ) ;
#19383=CARTESIAN_POINT ( 'NONE',  ( 0.6016956921910996403, 12.73580660312999946, -6.459985624991999131 ) ) ;
#19384=CARTESIAN_POINT ( 'NONE',  ( 19.42644257295000187, -9.760492247572999602, 5.443783144978000088 ) ) ;
#19387=CARTESIAN_POINT ( 'NONE',  ( 16.73383172034440136, 7.986707523212354332, 6.697168222554745753 ) ) ;
#19389=DIRECTION ( 'NONE',  ( 0.9996708941621516020, 0.02565352539211874019, 0.000000000000000000 ) ) ;
#19390=CARTESIAN_POINT ( 'NONE',  ( -24.47970833437427629, -10.31330985779443488, 7.136763535896974986 ) ) ;
#19392=CARTESIAN_POINT ( 'NONE',  ( 19.05233531832000082, -1.887707665395999879, 10.26617185442000135 ) ) ;
#19393=CARTESIAN_POINT ( 'NONE',  ( 11.29022434644563866, -9.635153832086475134, 8.311371697137628800 ) ) ;
#19397=CARTESIAN_POINT ( 'NONE',  ( -0.4132613886251360058, 12.80949096665309028, 6.652112558386988006 ) ) ;
#19398=CARTESIAN_POINT ( 'NONE',  ( 14.23072219092999902, -10.36232653785000046, -3.715438785038000180 ) ) ;
#19399=CARTESIAN_POINT ( 'NONE',  ( -20.41853216811167826, -5.563930387130748834, 7.399052236490962109 ) ) ;
#19400=CARTESIAN_POINT ( 'NONE',  ( 24.49999999999999289, -0.5123787730663437179, -12.50000000000000000 ) ) ;
#19404=DIRECTION ( 'NONE',  ( 1.000000000000000000, 0.000000000000000000, 0.000000000000000000 ) ) ;
#19407=CARTESIAN_POINT ( 'NONE',  ( -22.34454660583000063, -8.644092610980999680, 4.380640856105999958 ) ) ;
#19409=CARTESIAN_POINT ( 'NONE',  ( 20.90683333333332072, 8.045594964192355647, -4.637336234581411532 ) ) ;
#19410=CARTESIAN_POINT ( 'NONE',  ( 14.97268632185512516, 10.13434347433388893, 2.013073180653659922 ) ) ;
#19411=B_SPLINE_CURVE_WITH_KNOTS ( 'NONE', 3,
 ( #11475, #18497, #5652, #20316, #20670, #7718 ),
 .UNSPECIFIED., .F., .F.,
 ( 4, 1, 1, 4 ),
 ( 0.000000000000000000, 0.3333333333333000081, 0.6666666666667000474, 1.000000000000000000 ),
 .UNSPECIFIED. ) ;
#19412=CARTESIAN_POINT ( 'NONE',  ( -14.94614617458000083, 10.86682107414999976, -1.813459502821000102 ) ) ;
#19415=CARTESIAN_POINT ( 'NONE',  ( -19.96961337912605217, 2.058113591641633100, 10.28927962370347693 ) ) ;
#19416=CARTESIAN_POINT ( 'NONE',  ( -2.677512966247001192, 11.87892984889000303, -3.907459004194998808 ) ) ;
#19417=CARTESIAN_POINT ( 'NONE',  ( -13.84895371062999914, -11.26122607477999971, -0.8537354506236000118 ) ) ;
#19420=VERTEX_POINT ( 'NONE', #12932 ) ;
#19422=CARTESIAN_POINT ( 'NONE',  ( -14.98391979967643728, 10.15505035706891945, -2.115929780933073712 ) ) ;
#19424=CARTESIAN_POINT ( 'NONE',  ( -12.00000000000000000, 1.371604415045000054E-14, 0.000000000000000000 ) ) ;
#19425=CARTESIAN_POINT ( 'NONE',  ( 5.701809914176997118, 14.61127657005998159, -2.263870544078999014 ) ) ;
#19427=CARTESIAN_POINT ( 'NONE',  ( 12.00000000000000178, 0.2542798753839149439, -8.980062289379773688 ) ) ;
#19430=CARTESIAN_POINT ( 'NONE',  ( 12.95437642131000011, -1.177851786523999911, 9.550625374955998836 ) ) ;
#19432=CARTESIAN_POINT ( 'NONE',  ( -10.62189649291999949, -7.518817411396999439, -12.41885835890000145 ) ) ;
#19433=DIRECTION ( 'NONE',  ( 0.000000000000000000, 1.000000000000000000, 0.000000000000000000 ) ) ;
#19434=FILL_AREA_STYLE_COLOUR ( '', #285 ) ;
#19435=B_SPLINE_CURVE_WITH_KNOTS ( 'NONE', 3,
 ( #20955, #4360, #2538, #19126, #17315, #13675, #21070, #4483, #6778, #12367, #15852, #19754, #19631, #5099 ),
 .UNSPECIFIED., .F., .F.,
 ( 4, 2, 2, 2, 2, 2, 4 ),
 ( 0.000000000000000000, 0.2500000000000000555, 0.3750000000000001665, 0.5000000000000002220, 0.6250000000000003331, 0.7500000000000004441, 1.000000000000000000 ),
 .UNSPECIFIED. ) ;
#19436=EDGE_LOOP ( 'NONE', ( #56, #17537, #16843, #8357, #2816 ) ) ;
#19438=CARTESIAN_POINT ( 'NONE',  ( 11.85409292833919714, 13.07924560383835200, 2.346130611937419452 ) ) ;
#19441=CARTESIAN_POINT ( 'NONE',  ( -12.49032736094479290, 6.973667062827473728, -5.693396044204937390 ) ) ;
#19442=CARTESIAN_POINT ( 'NONE',  ( 16.27407586645121640, -0.09550682843461062721, -10.36543807879250956 ) ) ;
#19443=CARTESIAN_POINT ( 'NONE',  ( 11.99999999999999822, -8.311814688850533983, -5.425963580743933257 ) ) ;
#19446=CARTESIAN_POINT ( 'NONE',  ( 22.43704471257999700, 0.6835673466426999134, 11.23757390362000130 ) ) ;
#19449=CARTESIAN_POINT ( 'NONE',  ( 12.50898080071999985, 6.466862063081999956, -12.35567184454000156 ) ) ;
#19451=ORIENTED_EDGE ( 'NONE', *, *, #16904, .T. ) ;
#19452=CARTESIAN_POINT ( 'NONE',  ( 23.17835033931999789, 1.382018527918999817, -10.85292862796000080 ) ) ;
#19453=CARTESIAN_POINT ( 'NONE',  ( 23.70405517126128458, 5.919522458329209869, -8.807685190096355754 ) ) ;
#19456=CARTESIAN_POINT ( 'NONE',  ( 4.849422839656808648, 14.57858754772911603, 3.779267820556795332 ) ) ;
#19458=CONICAL_SURFACE ( 'NONE', #19855, 12.68487026514999982, 0.6105562205522639951 ) ;
#19459=CARTESIAN_POINT ( 'NONE',  ( -4.488611054452003479, 12.34747560695998558, -2.085835349536002248 ) ) ;
#19460=ORIENTED_EDGE ( 'NONE', *, *, #3025, .T. ) ;
#19461=CARTESIAN_POINT ( 'NONE',  ( -15.73057431336374101, -9.936106390668207666, 3.494968291668457905 ) ) ;
#19463=DIRECTION ( 'NONE',  ( -1.000000000000000000, 0.000000000000000000, 0.000000000000000000 ) ) ;
#19465=EDGE_CURVE ( 'NONE', #10425, #2252, #53, .T. ) ;
#19468=CARTESIAN_POINT ( 'NONE',  ( -4.364690642044310565, 15.35159745129469755, -4.297429366192518252 ) ) ;
#19469=CARTESIAN_POINT ( 'NONE',  ( -22.93483120822000032, -10.59336881657999996, -3.621420100782999807 ) ) ;
#19471=CARTESIAN_POINT ( 'NONE',  ( -17.05110591912999851, 10.19050343432999917, -3.717068697430999880 ) ) ;
#19472=CARTESIAN_POINT ( 'NONE',  ( -6.218877990892996976, 16.13966241814000213, 0.9717607918608996975 ) ) ;
#19474=CARTESIAN_POINT ( 'NONE',  ( 13.36494494526000132, 7.290979141362999627, -7.150624518174999444 ) ) ;
#19475=CARTESIAN_POINT ( 'NONE',  ( 5.302302355349000074, 1.578914512950999657E-14, -14.43375672973994917 ) ) ;
#19477=DIRECTION ( 'NONE',  ( -0.7071067811865474617, 0.7071067811865474617, 0.000000000000000000 ) ) ;
#19485=CARTESIAN_POINT ( 'NONE',  ( -14.50687460260128425, 1.490768935493058889, -8.918514818220842244 ) ) ;
#19487=EDGE_CURVE ( 'NONE', #18434, #8639, #1390, .T. ) ;
#19489=LINE ( 'NONE', #19367, #8086 ) ;
#19490=VERTEX_POINT ( 'NONE', #2269 ) ;
#19492=CARTESIAN_POINT ( 'NONE',  ( 3.928282035707792552, 12.12595830749078374, -2.822092405151465755 ) ) ;
#19495=FACE_OUTER_BOUND ( 'NONE', #15825, .T. ) ;
#19496=CARTESIAN_POINT ( 'NONE',  ( -11.82164471169000208, -0.5931465403154000393, 15.55754198224000007 ) ) ;
#19497=CARTESIAN_POINT ( 'NONE',  ( -13.44269301469999967, -0.9911996677733001526, -11.23901760903999936 ) ) ;
#19498=CARTESIAN_POINT ( 'NONE',  ( 15.99918875730999979, 7.956028365285000348, 4.607548929765999723 ) ) ;
#19499=CARTESIAN_POINT ( 'NONE',  ( 18.93524367559212607, 2.269347932775633403, 10.18482703568339787 ) ) ;
#19504=CARTESIAN_POINT ( 'NONE',  ( 0.2037756909558023355, 13.66463196969724869, -6.169302963772167026 ) ) ;
#19509=DIRECTION ( 'NONE',  ( -1.000000000000000000, 0.000000000000000000, 0.000000000000000000 ) ) ;
#19511=CARTESIAN_POINT ( 'NONE',  ( 14.22488390888686105, -1.430681673238417106, -10.26079249266155280 ) ) ;
#19514=AXIS2_PLACEMENT_3D ( 'NONE', #136, #15029, #14908 ) ;
#19517=CARTESIAN_POINT ( 'NONE',  ( -24.50000000000000000, -8.081477262649000792, -6.807253044743999837 ) ) ;
#19518=CARTESIAN_POINT ( 'NONE',  ( 12.52688711657000020, -7.716878364870000340, 11.63397459621999985 ) ) ;
#19522=CARTESIAN_POINT ( 'NONE',  ( 3.577690694476612254, 13.23335103741512775, 5.763370895648841419 ) ) ;
#19524=CARTESIAN_POINT ( 'NONE',  ( 6.152345744605784539, 14.11688686930400927, -0.2931242286481389181 ) ) ;
#19525=CARTESIAN_POINT ( 'NONE',  ( -20.88996149064833929, 7.734893377964897176, 5.108810731787540860 ) ) ;
#19526=DIRECTION ( 'NONE',  ( 0.9996708941621507138, 0.02565352539215873945, 0.000000000000000000 ) ) ;
#19529=CIRCLE ( 'NONE', #1357, 13.93375672974000068 ) ;
#19531=CARTESIAN_POINT ( 'NONE',  ( -19.10482910584000038, 1.458613477275000161E-14, 0.000000000000000000 ) ) ;
#19532=ORIENTED_EDGE ( 'NONE', *, *, #13562, .T. ) ;
#19533=CARTESIAN_POINT ( 'NONE',  ( -20.01793400091000308, 5.566461610995999898, -8.487890939669000545 ) ) ;
#19536=CARTESIAN_POINT ( 'NONE',  ( 14.95177042847206117, 10.28604982897092235, 1.247623827059667345 ) ) ;
#19539=FACE_OUTER_BOUND ( 'NONE', #2400, .T. ) ;
#19540=CARTESIAN_POINT ( 'NONE',  ( -22.33796067008437447, -9.002300166801388670, 2.420455048598586512 ) ) ;
#19541=CARTESIAN_POINT ( 'NONE',  ( -4.341996183777002472, 12.31336825867998641, -2.011830581554000297 ) ) ;
#19542=ORIENTED_EDGE ( 'NONE', *, *, #14392, .F. ) ;
#19543=CARTESIAN_POINT ( 'NONE',  ( -13.23956266673000037, 6.512279107760999608, -9.204720484723999618 ) ) ;
#19548=CARTESIAN_POINT ( 'NONE',  ( -14.40513632270981681, -2.351574831385553566, 10.08995167311471874 ) ) ;
#19551=CARTESIAN_POINT ( 'NONE',  ( 5.749772404096996858, 14.16353669839999441, -1.990178937412000471 ) ) ;
#19555=CARTESIAN_POINT ( 'NONE',  ( 12.65175158531000044, 9.909822556590000886, -2.072115565883000166 ) ) ;
#19556=ORIENTED_EDGE ( 'NONE', *, *, #13487, .F. ) ;
#19560=ORIENTED_EDGE ( 'NONE', *, *, #19584, .F. ) ;
#19562=CARTESIAN_POINT ( 'NONE',  ( 11.55284350195684340, 12.59061462091154837, 3.192208964413439709 ) ) ;
#19563=CARTESIAN_POINT ( 'NONE',  ( -23.50032910583999879, 3.801543240379000377, -8.459419100777001432 ) ) ;
#19564=AXIS2_PLACEMENT_3D ( 'NONE', #22846, #17163, #20683 ) ;
#19565=CARTESIAN_POINT ( 'NONE',  ( -5.091020417477109206, 13.90168003929542273, -5.423969081848736273 ) ) ;
#19566=CARTESIAN_POINT ( 'NONE',  ( 16.49585459645880192, 7.156609457148421782, -7.549996209224957511 ) ) ;
#19567=CARTESIAN_POINT ( 'NONE',  ( 23.99062354302999722, -7.716878364870000340, -11.63397459621999985 ) ) ;
#19569=CARTESIAN_POINT ( 'NONE',  ( -14.47826291725376358, 11.73192043637804893, -4.679722760534376746 ) ) ;
#19570=CARTESIAN_POINT ( 'NONE',  ( -3.826948838359951477, 14.04946500315414148, -4.851233642384933376 ) ) ;
#19573=CARTESIAN_POINT ( 'NONE',  ( -24.36724102301948847, -2.559142463821917346, 12.49991998441870145 ) ) ;
#19574=CARTESIAN_POINT ( 'NONE',  ( 19.89308446879999792, 10.49337901864999978, -2.757826031130999667 ) ) ;
#19575=CARTESIAN_POINT ( 'NONE',  ( 24.38501637916864340, 2.018571612540227544, 10.43313927157142729 ) ) ;
#19577=ORIENTED_EDGE ( 'NONE', *, *, #20092, .F. ) ;
#19578=CARTESIAN_POINT ( 'NONE',  ( -20.43006341542451310, 6.446850357970787648, -8.297382802253483902 ) ) ;
#19580=CARTESIAN_POINT ( 'NONE',  ( -24.46742986865170622, -11.46616815103349118, -5.140026613645124698 ) ) ;
#19582=CARTESIAN_POINT ( 'NONE',  ( -2.805898255323001411, 11.85722042793000952, -4.087626962984003853 ) ) ;
#19584=EDGE_CURVE ( 'NONE', #11532, #13012, #18761, .T. ) ;
#19585=CARTESIAN_POINT ( 'NONE',  ( -16.54000019300971402, 10.40780738326815680, -0.02728000515637632115 ) ) ;
#19588=CARTESIAN_POINT ( 'NONE',  ( -14.43045987140080300, -3.231330187232687834, -12.49999333233078325 ) ) ;
#19589=ORIENTED_EDGE ( 'NONE', *, *, #896, .F. ) ;
#19591=CARTESIAN_POINT ( 'NONE',  ( -12.09893706263999924, 13.67685060524999940, -6.159850446377999056 ) ) ;
#19592=CARTESIAN_POINT ( 'NONE',  ( -21.97131109840999841, 9.664045591200999041, 5.599833161489999434 ) ) ;
#19593=ADVANCED_FACE ( 'NONE', ( #17043 ), #16921, .F. ) ;
#19594=CARTESIAN_POINT ( 'NONE',  ( -17.52341705246000103, 5.107418338671999791, -8.973179355929001844 ) ) ;
#19595=CARTESIAN_POINT ( 'NONE',  ( 22.04058333333331987, -8.996523669780138732, -2.417618220618300562 ) ) ;
#19596=CARTESIAN_POINT ( 'NONE',  ( 17.22431994525999954, 10.31730248877000022, 0.2667559614094999754 ) ) ;
#19597=FACE_OUTER_BOUND ( 'NONE', #21366, .T. ) ;
#19600=CARTESIAN_POINT ( 'NONE',  ( 19.87622032598000033, -3.917852614669999234, 8.831257209013999798 ) ) ;
#19601=CARTESIAN_POINT ( 'NONE',  ( 15.35145833333333165, 5.570917836446059646, -7.249253927134781783 ) ) ;
#19603=CARTESIAN_POINT ( 'NONE',  ( 2.263570575011602859, 13.94136812588888041, 5.692591906759779441 ) ) ;
#19605=ADVANCED_FACE ( 'NONE', ( #5899 ), #4871, .F. ) ;
#19606=CARTESIAN_POINT ( 'NONE',  ( -19.50887077250665413, 5.636661757442777976, -7.334388769936609265 ) ) ;
#19607=CARTESIAN_POINT ( 'NONE',  ( -14.24706062280937502, 7.999159735059844678, -4.368120482967156271 ) ) ;
#19609=CARTESIAN_POINT ( 'NONE',  ( -4.744723115955535420, 12.41001117572974088, 0.9970819178471495015 ) ) ;
#19611=ADVANCED_FACE ( 'NONE', ( #15212 ), #687, .T. ) ;
#19612=CARTESIAN_POINT ( 'NONE',  ( 4.724609123937420385, 12.40245730446895323, -1.087195817531082076 ) ) ;
#19613=CARTESIAN_POINT ( 'NONE',  ( -3.963044985152003097, 14.56862624118001825, 4.679621608874002803 ) ) ;
#19614=EDGE_CURVE ( 'NONE', #17324, #20493, #11432, .T. ) ;
#19616=CARTESIAN_POINT ( 'NONE',  ( 11.49246134983401113, -8.135562067959659416, -3.829935661804423130 ) ) ;
#19619=CARTESIAN_POINT ( 'NONE',  ( -6.115711741633154119, 15.99577490368180044, -1.049722815977955026 ) ) ;
#19620=CARTESIAN_POINT ( 'NONE',  ( 14.81906392131000061, -2.842327771818999871, 9.244929856806999524 ) ) ;
#19621=CARTESIAN_POINT ( 'NONE',  ( 24.50000000000000000, 10.82531754731000007, -6.250000000000000000 ) ) ;
#19624=CARTESIAN_POINT ( 'NONE',  ( -22.34263658169068378, -2.418798806450678907, 9.002255236133725802 ) ) ;
#19626=CARTESIAN_POINT ( 'NONE',  ( -15.23841243917333266, 2.371928265978177741, 8.826509812641717190 ) ) ;
#19627=CARTESIAN_POINT ( 'NONE',  ( -6.250000000000000000, 16.31160201366999729, -2.000000000000000000 ) ) ;
#19630=CARTESIAN_POINT ( 'NONE',  ( -5.833999999999999631, 1.198997689148999791E-14, -12.89775331292463711 ) ) ;
#19631=CARTESIAN_POINT ( 'NONE',  ( -24.50000000000293099, 11.08154813084197698, -5.806195610872452839 ) ) ;
#19633=CARTESIAN_POINT ( 'NONE',  ( -12.50000000000000000, 6.606768802097000126, -6.099810110451000966 ) ) ;
#19635=CARTESIAN_POINT ( 'NONE',  ( -4.239658300008966485, 13.64990765111504167, 4.928031708687682588 ) ) ;
#19637=CARTESIAN_POINT ( 'NONE',  ( 20.01958103379666198, -1.202189832516999735, 9.185023618884988750 ) ) ;
#19642=ADVANCED_FACE ( 'NONE', ( #2508 ), #13643, .T. ) ;
#19643=CARTESIAN_POINT ( 'NONE',  ( 5.639929954731005779, 14.19535997545999351, 2.283685262506000235 ) ) ;
#19644=DIRECTION ( 'NONE',  ( -1.000000000000000000, 0.000000000000000000, 0.000000000000000000 ) ) ;
#19647=CARTESIAN_POINT ( 'NONE',  ( 6.232362344166777035, 13.72735485794549426, -1.446143930354119922 ) ) ;
#19648=DIRECTION ( 'NONE',  ( -1.000000000000000000, 0.000000000000000000, 0.000000000000000000 ) ) ;
#19652=CARTESIAN_POINT ( 'NONE',  ( -20.21721940389334193, -9.008888981094067105, 2.097083988089771811 ) ) ;
#19654=EDGE_CURVE ( 'NONE', #44, #7629, #5250, .T. ) ;
#19655=CARTESIAN_POINT ( 'NONE',  ( -24.73275700429000068, -10.85635561503000091, -0.8019128780756998864 ) ) ;
#19656=EDGE_CURVE ( 'NONE', #2037, #8899, #15659, .T. ) ;
#19657=CARTESIAN_POINT ( 'NONE',  ( 20.75566666666665583, 4.635148009726169249, -8.042302503330198249 ) ) ;
#19658=CARTESIAN_POINT ( 'NONE',  ( 15.06172671233659699, 9.055098203261204404, 4.981601320280216960 ) ) ;
#19659=DIRECTION ( 'NONE',  ( 1.000000000000000000, 0.000000000000000000, 0.000000000000000000 ) ) ;
#19661=CARTESIAN_POINT ( 'NONE',  ( -22.98076624016430713, 7.404256252206974587, 5.690969114276820839 ) ) ;
#19662=CARTESIAN_POINT ( 'NONE',  ( -1.402221074164999637, 11.71985185161000587, -4.549932804316000556 ) ) ;
#19664=AXIS2_PLACEMENT_3D ( 'NONE', #13516, #6367, #11829 ) ;
#19666=CARTESIAN_POINT ( 'NONE',  ( -24.43680486115877670, -9.658061704670100056, -3.574636863997652902 ) ) ;
#19669=CARTESIAN_POINT ( 'NONE',  ( -6.046835300290999804, 16.30334124114000360, 1.000000020649999932 ) ) ;
#19670=CARTESIAN_POINT ( 'NONE',  ( -17.41481040294117122, -7.305510571727924507, -7.454128842472707461 ) ) ;
#19671=ORIENTED_EDGE ( 'NONE', *, *, #18565, .F. ) ;
#19674=CARTESIAN_POINT ( 'NONE',  ( 5.383802162386005286, 13.84993582567999582, -3.902720988293997717 ) ) ;
#19675=CARTESIAN_POINT ( 'NONE',  ( 12.00000000000000355, -2.741782068716092535, -8.563895310330577715 ) ) ;
#19676=CARTESIAN_POINT ( 'NONE',  ( 17.54649695406000021, -10.67134204638000128, -3.051581116462999788 ) ) ;
#19677=CARTESIAN_POINT ( 'NONE',  ( 14.40675158531000122, 9.325397517960999139, -4.058504152148000088 ) ) ;
#19679=DIRECTION ( 'NONE',  ( 1.000000000000000000, 0.000000000000000000, 0.000000000000000000 ) ) ;
#19681=CARTESIAN_POINT ( 'NONE',  ( 0.000000000000000000, 14.43375672974000068, 0.000000000000000000 ) ) ;
#19684=CARTESIAN_POINT ( 'NONE',  ( 24.47069144955800368, -7.568636691949420126, 7.463144728829862018 ) ) ;
#19685=CARTESIAN_POINT ( 'NONE',  ( -13.99999999999999645, 3.409677747946862070, 8.987483889666412651 ) ) ;
#19686=CARTESIAN_POINT ( 'NONE',  ( 17.28855324646004021, -3.723961278307348799, 9.741530358186297534 ) ) ;
#19687=CARTESIAN_POINT ( 'NONE',  ( -19.05537077250666300, 7.325082484084620482, 5.629509844743244784 ) ) ;
#19689=CARTESIAN_POINT ( 'NONE',  ( -14.49454819745152356, 10.30763366379271062, -7.146668779517979964 ) ) ;
#19691=CONICAL_SURFACE ( 'NONE', #10791, 9.136555860486998526, 0.02565634000431304615 ) ;
#19692=CARTESIAN_POINT ( 'NONE',  ( -4.218945794843817154, 13.66537927080853976, -4.919477749078775553 ) ) ;
#19696=CARTESIAN_POINT ( 'NONE',  ( 21.82559380440000396, 10.77499779627999921, 1.666852620760000070 ) ) ;
#19697=CARTESIAN_POINT ( 'NONE',  ( 23.76080193858683742, 7.519392389711364366, -7.487444224767115131 ) ) ;
#19698=CARTESIAN_POINT ( 'NONE',  ( 12.00000000000000000, 10.65000000000000036, 0.000000000000000000 ) ) ;
#19700=ORIENTED_EDGE ( 'NONE', *, *, #9489, .T. ) ;
#19702=CARTESIAN_POINT ( 'NONE',  ( 4.852944915824914496, 14.55942026833422354, 3.781726298951809451 ) ) ;
#19703=B_SPLINE_CURVE_WITH_KNOTS ( 'NONE', 3,
 ( #1660, #7822, #9167, #12910, #22348, #9518, #15192, #9403, #2129, #14836, #20780, #18487, #5641, #7705, #13152, #20659, #13027, #11232 ),
 .UNSPECIFIED., .F., .F.,
 ( 4, 2, 2, 2, 2, 2, 2, 2, 4 ),
 ( 0.000000000000000000, 0.1249999999999999722, 0.2500000000000000000, 0.3750000000000000000, 0.5000000000000001110, 0.6250000000000001110, 0.7500000000000000000, 0.8750000000000000000, 1.000000000000000000 ),
 .UNSPECIFIED. ) ;
#19704=DIRECTION ( 'NONE',  ( -1.000000000000000000, 0.000000000000000000, 0.000000000000000000 ) ) ;
#19705=ORIENTED_EDGE ( 'NONE', *, *, #2464, .F. ) ;
#19707=CARTESIAN_POINT ( 'NONE',  ( -15.20026080601097540, -0.7701753238851960504, -10.34310266448994042 ) ) ;
#19708=LINE ( 'NONE', #21757, #20041 ) ;
#19711=CARTESIAN_POINT ( 'NONE',  ( 3.000000000000000000, 17.00000000000000000, 0.000000000000000000 ) ) ;
#19713=DIRECTION ( 'NONE',  ( -1.000000000000000000, 0.000000000000000000, 0.000000000000000000 ) ) ;
#19717=CARTESIAN_POINT ( 'NONE',  ( -12.23285353330000014, 13.67685060524999940, -6.159850446377999056 ) ) ;
#19718=CARTESIAN_POINT ( 'NONE',  ( -24.86648035909999876, 8.837410641880000028, -3.973955761889000016 ) ) ;
#19719=CARTESIAN_POINT ( 'NONE',  ( -18.67614870288999995, 10.39069081642000114, 3.268177410067999666 ) ) ;
#19720=CARTESIAN_POINT ( 'NONE',  ( -6.314291400897996454, 15.85600325500998942, 1.061606865039998571 ) ) ;
#19721=CARTESIAN_POINT ( 'NONE',  ( 17.83369494525999954, -5.541591344052999801, 8.726939668821000140 ) ) ;
#19722=CARTESIAN_POINT ( 'NONE',  ( -14.25699038479000080, -13.93375672974000068, -0.1440397836109000018 ) ) ;
#19723=CARTESIAN_POINT ( 'NONE',  ( 20.93851493891000004, 7.913501176053999053, -5.593456792387000220 ) ) ;
#19724=CIRCLE ( 'NONE', #8114, 10.65000000000000036 ) ;
#19726=CARTESIAN_POINT ( 'NONE',  ( 24.37713355803436599, -9.330746210554012876, 8.838673490789293652 ) ) ;
#19727=ORIENTED_EDGE ( 'NONE', *, *, #8923, .T. ) ;
#19728=CARTESIAN_POINT ( 'NONE',  ( 23.50918822630940141, 3.211384162367111550, 8.722405065347860642 ) ) ;
#19729=CARTESIAN_POINT ( 'NONE',  ( -1.736679406361667288, 13.83192101583320444, 5.887765559668492799 ) ) ;
#19733=CARTESIAN_POINT ( 'NONE',  ( -20.07574577250665016, -8.947317243346674331, -2.404655041047230934 ) ) ;
#19734=CARTESIAN_POINT ( 'NONE',  ( -19.74309982448999889, -9.328357949534000326, 5.911015106955000320 ) ) ;
#19735=CARTESIAN_POINT ( 'NONE',  ( -4.000693775878768399, 12.14919889384218443, 2.720895155930553866 ) ) ;
#19738=CARTESIAN_POINT ( 'NONE',  ( 4.469428354791611824, 12.30899859160570031, -1.869002996406054384 ) ) ;
#19742=DIRECTION ( 'NONE',  ( 0.000000000000000000, -1.000000000000000000, 0.000000000000000000 ) ) ;
#19743=CARTESIAN_POINT ( 'NONE',  ( -14.66147510250999808, 10.41001213865000175, 4.437054729469999792 ) ) ;
#19744=CARTESIAN_POINT ( 'NONE',  ( 18.21937642130999890, 4.597142045420999246, 8.611084490720001483 ) ) ;
#19745=CARTESIAN_POINT ( 'NONE',  ( 18.80775289361148239, 6.404165465825992776, 8.237156442842801241 ) ) ;
#19746=ORIENTED_EDGE ( 'NONE', *, *, #5047, .F. ) ;
#19750=CARTESIAN_POINT ( 'NONE',  ( -2.447170124667294555, 13.98365479988347282, -5.615010659020613026 ) ) ;
#19754=CARTESIAN_POINT ( 'NONE',  ( -24.48376588670971543, 11.33649700730286192, -5.364757780030492640 ) ) ;
#19755=EDGE_CURVE ( 'NONE', #1014, #14850, #12215, .T. ) ;
#19756=CARTESIAN_POINT ( 'NONE',  ( 15.65379166666666677, 9.072988859205175061, 1.187524516768785787 ) ) ;
#19758=CARTESIAN_POINT ( 'NONE',  ( 15.56298940832826894, -10.15326298562161789, 2.230701886652393551 ) ) ;
#19760=CARTESIAN_POINT ( 'NONE',  ( -4.944239625353997525, 12.51416432517001809, 0.1304284014165000838 ) ) ;
#19761=DIRECTION ( 'NONE',  ( -0.9865822012466877178, 0.000000000000000000, 0.1632653061223979518 ) ) ;
#19762=ORIENTED_EDGE ( 'NONE', *, *, #2254, .F. ) ;
#19765=ORIENTED_EDGE ( 'NONE', *, *, #10903, .T. ) ;
#19767=CARTESIAN_POINT ( 'NONE',  ( 4.903442944881004628, 14.89392636350999233, 3.684989539199001296 ) ) ;
#19769=CARTESIAN_POINT ( 'NONE',  ( 1.401856813186208361, 12.86851491854003449, 6.537411608044383371 ) ) ;
#19770=CARTESIAN_POINT ( 'NONE',  ( 19.75000000000000000, -1.659811535170000019, 9.026773995975998943 ) ) ;
#19771=CARTESIAN_POINT ( 'NONE',  ( 13.50000000000000000, 2.048741218006000064, 10.08990150394999930 ) ) ;
#19772=CARTESIAN_POINT ( 'NONE',  ( -6.042815832213999983, 16.39253418350000047, -0.9999999878869999526 ) ) ;
#19777=DIRECTION ( 'NONE',  ( 0.000000000000000000, 1.000000000000000000, 0.000000000000000000 ) ) ;
#19779=CARTESIAN_POINT ( 'NONE',  ( -21.11865610815000238, -7.328638157174999890, 7.800684107840000436 ) ) ;
#19780=CARTESIAN_POINT ( 'NONE',  ( 11.50000000000000000, -7.000000000000000000, 0.000000000000000000 ) ) ;
#19781=CARTESIAN_POINT ( 'NONE',  ( 15.23271754047294557, 4.697833125319701431, 9.209713511118009066 ) ) ;
#19782=PLANE ( 'NONE',  #14869 ) ;
#19785=CARTESIAN_POINT ( 'NONE',  ( -22.75389368601540951, 1.211706322581030504, 9.258003830841628812 ) ) ;
#19787=CARTESIAN_POINT ( 'NONE',  ( 4.738215136157003293, 12.61383557389999766, 0.1055552163494999779 ) ) ;
#19788=ORIENTED_EDGE ( 'NONE', *, *, #10008, .T. ) ;
#19789=CARTESIAN_POINT ( 'NONE',  ( -21.99722087121331526, -5.675724701917319592, -7.385631801182315215 ) ) ;
#19791=DIRECTION ( 'NONE',  ( 0.000000000000000000, 1.000000000000000000, 0.000000000000000000 ) ) ;
#19792=CARTESIAN_POINT ( 'NONE',  ( 8.124934037954998800, 10.59999999999999964, 0.000000000000000000 ) ) ;
#19793=ORIENTED_EDGE ( 'NONE', *, *, #42, .T. ) ;
#19794=CARTESIAN_POINT ( 'NONE',  ( 11.06619116163224170, -10.57612823871417973, -6.681605107878366923 ) ) ;
#19795=EDGE_CURVE ( 'NONE', #15508, #19254, #4662, .T. ) ;
#19796=CARTESIAN_POINT ( 'NONE',  ( 12.00000000000000000, 3.318092558720092899, -8.344102286361790632 ) ) ;
#19797=EDGE_CURVE ( 'NONE', #11336, #12531, #12613, .T. ) ;
#19798=CARTESIAN_POINT ( 'NONE',  ( 17.94122805071000215, 6.114706615795999944, -9.275782954962000559 ) ) ;
#19799=CARTESIAN_POINT ( 'NONE',  ( 19.04006424931000296, -6.376715009848999749, 8.397789983599000863 ) ) ;
#19800=EDGE_LOOP ( 'NONE', ( #5887, #3916, #21862 ) ) ;
#19801=CARTESIAN_POINT ( 'NONE',  ( -9.400026492921000454, -14.37830284610000042, 2.006256508544999484 ) ) ;
#19802=DIRECTION ( 'NONE',  ( 0.000000000000000000, 0.000000000000000000, 1.000000000000000000 ) ) ;
#19804=ORIENTED_EDGE ( 'NONE', *, *, #3047, .T. ) ;
#19805=FACE_OUTER_BOUND ( 'NONE', #12896, .T. ) ;
#19806=CARTESIAN_POINT ( 'NONE',  ( 21.38215989470702993, -4.982371934643452960, -9.480591854900188409 ) ) ;
#19808=CARTESIAN_POINT ( 'NONE',  ( 16.78527092655545516, 10.20993882797034580, 1.972386044144941231 ) ) ;
#19809=DIRECTION ( 'NONE',  ( 0.000000000000000000, 1.000000000000000000, 0.000000000000000000 ) ) ;
#19811=B_SPLINE_CURVE_WITH_KNOTS ( 'NONE', 3,
 ( #14192, #17838, #21340, #15872 ),
 .UNSPECIFIED., .F., .F.,
 ( 4, 4 ),
 ( 0.000000000000000000, 1.000000000000000000 ),
 .UNSPECIFIED. ) ;
#19812=CARTESIAN_POINT ( 'NONE',  ( -12.00000000000000000, 7.000000000000000000, 0.000000000000000000 ) ) ;
#19814=EDGE_LOOP ( 'NONE', ( #1144, #13841, #21564, #6096 ) ) ;
#19815=CARTESIAN_POINT ( 'NONE',  ( 23.73993940136630698, -9.222267920518611106, 1.215187501975043327 ) ) ;
#19816=CARTESIAN_POINT ( 'NONE',  ( 11.59051697471513442, 12.65550321735096340, -3.079847694010941606 ) ) ;
#19819=VERTEX_POINT ( 'NONE', #12004 ) ;
#19820=DIRECTION ( 'NONE',  ( -1.000000000000000000, 0.000000000000000000, 0.000000000000000000 ) ) ;
#19821=CARTESIAN_POINT ( 'NONE',  ( -5.158992055378997854, 13.96222552554998764, 5.500780647236995335 ) ) ;
#19822=CARTESIAN_POINT ( 'NONE',  ( 4.942230045011000605, 12.51340480292000024, 0.1092162673837999420 ) ) ;
#19823=VERTEX_POINT ( 'NONE', #842 ) ;
#19824=LINE ( 'NONE', #16403, #1075 ) ;
#19828=CARTESIAN_POINT ( 'NONE',  ( -23.75856372112270520, -13.93375672973999890, -0.09623564068393683502 ) ) ;
#19829=VERTEX_POINT ( 'NONE', #10182 ) ;
#19831=CARTESIAN_POINT ( 'NONE',  ( -12.34499313601000026, 9.613013645102999050, -12.04164784824000023 ) ) ;
#19832=CARTESIAN_POINT ( 'NONE',  ( -23.95495283385999841, -2.336932850305999843, 9.912667528692999497 ) ) ;
#19833=CARTESIAN_POINT ( 'NONE',  ( -16.91402600854999960, 5.062459437026999964, 8.979130132666000463 ) ) ;
#19834=CARTESIAN_POINT ( 'NONE',  ( -6.313141446900004894, 16.43093356584002862, 1.007231585192000400 ) ) ;
#19835=CARTESIAN_POINT ( 'NONE',  ( -22.98062309160115291, -9.860450425915699313, -3.810151497938129683 ) ) ;
#19837=CYLINDRICAL_SURFACE ( 'NONE', #22790, 12.44999999999999929 ) ;
#19839=ORIENTED_EDGE ( 'NONE', *, *, #10719, .T. ) ;
#19840=CARTESIAN_POINT ( 'NONE',  ( 23.54441667850668551, 2.130327776482009661, 9.046710258410779915 ) ) ;
#19847=DIRECTION ( 'NONE',  ( -0.9996708941621513800, 0.02565352539212875996, 1.659533453806920987E-14 ) ) ;
#19848=CARTESIAN_POINT ( 'NONE',  ( 3.033043484777522281, 11.87036368078775617, -3.754604677876629548 ) ) ;
#19849=LINE ( 'NONE', #16317, #20397 ) ;
#19850=CARTESIAN_POINT ( 'NONE',  ( 11.58073079862069221, -6.605128734743197505, -6.105076039591643244 ) ) ;
#19853=CARTESIAN_POINT ( 'NONE',  ( -7.034000000000000696, 1.310788454998999989E-14, 0.000000000000000000 ) ) ;
#19855=AXIS2_PLACEMENT_3D ( 'NONE', #9481, #17104, #1978 ) ;
#19856=CARTESIAN_POINT ( 'NONE',  ( 12.51562642131000125, 9.466654096131000173, 1.662047859332999922 ) ) ;
#19857=CARTESIAN_POINT ( 'NONE',  ( 18.81849951495625106, 6.078002649393266843, 8.477670823501638253 ) ) ;
#19859=CARTESIAN_POINT ( 'NONE',  ( 5.180641154517307001, 13.94961545970955186, 4.027129678755727582 ) ) ;
#19861=FACE_OUTER_BOUND ( 'NONE', #6316, .T. ) ;
#19862=CARTESIAN_POINT ( 'NONE',  ( 13.49999999999999822, -9.686451367697159753, 0.6268225021301814248 ) ) ;
#19863=ORIENTED_EDGE ( 'NONE', *, *, #23465, .T. ) ;
#19866=DIRECTION ( 'NONE',  ( -1.000000000000000000, 0.000000000000000000, 0.000000000000000000 ) ) ;
#19868=CARTESIAN_POINT ( 'NONE',  ( -23.79921766892433510, -7.721186627919117029, 5.741329154560525616 ) ) ;
#19869=CARTESIAN_POINT ( 'NONE',  ( 14.69879627327239824, 10.34603584791903508, -0.7108216309658257348 ) ) ;
#19873=ORIENTED_EDGE ( 'NONE', *, *, #7583, .F. ) ;
#19879=CARTESIAN_POINT ( 'NONE',  ( 13.65000000000000036, 1.057482511063999969E-14, 0.000000000000000000 ) ) ;
#19880=CARTESIAN_POINT ( 'NONE',  ( 11.36701043059877847, -2.759410678255084015, -12.49996441860402463 ) ) ;
#19882=CARTESIAN_POINT ( 'NONE',  ( 19.28616666666667712, 9.166202760740587152, 1.338597607047040894 ) ) ;
#19884=EDGE_CURVE ( 'NONE', #7890, #4095, #21106, .T. ) ;
#19888=DIRECTION ( 'NONE',  ( 0.000000000000000000, -0.8975663802247816347, -0.4408793407386908392 ) ) ;
#19889=DIRECTION ( 'NONE',  ( -1.000000000000000000, 0.000000000000000000, 0.000000000000000000 ) ) ;
#19891=CARTESIAN_POINT ( 'NONE',  ( -23.51779040664999698, 10.29309294087000026, 3.164445037656999915 ) ) ;
#19892=CARTESIAN_POINT ( 'NONE',  ( 20.86904166666665716, 7.362300873902134946, -5.658112305383654395 ) ) ;
#19893=CARTESIAN_POINT ( 'NONE',  ( 14.54704717614944798, 2.944910552188379160, -9.893351561282216267 ) ) ;
#19895=CARTESIAN_POINT ( 'NONE',  ( 21.55623526383000055, 5.754856272286999364, -9.648219475427001868 ) ) ;
#19898=CARTESIAN_POINT ( 'NONE',  ( 13.60028472826950541, 6.915518368012416595, -5.791054742020698143 ) ) ;
#19899=CARTESIAN_POINT ( 'NONE',  ( -2.101269504238999275, 11.75436161677999536, -4.249028463402999556 ) ) ;
#19901=CARTESIAN_POINT ( 'NONE',  ( -14.00000000000000000, -8.319952449050001420, 6.066771132503999020 ) ) ;
#19902=VERTEX_POINT ( 'NONE', #22638 ) ;
#19911=CIRCLE ( 'NONE', #19123, 1.000000000000000666 ) ;
#19912=CARTESIAN_POINT ( 'NONE',  ( 24.50000000000000000, 4.174438572590999431E-14, -12.50000000000000000 ) ) ;
#19914=EDGE_CURVE ( 'NONE', #17699, #21250, #13601, .T. ) ;
#19916=CARTESIAN_POINT ( 'NONE',  ( -8.883540065846000644, 13.80244821480000006, -4.188663184106999893 ) ) ;
#19917=CARTESIAN_POINT ( 'NONE',  ( 13.49999999999999822, 7.584517159776716255, 6.431457497586518635 ) ) ;
#19918=DIRECTION ( 'NONE',  ( 0.000000000000000000, 0.000000000000000000, 1.000000000000000000 ) ) ;
#19919=ORIENTED_EDGE ( 'NONE', *, *, #8615, .T. ) ;
#19921=CARTESIAN_POINT ( 'NONE',  ( 23.29410800009176796, -1.498401570910810054, -10.49305455072095228 ) ) ;
#19922=CARTESIAN_POINT ( 'NONE',  ( -5.372793533988000192, 16.07374366253000275, 2.940837684191000001 ) ) ;
#19923=CARTESIAN_POINT ( 'NONE',  ( 17.44105274156537533, -8.133647787183173605, 6.538978001247210514 ) ) ;
#19924=CARTESIAN_POINT ( 'NONE',  ( -17.54351602131999854, -8.091578619838001529, 7.581262777877999959 ) ) ;
#19926=ADVANCED_FACE ( 'NONE', ( #21803 ), #10680, .F. ) ;
#19928=CARTESIAN_POINT ( 'NONE',  ( -16.36737399056000086, -1.805578197078999914, -9.588658350757999216 ) ) ;
#19930=ORIENTED_EDGE ( 'NONE', *, *, #12341, .T. ) ;
#19931=CARTESIAN_POINT ( 'NONE',  ( 11.43887872963139252, 12.36312605253445085, -3.586317572249483998 ) ) ;
#19932=CARTESIAN_POINT ( 'NONE',  ( 23.59056163660901717, 2.084868816671024305, -10.39936085362623075 ) ) ;
#19933=CARTESIAN_POINT ( 'NONE',  ( 11.74999999482999868, 0.000000000000000000, 1.045589212608000028E-14 ) ) ;
#19935=CARTESIAN_POINT ( 'NONE',  ( 19.24399999999999977, 9.165120680968000144, 0.000000000000000000 ) ) ;
#19936=CARTESIAN_POINT ( 'NONE',  ( 4.905991498448432075, 14.36426274116703183, -3.820313869637216975 ) ) ;
#19937=CARTESIAN_POINT ( 'NONE',  ( 4.670439692284003463, 12.43658471589000492, -1.070905091827999867 ) ) ;
#19938=ORIENTED_EDGE ( 'NONE', *, *, #13392, .F. ) ;
#19939=CARTESIAN_POINT ( 'NONE',  ( 18.08325125730999972, 1.019414021290000028, 9.192347282599000025 ) ) ;
#19940=ORIENTED_EDGE ( 'NONE', *, *, #9672, .T. ) ;
#19941=CONICAL_SURFACE ( 'NONE', #22615, 9.152445778720998959, 0.02565634000431304615 ) ;
#19946=CARTESIAN_POINT ( 'NONE',  ( -19.37239492268833629, 7.702177344478975840, 5.087202664328104973 ) ) ;
#19947=CARTESIAN_POINT ( 'NONE',  ( 12.05662674931000033, -10.44547366770999908, -0.2303471896619999904 ) ) ;
#19948=CARTESIAN_POINT ( 'NONE',  ( -24.27612620378999964, 7.862241769065999364, 6.487233881142000058 ) ) ;
#19949=CARTESIAN_POINT ( 'NONE',  ( -15.76129435812999979, 9.303360818536997812, -2.884552524785000127 ) ) ;
#19952=EDGE_CURVE ( 'NONE', #18848, #9480, #204, .T. ) ;
#19953=CARTESIAN_POINT ( 'NONE',  ( -22.82621233711391895, -6.539040155037235458, -8.301165428859656359 ) ) ;
#19958=CARTESIAN_POINT ( 'NONE',  ( 12.52688711657000020, -6.216878364870000340, 12.50000000000000000 ) ) ;
#19959=LINE ( 'NONE', #14612, #3831 ) ;
#19963=CARTESIAN_POINT ( 'NONE',  ( 18.93264468355999952, 0.000000000000000000, 0.000000000000000000 ) ) ;
#19964=ORIENTED_EDGE ( 'NONE', *, *, #3894, .T. ) ;
#19965=CARTESIAN_POINT ( 'NONE',  ( 18.03466666666665574, -4.599982198591594518, 7.981289300288839428 ) ) ;
#19966=CARTESIAN_POINT ( 'NONE',  ( 4.443184208718807149, 12.29965960042665962, -1.929093012512449912 ) ) ;
#19968=CARTESIAN_POINT ( 'NONE',  ( 11.62486552301403897, -5.600815039373708615, -7.038964122195418227 ) ) ;
#19969=ORIENTED_EDGE ( 'NONE', *, *, #18731, .T. ) ;
#19972=AXIS2_PLACEMENT_3D ( 'NONE', #5904, #13290, #9078 ) ;
#19973=B_SPLINE_CURVE_WITH_KNOTS ( 'NONE', 3,
 ( #18815, #22097, #11325, #3690, #277, #18698, #7681, #14814, #2107, #7431, #20636, #9496 ),
 .UNSPECIFIED., .F., .F.,
 ( 4, 1, 1, 1, 1, 2, 2, 4 ),
 ( 0.000000000000000000, 0.2499999999999996114, 0.3749999999999996114, 0.4374999999999996669, 0.4687499999999997224, 0.4843749999999997224, 0.4999999999999997780, 1.000000000000000000 ),
 .UNSPECIFIED. ) ;
#19974=CARTESIAN_POINT ( 'NONE',  ( 12.07687642131000061, 2.140746470509000243, -9.358182000212998730 ) ) ;
#19975=CARTESIAN_POINT ( 'NONE',  ( 18.70306232122398526, 8.883973405854113992, 5.460658337303971877 ) ) ;
#19976=VERTEX_POINT ( 'NONE', #12485 ) ;
#19979=CARTESIAN_POINT ( 'NONE',  ( -12.51567934522000058, 6.525107353416999878, -6.187672237275999798 ) ) ;
#19980=CARTESIAN_POINT ( 'NONE',  ( 13.49999999999999822, -8.028714044826315899, 6.032243616578709222 ) ) ;
#19982=AXIS2_PLACEMENT_3D ( 'NONE', #13604, #770, #8170 ) ;
#19984=CARTESIAN_POINT ( 'NONE',  ( -23.74465998031000069, -13.93375672974000068, 0.8660254037843999608 ) ) ;
#19988=CARTESIAN_POINT ( 'NONE',  ( 2.948934117662000087, 11.89081811946000933, 3.984846700880998682 ) ) ;
#19990=CARTESIAN_POINT ( 'NONE',  ( -7.834000000000000519, 10.69999999999999929, 0.000000000000000000 ) ) ;
#19998=CARTESIAN_POINT ( 'NONE',  ( 11.55284350193982235, -3.530773253025947689, -12.49989659317496837 ) ) ;
#19999=CARTESIAN_POINT ( 'NONE',  ( 19.53916666666666302, 4.841071979630906519, 7.905488166010842477 ) ) ;
#20002=ORIENTED_EDGE ( 'NONE', *, *, #5430, .F. ) ;
#20003=CARTESIAN_POINT ( 'NONE',  ( -15.14859190273999801, -7.578844389069999465, 6.091136938512000221 ) ) ;
#20007=CARTESIAN_POINT ( 'NONE',  ( -24.78987924950000021, -10.60142683737000091, 1.295814263090999896 ) ) ;
#20008=AXIS2_PLACEMENT_3D ( 'NONE', #12951, #10914, #23852 ) ;
#20010=CARTESIAN_POINT ( 'NONE',  ( 14.42486780284139058, -1.324147059350222921, -10.23272323601588596 ) ) ;
#20012=CARTESIAN_POINT ( 'NONE',  ( 22.62059167554999917, -6.125430812571999617, 9.452137327804999600 ) ) ;
#20014=DIRECTION ( 'NONE',  ( -1.000000000000000000, 0.000000000000000000, 0.000000000000000000 ) ) ;
#20015=CARTESIAN_POINT ( 'NONE',  ( -4.528963122208002900, 12.53559761094001423, -1.650262910948000927 ) ) ;
#20016=B_SPLINE_CURVE_WITH_KNOTS ( 'NONE', 3,
 ( #22394, #16939, #5684, #9325, #13070, #11142, #15228, #11386, #16699, #9680, #1937, #20469, #7495, #3877, #15111, #13188, #342, #9794 ),
 .UNSPECIFIED., .F., .F.,
 ( 4, 2, 2, 2, 2, 2, 2, 2, 4 ),
 ( 0.000000000000000000, 0.1250000000000000000, 0.2500000000000000000, 0.3750000000000000000, 0.5000000000000000000, 0.6250000000000000000, 0.7500000000000000000, 0.8750000000000000000, 1.000000000000000000 ),
 .UNSPECIFIED. ) ;
#20017=CARTESIAN_POINT ( 'NONE',  ( -21.35476253787999923, 9.219287007783998789, 0.000000000000000000 ) ) ;
#20021=DIRECTION ( 'NONE',  ( 0.000000000000000000, 0.000000000000000000, 1.000000000000000000 ) ) ;
#20022=AXIS2_PLACEMENT_3D ( 'NONE', #17090, #3904, #22298 ) ;
#20026=CARTESIAN_POINT ( 'NONE',  ( 16.67416666666665392, -7.950782698768437129, -4.582399293024413289 ) ) ;
#20027=AXIS2_PLACEMENT_3D ( 'NONE', #22134, #11117, #12816 ) ;
#20028=CARTESIAN_POINT ( 'NONE',  ( 12.00000000000000000, 5.273090321616999532, -7.267806174758000282 ) ) ;
#20029=CARTESIAN_POINT ( 'NONE',  ( 14.69311188949999902, 10.43397013479000002, 3.548706328086999928 ) ) ;
#20033=CARTESIAN_POINT ( 'NONE',  ( -12.10791923250999957, 4.794444003321999936, -13.75758207492000018 ) ) ;
#20034=CARTESIAN_POINT ( 'NONE',  ( 13.50000000000000178, 5.145877244135721007, 8.714246119701103410 ) ) ;
#20035=CARTESIAN_POINT ( 'NONE',  ( -14.40719396494441185, -12.69649082865952927, -3.008800086024487452 ) ) ;
#20036=ORIENTED_EDGE ( 'NONE', *, *, #3618, .T. ) ;
#20038=CARTESIAN_POINT ( 'NONE',  ( 23.55883927622098639, 7.420590745144572509, -7.577917290854461640 ) ) ;
#20039=CARTESIAN_POINT ( 'NONE',  ( -14.00000000000000178, -0.8805840824569890479, 9.770682771554191959 ) ) ;
#20040=CARTESIAN_POINT ( 'NONE',  ( 15.99032225483610148, -8.667267649197352597, -5.673782229705955693 ) ) ;
#20041=VECTOR ( 'NONE', #3121, 999.9999999999998863 ) ;
#20044=CARTESIAN_POINT ( 'NONE',  ( -6.142578036165183164, 15.03063358819925810, 3.518293753452066408 ) ) ;
#20046=CARTESIAN_POINT ( 'NONE',  ( -14.94546155477000049, -9.714114572133000891, -0.2583773470232999525 ) ) ;
#20050=CARTESIAN_POINT ( 'NONE',  ( 19.33455408719442659, -9.641156592198640851, 4.152421770286800928 ) ) ;
#20053=CARTESIAN_POINT ( 'NONE',  ( 24.35625626386760700, -9.206804001270699089, -9.053347694469197293 ) ) ;
#20054=CARTESIAN_POINT ( 'NONE',  ( 5.110054639284849820, 14.01663359027072886, -3.973409363128503458 ) ) ;
#20055=CIRCLE ( 'NONE', #5357, 0.8000000000000003775 ) ;
#20056=CARTESIAN_POINT ( 'NONE',  ( 4.761848349162001170, 12.47239002814000131, -0.5119988763560997524 ) ) ;
#20060=ORIENTED_EDGE ( 'NONE', *, *, #21265, .T. ) ;
#20061=CARTESIAN_POINT ( 'NONE',  ( -14.25547409885999883, 6.467346689388999259, -12.35539204541999858 ) ) ;
#20064=AXIS2_PLACEMENT_3D ( 'NONE', #14753, #14638, #98 ) ;
#20066=CARTESIAN_POINT ( 'NONE',  ( -19.40606844572667455, 8.247006132493126529, 4.148077805920550531 ) ) ;
#20067=VECTOR ( 'NONE', #4419, 1000.000000000000227 ) ;
#20068=AXIS2_PLACEMENT_3D ( 'NONE', #19184, #8173, #8292 ) ;
#20069=CARTESIAN_POINT ( 'NONE',  ( -22.50967266913999865, 8.778109831006000618, 5.086562693550999548 ) ) ;
#20070=( BOUNDED_SURFACE ( )  B_SPLINE_SURFACE ( 3, 3, ( 
 ( #9164, #12687, #16540, #16419, #1897 ),
 ( #12905, #11228, #18148, #18607, #20076 ),
 ( #20305, #5526, #8936, #65, #21885 ),
 ( #18484, #2013, #23808, #7451, #20424 ) ),
 .UNSPECIFIED., .F., .F., .T. ) 
 B_SPLINE_SURFACE_WITH_KNOTS ( ( 4, 4 ),
 ( 4, 1, 4 ),
 ( 0.000000000000000000, 1.000000000000000000 ),
 ( 0.9387615814217999954, 0.9657285282888999900, 0.9947468880704000149 ),
 .UNSPECIFIED. ) 
 GEOMETRIC_REPRESENTATION_ITEM ( )  RATIONAL_B_SPLINE_SURFACE ( (
 ( 1.226462146532000030, 1.226462146532000030, 1.226462146532000030, 1.226462146532000030, 1.226462146532000030),
 ( 0.9245126178228000313, 0.9245126178228000313, 0.9245126178228000313, 0.9245126178228000313, 0.9245126178228000313),
 ( 0.9245126178228000313, 0.9245126178228000313, 0.9245126178228000313, 0.9245126178228000313, 0.9245126178228000313),
 ( 1.226462146532000030, 1.226462146532000030, 1.226462146532000030, 1.226462146532000030, 1.226462146532000030) ) ) 
 REPRESENTATION_ITEM ( '' )  SURFACE ( )  );
#20071=CARTESIAN_POINT ( 'NONE',  ( -18.80824957768000161, -1.381956751031999886, 9.727523358913000351 ) ) ;
#20073=CARTESIAN_POINT ( 'NONE',  ( -24.31884963048089077, 4.568789909715829545, -9.568519739173572347 ) ) ;
#20076=CARTESIAN_POINT ( 'NONE',  ( -5.790984316780003027, 15.02418496909000112, 3.017193391611002085 ) ) ;
#20080=ADVANCED_FACE ( 'NONE', ( #11375 ), #23964, .T. ) ;
#20081=CARTESIAN_POINT ( 'NONE',  ( 23.43873132191483322, 5.239923916412018379, 7.729598312681994265 ) ) ;
#20083=CARTESIAN_POINT ( 'NONE',  ( 14.93123391489891283, -8.895217880621389739, 1.951093223186516568 ) ) ;
#20087=CARTESIAN_POINT ( 'NONE',  ( -1.299969483453414343, 11.55360400645373709, -4.638995061499023187 ) ) ;
#20089=EDGE_CURVE ( 'NONE', #4654, #21095, #2043, .T. ) ;
#20091=B_SPLINE_CURVE_WITH_KNOTS ( 'NONE', 3,
 ( #14391, #23600, #1564, #8950, #4963, #19612, #8837, #6521, #6760, #1068, #21784, #7003, #3021, #19738, #19966, #16316, #12464, #3149, #13907, #4718, #10531, #21548, #17916, #19492, #16072, #23472, #14032, #6881, #3386, #14276, #2898, #15835, #15951, #21671, #5083, #19848, #10648, #10768, #18035, #12223, #18162, #10280, #10408, #17670, #8469, #23225, #21423, #17801, #23344, #12812, #12919, #13160, #9528, #5651, #1668, #13037, #23707, #7351, #11240, #18496, #5309, #14734, #9412, #7228, #11356, #9058, #9298, #10992, #20087, #20202, #2138, #1908, #7114, #3845, #14504, #21898, #14962, #22360, #9175, #12698, #23818, #5776, #16430, #20552, #11112, #10882, #18269, #14620, #3965, #2024, #16671, #18728, #18618, #22016, #16554, #16784, #3609, #3502, #191, #22130, #5429, #23944, #18377, #1787, #78, #7584, #5538, #20315, #3721, #7463, #14847, #22237, #20434, #15321 ),
 .UNSPECIFIED., .F., .F.,
 ( 4, 1, 1, 1, 1, 2, 2, 2, 1, 1, 1, 2, 2, 2, 1, 1, 1, 2, 2, 2, 1, 1, 1, 2, 2, 2, 1, 2, 2, 2, 2, 2, 2, 1, 1, 2, 2, 2, 2, 1, 1, 2, 2, 2, 1, 1, 1, 2, 2, 2, 1, 1, 1, 2, 2, 2, 1, 1, 1, 2, 2, 2, 1, 1, 1, 2, 2, 2, 1, 1, 2, 2, 4 ),
 ( 0.000000000000000000, 0.03125000000000074940, 0.04687500000000113798, 0.05468750000000132533, 0.05859375000000146411, 0.06054687500000152656, 0.06250000000000159595, 0.09375000000000288658, 0.1093750000000035666, 0.1171875000000038858, 0.1210937500000039968, 0.1230468750000041078, 0.1250000000000041911, 0.1562500000000040246, 0.1718750000000038858, 0.1796875000000039413, 0.1835937500000039413, 0.1855468750000038858, 0.1875000000000038580, 0.2187500000000034417, 0.2343750000000032196, 0.2421875000000031086, 0.2460937500000030531, 0.2480468750000029421, 0.2500000000000028311, 0.2656250000000020539, 0.2734375000000016098, 0.2773437500000014433, 0.2812500000000012212, 0.2968750000000006106, 0.3125000000000000000, 0.3437499999999987232, 0.3593749999999980571, 0.3671874999999977796, 0.3710937499999975575, 0.3730468749999975020, 0.3749999999999974465, 0.4062499999999961697, 0.4218749999999955591, 0.4296874999999952816, 0.4335937499999951150, 0.4355468749999950595, 0.4374999999999950040, 0.4687499999999941158, 0.4843749999999937272, 0.4921874999999935607, 0.4960937499999933942, 0.4980468749999933942, 0.4999999999999933942, 0.5312499999999928946, 0.5468749999999926725, 0.5546874999999925615, 0.5585937499999925615, 0.5605468749999924505, 0.5624999999999923395, 0.5937499999999921174, 0.6093749999999920064, 0.6171874999999918954, 0.6210937499999918954, 0.6230468749999920064, 0.6249999999999920064, 0.6874999999999917843, 0.7187499999999918954, 0.7343749999999920064, 0.7421874999999920064, 0.7460937499999921174, 0.7499999999999922284, 0.8124999999999941158, 0.8437499999999952260, 0.8593749999999957812, 0.8671874999999960032, 0.8749999999999963363, 1.000000000000000000 ),
 .UNSPECIFIED. ) ;
#20092=EDGE_CURVE ( 'NONE', #14850, #2766, #18397, .T. ) ;
#20098=CARTESIAN_POINT ( 'NONE',  ( 15.50362658531000193, -9.889101471244000408, -2.495492728532000104 ) ) ;
#20099=CARTESIAN_POINT ( 'NONE',  ( 18.44061664567739456, 9.767409168246320661, -3.641564553964325324 ) ) ;
#20105=CARTESIAN_POINT ( 'NONE',  ( 13.50000000000000178, -9.660468571430653739, -0.1198354625297687187 ) ) ;
#20108=CARTESIAN_POINT ( 'NONE',  ( -24.41904027019043255, 11.84953030585170985, 4.475986625696044996 ) ) ;
#20109=CARTESIAN_POINT ( 'NONE',  ( 19.68770938589000252, -10.68602309994999899, -0.7848986935476999216 ) ) ;
#20110=CARTESIAN_POINT ( 'NONE',  ( -24.39641198927269983, 7.916710863778032348, -6.620963688920025625 ) ) ;
#20111=CARTESIAN_POINT ( 'NONE',  ( 24.50000000000000711, -5.724380115368404631, 8.895336411110607244 ) ) ;
#20113=CARTESIAN_POINT ( 'NONE',  ( -4.914666472637005512, 12.43931986496000874, -0.06122609934487997785 ) ) ;
#20116=CARTESIAN_POINT ( 'NONE',  ( -23.48034867834999773, 8.702766563787999843, 6.962597091951999495 ) ) ;
#20117=ORIENTED_EDGE ( 'NONE', *, *, #18004, .T. ) ;
#20119=ORIENTED_EDGE ( 'NONE', *, *, #18579, .F. ) ;
#20123=CARTESIAN_POINT ( 'NONE',  ( 4.157699912148990151, 13.38119708362450666, 5.410788887539548675 ) ) ;
#20124=CARTESIAN_POINT ( 'NONE',  ( 18.91915022178003625, -1.886358478162994956, 10.25880577272608107 ) ) ;
#20125=CARTESIAN_POINT ( 'NONE',  ( 13.50000000000000355, 1.456528203957302647, 10.21014957686530344 ) ) ;
#20126=ORIENTED_EDGE ( 'NONE', *, *, #1055, .T. ) ;
#20127=CARTESIAN_POINT ( 'NONE',  ( -16.57050433853000015, -7.584645295112999897, -6.147042915735999813 ) ) ;
#20128=AXIS2_PLACEMENT_3D ( 'NONE', #7215, #17017, #14829 ) ;
#20132=CARTESIAN_POINT ( 'NONE',  ( -10.95209178422446605, 15.32973516857846796, -1.791032230336580211 ) ) ;
#20134=CARTESIAN_POINT ( 'NONE',  ( 14.66098616093672469, 6.531434504799800145, -7.997021604459393807 ) ) ;
#20136=CARTESIAN_POINT ( 'NONE',  ( 20.38110275387000314, 11.05129809220999881, 1.830737130756000086 ) ) ;
#20137=DIRECTION ( 'NONE',  ( 0.000000000000000000, -1.000000000000000000, 0.000000000000000000 ) ) ;
#20138=CARTESIAN_POINT ( 'NONE',  ( 13.80182517639457274, 9.025292127787466256, 0.004672145026744048760 ) ) ;
#20143=CARTESIAN_POINT ( 'NONE',  ( -14.84820223132186356, -7.755096387757968834, -4.693416038378982691 ) ) ;
#20145=ORIENTED_EDGE ( 'NONE', *, *, #19656, .T. ) ;
#20146=CARTESIAN_POINT ( 'NONE',  ( 19.05233531832000082, -1.887707665395999879, 10.26617185442000135 ) ) ;
#20148=FACE_OUTER_BOUND ( 'NONE', #13578, .T. ) ;
#20149=CARTESIAN_POINT ( 'NONE',  ( 24.34804274388871193, 3.330488627411498204, -12.50000000000000355 ) ) ;
#20150=CARTESIAN_POINT ( 'NONE',  ( -16.45626648132295955, 9.977493378410441593, 2.951365295957959489 ) ) ;
#20153=CARTESIAN_POINT ( 'NONE',  ( -9.392652565846001167, -11.23270293799999919, -9.740851948633999058 ) ) ;
#20154=CARTESIAN_POINT ( 'NONE',  ( 13.49999999999999822, 9.583219496692837680, 0.7036459153352878637 ) ) ;
#20155=CARTESIAN_POINT ( 'NONE',  ( -14.45561352951336964, -12.11761689492659677, -4.011600805616156507 ) ) ;
#20156=EDGE_CURVE ( 'NONE', #19018, #14183, #4398, .T. ) ;
#20158=CARTESIAN_POINT ( 'NONE',  ( 22.94113296525130252, -10.36727481655944771, -2.169730993702538413 ) ) ;
#20159=CARTESIAN_POINT ( 'NONE',  ( 12.52688711657000020, -13.93375672974000068, 0.8660254037843999608 ) ) ;
#20160=CARTESIAN_POINT ( 'NONE',  ( 15.97207963789832164, -9.022303258340008014, -5.088742242062048504 ) ) ;
#20161=FACE_OUTER_BOUND ( 'NONE', #4401, .T. ) ;
#20163=CIRCLE ( 'NONE', #798, 9.287173237303996132 ) ;
#20164=CARTESIAN_POINT ( 'NONE',  ( -19.04882659540000134, -6.818301851232999589, 6.682161380682999585 ) ) ;
#20167=VERTEX_POINT ( 'NONE', #99 ) ;
#20169=CARTESIAN_POINT ( 'NONE',  ( 19.87364837678908813, -1.149180406892156281, -10.44631844158005407 ) ) ;
#20172=CARTESIAN_POINT ( 'NONE',  ( 4.851389421338315522, 14.56759478981999933, -3.780608026316847337 ) ) ;
#20173=CARTESIAN_POINT ( 'NONE',  ( -4.197096011533001381, 12.18682765224999187, -2.415895191620001992 ) ) ;
#20175=CARTESIAN_POINT ( 'NONE',  ( 17.75418875731000057, 8.769310764750999354, 2.911614084577999861 ) ) ;
#20176=ORIENTED_EDGE ( 'NONE', *, *, #7863, .F. ) ;
#20179=CARTESIAN_POINT ( 'NONE',  ( 18.51344355829000321, -13.93375672974000068, 0.000000000000000000 ) ) ;
#20183=CARTESIAN_POINT ( 'NONE',  ( -22.24049188378000252, 9.221077711103999874, 5.343197927521000423 ) ) ;
#20184=CARTESIAN_POINT ( 'NONE',  ( -17.38633714188999946, 9.179352961803999733, 3.390708539619000206 ) ) ;
#20185=CARTESIAN_POINT ( 'NONE',  ( -5.123170459737996119, 14.39942909848998909, -4.079011992021998267 ) ) ;
#20186=CARTESIAN_POINT ( 'NONE',  ( -22.44018545090364469, 6.612455538562568513, -8.384770958092557791 ) ) ;
#20188=PLANE ( 'NONE',  #22032 ) ;
#20189=EDGE_CURVE ( 'NONE', #2380, #1933, #4889, .T. ) ;
#20192=CARTESIAN_POINT ( 'NONE',  ( 23.96715810487390286, -8.818041421502185173, 3.119150737227263992 ) ) ;
#20193=DIRECTION ( 'NONE',  ( 0.9996708941621511579, 0.02565352539213875543, 0.000000000000000000 ) ) ;
#20194=CARTESIAN_POINT ( 'NONE',  ( 14.30901013702234081, 6.517998721482895164, 6.337184079108406642 ) ) ;
#20196=DIRECTION ( 'NONE',  ( -1.000000000000000000, 0.000000000000000000, 0.000000000000000000 ) ) ;
#20198=CARTESIAN_POINT ( 'NONE',  ( -14.25243324638999809, -13.93375672974000068, -0.8660254037843999608 ) ) ;
#20199=CARTESIAN_POINT ( 'NONE',  ( 2.248627110350167158, 11.69740771678675451, 4.262999372637977125 ) ) ;
#20201=ADVANCED_FACE ( 'NONE', ( #10905 ), #7575, .F. ) ;
#20202=CARTESIAN_POINT ( 'NONE',  ( -1.562092572808364777, 11.58646502489367869, -4.556008495004664205 ) ) ;
#20205=ORIENTED_EDGE ( 'NONE', *, *, #11327, .F. ) ;
#20208=EDGE_CURVE ( 'NONE', #19206, #2201, #18261, .T. ) ;
#20210=CARTESIAN_POINT ( 'NONE',  ( -16.40405420454666086, -1.190044756772769441, -9.092242074617137959 ) ) ;
#20211=CARTESIAN_POINT ( 'NONE',  ( 16.60050158530999909, 6.318772076511000257, 8.042630855556000213 ) ) ;
#20212=CARTESIAN_POINT ( 'NONE',  ( 18.54963726174204552, 10.44196517788747336, 0.1308933847890557112 ) ) ;
#20213=CARTESIAN_POINT ( 'NONE',  ( 12.52688711657000020, 6.216878364870000340, 12.50000000000000000 ) ) ;
#20215=CARTESIAN_POINT ( 'NONE',  ( -12.50492312419000207, 6.877612380107000156, -5.798846373018999856 ) ) ;
#20216=CARTESIAN_POINT ( 'NONE',  ( 13.50000000000000355, -9.024405030093623381, -2.976340912779337433 ) ) ;
#20217=CIRCLE ( 'NONE', #2021, 12.50000000000000000 ) ;
#20219=CARTESIAN_POINT ( 'NONE',  ( -24.46742986864630964, 11.46616815105915244, 5.140026613611447637 ) ) ;
#20220=CARTESIAN_POINT ( 'NONE',  ( 19.23935571152999913, -9.634227767086001037, 5.773988190026000389 ) ) ;
#20222=CARTESIAN_POINT ( 'NONE',  ( -14.25699038479000080, 13.93375672974000068, 0.000000000000000000 ) ) ;
#20225=CARTESIAN_POINT ( 'NONE',  ( 24.50000000000000000, -1.624284714732273649, 10.43931695975270202 ) ) ;
#20228=CARTESIAN_POINT ( 'NONE',  ( -22.31075685788999863, 0.1502046266062000146, -11.11246732393999892 ) ) ;
#20229=ORIENTED_EDGE ( 'NONE', *, *, #2904, .T. ) ;
#20231=ORIENTED_EDGE ( 'NONE', *, *, #7592, .T. ) ;
#20236=CARTESIAN_POINT ( 'NONE',  ( -16.81976253787999909, -9.102909969768001375, 0.000000000000000000 ) ) ;
#20238=CARTESIAN_POINT ( 'NONE',  ( 16.27143908530999639, 9.938600131338999333, -2.378686727414999869 ) ) ;
#20241=CARTESIAN_POINT ( 'NONE',  ( -13.72667946694999941, 4.336095440212999641, 8.658528082053999597 ) ) ;
#20244=ORIENTED_EDGE ( 'NONE', *, *, #9614, .F. ) ;
#20245=CARTESIAN_POINT ( 'NONE',  ( -19.82024391687000175, 2.079266777114999964, 10.99594615337999848 ) ) ;
#20247=CARTESIAN_POINT ( 'NONE',  ( 14.86624431231352439, 10.19680779959737471, -1.809567902645908166 ) ) ;
#20248=CARTESIAN_POINT ( 'NONE',  ( -17.99130420454667245, 5.612729004169484170, -7.303246745062192957 ) ) ;
#20249=CARTESIAN_POINT ( 'NONE',  ( 24.38221057305000272, 6.592218218594999790, 9.192201995134999137 ) ) ;
#20251=EDGE_CURVE ( 'NONE', #21708, #17770, #18030, .T. ) ;
#20252=CARTESIAN_POINT ( 'NONE',  ( 14.05462922766051648, 5.715449972624886854, 7.003620237176114038 ) ) ;
#20253=CARTESIAN_POINT ( 'NONE',  ( -4.159224151219002685, 12.40416002829998732, -2.437210981237998730 ) ) ;
#20255=CARTESIAN_POINT ( 'NONE',  ( -22.22397087121331438, -9.241592606737556892, -1.209848591021944531 ) ) ;
#20257=CARTESIAN_POINT ( 'NONE',  ( -14.55352821834695298, 0.01803078645220980436, -9.054618933368537625 ) ) ;
#20258=CARTESIAN_POINT ( 'NONE',  ( -14.11574458423267586, -9.891920035128775268, 3.515509136289259207 ) ) ;
#20259=CIRCLE ( 'NONE', #12137, 0.09999993872260067029 ) ;
#20260=ORIENTED_EDGE ( 'NONE', *, *, #5527, .F. ) ;
#20261=CARTESIAN_POINT ( 'NONE',  ( -16.37216243917331582, -7.943913672023831474, -4.578730802673559808 ) ) ;
#20263=CARTESIAN_POINT ( 'NONE',  ( -23.50032910583999879, 3.801543240379000377, -8.459419100777001432 ) ) ;
#20264=CARTESIAN_POINT ( 'NONE',  ( 15.02018438422999935, 6.390136118733999560, 8.990257899662001506 ) ) ;
#20265=DIRECTION ( 'NONE',  ( -0.7071067811865975328, 0.7071067811864976127, 1.204882835872995245E-09 ) ) ;
#20267=VERTEX_POINT ( 'NONE', #16192 ) ;
#20268=CARTESIAN_POINT ( 'NONE',  ( -9.799942565846000875, -8.137225276125999329, 12.44360880412000014 ) ) ;
#20269=B_SPLINE_CURVE_WITH_KNOTS ( 'NONE', 3,
 ( #11859, #8113, #8472, #22864, #8591 ),
 .UNSPECIFIED., .F., .F.,
 ( 4, 1, 4 ),
 ( 0.000000000000000000, 0.5000000000000000000, 1.000000000000000000 ),
 .UNSPECIFIED. ) ;
#20270=DIRECTION ( 'NONE',  ( -1.000000000000000000, 5.341664343519000084E-12, -4.885518282254999468E-11 ) ) ;
#20272=ORIENTED_EDGE ( 'NONE', *, *, #9193, .F. ) ;
#20273=CARTESIAN_POINT ( 'NONE',  ( 20.85099770046331358, -1.205236576247627367, -9.206359409188111798 ) ) ;
#20274=CARTESIAN_POINT ( 'NONE',  ( 24.15736593521593178, 8.253730364077119575, -10.70411965744399119 ) ) ;
#20275=CARTESIAN_POINT ( 'NONE',  ( 16.18754222806948562, -3.151203986297408388, -9.872908633960614466 ) ) ;
#20276=CARTESIAN_POINT ( 'NONE',  ( -19.13544413845999870, -9.637273350829000051, -5.571910801056999318 ) ) ;
#20279=CARTESIAN_POINT ( 'NONE',  ( -16.81439276773000202, -8.006006257143999605, -6.488443847660000152 ) ) ;
#20281=VERTEX_POINT ( 'NONE', #8702 ) ;
#20283=CARTESIAN_POINT ( 'NONE',  ( 20.12900882975453243, 7.359272468721639093, -7.512247993263142298 ) ) ;
#20285=ORIENTED_EDGE ( 'NONE', *, *, #19614, .T. ) ;
#20286=EDGE_CURVE ( 'NONE', #17545, #20307, #18803, .T. ) ;
#20287=CARTESIAN_POINT ( 'NONE',  ( 4.860820541961833996, 14.52075968249973670, -3.787349904231070763 ) ) ;
#20288=CARTESIAN_POINT ( 'NONE',  ( -4.832579888156002035, 12.42138610322999526, -0.3261195631766998226 ) ) ;
#20290=CARTESIAN_POINT ( 'NONE',  ( 12.16012625731000085, 8.900490462747001175, -1.861105101465000189 ) ) ;
#20292=CARTESIAN_POINT ( 'NONE',  ( -3.776477861809037329, 14.59612568772429952, 4.825021002418410809 ) ) ;
#20294=CARTESIAN_POINT ( 'NONE',  ( -14.49284521823309824, 1.036537809063993176, -12.49997544920737802 ) ) ;
#20299=CARTESIAN_POINT ( 'NONE',  ( 12.00000000000000178, 3.061724608921426949, -8.619331017259337813 ) ) ;
#20300=CARTESIAN_POINT ( 'NONE',  ( -19.82390131753000162, -2.296328123436000457, -9.582100204323001691 ) ) ;
#20301=CARTESIAN_POINT ( 'NONE',  ( 18.48816666666665398, -7.991458167462555551, -4.605843167114078263 ) ) ;
#20302=CARTESIAN_POINT ( 'NONE',  ( -22.92915284010549470, -9.027613226242038991, -5.491954109625697633 ) ) ;
#20303=CARTESIAN_POINT ( 'NONE',  ( 11.01624327026000039, -12.44999999999999929, 0.000000000000000000 ) ) ;
#20304=CARTESIAN_POINT ( 'NONE',  ( 15.80495833333332634, 7.258560212986407301, 5.578069749145255329 ) ) ;
#20305=CARTESIAN_POINT ( 'NONE',  ( -5.983850654344998077, 15.83682997010998506, 0.8930707396852997082 ) ) ;
#20307=VERTEX_POINT ( 'NONE', #19203 ) ;
#20309=CARTESIAN_POINT ( 'NONE',  ( 4.495985175916063170, 13.47622785279660462, -5.169691691112981324 ) ) ;
#20311=CARTESIAN_POINT ( 'NONE',  ( -23.02737179241879772, -9.363639631091235316, 4.904215814585074718 ) ) ;
#20315=CARTESIAN_POINT ( 'NONE',  ( -4.637553514248847542, 12.37005176196437262, -1.410038579757167509 ) ) ;
#20316=CARTESIAN_POINT ( 'NONE',  ( 24.00034722001000276, -7.216970193686000457, -11.92259671342000082 ) ) ;
#20318=ORIENTED_EDGE ( 'NONE', *, *, #2254, .T. ) ;
#20321=CARTESIAN_POINT ( 'NONE',  ( 14.62612658531000243, 9.561303730670999812, 3.483288127948000135 ) ) ;
#20322=CARTESIAN_POINT ( 'NONE',  ( 17.80562055465178517, -8.706723506620447139, -5.795109365428579906 ) ) ;
#20326=CARTESIAN_POINT ( 'NONE',  ( 13.49999999999999645, -8.571874797152489123, 5.143046839193468500 ) ) ;
#20328=VERTEX_POINT ( 'NONE', #23679 ) ;
#20331=CARTESIAN_POINT ( 'NONE',  ( 19.06230660937999843, -4.552702152812999614, 10.26188179881000018 ) ) ;
#20332=CARTESIAN_POINT ( 'NONE',  ( -24.50000000000000000, 3.293267271483000247, -9.759323269498999309 ) ) ;
#20335=CARTESIAN_POINT ( 'NONE',  ( 18.75008227645999881, 0.000000000000000000, 0.000000000000000000 ) ) ;
#20336=CARTESIAN_POINT ( 'NONE',  ( 4.023773140947001004, 12.12796709211999513, 2.696238718279999169 ) ) ;
#20338=ADVANCED_FACE ( 'NONE', ( #18124 ), #1286, .F. ) ;
#20339=CARTESIAN_POINT ( 'NONE',  ( 12.51793260380000028, 13.93375672974000068, -0.7216754077441999149 ) ) ;
#20341=CARTESIAN_POINT ( 'NONE',  ( -7.034000000000000696, 10.69999999999999929, -6.692428833332999144E-10 ) ) ;
#20344=( BOUNDED_SURFACE ( )  B_SPLINE_SURFACE ( 3, 3, ( 
 ( #15384, #15506, #4267, #21088, #20855, #6190, #19025, #2437 ),
 ( #23013, #13576, #2555, #9945, #8140, #6430, #13815, #21214 ),
 ( #4629, #2813, #8379, #12497, #3180, #8981, #14064, #17834 ),
 ( #5116, #8621, #16353, #15982, #18302, #14188, #21458, #9092 ) ),
 .UNSPECIFIED., .F., .F., .T. ) 
 B_SPLINE_SURFACE_WITH_KNOTS ( ( 4, 4 ),
 ( 4, 1, 1, 1, 1, 4 ),
 ( 0.000000000000000000, 1.000000000000000000 ),
 ( 0.005250863527401000187, 0.01452849757938999911, 0.02864204905892000011, 0.04333368315689999778, 0.05817056875622000217, 0.06131925226894999886 ),
 .UNSPECIFIED. ) 
 GEOMETRIC_REPRESENTATION_ITEM ( )  RATIONAL_B_SPLINE_SURFACE ( (
 ( 1.226455171705000069, 1.226455171705000069, 1.226455171705000069, 1.226455171705000069, 1.226455171705000069, 1.226455171705000069, 1.226455171705000069, 1.226455171705000069),
 ( 0.9245149427651999652, 0.9245149427651999652, 0.9245149427651999652, 0.9245149427651999652, 0.9245149427651999652, 0.9245149427651999652, 0.9245149427651999652, 0.9245149427651999652),
 ( 0.9245149427651999652, 0.9245149427651999652, 0.9245149427651999652, 0.9245149427651999652, 0.9245149427651999652, 0.9245149427651999652, 0.9245149427651999652, 0.9245149427651999652),
 ( 1.226455171705000069, 1.226455171705000069, 1.226455171705000069, 1.226455171705000069, 1.226455171705000069, 1.226455171705000069, 1.226455171705000069, 1.226455171705000069) ) ) 
 REPRESENTATION_ITEM ( '' )  SURFACE ( )  );
#20345=CARTESIAN_POINT ( 'NONE',  ( 5.991097115754002722, 13.66124479386999546, 2.878337485509001592 ) ) ;
#20347=CARTESIAN_POINT ( 'NONE',  ( 5.506614905180002850, 13.75449879388000518, 4.409302736622996655 ) ) ;
#20351=CARTESIAN_POINT ( 'NONE',  ( 17.50443924930999984, -10.75095007791999890, -0.4607405056646999841 ) ) ;
#20353=VERTEX_POINT ( 'NONE', #19935 ) ;
#20354=CARTESIAN_POINT ( 'NONE',  ( -13.52354911898000012, -2.293961044660999704, 9.402123702338000655 ) ) ;
#20358=CARTESIAN_POINT ( 'NONE',  ( -10.60269991523250610, 15.46630580253647835, -1.465288580574494404 ) ) ;
#20360=CARTESIAN_POINT ( 'NONE',  ( 14.54356512408170587, 2.819943630748654506, -9.929365919741389490 ) ) ;
#20362=CARTESIAN_POINT ( 'NONE',  ( 22.73028790635000007, 0.6840553180648999421, 11.24560851965999930 ) ) ;
#20364=CARTESIAN_POINT ( 'NONE',  ( 13.80157322160490629, 9.025297321909626191, -0.003338010211690475675 ) ) ;
#20365=CARTESIAN_POINT ( 'NONE',  ( -6.319385089483436246, 15.63721120038809609, -1.258692299061803466 ) ) ;
#20370=CARTESIAN_POINT ( 'NONE',  ( 12.12543434882655902, 13.45291906885516298, -1.698934468806289733 ) ) ;
#20371=ORIENTED_EDGE ( 'NONE', *, *, #2278, .F. ) ;
#20372=B_SPLINE_CURVE_WITH_KNOTS ( 'NONE', 3,
 ( #6751, #12096, #12213, #15582, #6512, #13896, #12337, #14144, #21298, #19227, #2890, #23216, #4582, #14022, #19729, #10270, #17538, #13768, #15941, #933, #19361, #3140, #10152, #10524, #17907, #16064, #23460, #4711, #8699, #8331, #21170, #17661, #11973, #6873, #21045, #4457, #1058, #19603, #11848, #2767, #8459, #6632, #21413, #3011, #10398, #17790, #1188, #12691, #12458, #18488, #16543, #16189, #23812, #1556, #10640, #5422, #22008, #1432, #23935, #18369, #23590, #10984, #21890 ),
 .UNSPECIFIED., .F., .F.,
 ( 4, 2, 2, 1, 1, 1, 1, 1, 2, 2, 2, 2, 1, 1, 1, 1, 2, 2, 2, 1, 1, 1, 2, 2, 2, 2, 1, 1, 1, 1, 2, 2, 2, 2, 1, 1, 1, 2, 2, 2, 4 ),
 ( 0.000000000000000000, 0.1249999999999909239, 0.1874999999999864830, 0.2187499999999842903, 0.2343749999999831524, 0.2421874999999825140, 0.2460937499999820144, 0.2480468749999818479, 0.2490234374999818479, 0.2499999999999818201, 0.3749999999999766298, 0.4374999999999740763, 0.4687499999999727440, 0.4843749999999720224, 0.4921874999999716893, 0.4960937499999715228, 0.4980468749999714673, 0.4999999999999713562, 0.5624999999999680256, 0.5937499999999663602, 0.6093749999999654721, 0.6171874999999651390, 0.6210937499999650280, 0.6249999999999648059, 0.6874999999999620304, 0.7187499999999605871, 0.7343749999999598099, 0.7421874999999594769, 0.7460937499999591438, 0.7480468749999590328, 0.7490234374999588107, 0.7499999999999585887, 0.8124999999999679146, 0.8437499999999724665, 0.8593749999999746869, 0.8671874999999759082, 0.8710937499999764633, 0.8730468749999767963, 0.8749999999999771294, 0.9374999999999885647, 1.000000000000000000 ),
 .UNSPECIFIED. ) ;
#20375=ORIENTED_EDGE ( 'NONE', *, *, #10462, .T. ) ;
#20377=DIRECTION ( 'NONE',  ( -0.9996708941621513800, 0.02565352539213145919, 0.000000000000000000 ) ) ;
#20378=CARTESIAN_POINT ( 'NONE',  ( 12.00000000000000355, 4.044007772105016940, -8.050681685784468300 ) ) ;
#20380=CARTESIAN_POINT ( 'NONE',  ( 17.65928924998999960, -10.44232512227000065, 3.770426973323999675 ) ) ;
#20381=CARTESIAN_POINT ( 'NONE',  ( -23.75395899076999839, -6.467918998394999619, 12.35506162266000096 ) ) ;
#20383=ADVANCED_FACE ( 'NONE', ( #3116 ), #15918, .F. ) ;
#20387=CARTESIAN_POINT ( 'NONE',  ( -10.41087756584999902, 13.64079441408000015, -5.914944034101999648 ) ) ;
#20390=ORIENTED_EDGE ( 'NONE', *, *, #13203, .T. ) ;
#20391=CARTESIAN_POINT ( 'NONE',  ( -14.25243324638999809, 13.93375672974000068, 0.8660254037843999608 ) ) ;
#20392=CARTESIAN_POINT ( 'NONE',  ( 20.43528936713000377, -9.195691514035999603, 0.000000000000000000 ) ) ;
#20393=CARTESIAN_POINT ( 'NONE',  ( 6.243178309830739181, 13.63940964843087578, 1.910546506728590499 ) ) ;
#20394=CARTESIAN_POINT ( 'NONE',  ( 16.01370422644536262, -8.164120605562965594, -6.375661808576880141 ) ) ;
#20395=CARTESIAN_POINT ( 'NONE',  ( -14.11091303572000122, -1.546633701460999877, 10.88482645332999965 ) ) ;
#20397=VECTOR ( 'NONE', #6882, 1000.000000000000000 ) ;
#20402=CARTESIAN_POINT ( 'NONE',  ( 21.83141184951952596, 4.028956422608725774, -9.926641748303772772 ) ) ;
#20404=B_SPLINE_CURVE_WITH_KNOTS ( 'NONE', 3,
 ( #4796, #12180, #18917, #9832, #5948, #22543, #20860, #6195, #4271, #13700 ),
 .UNSPECIFIED., .F., .F.,
 ( 4, 2, 2, 2, 4 ),
 ( 0.000000000000000000, 0.1249999999999998335, 0.2499999999999996669, 0.4999999999999996669, 1.000000000000000000 ),
 .UNSPECIFIED. ) ;
#20405=EDGE_LOOP ( 'NONE', ( #16972, #13445 ) ) ;
#20406=CONICAL_SURFACE ( 'NONE', #21178, 13.97499999999999964, 1.402900403544236729 ) ;
#20408=CARTESIAN_POINT ( 'NONE',  ( -23.75856372112281178, -13.93375672973999890, -3.388131789017201356E-17 ) ) ;
#20409=CARTESIAN_POINT ( 'NONE',  ( 18.32906392130999862, 1.076221949391999999, 9.704785274157000430 ) ) ;
#20410=ORIENTED_EDGE ( 'NONE', *, *, #18408, .T. ) ;
#20413=DIRECTION ( 'NONE',  ( 0.000000000000000000, 0.000000000000000000, -1.000000000000000000 ) ) ;
#20415=CARTESIAN_POINT ( 'NONE',  ( -15.53484587121333504, 2.373919399437545152, 8.833918887178354495 ) ) ;
#20416=CARTESIAN_POINT ( 'NONE',  ( 4.619606713675000087, 12.56765075308000768, 1.087864528862000579 ) ) ;
#20417=CARTESIAN_POINT ( 'NONE',  ( -21.33357328978999945, 7.007277454522999882, -6.553624248108999240 ) ) ;
#20419=CARTESIAN_POINT ( 'NONE',  ( 11.45478115325934709, -9.254429737870434991, -8.970723317480709724 ) ) ;
#20420=CARTESIAN_POINT ( 'NONE',  ( -4.823558943698996515, 13.17409018072999238, -5.974474971606000828 ) ) ;
#20422=LINE ( 'NONE', #5989, #19343 ) ;
#20423=CARTESIAN_POINT ( 'NONE',  ( 5.699442596042000098, 1.578914512950999657E-14, 0.000000000000000000 ) ) ;
#20424=CARTESIAN_POINT ( 'NONE',  ( -5.339911154187996445, 16.17862129490001877, 3.014836506089000334 ) ) ;
#20428=CARTESIAN_POINT ( 'NONE',  ( 14.12234300365937045, 9.014876618753284276, 1.130911957320933858 ) ) ;
#20430=CARTESIAN_POINT ( 'NONE',  ( -23.32191191764427529, -0.7265626699458933579, 10.55370311345722634 ) ) ;
#20432=CARTESIAN_POINT ( 'NONE',  ( 1.043766574049543872, 11.52930182343673593, 4.698691617476282723 ) ) ;
#20433=VERTEX_POINT ( 'NONE', #16399 ) ;
#20434=CARTESIAN_POINT ( 'NONE',  ( -4.849982476240733753, 12.44999999999999929, -0.4215379369927308995 ) ) ;
#20440=CARTESIAN_POINT ( 'NONE',  ( 16.81987658530999852, -0.9597138970337001362, 10.18860816546999892 ) ) ;
#20441=CARTESIAN_POINT ( 'NONE',  ( 18.32386509258522267, 7.507573501765766544, -7.224273886700561143 ) ) ;
#20442=EDGE_CURVE ( 'NONE', #9910, #10482, #8919, .T. ) ;
#20445=DIRECTION ( 'NONE',  ( -1.000000000000000000, 0.000000000000000000, 0.000000000000000000 ) ) ;
#20449=CARTESIAN_POINT ( 'NONE',  ( 20.75000399882000224, 8.798721959408998927, 6.165518250330999983 ) ) ;
#20451=CARTESIAN_POINT ( 'NONE',  ( -24.43053737900748246, 6.547205609487094513, -7.918560603455738089 ) ) ;
#20453=CARTESIAN_POINT ( 'NONE',  ( 6.243179582884000212, 1.148189900220999940E-14, 0.000000000000000000 ) ) ;
#20455=DIRECTION ( 'NONE',  ( -1.000000000000000000, 0.000000000000000000, 0.000000000000000000 ) ) ;
#20457=CARTESIAN_POINT ( 'NONE',  ( 2.334980371411002231, 11.67499751873000591, 4.254577570424000754 ) ) ;
#20459=EDGE_CURVE ( 'NONE', #5746, #9506, #10148, .T. ) ;
#20460=CARTESIAN_POINT ( 'NONE',  ( -19.80448867117999967, 7.367983127705000079, 8.228944869744001522 ) ) ;
#20461=VERTEX_POINT ( 'NONE', #5054 ) ;
#20464=AXIS2_PLACEMENT_3D ( 'NONE', #13931, #16095, #14413 ) ;
#20467=CARTESIAN_POINT ( 'NONE',  ( 5.615220178540004881, 13.77392129510000451, 3.559094044476999397 ) ) ;
#20469=CARTESIAN_POINT ( 'NONE',  ( 16.50495603379667031, -4.580212439236231781, 7.946988475063720969 ) ) ;
#20472=CARTESIAN_POINT ( 'NONE',  ( 15.85912674931000055, -8.678267488395999152, -6.289192543930000490 ) ) ;
#20474=CARTESIAN_POINT ( 'NONE',  ( -16.77363468649999945, -9.766024879818999693, 0.2197783339474000119 ) ) ;
#20478=EDGE_CURVE ( 'NONE', #9831, #4023, #1493, .T. ) ;
#20479=ORIENTED_EDGE ( 'NONE', *, *, #22112, .F. ) ;
#20480=CARTESIAN_POINT ( 'NONE',  ( -21.53391127295000018, -1.797407140843000128, 11.09281522174999957 ) ) ;
#20482=CARTESIAN_POINT ( 'NONE',  ( 14.09191795553696913, -9.926564809749867990, -2.934343053110770594 ) ) ;
#20484=DIRECTION ( 'NONE',  ( 0.000000000000000000, -0.8660254037844288266, 0.5000000000000169864 ) ) ;
#20485=CARTESIAN_POINT ( 'NONE',  ( 23.86849505023999996, 10.71391760736999998, -3.584493356444999890 ) ) ;
#20487=CARTESIAN_POINT ( 'NONE',  ( 13.79821159651314311, 9.024933071421822106, -0.1076915288274838262 ) ) ;
#20491=ADVANCED_FACE ( 'NONE', ( #3931 ), #10697, .F. ) ;
#20492=CARTESIAN_POINT ( 'NONE',  ( 22.84441020264000244, -10.91804186159999901, 3.505057996334000503 ) ) ;
#20493=VERTEX_POINT ( 'NONE', #15055 ) ;
#20496=AXIS2_PLACEMENT_3D ( 'NONE', #4755, #6435, #13945 ) ;
#20497=ORIENTED_EDGE ( 'NONE', *, *, #4648, .T. ) ;
#20501=CARTESIAN_POINT ( 'NONE',  ( 19.13672573371000141, -5.603022739495999716, 8.809601378027998919 ) ) ;
#20502=CARTESIAN_POINT ( 'NONE',  ( -17.43032910583999850, 9.118578311265999048, 0.000000000000000000 ) ) ;
#20504=ORIENTED_EDGE ( 'NONE', *, *, #6996, .F. ) ;
#20506=CARTESIAN_POINT ( 'NONE',  ( -11.52355113877000115, -6.819129568044999701, 13.60514851516999890 ) ) ;
#20508=CARTESIAN_POINT ( 'NONE',  ( -14.47158024777374052, -9.790304928767106674, -8.042633409158213453 ) ) ;
#20512=CARTESIAN_POINT ( 'NONE',  ( -24.41513307467224436, 9.801374016728995997, 8.023466425259611512 ) ) ;
#20513=CARTESIAN_POINT ( 'NONE',  ( 4.834780805419000238, 12.45065217972999960, 0.000000000000000000 ) ) ;
#20514=FACE_BOUND ( 'NONE', #3289, .T. ) ;
#20515=CARTESIAN_POINT ( 'NONE',  ( 16.03895867897560734, -7.582969449584280319, -7.062017480966269467 ) ) ;
#20516=CARTESIAN_POINT ( 'NONE',  ( -17.65609590006000218, -11.00188783733999998, 1.405720899317999928 ) ) ;
#20518=CARTESIAN_POINT ( 'NONE',  ( -15.02697771723000031, -1.474210749020000044, -10.68967233462999999 ) ) ;
#20521=VERTEX_POINT ( 'NONE', #22326 ) ;
#20523=EDGE_CURVE ( 'NONE', #15500, #1220, #19973, .T. ) ;
#20524=CARTESIAN_POINT ( 'NONE',  ( 20.21412898074317965, 9.226432912327343416, -5.052731391976187147 ) ) ;
#20526=EDGE_LOOP ( 'NONE', ( #18629, #3539, #2472, #3759 ) ) ;
#20528=CARTESIAN_POINT ( 'NONE',  ( -23.75701756406583343, -13.93375672974000068, 0.3849425536981887497 ) ) ;
#20529=CARTESIAN_POINT ( 'NONE',  ( 17.56125142131000061, 3.538711643716999866, -9.078802261343000168 ) ) ;
#20530=ORIENTED_EDGE ( 'NONE', *, *, #2779, .T. ) ;
#20531=CARTESIAN_POINT ( 'NONE',  ( -14.25851234816000002, 6.967815116019000499, -12.06644646457999848 ) ) ;
#20532=CARTESIAN_POINT ( 'NONE',  ( -14.44097977832075941, 2.973612400766980635, -12.49999313495041697 ) ) ;
#20534=CARTESIAN_POINT ( 'NONE',  ( -23.23831814003093399, 2.819964850040427518, -8.988637406128791696 ) ) ;
#20535=CARTESIAN_POINT ( 'NONE',  ( -4.694474657144001029, 12.59750342685999591, 1.086550191527999143 ) ) ;
#20537=CARTESIAN_POINT ( 'NONE',  ( 12.00000000000000000, -2.090383947266901465, -9.242149839633347241 ) ) ;
#20538=CARTESIAN_POINT ( 'NONE',  ( 19.49049770046332242, 9.171446297783335311, -1.200666460651649947 ) ) ;
#20545=CARTESIAN_POINT ( 'NONE',  ( 23.07322687843999987, 9.811823008121001166, -1.038166454746999978 ) ) ;
#20547=CARTESIAN_POINT ( 'NONE',  ( 14.49567727038531650, 1.385394744686596846, 8.990065437785395019 ) ) ;
#20552=CARTESIAN_POINT ( 'NONE',  ( -2.792997288517848897, 11.81229427091517792, -3.933476770808612244 ) ) ;
#20553=LINE ( 'NONE', #9299, #14959 ) ;
#20555=ORIENTED_EDGE ( 'NONE', *, *, #16173, .T. ) ;
#20556=CARTESIAN_POINT ( 'NONE',  ( 13.52925158531000172, -9.668754250937999117, 3.079128054934999525 ) ) ;
#20557=CARTESIAN_POINT ( 'NONE',  ( 24.50000000000000000, 4.174438572590999431E-14, -12.50000000000000000 ) ) ;
#20559=CARTESIAN_POINT ( 'NONE',  ( 15.53114037305999950, 2.007458543610999957, 10.62532755895000136 ) ) ;
#20560=CARTESIAN_POINT ( 'NONE',  ( 13.50000000000000178, -7.707699124303561078, -5.256970985969869226 ) ) ;
#20562=CARTESIAN_POINT ( 'NONE',  ( 22.87459322467000078, -1.252498931826999895, 10.72907436738999998 ) ) ;
#20563=VECTOR ( 'NONE', #3367, 1000.000000000000227 ) ;
#20565=ORIENTED_EDGE ( 'NONE', *, *, #8212, .T. ) ;
#20568=CARTESIAN_POINT ( 'NONE',  ( 4.833443960760002156, 12.42174102045999895, -0.1521463468820001830 ) ) ;
#20570=CARTESIAN_POINT ( 'NONE',  ( -24.12822391257000021, 5.443199013828000865, -9.745701579671997905 ) ) ;
#20573=AXIS2_PLACEMENT_3D ( 'NONE', #16112, #18418, #1827 ) ;
#20574=VERTEX_POINT ( 'NONE', #17000 ) ;
#20575=EDGE_CURVE ( 'NONE', #11791, #21237, #1407, .T. ) ;
#20579=DIRECTION ( 'NONE',  ( 1.000000000000000000, 0.000000000000000000, 0.000000000000000000 ) ) ;
#20580=CARTESIAN_POINT ( 'NONE',  ( 18.93264468355999952, 0.000000000000000000, 0.000000000000000000 ) ) ;
#20582=CARTESIAN_POINT ( 'NONE',  ( 15.20100174931000048, 0.8726850093137999975, 10.66462197497000020 ) ) ;
#20583=( NAMED_UNIT ( * ) SI_UNIT ( $, .STERADIAN. ) SOLID_ANGLE_UNIT ( ) );
#20584=CARTESIAN_POINT ( 'NONE',  ( -15.39248033193999987, -8.001506135565000122, 6.430926145009000727 ) ) ;
#20587=CARTESIAN_POINT ( 'NONE',  ( -14.42499035157292298, 3.357933904594045948, 12.49997221285009452 ) ) ;
#20588=ORIENTED_EDGE ( 'NONE', *, *, #8923, .F. ) ;
#20592=CARTESIAN_POINT ( 'NONE',  ( 13.69973086387940242, -4.969862238816942224, 9.044112284830802651 ) ) ;
#20593=CARTESIAN_POINT ( 'NONE',  ( -11.00000000000000000, -10.59999999999999964, 0.000000000000000000 ) ) ;
#20594=CARTESIAN_POINT ( 'NONE',  ( 24.19866361008999789, 10.75771654126000065, 3.480411140149000104 ) ) ;
#20596=CARTESIAN_POINT ( 'NONE',  ( 14.37697681739622091, -3.685858481565998268, 8.257677185639298756 ) ) ;
#20597=CARTESIAN_POINT ( 'NONE',  ( 20.43528936713000377, -9.195691514035999603, 0.000000000000000000 ) ) ;
#20598=CARTESIAN_POINT ( 'NONE',  ( -6.559180854920310111, 15.42694216100158044, 1.532439657023070723 ) ) ;
#20599=CARTESIAN_POINT ( 'NONE',  ( 11.07373617190084403, 10.57520287783416002, -6.683140124535795756 ) ) ;
#20602=DIRECTION ( 'NONE',  ( -1.000000000000000000, 0.000000000000000000, 0.000000000000000000 ) ) ;
#20605=EDGE_CURVE ( 'NONE', #8738, #11139, #11446, .T. ) ;
#20606=B_SPLINE_SURFACE_WITH_KNOTS ( 'NONE', 3, 3, ( 
 ( #1267, #14098, #21493, #3097, #16018, #23412, #10600, #1387, #16142, #22548, #8267, #19407, #6071, #20979, #17103, #9721, #8020, #745, #22782, #15631, #16985, #21225, #387, #11780, #7784, #15514, #15153, #5955, #19154, #11543, #8149, #9956, #22902, #13462, #2564 ),
 ( #501, #4147, #20865, #6318, #4275, #21096, #18923, #11901, #2332, #7902, #15271, #11663, #19035, #2445, #9837, #17219, #617, #15876, #1361, #21467, #8750, #5238, #10571, #21344, #23144, #1484, #19533, #2939, #10688, #5009, #8389, #14072, #16115, #1115, #4880 ),
 ( #6566, #23517, #21594, #18077, #17957, #6928, #17843, #19891, #12395, #13950, #988, #3307, #15755, #10455, #6680, #7047, #8517, #3189, #12623, #8628, #8878, #19779, #14324, #21713, #4759, #12145, #5123, #14430, #15991, #12506, #16248, #23640, #21825, #12268, #23266 ),
 ( #20007, #19655, #10327, #17594, #10201, #17718, #3070, #1237, #23384, #6803, #14196, #5695, #13080, #16596, #11037, #12961, #5349, #13197, #2062, #12849, #20480, #3888, #18420, #11155, #14544, #22058, #5467, #11279, #18656, #15008, #20245, #18541, #12738, #14663, #7631 ) ),
 .UNSPECIFIED., .F., .F., .F.,
 ( 4, 4 ),
 ( 4, 1, 1, 1, 1, 1, 1, 1, 1, 1, 1, 1, 1, 1, 1, 1, 1, 1, 1, 1, 1, 1, 1, 1, 1, 1, 1, 1, 1, 1, 1, 1, 4 ),
 ( -0.08408083179840999954, 1.084080831798000188 ),
 ( 0.1394980018163999858, 0.1669159576409000034, 0.1943339134653999933, 0.2217518692897999799, 0.2491698251142999976, 0.2765877809387999875, 0.3040057367633000052, 0.3314236925876999917, 0.3588416484122000094, 0.3862596042366999716, 0.4136775600611999892, 0.4410955158857000069, 0.4685134717100999935, 0.4959314275345999556, 0.5233493833590999733, 0.5507673391835999910, 0.5781852950080000886, 0.6056032508324999952, 0.6330212066570000129, 0.6604391624814999195, 0.6878571183060000482, 0.7152750741304000348, 0.7426930299549000525, 0.7701109857793999591, 0.7975289416039000878, 0.8249468974282999634, 0.8523648532527999810, 0.8797828090773001097, 0.9072007649018000164, 0.9346187207262000030, 0.9620366765507000206, 0.9894546323751999273, 1.016872588200000038 ),
 .UNSPECIFIED. ) ;
#20609=CARTESIAN_POINT ( 'NONE',  ( -23.74465998031000069, -6.216878364870000340, -12.50000000000000000 ) ) ;
#20610=CARTESIAN_POINT ( 'NONE',  ( 13.27582570505999904, 3.894665007329999540, 9.762755509399999809 ) ) ;
#20611=CARTESIAN_POINT ( 'NONE',  ( -14.25243324638999809, -7.716878364870000340, -11.63397459621999985 ) ) ;
#20615=LINE ( 'NONE', #19031, #10340 ) ;
#20618=CARTESIAN_POINT ( 'NONE',  ( 18.22028936713000036, -1.652712406954000013, 8.988165862088999702 ) ) ;
#20621=CARTESIAN_POINT ( 'NONE',  ( -14.45561352951336609, 12.11761689492931282, 4.011600805608035891 ) ) ;
#20622=CARTESIAN_POINT ( 'NONE',  ( 20.38206396265981368, 7.578948228821809963, 7.305733806372995076 ) ) ;
#20623=CARTESIAN_POINT ( 'NONE',  ( 6.195288800946270769, 13.89803996554030974, 0.8525294906254528016 ) ) ;
#20624=CARTESIAN_POINT ( 'NONE',  ( 15.75587683109987580, -10.06225463003949194, 2.437168688431326391 ) ) ;
#20625=CARTESIAN_POINT ( 'NONE',  ( -16.78682104303999978, 7.979255941467000568, -7.669513122050999776 ) ) ;
#20627=CARTESIAN_POINT ( 'NONE',  ( -18.31782136596999777, 10.89202446812999980, 3.425794516969999925 ) ) ;
#20635=EDGE_CURVE ( 'NONE', #23530, #17452, #3357, .T. ) ;
#20636=CARTESIAN_POINT ( 'NONE',  ( 24.50000000000001066, -1.022558425349066269, 12.50000000000000533 ) ) ;
#20639=CARTESIAN_POINT ( 'NONE',  ( -13.99999999999999822, -9.939587166035000365, 2.689278564876886435 ) ) ;
#20640=CARTESIAN_POINT ( 'NONE',  ( 12.59887625730999972, 2.316137192978999781, 8.804988873405999783 ) ) ;
#20641=ORIENTED_EDGE ( 'NONE', *, *, #4070, .T. ) ;
#20642=CARTESIAN_POINT ( 'NONE',  ( -6.310601434888994277, 16.13748856436002654, -0.9718497405647000820 ) ) ;
#20643=LINE ( 'NONE', #644, #3256 ) ;
#20645=ORIENTED_EDGE ( 'NONE', *, *, #9282, .T. ) ;
#20647=CARTESIAN_POINT ( 'NONE',  ( -15.98834587121332795, 8.845253692700577375, -2.376965543786443202 ) ) ;
#20649=CARTESIAN_POINT ( 'NONE',  ( 0.8060258553945994775, 11.68578183133999282, 4.773271256242001215 ) ) ;
#20650=CARTESIAN_POINT ( 'NONE',  ( 12.00000000000000000, -1.414133744360243083, -9.331047239918021319 ) ) ;
#20652=CARTESIAN_POINT ( 'NONE',  ( -4.588766208978104721, 13.47548078768067192, 5.171706116033917056 ) ) ;
#20656=AXIS2_PLACEMENT_3D ( 'NONE', #6354, #9871, #10237 ) ;
#20658=ORIENTED_EDGE ( 'NONE', *, *, #19013, .T. ) ;
#20659=CARTESIAN_POINT ( 'NONE',  ( -17.50591243917333983, 8.883183840251577479, -2.387158987722542314 ) ) ;
#20660=CARTESIAN_POINT ( 'NONE',  ( 23.12578860888000065, 7.434166750538000912, -7.277889744973999875 ) ) ;
#20661=CARTESIAN_POINT ( 'NONE',  ( 0.8894771940131762644, 12.83047529882638926, -6.611550444528325521 ) ) ;
#20662=LINE ( 'NONE', #22351, #23897 ) ;
#20663=ADVANCED_FACE ( 'NONE', ( #13717 ), #13359, .T. ) ;
#20664=CARTESIAN_POINT ( 'NONE',  ( -23.08092454245977976, -8.305383183722334195, 6.545568425691888237 ) ) ;
#20669=CARTESIAN_POINT ( 'NONE',  ( -17.29360359819550297, -9.005800717077383055, -5.261463894023568955 ) ) ;
#20670=CARTESIAN_POINT ( 'NONE',  ( 23.99478584078000054, -7.550251870568999379, -11.73017644755000077 ) ) ;
#20674=EDGE_CURVE ( 'NONE', #8671, #4654, #11910, .T. ) ;
#20678=CARTESIAN_POINT ( 'NONE',  ( 12.43237658531000100, 5.753414546153999609, -8.323445001914000940 ) ) ;
#20679=CARTESIAN_POINT ( 'NONE',  ( -17.59444652563999867, -11.39502044605000108, 0.2566590569923999920 ) ) ;
#20681=CARTESIAN_POINT ( 'NONE',  ( 14.24421080085999947, -6.039990374987000088, -9.570627441890000142 ) ) ;
#20682=CARTESIAN_POINT ( 'NONE',  ( 13.49999999999999822, -8.457508417532315192, -4.109938046728712990 ) ) ;
#20683=DIRECTION ( 'NONE',  ( 0.000000000000000000, 0.000000000000000000, -1.000000000000000000 ) ) ;
#20684=CARTESIAN_POINT ( 'NONE',  ( 24.03114330764999806, 0.4208889323872999633, -10.29577946621999907 ) ) ;
#20685=CARTESIAN_POINT ( 'NONE',  ( 3.000000000000000000, 20.00000000000000000, 0.000000000000000000 ) ) ;
#20686=ORIENTED_EDGE ( 'NONE', *, *, #15224, .F. ) ;
#20687=CARTESIAN_POINT ( 'NONE',  ( -14.25243324638999809, -6.216878364870000340, -12.50000000000000000 ) ) ;
#20690=CARTESIAN_POINT ( 'NONE',  ( -3.189163304378001218, 11.94355460396000268, 3.580087194034999865 ) ) ;
#20692=CARTESIAN_POINT ( 'NONE',  ( -23.10525368899999776, -11.00684294169000133, 1.684798661880999804 ) ) ;
#20694=DIRECTION ( 'NONE',  ( 0.000000000000000000, 1.000000000000000000, 0.000000000000000000 ) ) ;
#20695=VERTEX_POINT ( 'NONE', #517 ) ;
#20696=CARTESIAN_POINT ( 'NONE',  ( -24.50000000000453326, 0.5124611672102585835, -12.50000000000234301 ) ) ;
#20697=CARTESIAN_POINT ( 'NONE',  ( 1.254873950010960026, 11.63135044190335599, 4.623136993607071865 ) ) ;
#20701=CARTESIAN_POINT ( 'NONE',  ( 15.74943924931000083, -10.38900229657999930, -2.621660623529000311 ) ) ;
#20702=CARTESIAN_POINT ( 'NONE',  ( -18.48019363270999804, 4.914628609928000103, -9.714689191606000307 ) ) ;
#20705=CARTESIAN_POINT ( 'NONE',  ( -14.46758738532042798, 2.198682497491741383, 12.49996900094042473 ) ) ;
#20709=CARTESIAN_POINT ( 'NONE',  ( 14.31900924450000723, -4.887163463281674503, -9.111456757049891664 ) ) ;
#20710=CARTESIAN_POINT ( 'NONE',  ( 2.121949948620001081, 12.82851042524998597, -6.764654941373005492 ) ) ;
#20711=FACE_OUTER_BOUND ( 'NONE', #21685, .T. ) ;
#20714=CARTESIAN_POINT ( 'NONE',  ( 14.68340655888479596, -9.046510072424961635, 0.7085215494182042217 ) ) ;
#20715=FACE_OUTER_BOUND ( 'NONE', #14708, .T. ) ;
#20717=VECTOR ( 'NONE', #9747, 1000.000000000000000 ) ;
#20718=CARTESIAN_POINT ( 'NONE',  ( 24.38510397947349162, -12.27045979993889802, -3.746940194273108204 ) ) ;
#20719=ORIENTED_EDGE ( 'NONE', *, *, #2453, .T. ) ;
#20726=B_SPLINE_CURVE_WITH_KNOTS ( 'NONE', 3,
 ( #10569, #2697, #12025, #862 ),
 .UNSPECIFIED., .F., .F.,
 ( 4, 4 ),
 ( 0.000000000000000000, 1.000000000000000000 ),
 .UNSPECIFIED. ) ;
#20728=ORIENTED_EDGE ( 'NONE', *, *, #13055, .F. ) ;
#20729=CARTESIAN_POINT ( 'NONE',  ( 14.11792989500000139, -6.227520601336999917, -9.073701378510998339 ) ) ;
#20730=CARTESIAN_POINT ( 'NONE',  ( -6.130190774865132752, 15.95791884716732767, 1.063281737135261418 ) ) ;
#20734=CARTESIAN_POINT ( 'NONE',  ( -14.00000000000000000, 3.582449869577975399, -8.571500952496775128 ) ) ;
#20735=CARTESIAN_POINT ( 'NONE',  ( -9.581549711695000582, -0.05265680612012000467, -15.56874310937000061 ) ) ;
#20737=CARTESIAN_POINT ( 'NONE',  ( -9.042815982636001948, 21.50000000000000000, 1.000000000000000000 ) ) ;
#20741=CARTESIAN_POINT ( 'NONE',  ( 6.151787191419744616, 14.12035391479590452, 0.2847419465408779216 ) ) ;
#20742=CARTESIAN_POINT ( 'NONE',  ( 15.42724554293097938, -1.981222823747588402, 10.15954205669230959 ) ) ;
#20744=CARTESIAN_POINT ( 'NONE',  ( -14.47223966578000010, 9.858263368903999790, 4.889297467510999695 ) ) ;
#20747=CARTESIAN_POINT ( 'NONE',  ( -13.56430720021000091, -8.266217267278999969, 6.000601104121999541 ) ) ;
#20749=VERTEX_POINT ( 'NONE', #23401 ) ;
#20751=CARTESIAN_POINT ( 'NONE',  ( -18.05147222760578174, -1.660822553031731763, 10.32521625223683870 ) ) ;
#20753=DIRECTION ( 'NONE',  ( -1.000000000000000000, 0.000000000000000000, 0.000000000000000000 ) ) ;
#20757=CARTESIAN_POINT ( 'NONE',  ( -12.50000000000000000, -7.500000000000000000, 0.000000000000000000 ) ) ;
#20758=CARTESIAN_POINT ( 'NONE',  ( 17.14893908531000122, -9.665900270332999256, 3.387665420544000217 ) ) ;
#20760=DIRECTION ( 'NONE',  ( 0.000000000000000000, 0.9780930753991020632, -0.2081680471550005351 ) ) ;
#20764=CARTESIAN_POINT ( 'NONE',  ( -12.50000000000000000, 6.606768802097000126, -6.099810110451000966 ) ) ;
#20765=AXIS2_PLACEMENT_3D ( 'NONE', #2694, #4141, #22776 ) ;
#20766=CARTESIAN_POINT ( 'NONE',  ( -12.48243343204000055, 6.965111533508000718, -5.686492047758000545 ) ) ;
#20767=CARTESIAN_POINT ( 'NONE',  ( 3.311115755811001371, 12.13908021832000372, 3.509723945568998360 ) ) ;
#20768=CARTESIAN_POINT ( 'NONE',  ( -14.00000000000000355, -1.546932818872876814, 9.717798975675457029 ) ) ;
#20771=CARTESIAN_POINT ( 'NONE',  ( -22.45768008457000064, -0.6428547435799999432, 9.603249762923001143 ) ) ;
#20773=CARTESIAN_POINT ( 'NONE',  ( 19.26374770046332330, 5.632616517831162462, -7.329538123794997695 ) ) ;
#20776=CARTESIAN_POINT ( 'NONE',  ( 5.274219629769681283, 13.82795425090464114, -4.206144534439919980 ) ) ;
#20780=CARTESIAN_POINT ( 'NONE',  ( -17.80824577250665897, 2.389424319302919653, -8.890643215737140892 ) ) ;
#20781=CARTESIAN_POINT ( 'NONE',  ( 19.78796100793000079, 4.592772578639999992, 8.629704802492000226 ) ) ;
#20782=CARTESIAN_POINT ( 'NONE',  ( 0.2655874759832465570, 12.80453501645971137, -6.661713502021730626 ) ) ;
#20784=CARTESIAN_POINT ( 'NONE',  ( -22.03664591665549821, 10.47998752884019957, -2.062401532638290735 ) ) ;
#20790=CARTESIAN_POINT ( 'NONE',  ( -18.41005308736142965, 10.25486752108468202, -2.049228009546027351 ) ) ;
#20791=CARTESIAN_POINT ( 'NONE',  ( 24.43449445986659896, 11.92557563953692856, 4.344297082815015365 ) ) ;
#20792=VECTOR ( 'NONE', #22483, 1000.000000000000227 ) ;
#20795=ORIENTED_EDGE ( 'NONE', *, *, #11594, .F. ) ;
#20796=CARTESIAN_POINT ( 'NONE',  ( 17.10962270046334055, -4.588261632613977348, -7.960449803099588273 ) ) ;
#20797=CARTESIAN_POINT ( 'NONE',  ( 15.09131424931000076, 4.764171260128000185, 9.577928620034999341 ) ) ;
#20800=CARTESIAN_POINT ( 'NONE',  ( 22.68304166666665367, 7.399526017309272063, -5.686719956180886548 ) ) ;
#20801=EDGE_CURVE ( 'NONE', #12095, #21674, #17655, .T. ) ;
#20802=CARTESIAN_POINT ( 'NONE',  ( 14.92176537305999950, 8.069302409968999612, -7.172646714567000537 ) ) ;
#20805=CARTESIAN_POINT ( 'NONE',  ( 24.38524151196000034, 9.842852006268000054, -3.081908802582999485 ) ) ;
#20806=PRODUCT ( 'MAS-673 Main Body', 'MAS-673 Main Body', '', ( #18011 ) ) ;
#20809=CARTESIAN_POINT ( 'NONE',  ( 11.85282401169000188, -8.499855654764999713, -2.882903103473000161 ) ) ;
#20811=CARTESIAN_POINT ( 'NONE',  ( -4.719941065002002389, 12.37770080416001051, 1.073222396542000023 ) ) ;
#20812=CARTESIAN_POINT ( 'NONE',  ( 24.39856360185587647, -9.628104977245440566, -2.325364009612112870 ) ) ;
#20813=CARTESIAN_POINT ( 'NONE',  ( -21.28778663430999885, -8.840331526475999624, 6.688932671969999078 ) ) ;
#20814=ORIENTED_EDGE ( 'NONE', *, *, #2750, .F. ) ;
#20818=ORIENTED_EDGE ( 'NONE', *, *, #9402, .F. ) ;
#20821=CARTESIAN_POINT ( 'NONE',  ( -1.857441216906001724, 12.79832155229998314, 6.826339096581000021 ) ) ;
#20824=CARTESIAN_POINT ( 'NONE',  ( 13.99443924931000005, -9.599271117524001085, -4.655318192544999789 ) ) ;
#20825=CARTESIAN_POINT ( 'NONE',  ( -18.07393293677000301, 10.37468091520999991, 3.263143967163999903 ) ) ;
#20826=CARTESIAN_POINT ( 'NONE',  ( 15.67012625730999886, 7.503068644359999873, -5.298384255253999697 ) ) ;
#20827=DIRECTION ( 'NONE',  ( -1.000000000000000000, 0.000000000000000000, 0.000000000000000000 ) ) ;
#20832=AXIS2_PLACEMENT_3D ( 'NONE', #13025, #7218, #7452 ) ;
#20833=CARTESIAN_POINT ( 'NONE',  ( 13.50000000000000000, 2.048741218006000064, 10.08990150394999930 ) ) ;
#20836=CARTESIAN_POINT ( 'NONE',  ( 0.5469854966064994217, 13.20286669322999806, -6.078858689229004852 ) ) ;
#20837=CARTESIAN_POINT ( 'NONE',  ( 19.24289560999000059, -4.617872442541000488, 10.17084159971000012 ) ) ;
#20839=CARTESIAN_POINT ( 'NONE',  ( 14.40622728660040508, -4.514104690157912714, 7.833270047916061962 ) ) ;
#20844=CARTESIAN_POINT ( 'NONE',  ( 23.99062354302999722, -13.93375672974000068, -0.8660254037843999608 ) ) ;
#20846=DIRECTION ( 'NONE',  ( 0.000000000000000000, 0.5009995559142040866, -0.8654475402783060600 ) ) ;
#20854=CARTESIAN_POINT ( 'NONE',  ( -14.25243324638999809, 13.93375672974000068, -0.8660254037843999608 ) ) ;
#20855=CARTESIAN_POINT ( 'NONE',  ( -6.990117763008002250, 15.33795737441000995, -1.812023283503998883 ) ) ;
#20860=CARTESIAN_POINT ( 'NONE',  ( -24.37124162824695617, 9.546779961769933820, -8.464497487737872916 ) ) ;
#20863=CARTESIAN_POINT ( 'NONE',  ( -24.16119556689903902, -8.771053125573958553, -9.807567373703745872 ) ) ;
#20865=CARTESIAN_POINT ( 'NONE',  ( -24.13073565549000321, -9.140001432355999711, -4.665568137828999262 ) ) ;
#20866=CARTESIAN_POINT ( 'NONE',  ( -24.11803009771418616, 8.641091274403159161, 10.03259869781534519 ) ) ;
#20867=CARTESIAN_POINT ( 'NONE',  ( 6.141065191050296690, 14.19649558781827103, 0.04858547980339427558 ) ) ;
#20868=CARTESIAN_POINT ( 'NONE',  ( 15.65124655084372840, -8.589975589872866024, 5.797750052853028357 ) ) ;
#20869=CARTESIAN_POINT ( 'NONE',  ( -15.63475771655999758, -5.016338890459000055, -9.829993491887998758 ) ) ;
#20874=CARTESIAN_POINT ( 'NONE',  ( -15.23010806520000138, -8.044096712135001326, -7.201187562783000651 ) ) ;
#20878=CARTESIAN_POINT ( 'NONE',  ( -18.48555983533165303, 10.20055682982866685, 2.347179025034034971 ) ) ;
#20879=ORIENTED_EDGE ( 'NONE', *, *, #13937, .T. ) ;
#20881=CARTESIAN_POINT ( 'NONE',  ( -4.860485347078998153, 13.74172132047000794, 4.702795991816000942 ) ) ;
#20884=CARTESIAN_POINT ( 'NONE',  ( 14.05125142131000082, 6.790538403688000102, -6.859017754185999571 ) ) ;
#20886=CARTESIAN_POINT ( 'NONE',  ( -6.017198780830001148, 15.84372863255997821, -1.061654000538000409 ) ) ;
#20887=CARTESIAN_POINT ( 'NONE',  ( -4.850000000102999920, 12.44999864901999942, -1.732907964652000048E-09 ) ) ;
#20891=CARTESIAN_POINT ( 'NONE',  ( 21.66266666666665941, -4.646869946770923576, 8.062640237677072719 ) ) ;
#20892=CARTESIAN_POINT ( 'NONE',  ( -3.580425678944999301, 12.20479645082998843, 3.123592402036998283 ) ) ;
#20893=CARTESIAN_POINT ( 'NONE',  ( 4.835083642289389694, 12.44448910615697912, 0.3758261001295359338 ) ) ;
#20894=CARTESIAN_POINT ( 'NONE',  ( 18.39048037518193368, 8.950322807170842054, -5.337459449838163117 ) ) ;
#20895=CIRCLE ( 'NONE', #1173, 10.65000000000000036 ) ;
#20896=DIRECTION ( 'NONE',  ( -1.000000000000000000, 0.000000000000000000, 0.000000000000000000 ) ) ;
#20899=CARTESIAN_POINT ( 'NONE',  ( -5.147503733180995411, 15.83089091750001742, -2.717754031361000688 ) ) ;
#20900=DIRECTION ( 'NONE',  ( 1.000000000000000000, 0.000000000000000000, 0.000000000000000000 ) ) ;
#20901=CARTESIAN_POINT ( 'NONE',  ( 5.243253597151068313, 14.63899575032571221, 3.172841098946398208 ) ) ;
#20906=CARTESIAN_POINT ( 'NONE',  ( 2.046202797321268196, 12.94580643705319645, -6.382747573611354142 ) ) ;
#20908=CARTESIAN_POINT ( 'NONE',  ( -19.78743041492825583, 2.646772407754812928, 10.15050686662911872 ) ) ;
#20913=CARTESIAN_POINT ( 'NONE',  ( -17.37733730988356839, -10.13133732267558074, -2.466463703678301478 ) ) ;
#20915=DIRECTION ( 'NONE',  ( 0.000000000000000000, 0.8660254037844288266, -0.5000000000000169864 ) ) ;
#20917=DIRECTION ( 'NONE',  ( 0.000000000000000000, 1.000000000000000000, 0.000000000000000000 ) ) ;
#20918=VERTEX_POINT ( 'NONE', #16969 ) ;
#20919=CARTESIAN_POINT ( 'NONE',  ( 17.33637270046333612, 2.386020194961869123, -8.878946354107190686 ) ) ;
#20920=CARTESIAN_POINT ( 'NONE',  ( 16.07850174930999998, -1.960161522604999762, -10.54265994730999978 ) ) ;
#20921=EDGE_CURVE ( 'NONE', #12884, #12435, #17345, .T. ) ;
#20923=CARTESIAN_POINT ( 'NONE',  ( 0.000000000000000000, 7.216878364870000340, 12.50000000000000000 ) ) ;
#20924=CARTESIAN_POINT ( 'NONE',  ( 13.70301537305999950, 2.512834476447000309, 10.46490100832000003 ) ) ;
#20925=CARTESIAN_POINT ( 'NONE',  ( 13.50000000000000178, -4.872488826576057974, -7.717741468829464324 ) ) ;
#20926=CARTESIAN_POINT ( 'NONE',  ( 20.49016126455000020, 3.425869769563000045, -9.615571166989999696 ) ) ;
#20931=CARTESIAN_POINT ( 'NONE',  ( -3.577956154687000900, 12.12797091520000592, 3.101079032933002466 ) ) ;
#20933=CARTESIAN_POINT ( 'NONE',  ( 24.19085492956958561, -9.549256642876626344, 0.0002501093553063627687 ) ) ;
#20934=CARTESIAN_POINT ( 'NONE',  ( -20.59898550229000236, 6.916942397327000336, -8.639163530769000232 ) ) ;
#20935=EDGE_LOOP ( 'NONE', ( #6964, #21524, #2444, #1768, #13417 ) ) ;
#20936=CARTESIAN_POINT ( 'NONE',  ( -5.529771451991000397, 1.198997689148999791E-14, -12.68487026514986837 ) ) ;
#20939=CARTESIAN_POINT ( 'NONE',  ( -20.25016455292000117, -8.657612072530000091, 3.085311466348000131 ) ) ;
#20941=CARTESIAN_POINT ( 'NONE',  ( 24.25008227645999881, 0.000000000000000000, 0.000000000000000000 ) ) ;
#20942=EDGE_CURVE ( 'NONE', #4204, #19823, #7824, .T. ) ;
#20944=CARTESIAN_POINT ( 'NONE',  ( 13.33631424930999998, 2.709556187140999661, 10.30084784107000040 ) ) ;
#20945=CARTESIAN_POINT ( 'NONE',  ( -17.26141154489999963, -10.85036612823000013, 0.2443279951607999767 ) ) ;
#20946=CARTESIAN_POINT ( 'NONE',  ( 11.94075125730999964, 5.167059442038000050, -7.475232529384999047 ) ) ;
#20947=CARTESIAN_POINT ( 'NONE',  ( 24.36165043081783921, 12.41271798542465810, -3.500541789220333211 ) ) ;
#20948=ORIENTED_EDGE ( 'NONE', *, *, #20942, .T. ) ;
#20949=EDGE_CURVE ( 'NONE', #93, #21190, #7514, .T. ) ;
#20951=EDGE_CURVE ( 'NONE', #12236, #10709, #3211, .T. ) ;
#20953=CARTESIAN_POINT ( 'NONE',  ( 14.16427405790947525, -8.883215205009282300, -5.323156792243073809 ) ) ;
#20954=CARTESIAN_POINT ( 'NONE',  ( 5.223518823337998995, 13.88591009669999643, -3.771757984836998201 ) ) ;
#20955=CARTESIAN_POINT ( 'NONE',  ( -23.74465998031000069, 13.93375672974000068, -0.8660254037843999608 ) ) ;
#20957=CARTESIAN_POINT ( 'NONE',  ( 12.52688711657000020, 6.216878364870000340, 12.50000000000000000 ) ) ;
#20958=PLANE ( 'NONE',  #6920 ) ;
#20959=DIRECTION ( 'NONE',  ( 0.000000000000000000, 1.000000000000000000, 0.000000000000000000 ) ) ;
#20961=CARTESIAN_POINT ( 'NONE',  ( 23.99895687519799381, 13.93375672974000068, -0.3849913042976704780 ) ) ;
#20962=ORIENTED_EDGE ( 'NONE', *, *, #22865, .F. ) ;
#20963=CARTESIAN_POINT ( 'NONE',  ( 4.749995115181361527, 12.55003697659937778, -0.6285192019201937264 ) ) ;
#20965=CARTESIAN_POINT ( 'NONE',  ( 23.99062354302999722, 7.716878364870000340, 11.63397459621999985 ) ) ;
#20966=CARTESIAN_POINT ( 'NONE',  ( -2.212704257922113005, 11.69046487145196878, 4.282078202130872313 ) ) ;
#20969=CARTESIAN_POINT ( 'NONE',  ( 13.68936949739000042, -0.4386406477174999985, 10.98417168335999961 ) ) ;
#20970=CARTESIAN_POINT ( 'NONE',  ( -10.04281598263999875, 16.40330333352000025, 0.9999999999983999466 ) ) ;
#20972=ORIENTED_EDGE ( 'NONE', *, *, #19914, .F. ) ;
#20973=EDGE_LOOP ( 'NONE', ( #19377, #14739 ) ) ;
#20974=CARTESIAN_POINT ( 'NONE',  ( -14.00000000000000355, -2.579277104765260287, -9.307187374249766165 ) ) ;
#20975=DIRECTION ( 'NONE',  ( -1.000000000000000000, 0.000000000000000000, 0.000000000000000000 ) ) ;
#20977=ORIENTED_EDGE ( 'NONE', *, *, #9399, .T. ) ;
#20978=EDGE_CURVE ( 'NONE', #15392, #19135, #13005, .T. ) ;
#20979=CARTESIAN_POINT ( 'NONE',  ( -22.00181313460999988, -7.290803318660999288, -6.369760926427000314 ) ) ;
#20982=CARTESIAN_POINT ( 'NONE',  ( 15.83035365568370345, -10.35462237868133251, -0.2935575748633351134 ) ) ;
#20983=CARTESIAN_POINT ( 'NONE',  ( -15.48813611968000004, -5.014512979174000407, -9.826416270666999964 ) ) ;
#20985=CARTESIAN_POINT ( 'NONE',  ( -21.20489941501549680, -10.23248319439458598, -2.462552185894037571 ) ) ;
#20987=CARTESIAN_POINT ( 'NONE',  ( -12.75178580833000019, 5.886008164689000566, -8.319303600761999817 ) ) ;
#20991=CARTESIAN_POINT ( 'NONE',  ( -18.74601239996717084, 8.305110545182456505, -6.624969937855211377 ) ) ;
#20994=CARTESIAN_POINT ( 'NONE',  ( 6.258925775870999075, 13.70565998269001007, -0.4762665460848001797 ) ) ;
#20995=CARTESIAN_POINT ( 'NONE',  ( -9.042815982636001948, 21.50000000000000000, -1.000000000000000000 ) ) ;
#20996=CARTESIAN_POINT ( 'NONE',  ( -19.61634587121332984, 8.935932136875853971, -2.401334698577377136 ) ) ;
#20997=CARTESIAN_POINT ( 'NONE',  ( 17.36831408530999710, -9.345903658884999743, -4.204539402675000481 ) ) ;
#20999=VECTOR ( 'NONE', #14770, 1000.000000000000114 ) ;
#21000=CYLINDRICAL_SURFACE ( 'NONE', #17183, 4.750000000000000000 ) ;
#21001=DIRECTION ( 'NONE',  ( 0.000000000000000000, -0.8660254037844288266, -0.5000000000000169864 ) ) ;
#21004=CARTESIAN_POINT ( 'NONE',  ( -12.50000000000000000, 6.907686671057999384, -5.757541812536000059 ) ) ;
#21005=CARTESIAN_POINT ( 'NONE',  ( 21.20916666666666828, 8.052471370503557324, 4.641008978248494010 ) ) ;
#21008=CARTESIAN_POINT ( 'NONE',  ( 17.66429342642312506, -10.35204213498203529, -1.010235597007892450 ) ) ;
#21009=DIRECTION ( 'NONE',  ( 0.000000000000000000, -1.000000000000000000, 0.000000000000000000 ) ) ;
#21010=CARTESIAN_POINT ( 'NONE',  ( -14.44633174692025257, -9.404057468159601640, 8.711677720893282739 ) ) ;
#21011=CARTESIAN_POINT ( 'NONE',  ( 20.05093419402000166, 9.971126252470000395, -5.084926271798999586 ) ) ;
#21012=CARTESIAN_POINT ( 'NONE',  ( -24.50000000000000000, -9.995791495354000133, -2.484784171996999635 ) ) ;
#21015=EDGE_CURVE ( 'NONE', #5364, #6975, #14180, .T. ) ;
#21017=VERTEX_POINT ( 'NONE', #20965 ) ;
#21018=CARTESIAN_POINT ( 'NONE',  ( 21.57978114040000150, 10.23905130607999858, 1.583883726447000040 ) ) ;
#21019=CARTESIAN_POINT ( 'NONE',  ( 1.988887572331500264, 12.93803022255735513, -6.398493247991286381 ) ) ;
#21023=CARTESIAN_POINT ( 'NONE',  ( 12.49102043339000012, -6.966941063182999549, 12.06695109921999887 ) ) ;
#21025=CARTESIAN_POINT ( 'NONE',  ( -18.63334298519549037, 5.912611358794215732, -8.628805914905690599 ) ) ;
#21028=ORIENTED_EDGE ( 'NONE', *, *, #20575, .F. ) ;
#21029=ORIENTED_EDGE ( 'NONE', *, *, #1522, .F. ) ;
#21030=DIRECTION ( 'NONE',  ( -1.000000000000000000, 0.000000000000000000, 0.000000000000000000 ) ) ;
#21031=CARTESIAN_POINT ( 'NONE',  ( 15.42037674930999991, -6.716928621565999791, 8.336789182003000676 ) ) ;
#21033=CARTESIAN_POINT ( 'NONE',  ( -24.75634994828000046, -3.427561506178000261, -9.776571129776000291 ) ) ;
#21034=FACE_OUTER_BOUND ( 'NONE', #1694, .T. ) ;
#21035=CARTESIAN_POINT ( 'NONE',  ( 20.15099999999999980, -9.188396088570998543, 0.000000000000000000 ) ) ;
#21036=CARTESIAN_POINT ( 'NONE',  ( 17.49562451746000136, 9.785307064097999330, 0.2529327338658999835 ) ) ;
#21038=DIRECTION ( 'NONE',  ( 0.000000000000000000, 0.000000000000000000, 1.000000000000000000 ) ) ;
#21039=CARTESIAN_POINT ( 'NONE',  ( 24.83359518631000284, 9.330707640295999639, 2.986814357572999956 ) ) ;
#21045=CARTESIAN_POINT ( 'NONE',  ( 1.498680770896810621, 13.80134043704015134, 5.938834979248682977 ) ) ;
#21047=CARTESIAN_POINT ( 'NONE',  ( 2.856683780965000974, 11.85702083262999551, 3.848598579512004125 ) ) ;
#21049=CARTESIAN_POINT ( 'NONE',  ( -24.29530845835000008, -0.7740144453498000177, -11.14062775012999928 ) ) ;
#21052=CARTESIAN_POINT ( 'NONE',  ( 15.37120603379664452, -2.373054804797890771, -8.829731701983224212 ) ) ;
#21055=CARTESIAN_POINT ( 'NONE',  ( 2.032271969870999673, 13.38796172288000008, 5.759841364760997173 ) ) ;
#21057=CYLINDRICAL_SURFACE ( 'NONE', #16919, 3.000000000000000000 ) ;
#21058=CARTESIAN_POINT ( 'NONE',  ( -19.29271502458999876, -7.174960688273000819, 7.031698840148000507 ) ) ;
#21059=CARTESIAN_POINT ( 'NONE',  ( 11.72137625731000021, -1.402369408125999861, -8.972525410429000203 ) ) ;
#21061=CARTESIAN_POINT ( 'NONE',  ( 19.02704979327631563, -1.056774037771824659, 10.41726730992272287 ) ) ;
#21063=CARTESIAN_POINT ( 'NONE',  ( 18.88192006459015815, -2.931848336738577920, 10.06696835938748613 ) ) ;
#21066=CARTESIAN_POINT ( 'NONE',  ( 2.185944241689015577, 13.92477108654476226, -5.721947785552420562 ) ) ;
#21068=B_SPLINE_CURVE_WITH_KNOTS ( 'NONE', 3,
 ( #16848, #12981, #4135, #20381, #6061 ),
 .UNSPECIFIED., .F., .F.,
 ( 4, 1, 4 ),
 ( 0.000000000000000000, 0.5000000000000000000, 1.000000000000000000 ),
 .UNSPECIFIED. ) ;
#21070=CARTESIAN_POINT ( 'NONE',  ( -24.27585716844903629, 12.49018833524722005, -3.366221553795681665 ) ) ;
#21073=CARTESIAN_POINT ( 'NONE',  ( 14.51215565209456493, -7.098368344587701273, 5.661432951517745948 ) ) ;
#21074=CARTESIAN_POINT ( 'NONE',  ( 18.65735837579211065, 4.963167965536912973, 9.221758217482731723 ) ) ;
#21075=CARTESIAN_POINT ( 'NONE',  ( -4.544324455327999779, 13.49053734526000170, 5.132126114358000812 ) ) ;
#21078=CARTESIAN_POINT ( 'NONE',  ( 12.52688711657000020, 7.716878364870000340, -11.63397459621999985 ) ) ;
#21079=EDGE_LOOP ( 'NONE', ( #15264, #931, #7530, #12515, #15060 ) ) ;
#21081=CARTESIAN_POINT ( 'NONE',  ( 11.53663804757020372, -12.55807338463293377, 3.248594360953877214 ) ) ;
#21082=ORIENTED_EDGE ( 'NONE', *, *, #21974, .T. ) ;
#21085=ADVANCED_FACE ( 'NONE', ( #2683 ), #4260, .T. ) ;
#21086=CARTESIAN_POINT ( 'NONE',  ( -2.485727719834888827, 13.00711836349921846, 6.259936974863422599 ) ) ;
#21087=CARTESIAN_POINT ( 'NONE',  ( 6.142597811584451506, 14.18464560812138409, -0.09518466390937729837 ) ) ;
#21088=CARTESIAN_POINT ( 'NONE',  ( -6.803841411146002827, 15.25658587585999904, -2.419657731435000958 ) ) ;
#21089=CARTESIAN_POINT ( 'NONE',  ( -6.707538334066213359, 15.26746356158001205, 2.299058024840869852 ) ) ;
#21090=ORIENTED_EDGE ( 'NONE', *, *, #23079, .T. ) ;
#21091=ORIENTED_EDGE ( 'NONE', *, *, #9180, .T. ) ;
#21092=LINE ( 'NONE', #11420, #14579 ) ;
#21095=VERTEX_POINT ( 'NONE', #13810 ) ;
#21096=CARTESIAN_POINT ( 'NONE',  ( -23.61663544866999587, 6.459431347288000502, -7.956344550455000331 ) ) ;
#21098=CARTESIAN_POINT ( 'NONE',  ( 6.145997960467107113, 14.15927157517049118, 0.1820614432005297212 ) ) ;
#21099=CARTESIAN_POINT ( 'NONE',  ( 15.76307053266625857, -10.12283687570989521, 2.174611644706195612 ) ) ;
#21100=CARTESIAN_POINT ( 'NONE',  ( -15.81542103158999701, -9.827833029818000554, -5.031439001898000640 ) ) ;
#21104=CARTESIAN_POINT ( 'NONE',  ( -19.68652699590384358, -7.391915032640794969, 7.432987506013617462 ) ) ;
#21106=CIRCLE ( 'NONE', #21496, 10.65000000000000036 ) ;
#21107=CARTESIAN_POINT ( 'NONE',  ( 23.99062354302999722, 13.93375672974000068, -0.8660254037843999608 ) ) ;
#21111=CARTESIAN_POINT ( 'NONE',  ( -16.11254757976368168, -5.837216003886290139, 8.603859594677571110 ) ) ;
#21113=CARTESIAN_POINT ( 'NONE',  ( 6.021392403978000907, 13.76381744684999830, -1.771980677399001669 ) ) ;
#21114=ADVANCED_FACE ( 'NONE', ( #4229 ), #9677, .F. ) ;
#21116=EDGE_CURVE ( 'NONE', #4654, #12558, #17656, .T. ) ;
#21119=( BOUNDED_SURFACE ( )  B_SPLINE_SURFACE ( 3, 3, ( 
 ( #1758, #1878, #7432, #5398, #23910, #12783, #12437, #19821, #3235, #5971, #18589 ),
 ( #22678, #401, #4165, #13004, #1994, #22208, #13244, #20881, #9379, #14931, #17001 ),
 ( #18816, #11678, #18939, #9736, #9855, #22327, #11440, #2346, #11209, #518, #16749 ),
 ( #13353, #7798, #5743, #15056, #22449, #5861, #15285, #7919, #11326, #6086, #13480 ) ),
 .UNSPECIFIED., .F., .F., .T. ) 
 B_SPLINE_SURFACE_WITH_KNOTS ( ( 4, 4 ),
 ( 4, 1, 1, 1, 1, 1, 1, 1, 4 ),
 ( 0.000000000000000000, 1.000000000000000000 ),
 ( -0.005484827698312000517, 0.000000000000000000, 0.03886970175601000416, 0.08091373131045999367, 0.1291622851901999824, 0.1818598879200999940, 0.2344112070881000098, 0.2830789767138000013, 0.3223009594510999887 ),
 .UNSPECIFIED. ) 
 GEOMETRIC_REPRESENTATION_ITEM ( )  RATIONAL_B_SPLINE_SURFACE ( (
 ( 1.339323776348000150, 1.339323776348000150, 1.339323776348000150, 1.339323776348000150, 1.339323776348000150, 1.339323776348000150, 1.339323776348000150, 1.339323776348000150, 1.339323776348000150, 1.339323776348000150, 1.339323776348000150),
 ( 0.8868920745505000092, 0.8868920745505000092, 0.8868920745505000092, 0.8868920745505000092, 0.8868920745505000092, 0.8868920745505000092, 0.8868920745505000092, 0.8868920745505000092, 0.8868920745505000092, 0.8868920745505000092, 0.8868920745505000092),
 ( 0.8868920745505000092, 0.8868920745505000092, 0.8868920745505000092, 0.8868920745505000092, 0.8868920745505000092, 0.8868920745505000092, 0.8868920745505000092, 0.8868920745505000092, 0.8868920745505000092, 0.8868920745505000092, 0.8868920745505000092),
 ( 1.339323776348000150, 1.339323776348000150, 1.339323776348000150, 1.339323776348000150, 1.339323776348000150, 1.339323776348000150, 1.339323776348000150, 1.339323776348000150, 1.339323776348000150, 1.339323776348000150, 1.339323776348000150) ) ) 
 REPRESENTATION_ITEM ( '' )  SURFACE ( )  );
#21120=CARTESIAN_POINT ( 'NONE',  ( 13.72218892130999990, -3.391610850449999770, -9.027048835217000189 ) ) ;
#21122=CARTESIAN_POINT ( 'NONE',  ( 18.62128936713000371, -9.149140698829999252, 0.000000000000000000 ) ) ;
#21123=LINE ( 'NONE', #886, #4939 ) ;
#21127=CARTESIAN_POINT ( 'NONE',  ( 21.09579166666667049, 9.212641304824277455, 1.205804979152653722 ) ) ;
#21128=CARTESIAN_POINT ( 'NONE',  ( 24.20596017342987238, 1.317034122686029374, 10.54188528362805677 ) ) ;
#21129=CARTESIAN_POINT ( 'NONE',  ( 18.93264468355999952, 0.000000000000000000, 0.000000000000000000 ) ) ;
#21130=CARTESIAN_POINT ( 'NONE',  ( 18.32432198088978836, 7.518497202265214341, -7.212943697349772698 ) ) ;
#21133=CARTESIAN_POINT ( 'NONE',  ( -14.40719418339326907, -8.953944931993278900, 9.491079701373102750 ) ) ;
#21134=CARTESIAN_POINT ( 'NONE',  ( 23.57525185645999954, 10.70628383877999923, -3.581940172122999755 ) ) ;
#21136=CARTESIAN_POINT ( 'NONE',  ( -3.692138345368964014, 14.24529764263220066, -4.891414090216523292 ) ) ;
#21139=CARTESIAN_POINT ( 'NONE',  ( 22.87199999999999989, 9.258222311379999070, 0.000000000000000000 ) ) ;
#21140=CARTESIAN_POINT ( 'NONE',  ( 19.45402087125000179, 6.188800432692000975, -8.235960022457000207 ) ) ;
#21141=CARTESIAN_POINT ( 'NONE',  ( 2.953635558952001361, 13.09662707700965889, -6.068300655576388536 ) ) ;
#21145=CARTESIAN_POINT ( 'NONE',  ( -20.37651066538352040, 7.859203411085292856, -6.967962737658316641 ) ) ;
#21146=DIRECTION ( 'NONE',  ( -1.000000000000000000, 0.000000000000000000, 0.000000000000000000 ) ) ;
#21147=DIRECTION ( 'NONE',  ( 1.000000000000000000, 0.000000000000000000, 0.000000000000000000 ) ) ;
#21149=CARTESIAN_POINT ( 'NONE',  ( -18.46587556182016243, 9.669871375868556385, -3.975206490073679877 ) ) ;
#21155=CARTESIAN_POINT ( 'NONE',  ( 11.47028936713000036, -8.379193606113998882, -3.189305674207999708 ) ) ;
#21158=AXIS2_PLACEMENT_3D ( 'NONE', #20580, #7497, #110 ) ;
#21159=CARTESIAN_POINT ( 'NONE',  ( 17.06568924931000097, -1.008082813539000089, 10.70191082552000061 ) ) ;
#21160=CARTESIAN_POINT ( 'NONE',  ( -21.00779098860000005, -8.370598903416999192, -7.355548942906000143 ) ) ;
#21161=CARTESIAN_POINT ( 'NONE',  ( -13.46246977166000036, 9.006734844048001065, -4.712226836624999748 ) ) ;
#21162=CARTESIAN_POINT ( 'NONE',  ( 22.00279166666665631, -9.235916712427657771, -1.208851722883304225 ) ) ;
#21163=CARTESIAN_POINT ( 'NONE',  ( 17.63056994525999954, 1.419371566880999858, 10.23411406235000065 ) ) ;
#21165=B_SPLINE_CURVE_WITH_KNOTS ( 'NONE', 3,
 ( #1351, #18066, #7380, #18409, #6917, #3531, #3418, #21703, #9205, #5457, #16584, #18194, #10913, #3638, #1700, #3296, #3992, #10801, #21813, #1473, #16238, #23629, #14652, #17945, #22048, #8978, #16104, #9090, #8741, #19880, #14311, #7035, #5340, #19998, #23739, #14762, #23851, #12840, #22160, #14421, #16350, #16461 ),
 .UNSPECIFIED., .F., .F.,
 ( 4, 2, 1, 2, 2, 2, 1, 2, 2, 2, 2, 2, 2, 2, 2, 1, 2, 2, 2, 1, 2, 2, 4 ),
 ( 0.000000000000000000, 0.06250000000000038858, 0.09375000000000058287, 0.1093750000000006800, 0.1250000000000007772, 0.1875000000000011102, 0.2187500000000012768, 0.2343750000000013045, 0.2500000000000013323, 0.3125000000000011657, 0.3750000000000009992, 0.5000000000000006661, 0.5625000000000004441, 0.6250000000000003331, 0.6875000000000001110, 0.7187500000000000000, 0.7343749999999998890, 0.7499999999999997780, 0.8124999999999997780, 0.8437499999999997780, 0.8593749999999996669, 0.8749999999999995559, 1.000000000000000000 ),
 .UNSPECIFIED. ) ;
#21167=CARTESIAN_POINT ( 'NONE',  ( 23.24015326692000016, 4.650820575430000048, 8.573381078705001102 ) ) ;
#21168=CARTESIAN_POINT ( 'NONE',  ( 6.243179582884000212, 13.63342035941999875, -1.952365010387999922 ) ) ;
#21170=CARTESIAN_POINT ( 'NONE',  ( 1.314425600296815544, 13.77569882054628359, 5.982788395604068832 ) ) ;
#21172=CARTESIAN_POINT ( 'NONE',  ( 4.739989412068003283, 12.46385783664001323, 0.6598078427890002873 ) ) ;
#21174=CARTESIAN_POINT ( 'NONE',  ( -24.08729801477999999, 11.11025767225000038, 1.070257339459000034 ) ) ;
#21175=LINE ( 'NONE', #20936, #6131 ) ;
#21176=EDGE_LOOP ( 'NONE', ( #17740, #10082, #493, #17129, #19964 ) ) ;
#21177=CARTESIAN_POINT ( 'NONE',  ( 15.06887270046331651, -8.822272326497644812, -2.370789473217528087 ) ) ;
#21178=AXIS2_PLACEMENT_3D ( 'NONE', #11832, #19212, #5891 ) ;
#21180=CARTESIAN_POINT ( 'NONE',  ( -1.497298415485000200, 13.90645643049002089, 5.974715374002997237 ) ) ;
#21185=CARTESIAN_POINT ( 'NONE',  ( -6.201796767088660900, 15.80323617239661260, -1.134441279322979668 ) ) ;
#21186=AXIS2_PLACEMENT_3D ( 'NONE', #11822, #2614, #11466 ) ;
#21187=CARTESIAN_POINT ( 'NONE',  ( 16.76700125730999957, -9.205641116351999997, -0.3944625347444000174 ) ) ;
#21188=CARTESIAN_POINT ( 'NONE',  ( 24.37173283531060264, 3.055078579629053159, 12.50000000000000533 ) ) ;
#21189=B_SPLINE_CURVE_WITH_KNOTS ( 'NONE', 3,
 ( #13400, #5895, #11718, #9774, #15209 ),
 .UNSPECIFIED., .F., .F.,
 ( 4, 1, 4 ),
 ( 0.000000000000000000, 0.5000000000000000000, 1.000000000000000000 ),
 .UNSPECIFIED. ) ;
#21190=VERTEX_POINT ( 'NONE', #4466 ) ;
#21191=CARTESIAN_POINT ( 'NONE',  ( -22.83407172560354326, 9.257125376469652167, 1.211339697711120156 ) ) ;
#21193=CARTESIAN_POINT ( 'NONE',  ( -15.20062077250666377, 1.186002250417414805, 9.061359600907872291 ) ) ;
#21194=CARTESIAN_POINT ( 'NONE',  ( 1.859456552709266575, 13.85899723262824423, -5.839145259044595804 ) ) ;
#21195=CARTESIAN_POINT ( 'NONE',  ( 20.89481827668999969, 1.510888802920000051, 11.11378095030000068 ) ) ;
#21197=EDGE_CURVE ( 'NONE', #4978, #21807, #3508, .T. ) ;
#21198=CARTESIAN_POINT ( 'NONE',  ( 11.36701043058742044, 2.759410678195907352, 12.49996441860552743 ) ) ;
#21199=CARTESIAN_POINT ( 'NONE',  ( 16.56656853291420006, 10.34692677961490226, 1.231521008520755966 ) ) ;
#21200=DIRECTION ( 'NONE',  ( 0.000000000000000000, 1.000000000000000000, 0.000000000000000000 ) ) ;
#21201=CARTESIAN_POINT ( 'NONE',  ( -21.20949577250664575, 8.052478750070527269, -4.641013231564889985 ) ) ;
#21202=CARTESIAN_POINT ( 'NONE',  ( 24.36881528991174406, -12.37037615450637240, -3.573879991655171562 ) ) ;
#21204=CARTESIAN_POINT ( 'NONE',  ( -24.50000000000001066, -9.922076442417122166, -2.874310295333110332 ) ) ;
#21208=B_SPLINE_SURFACE_WITH_KNOTS ( 'NONE', 3, 3, ( 
 ( #14407, #17818, #3404, #18393, #12828, #16447, #9074, #16685, #16335, #1686, #207, #23835, #9311, #5445, #95, #13173, #18512, #5326, #7131, #9429, #3518, #10899, #18631, #12933, #7246, #7600, #14635, #14979, #22036, #23961, #5555, #20220, #20331, #3626, #22252 ),
 ( #1804, #3862, #3737, #21913, #8965, #11253, #23725, #9192, #11009, #22375, #16569, #11127, #20562, #7365, #16800, #1924, #7480, #14862, #12714, #14521, #5668, #5790, #14750, #13054, #20449, #2039, #3977, #22146, #18180, #1581, #20109, #18286, #2270, #13285, #18742 ),
 ( #6140, #16922, #19224, #22490, #13404, #20805, #559, #20684, #324, #4093, #4214, #2153, #7966, #11489, #13765, #8211, #22727, #2388, #18865, #13529, #11608, #15337, #812, #8094, #22847, #22966, #9664, #20926, #15462, #7729, #13644, #5900, #17417, #2509, #4331 ),
 ( #6260, #15213, #17044, #15095, #21039, #6381, #442, #11723, #7845, #22610, #6019, #17287, #9899, #21167, #11370, #11845, #4454, #9779, #2637, #688, #10032, #18979, #19097, #17164, #15578, #9543, #19723, #17658, #17785, #2885, #16059, #6744, #19600, #4824, #8695 ) ),
 .UNSPECIFIED., .F., .F., .F.,
 ( 4, 4 ),
 ( 4, 1, 1, 1, 1, 1, 1, 1, 1, 1, 1, 1, 1, 1, 1, 1, 1, 1, 1, 1, 1, 1, 1, 1, 1, 1, 1, 1, 1, 1, 1, 1, 4 ),
 ( -0.08331297109794000288, 1.083312971098000066 ),
 ( 0.1767973369902999803, 0.2030268336058000112, 0.2292563302213000143, 0.2554858268368000451, 0.2817153234522999927, 0.3079448200677999958, 0.3341743166833000545, 0.3604038132988000021, 0.3866333099143000052, 0.4128628065298000083, 0.4390923031453000114, 0.4653217997607999590, 0.4915512963763000176, 0.5177807929918000207, 0.5440102896073000238, 0.5702397862229000580, 0.5964692828384000611, 0.6226987794539000642, 0.6489282760694000673, 0.6751577726849000705, 0.7013872693004000736, 0.7276167659159000767, 0.7538462625314000798, 0.7800757591469000829, 0.8063052557624000860, 0.8325347523779000891, 0.8587642489933999812, 0.8849937456089000953, 0.9112232422244000984, 0.9374527388398999905, 0.9636822354555000247, 0.9899117320710000278, 1.016141228685999875 ),
 .UNSPECIFIED. ) ;
#21211=CARTESIAN_POINT ( 'NONE',  ( -2.924596640938022851, 13.09248804016575285, 6.076189607320904074 ) ) ;
#21212=B_SPLINE_CURVE_WITH_KNOTS ( 'NONE', 3,
 ( #4742, #4617, #8367, #19390, #17698, #15859, #14055, #15736, #1095, #21448 ),
 .UNSPECIFIED., .F., .F.,
 ( 4, 2, 2, 2, 4 ),
 ( 0.000000000000000000, 0.1249999999999998890, 0.2499999999999997780, 0.4999999999999998890, 1.000000000000000000 ),
 .UNSPECIFIED. ) ;
#21213=CARTESIAN_POINT ( 'NONE',  ( 6.154459514182900826, 14.10386533427145395, -0.3250634448250298014 ) ) ;
#21214=CARTESIAN_POINT ( 'NONE',  ( -6.460131137950000380, 15.34438815028998704, -0.9341689219261994914 ) ) ;
#21215=AXIS2_PLACEMENT_3D ( 'NONE', #9286, #14171, #5101 ) ;
#21217=ADVANCED_FACE ( 'NONE', ( #1195 ), #6440, .T. ) ;
#21218=CARTESIAN_POINT ( 'NONE',  ( -6.249999999916000526, 15.09564573669999987, 3.212813967733000098 ) ) ;
#21220=EDGE_LOOP ( 'NONE', ( #4024, #20272, #6182, #14356, #17640, #22656 ) ) ;
#21224=EDGE_LOOP ( 'NONE', ( #9588, #15420, #12584, #16748 ) ) ;
#21225=CARTESIAN_POINT ( 'NONE',  ( -20.63087924974999865, -6.603491279182000184, 7.028696436783999246 ) ) ;
#21228=CARTESIAN_POINT ( 'NONE',  ( 14.99956892033451972, 9.898833753622279019, 2.972387950973069959 ) ) ;
#21230=CARTESIAN_POINT ( 'NONE',  ( -19.72979285727999965, -9.249309651556000489, 5.317383783821999721 ) ) ;
#21233=CARTESIAN_POINT ( 'NONE',  ( -20.12402413361354903, 7.018225891280687634, 7.806669810472256721 ) ) ;
#21234=CARTESIAN_POINT ( 'NONE',  ( 1.371414133342000685, 11.63072304285000236, -4.560271503704002249 ) ) ;
#21235=CARTESIAN_POINT ( 'NONE',  ( -15.06773579844999844, 6.079600582824999933, -9.557752359651999541 ) ) ;
#21237=VERTEX_POINT ( 'NONE', #1067 ) ;
#21239=CARTESIAN_POINT ( 'NONE',  ( -16.05466923206691021, -7.433158090429714093, 7.276088876722277554 ) ) ;
#21240=VERTEX_POINT ( 'NONE', #14031 ) ;
#21242=CARTESIAN_POINT ( 'NONE',  ( 5.808047881160999459, 14.58015161914997648, -1.975228513291002574 ) ) ;
#21248=CARTESIAN_POINT ( 'NONE',  ( 16.24500142131000047, 8.402176888622001627, 4.865949138796000106 ) ) ;
#21250=VERTEX_POINT ( 'NONE', #4961 ) ;
#21251=CARTESIAN_POINT ( 'NONE',  ( -8.721209826254002095, 12.89567489919000032, -6.006002783705000070 ) ) ;
#21257=CARTESIAN_POINT ( 'NONE',  ( 0.000000000000000000, 22.00000000000000000, 0.000000000000000000 ) ) ;
#21258=CARTESIAN_POINT ( 'NONE',  ( 4.815594511070003136, 12.64391016021000702, -0.02336859300116998425 ) ) ;
#21259=CARTESIAN_POINT ( 'NONE',  ( -13.99999999999999645, -7.071987877914798659, 7.398104326063183578 ) ) ;
#21261=CARTESIAN_POINT ( 'NONE',  ( 16.27419025256129004, -0.09153522013711405669, -10.36548162492280412 ) ) ;
#21262=DIRECTION ( 'NONE',  ( 1.000000000000000000, -0.000000000000000000, -0.000000000000000000 ) ) ;
#21264=CARTESIAN_POINT ( 'NONE',  ( 19.35367170822999938, -8.078004626089001050, -7.719962156281999555 ) ) ;
#21265=EDGE_CURVE ( 'NONE', #1933, #2511, #8774, .T. ) ;
#21270=DIRECTION ( 'NONE',  ( 0.000000000000000000, 1.000000000000000000, 0.000000000000000000 ) ) ;
#21273=CARTESIAN_POINT ( 'NONE',  ( 18.48776620345000055, -4.367899469603999663, 9.299952195460999604 ) ) ;
#21274=CARTESIAN_POINT ( 'NONE',  ( 23.98778900788900970, 10.71396164900311021, 0.03587804490455098749 ) ) ;
#21276=VECTOR ( 'NONE', #17029, 1000.000000000000000 ) ;
#21277=CARTESIAN_POINT ( 'NONE',  ( -20.45683979044500944, 5.645737104002305884, -8.860185778984789096 ) ) ;
#21279=CARTESIAN_POINT ( 'NONE',  ( 3.897341104911002940, 12.15007725568001362, -3.081013383565999852 ) ) ;
#21281=CARTESIAN_POINT ( 'NONE',  ( -16.12133163457191287, 1.276676612278212497, 10.31581741333146240 ) ) ;
#21286=DIRECTION ( 'NONE',  ( -1.000000000000000000, 0.000000000000000000, 0.000000000000000000 ) ) ;
#21289=CARTESIAN_POINT ( 'NONE',  ( -12.02109039332999885, 12.23011958036999935, -9.372058967585999767 ) ) ;
#21290=CARTESIAN_POINT ( 'NONE',  ( -20.36544424872999670, 10.91338584732999983, -2.163915618822000120 ) ) ;
#21291=CARTESIAN_POINT ( 'NONE',  ( -16.10150461667999977, -7.663156287736000216, -6.860248635285000063 ) ) ;
#21292=CARTESIAN_POINT ( 'NONE',  ( -6.307433260514002882, 15.63766309337001204, 1.260389944764000125 ) ) ;
#21293=CARTESIAN_POINT ( 'NONE',  ( 13.22952827859000102, 3.056853952720000045, -9.159678806024000863 ) ) ;
#21297=EDGE_LOOP ( 'NONE', ( #21452, #13456, #21029, #18381, #15200, #12441 ) ) ;
#21298=CARTESIAN_POINT ( 'NONE',  ( -2.168773205512959823, 13.92118792069584998, 5.728215446730930971 ) ) ;
#21301=CARTESIAN_POINT ( 'NONE',  ( -21.58102982807999837, -8.846676569589000394, 6.693734360802999994 ) ) ;
#21308=CARTESIAN_POINT ( 'NONE',  ( -24.00016455340000121, 1.715543117993999783E-14, -9.787173237795000702 ) ) ;
#21310=CARTESIAN_POINT ( 'NONE',  ( -13.64582336266999896, -8.030615239332000499, -7.932400521014000283 ) ) ;
#21311=CARTESIAN_POINT ( 'NONE',  ( 12.48918875731000000, 5.414613097170000167, 7.315858880121999697 ) ) ;
#21312=CARTESIAN_POINT ( 'NONE',  ( 18.93546403748226936, 2.261952095453904299, 10.18648252659528453 ) ) ;
#21316=CARTESIAN_POINT ( 'NONE',  ( -15.01166243917333176, -4.561147897106140547, 7.913407070503003737 ) ) ;
#21317=CARTESIAN_POINT ( 'NONE',  ( 3.087353659563723873, 14.15392277165757662, -5.289980554907421251 ) ) ;
#21323=CARTESIAN_POINT ( 'NONE',  ( 15.53511221042325907, -9.890698584888076184, 3.204571028146030010 ) ) ;
#21325=FACE_OUTER_BOUND ( 'NONE', #3835, .T. ) ;
#21330=CARTESIAN_POINT ( 'NONE',  ( 11.22285964979965023, -11.82554192023893158, 4.517540867111200953 ) ) ;
#21331=ORIENTED_EDGE ( 'NONE', *, *, #15253, .T. ) ;
#21334=CARTESIAN_POINT ( 'NONE',  ( 2.190908539898643426, 12.96599634601801831, 6.341814094140324265 ) ) ;
#21335=CARTESIAN_POINT ( 'NONE',  ( 6.156454711165042504, 14.09190061863668575, -0.3541682061968411399 ) ) ;
#21338=ADVANCED_FACE ( 'NONE', ( #3148 ), #16071, .T. ) ;
#21339=ORIENTED_EDGE ( 'NONE', *, *, #13472, .T. ) ;
#21340=CARTESIAN_POINT ( 'NONE',  ( -12.35782623356324095, 9.652455568630072591, -11.96866129963372849 ) ) ;
#21344=CARTESIAN_POINT ( 'NONE',  ( -20.53203420772999976, -9.474484991426001201, -3.680778544930999985 ) ) ;
#21346=CARTESIAN_POINT ( 'NONE',  ( 20.22658333333333047, -8.951184447692499546, -2.405433643222833151 ) ) ;
#21347=CARTESIAN_POINT ( 'NONE',  ( 15.24105989044193166, 4.435666536080931976, 9.339999123369469913 ) ) ;
#21348=CARTESIAN_POINT ( 'NONE',  ( -17.26072755184999963, 1.977436118132999798, -10.90262414946000114 ) ) ;
#21350=CARTESIAN_POINT ( 'NONE',  ( -23.01857833252245911, 8.092376861233656626, 4.663496906030524691 ) ) ;
#21351=CARTESIAN_POINT ( 'NONE',  ( -4.097103695893997255, 12.37558244084000059, -2.395384390973998467 ) ) ;
#21352=DIRECTION ( 'NONE',  ( 1.000000000000000000, 0.000000000000000000, 0.000000000000000000 ) ) ;
#21353=EDGE_CURVE ( 'NONE', #17213, #17895, #23471, .T. ) ;
#21357=CARTESIAN_POINT ( 'NONE',  ( -17.35693205524438909, -5.675076331185680445, -8.750869078049179350 ) ) ;
#21358=ORIENTED_EDGE ( 'NONE', *, *, #20251, .F. ) ;
#21359=CARTESIAN_POINT ( 'NONE',  ( -23.75392853996000042, 6.467096933425000138, -12.35553624208999857 ) ) ;
#21360=CARTESIAN_POINT ( 'NONE',  ( 6.131903631775997177, 14.49480975922001491, 0.05943612597242994150 ) ) ;
#21363=CARTESIAN_POINT ( 'NONE',  ( 17.58116666666665395, 7.971120433115317816, 4.594121230069161399 ) ) ;
#21365=CARTESIAN_POINT ( 'NONE',  ( 15.06487658531000129, -2.993859790429000078, 9.737735315623000432 ) ) ;
#21366=EDGE_LOOP ( 'NONE', ( #12051, #15618 ) ) ;
#21367=DIRECTION ( 'NONE',  ( 0.000000000000000000, 0.000000000000000000, -1.000000000000000000 ) ) ;
#21370=CARTESIAN_POINT ( 'NONE',  ( 11.12576011241313090, 11.44859199039787789, 5.170472096583769606 ) ) ;
#21372=VECTOR ( 'NONE', #20270, 1000.000000000000000 ) ;
#21373=CARTESIAN_POINT ( 'NONE',  ( -4.820914651057999656, 13.20110358117000082, -5.836454220812999694 ) ) ;
#21374=CARTESIAN_POINT ( 'NONE',  ( 16.28472136693522998, 0.2845602576508600157, -10.36427326206977462 ) ) ;
#21376=CARTESIAN_POINT ( 'NONE',  ( 12.00000000000000533, -5.815948216832730999, -7.788256740848641613 ) ) ;
#21377=CARTESIAN_POINT ( 'NONE',  ( -14.46758741243234603, -9.725949910454726677, 8.154098604260809680 ) ) ;
#21378=CARTESIAN_POINT ( 'NONE',  ( -4.062430690931376986, 13.79341706565821291, -4.866449934628417573 ) ) ;
#21379=FACE_OUTER_BOUND ( 'NONE', #11292, .T. ) ;
#21380=EDGE_CURVE ( 'NONE', #1857, #1455, #15313, .T. ) ;
#21382=ORIENTED_EDGE ( 'NONE', *, *, #1948, .F. ) ;
#21384=CARTESIAN_POINT ( 'NONE',  ( -24.48376588671094822, -1.022231981026950676, 12.50007328825939901 ) ) ;
#21385=CARTESIAN_POINT ( 'NONE',  ( 24.97017047179999949, -7.684332283202000013, -7.441023909770999367 ) ) ;
#21386=CARTESIAN_POINT ( 'NONE',  ( 23.07984073068213959, -10.59120176776928268, 0.003446602559681892844 ) ) ;
#21387=CARTESIAN_POINT ( 'NONE',  ( -20.15132910583999859, -9.188404534074999574, 1.125025998286999896E-14 ) ) ;
#21392=DIRECTION ( 'NONE',  ( 0.000000000000000000, 1.000000000000000000, 0.000000000000000000 ) ) ;
#21394=CARTESIAN_POINT ( 'NONE',  ( -12.52176908877999928, 6.525220749543999332, -6.187779769309999622 ) ) ;
#21396=LINE ( 'NONE', #15322, #12313 ) ;
#21399=FACE_OUTER_BOUND ( 'NONE', #6577, .T. ) ;
#21400=ORIENTED_EDGE ( 'NONE', *, *, #15151, .F. ) ;
#21402=CARTESIAN_POINT ( 'NONE',  ( 12.67818924931000168, 6.046592098211998945, -8.747551238178997934 ) ) ;
#21403=CARTESIAN_POINT ( 'NONE',  ( -14.59110758819998743, -8.342498430116506825, -3.617375204252647247 ) ) ;
#21404=CARTESIAN_POINT ( 'NONE',  ( -20.09640146007999917, -8.409358971373999125, 5.097095819920999027 ) ) ;
#21406=CARTESIAN_POINT ( 'NONE',  ( 19.86541618412999810, -3.495432200175000226, 8.640661540007000596 ) ) ;
#21409=ADVANCED_FACE ( 'NONE', ( #13354 ), #7800, .T. ) ;
#21412=EDGE_CURVE ( 'NONE', #13414, #2324, #21720, .T. ) ;
#21413=CARTESIAN_POINT ( 'NONE',  ( 2.773360020023811323, 14.06573755500684086, 5.461184526572689713 ) ) ;
#21416=CARTESIAN_POINT ( 'NONE',  ( -19.66003743917331903, 1.201235969070638454, -9.175797021623829153 ) ) ;
#21417=CARTESIAN_POINT ( 'NONE',  ( -14.50888678659720199, 1.427758690254528950, -8.929076806151241996 ) ) ;
#21418=CARTESIAN_POINT ( 'NONE',  ( -21.41394528229999850, -11.06275857470000012, 0.7645690033980999667 ) ) ;
#21420=CARTESIAN_POINT ( 'NONE',  ( -4.750876579451202453, 12.41232746058178371, 0.9678923958058619492 ) ) ;
#21421=VERTEX_POINT ( 'NONE', #7683 ) ;
#21423=CARTESIAN_POINT ( 'NONE',  ( 1.888264321221249542, 11.63400096833999697, -4.433377897947928581 ) ) ;
#21424=EDGE_CURVE ( 'NONE', #23352, #10646, #18590, .T. ) ;
#21428=CARTESIAN_POINT ( 'NONE',  ( 11.69106760960404934, -3.854957646731009380, -8.129799737674142435 ) ) ;
#21431=CARTESIAN_POINT ( 'NONE',  ( -12.50046137836000071, 5.020438948778999766, -14.40607103599000105 ) ) ;
#21432=CARTESIAN_POINT ( 'NONE',  ( 11.82343232744396921, -8.387570696992149522, -3.192494120993503604 ) ) ;
#21433=CARTESIAN_POINT ( 'NONE',  ( 12.95437642131000011, -1.177851786523999911, 9.550625374955998836 ) ) ;
#21435=EDGE_LOOP ( 'NONE', ( #22574, #1165, #5492, #13541, #14020 ) ) ;
#21438=CARTESIAN_POINT ( 'NONE',  ( -15.31399577250666688, 4.564820640773371352, 7.920283476814353740 ) ) ;
#21439=DIRECTION ( 'NONE',  ( 1.000000000000000000, 0.000000000000000000, 0.000000000000000000 ) ) ;
#21443=CARTESIAN_POINT ( 'NONE',  ( -24.50000000000000000, -12.50000000001108091, 0.000000000000000000 ) ) ;
#21444=CARTESIAN_POINT ( 'NONE',  ( -6.042815635770000249, 16.39253429789999927, 0.9999999720525000191 ) ) ;
#21445=CARTESIAN_POINT ( 'NONE',  ( 14.55941028374722812, 8.833975226579921625, -5.424247256400066775 ) ) ;
#21447=CARTESIAN_POINT ( 'NONE',  ( -21.92753743917333864, -9.233985540631776345, -1.208852828397224632 ) ) ;
#21448=CARTESIAN_POINT ( 'NONE',  ( -23.74465998031000069, -7.716878364870000340, 11.63397459621999985 ) ) ;
#21449=ORIENTED_EDGE ( 'NONE', *, *, #3894, .F. ) ;
#21451=CARTESIAN_POINT ( 'NONE',  ( 11.48696334738999347, -12.46086172551006577, 3.416997251935109059 ) ) ;
#21452=ORIENTED_EDGE ( 'NONE', *, *, #10996, .T. ) ;
#21455=CARTESIAN_POINT ( 'NONE',  ( 3.871436389726701233, 13.30584025295970640, 5.593675438725219884 ) ) ;
#21456=AXIS2_PLACEMENT_3D ( 'NONE', #11925, #19309, #2721 ) ;
#21457=CARTESIAN_POINT ( 'NONE',  ( 6.188762112849826025, 13.92751971542314138, -0.7696703758847552868 ) ) ;
#21458=CARTESIAN_POINT ( 'NONE',  ( -6.051726996036002504, 16.51353013550999194, -0.9910466829373008046 ) ) ;
#21459=CARTESIAN_POINT ( 'NONE',  ( -3.000000000000000000, 20.00000000000000000, 0.000000000000000000 ) ) ;
#21462=CIRCLE ( 'NONE', #4044, 12.89775331292476857 ) ;
#21465=EDGE_CURVE ( 'NONE', #8871, #8984, #17988, .T. ) ;
#21466=VERTEX_POINT ( 'NONE', #20757 ) ;
#21467=CARTESIAN_POINT ( 'NONE',  ( -21.21750115016000393, 4.272008970125000360, 9.243565099026998411 ) ) ;
#21468=CARTESIAN_POINT ( 'NONE',  ( 20.98241666666665850, 8.969978628699989187, -2.410745119152057914 ) ) ;
#21469=CARTESIAN_POINT ( 'NONE',  ( 14.97544413412106756, 10.11390979503470078, 2.113747987315613752 ) ) ;
#21470=DIRECTION ( 'NONE',  ( -1.000000000000000000, 0.000000000000000000, 0.000000000000000000 ) ) ;
#21472=CARTESIAN_POINT ( 'NONE',  ( -22.30014857772672343, -9.241084326725088616, 1.209620885877401131 ) ) ;
#21473=CARTESIAN_POINT ( 'NONE',  ( -4.719398433761999634, 12.53456689658000656, -0.3214035655570999239 ) ) ;
#21474=ORIENTED_EDGE ( 'NONE', *, *, #14863, .T. ) ;
#21475=CARTESIAN_POINT ( 'NONE',  ( -13.64582336266999896, -8.030615239332000499, -7.932400521014000283 ) ) ;
#21480=CARTESIAN_POINT ( 'NONE',  ( -17.70420214142508541, -10.38169273393352299, 2.154482946468162297 ) ) ;
#21482=ORIENTED_EDGE ( 'NONE', *, *, #21116, .T. ) ;
#21484=CARTESIAN_POINT ( 'NONE',  ( 4.725397782510998290, 14.52029874379999264, -3.829245615367002031 ) ) ;
#21486=CARTESIAN_POINT ( 'NONE',  ( 15.95626817440999901, -0.1031805989180999972, -11.05505056420000010 ) ) ;
#21487=CARTESIAN_POINT ( 'NONE',  ( 15.61331408530999987, -8.260803322383997838, -5.986632065681000370 ) ) ;
#21488=EDGE_LOOP ( 'NONE', ( #4618, #20285, #2667, #21091 ) ) ;
#21489=CARTESIAN_POINT ( 'NONE',  ( -9.094558992920999785, -6.050585292417999916, -13.19663489122999955 ) ) ;
#21493=CARTESIAN_POINT ( 'NONE',  ( -23.88684722629999868, -8.668318262646000250, -4.424847982898000964 ) ) ;
#21494=CARTESIAN_POINT ( 'NONE',  ( 11.36701043060024041, 12.20499207204542280, 3.860262462447420440 ) ) ;
#21495=DIRECTION ( 'NONE',  ( 0.000000000000000000, 1.000000000000000000, 0.000000000000000000 ) ) ;
#21496=AXIS2_PLACEMENT_3D ( 'NONE', #9933, #13566, #20959 ) ;
#21497=CARTESIAN_POINT ( 'NONE',  ( 23.99062354302999722, -7.716878364870000340, 11.63397459621999985 ) ) ;
#21498=CARTESIAN_POINT ( 'NONE',  ( 16.35004977966324446, 2.603377162649796350, -10.05366246871247959 ) ) ;
#21501=B_SPLINE_CURVE_WITH_KNOTS ( 'NONE', 3,
 ( #15328, #22719, #14253, #6860, #8447, #4815, #3128, #18138, #23206, #6983, #16052, #12680, #10386, #19946, #20066, #21525, #23445, #1543 ),
 .UNSPECIFIED., .F., .F.,
 ( 4, 2, 2, 2, 2, 2, 2, 2, 4 ),
 ( 0.000000000000000000, 0.1249999999999999167, 0.2499999999999998335, 0.3749999999999998335, 0.4999999999999998890, 0.6249999999999998890, 0.7499999999999998890, 0.8750000000000000000, 1.000000000000000000 ),
 .UNSPECIFIED. ) ;
#21503=FACE_OUTER_BOUND ( 'NONE', #21977, .T. ) ;
#21508=CARTESIAN_POINT ( 'NONE',  ( 18.73357886744999945, -4.598493306945000469, 9.790775688502000307 ) ) ;
#21509=CARTESIAN_POINT ( 'NONE',  ( 22.76773351039173221, -4.982168945016796968, 9.336842154732323706 ) ) ;
#21512=DIRECTION ( 'NONE',  ( 0.000000000000000000, 1.000000000000000000, 0.000000000000000000 ) ) ;
#21513=CARTESIAN_POINT ( 'NONE',  ( 5.064386902162485882, 14.06000371052163445, 3.938615721984927820 ) ) ;
#21517=CARTESIAN_POINT ( 'NONE',  ( -15.28399451769901773, -3.699222542850097550, -9.694524040023539513 ) ) ;
#21518=DIRECTION ( 'NONE',  ( 0.000000000000000000, -1.000000000000000000, 0.000000000000000000 ) ) ;
#21520=LINE ( 'NONE', #10509, #22968 ) ;
#21523=EDGE_CURVE ( 'NONE', #20749, #20574, #4998, .T. ) ;
#21524=ORIENTED_EDGE ( 'NONE', *, *, #15129, .F. ) ;
#21525=CARTESIAN_POINT ( 'NONE',  ( -19.47341549180334752, 8.981945570196975481, 2.139161086732093153 ) ) ;
#21526=CARTESIAN_POINT ( 'NONE',  ( -4.178937961678600210, 15.14834147970980283, -4.478992075710971577 ) ) ;
#21527=CARTESIAN_POINT ( 'NONE',  ( -19.56251082389000118, -9.430400074637001140, 5.862072811040999198 ) ) ;
#21528=CARTESIAN_POINT ( 'NONE',  ( -15.89837426871000226, -1.404306094088999979, -10.18324534259000025 ) ) ;
#21529=CARTESIAN_POINT ( 'NONE',  ( -6.089104266536998544, 16.42834722451999241, 1.007215775395999602 ) ) ;
#21530=CARTESIAN_POINT ( 'NONE',  ( 16.41181994525999954, -9.662517015497000372, -3.561852019405000291 ) ) ;
#21534=LINE ( 'NONE', #4948, #17376 ) ;
#21536=CARTESIAN_POINT ( 'NONE',  ( 15.01133333333333120, -4.561143643790010138, -7.913399690936467223 ) ) ;
#21537=ORIENTED_EDGE ( 'NONE', *, *, #3047, .F. ) ;
#21542=CARTESIAN_POINT ( 'NONE',  ( -14.28497649141528214, 7.354848982022818227, -5.390649801475187353 ) ) ;
#21543=CARTESIAN_POINT ( 'NONE',  ( -21.74811437386000179, -3.746343007632000344, 10.44678391489000013 ) ) ;
#21544=CONICAL_SURFACE ( 'NONE', #11476, 9.879748406101001024, 0.7982263333994560339 ) ;
#21545=CARTESIAN_POINT ( 'NONE',  ( -3.822473297103945455, 12.09266017900104018, 2.961494058630956161 ) ) ;
#21547=CARTESIAN_POINT ( 'NONE',  ( -24.12232999016000079, 1.520060141252000183E-14, 0.000000000000000000 ) ) ;
#21548=CARTESIAN_POINT ( 'NONE',  ( 4.059701995908764793, 12.16834275931829978, -2.635041455870243965 ) ) ;
#21549=CARTESIAN_POINT ( 'NONE',  ( -10.16272095229482986, 15.91915081437118218, 1.078441560784934250 ) ) ;
#21552=EDGE_CURVE ( 'NONE', #2832, #12931, #1515, .T. ) ;
#21554=CARTESIAN_POINT ( 'NONE',  ( 5.155702020191999857, 13.97328941143999970, -4.008166040501000893 ) ) ;
#21555=CARTESIAN_POINT ( 'NONE',  ( -14.25243324638999809, -7.716878364870000340, 11.63397459621999985 ) ) ;
#21556=CARTESIAN_POINT ( 'NONE',  ( 14.27062642131000025, 9.653071988928001446, -0.2951073761277999696 ) ) ;
#21557=CARTESIAN_POINT ( 'NONE',  ( 24.50000000000000000, 0.000000000000000000, 12.50000000000000000 ) ) ;
#21559=CARTESIAN_POINT ( 'NONE',  ( 5.230516336068609107, 13.89302811135363669, 4.095895456715770599 ) ) ;
#21562=CARTESIAN_POINT ( 'NONE',  ( 4.160050682987502135, 14.52062904459194392, -4.495645836896323466 ) ) ;
#21563=CIRCLE ( 'NONE', #3761, 13.93375672974000068 ) ;
#21564=ORIENTED_EDGE ( 'NONE', *, *, #10881, .T. ) ;
#21566=CARTESIAN_POINT ( 'NONE',  ( -24.36724102302906658, -12.10481948363803539, 4.033677606734435983 ) ) ;
#21567=B_SPLINE_SURFACE_WITH_KNOTS ( 'NONE', 3, 3, ( 
 ( #5894, #15089, #3971, #6134, #9538, #7724, #4449, #2146, #19219, #17039, #22842, #20679, #4088, #682, #11483, #9658, #18859, #10027, #2383, #4326, #2265, #15208, #8089, #22605, #7960, #6014, #15456, #9773, #554, #13399, #4209, #15332, #200, #22721, #6255 ),
 ( #13638, #5784, #7593, #13524, #13167, #19092, #15932, #19719, #3132, #6625, #1050, #3004, #19353, #10263, #2760, #19471, #10389, #10516, #8451, #1180, #4572, #12088, #2880, #17899, #10143, #22961, #13759, #23327, #12450, #1300, #8691, #15818, #14014, #21161, #8573 ),
 ( #4819, #21404, #17781, #17651, #15689, #8324, #6740, #23449, #23209, #806, #12205, #17530, #16055, #5067, #19594, #21654, #6864, #19833, #3246, #14135, #17412, #21291, #21528, #4943, #8206, #924, #12328, #15573, #13888, #11964, #23080, #4703, #1420, #5634, #16300 ),
 ( #21999, #7212, #9159, #8819, #20300, #16179, #10866, #13018, #7099, #20071, #1653, #23582, #6986, #14375, #12900, #12796, #20184, #21769, #5181, #16414, #3594, #9042, #12563, #60, #19949, #8932, #23925, #3702, #3370, #5290, #18019, #12683, #14826, #10748, #16657 ) ),
 .UNSPECIFIED., .F., .F., .F.,
 ( 4, 4 ),
 ( 4, 1, 1, 1, 1, 1, 1, 1, 1, 1, 1, 1, 1, 1, 1, 1, 1, 1, 1, 1, 1, 1, 1, 1, 1, 1, 1, 1, 1, 1, 1, 1, 4 ),
 ( -0.08408083179837000376, 1.084080831798000188 ),
 ( -0.02000000000000000042, 0.01250000000000000069, 0.04499999999999999833, 0.07749999999999999944, 0.1100000000000000006, 0.1424999999999999878, 0.1749999999999999889, 0.2074999999999999900, 0.2399999999999999911, 0.2725000000000000200, 0.3049999999999999933, 0.3375000000000000222, 0.3699999999999999956, 0.4025000000000000244, 0.4349999999999999978, 0.4675000000000000266, 0.5000000000000000000, 0.5324999999999999734, 0.5649999999999999467, 0.5975000000000000311, 0.6300000000000000044, 0.6624999999999999778, 0.6949999999999999512, 0.7275000000000000355, 0.7600000000000000089, 0.7924999999999999822, 0.8249999999999999556, 0.8575000000000000400, 0.8900000000000000133, 0.9224999999999999867, 0.9549999999999999600, 0.9875000000000000444, 1.020000000000000018 ),
 .UNSPECIFIED. ) ;
#21568=CARTESIAN_POINT ( 'NONE',  ( 15.99391666666666367, 2.377237531314461361, 8.845295767958798905 ) ) ;
#21571=EDGE_CURVE ( 'NONE', #1942, #8248, #7538, .T. ) ;
#21572=CARTESIAN_POINT ( 'NONE',  ( 15.11695424184799386, 1.968991340098076304, 10.34192823185278343 ) ) ;
#21574=CARTESIAN_POINT ( 'NONE',  ( -3.835584729116002123, 14.03840790544035144, 4.850097248418875573 ) ) ;
#21575=DIRECTION ( 'NONE',  ( 1.000000000000000000, 0.000000000000000000, 0.000000000000000000 ) ) ;
#21576=CARTESIAN_POINT ( 'NONE',  ( 23.99478584076000232, 13.93375672974000068, -0.6736217021363000157 ) ) ;
#21577=ORIENTED_EDGE ( 'NONE', *, *, #10251, .T. ) ;
#21582=CARTESIAN_POINT ( 'NONE',  ( 5.701363503176997583, 14.61139651266002026, 2.265470104175000721 ) ) ;
#21583=CARTESIAN_POINT ( 'NONE',  ( 0.8910436668603369803, 12.82851146553231203, 6.615463406976411775 ) ) ;
#21585=CARTESIAN_POINT ( 'NONE',  ( 6.224861414451202890, 13.76529413338021612, -1.291206515654964804 ) ) ;
#21587=LINE ( 'NONE', #21459, #4768 ) ;
#21588=B_SPLINE_CURVE_WITH_KNOTS ( 'NONE', 3,
 ( #12249, #21447, #8493, #17823, #1218, #6418, #15858, #19261, #11759, #13803, #8131, #4861, #15371, #6180, #21201, #23120, #13567, #15496 ),
 .UNSPECIFIED., .F., .F.,
 ( 4, 2, 2, 2, 2, 2, 2, 2, 4 ),
 ( 0.000000000000000000, 0.1250000000000000278, 0.2500000000000000000, 0.3749999999999999445, 0.4999999999999999445, 0.6249999999999998890, 0.7499999999999998890, 0.8750000000000000000, 1.000000000000000000 ),
 .UNSPECIFIED. ) ;
#21589=EDGE_LOOP ( 'NONE', ( #5307, #9049, #7732, #7219 ) ) ;
#21591=CARTESIAN_POINT ( 'NONE',  ( 13.50000000000000000, 10.65000000000000036, 0.000000000000000000 ) ) ;
#21592=LINE ( 'NONE', #11898, #8680 ) ;
#21593=EDGE_LOOP ( 'NONE', ( #10539, #941, #5165, #11542 ) ) ;
#21594=CARTESIAN_POINT ( 'NONE',  ( -24.37462408469000152, -9.611684602066999261, -4.906288292759999337 ) ) ;
#21596=CARTESIAN_POINT ( 'NONE',  ( 15.14795571169218924, 7.213078467210109146, 7.405181219479683108 ) ) ;
#21599=CARTESIAN_POINT ( 'NONE',  ( -12.25000000000000000, 1.374666032043000015E-14, 0.000000000000000000 ) ) ;
#21600=CARTESIAN_POINT ( 'NONE',  ( 4.721486246517997643, 12.60723799037000070, -0.5132971997070995274 ) ) ;
#21602=CARTESIAN_POINT ( 'NONE',  ( -23.74228231688656976, 8.693394395448456762E-05, -9.522797051439189531 ) ) ;
#21604=ORIENTED_EDGE ( 'NONE', *, *, #11058, .F. ) ;
#21606=CARTESIAN_POINT ( 'NONE',  ( -14.49195384425397215, 0.7433570823107922276, 10.32670728092745804 ) ) ;
#21610=CARTESIAN_POINT ( 'NONE',  ( 16.71195833333331748, -7.277172784690141505, -5.592373574543976211 ) ) ;
#21611=CARTESIAN_POINT ( 'NONE',  ( 11.99999999999999645, -4.526363629865546301, -7.766451825080983085 ) ) ;
#21613=CARTESIAN_POINT ( 'NONE',  ( 16.49762086794999760, 10.59225851661000206, 3.218213586410000104 ) ) ;
#21614=CARTESIAN_POINT ( 'NONE',  ( 12.10331408531000008, -5.154040300995999857, -8.697259314724000490 ) ) ;
#21616=CARTESIAN_POINT ( 'NONE',  ( -9.501848992921001269, -12.26021964927999974, 7.774810108354999194 ) ) ;
#21617=CARTESIAN_POINT ( 'NONE',  ( -24.50000000000000000, -7.216878364870000340, -12.50000000000000000 ) ) ;
#21618=( NAMED_UNIT ( * ) SI_UNIT ( $, .STERADIAN. ) SOLID_ANGLE_UNIT ( ) );
#21621=CARTESIAN_POINT ( 'NONE',  ( 21.44098906717976405, -2.902397506967778096, -10.31605076386551545 ) ) ;
#21622=CARTESIAN_POINT ( 'NONE',  ( 11.00000000000000000, 0.000000000000000000, 0.000000000000000000 ) ) ;
#21623=CARTESIAN_POINT ( 'NONE',  ( 16.27506522991737725, -0.06060872261240779491, -10.36580276523552158 ) ) ;
#21624=CARTESIAN_POINT ( 'NONE',  ( -6.020246122619357543, 14.94718218489679451, 3.809753413873187888 ) ) ;
#21631=CARTESIAN_POINT ( 'NONE',  ( 12.52688711657000020, 13.93375672974000068, -0.8660254037843999608 ) ) ;
#21632=CARTESIAN_POINT ( 'NONE',  ( 24.47013653015837775, -1.097897350813762829, 10.57183604653516440 ) ) ;
#21634=VECTOR ( 'NONE', #10940, 1000.000000000000000 ) ;
#21637=CARTESIAN_POINT ( 'NONE',  ( 24.50000000000000000, -10.82531754731000007, -6.250000000000000000 ) ) ;
#21639=CARTESIAN_POINT ( 'NONE',  ( -4.024865567630999230, 12.19225766109002329, -2.884015414602999705 ) ) ;
#21640=EDGE_LOOP ( 'NONE', ( #18131, #10582 ) ) ;
#21642=CARTESIAN_POINT ( 'NONE',  ( 17.20575125731000199, -0.07625726307336000431, -9.225306777752001253 ) ) ;
#21644=CIRCLE ( 'NONE', #1921, 15.43375672974000068 ) ;
#21645=CARTESIAN_POINT ( 'NONE',  ( -14.00000000000000000, 1.396097351027999937E-14, 0.000000000000000000 ) ) ;
#21647=CARTESIAN_POINT ( 'NONE',  ( -14.42499035157127985, -3.357933904613944254, -12.49997221285484983 ) ) ;
#21649=EDGE_LOOP ( 'NONE', ( #2499, #20119, #7081, #8894, #22502 ) ) ;
#21652=CARTESIAN_POINT ( 'NONE',  ( 12.23943924931000105, -8.418214415862998123, -6.478404025908999664 ) ) ;
#21653=CARTESIAN_POINT ( 'NONE',  ( -21.11638508900000133, -3.075672562904000262, -10.17210945827999957 ) ) ;
#21654=CARTESIAN_POINT ( 'NONE',  ( -17.32028670448999819, 9.694482879840998990, -3.536072490757000253 ) ) ;
#21656=CARTESIAN_POINT ( 'NONE',  ( -24.24164425323710503, 6.933586358082536982, -8.021408670079015479 ) ) ;
#21658=DIRECTION ( 'NONE',  ( -1.000000000000000000, 0.000000000000000000, 0.000000000000000000 ) ) ;
#21662=CARTESIAN_POINT ( 'NONE',  ( 23.33304596532290276, 7.619942348972831070, 5.313059321050398687 ) ) ;
#21666=CARTESIAN_POINT ( 'NONE',  ( 5.982801910263268574, 14.41040939236866514, -1.321542980959287794 ) ) ;
#21668=CARTESIAN_POINT ( 'NONE',  ( -4.850001362640682601, 12.45000000000000284, 0.1690184008927609061 ) ) ;
#21671=CARTESIAN_POINT ( 'NONE',  ( 3.061958301202284627, 11.87766433303262126, -3.731442317003270226 ) ) ;
#21673=CARTESIAN_POINT ( 'NONE',  ( -20.75009587121333254, -4.635310582250941280, 8.042080427403897502 ) ) ;
#21674=VERTEX_POINT ( 'NONE', #6586 ) ;
#21675=EDGE_CURVE ( 'NONE', #5630, #9908, #7840, .T. ) ;
#21677=CARTESIAN_POINT ( 'NONE',  ( -17.50529997408999705, -11.39253675243999986, 0.2566028257674999868 ) ) ;
#21678=CARTESIAN_POINT ( 'NONE',  ( 14.59968892130999940, 4.304969983318999383, 8.654667617400001234 ) ) ;
#21679=CARTESIAN_POINT ( 'NONE',  ( 18.70390242685546411, 8.868690283753592141, 5.485530365214523307 ) ) ;
#21684=CARTESIAN_POINT ( 'NONE',  ( 13.49999999999999645, -9.465184455976315192, 2.727039375416640876 ) ) ;
#21685=EDGE_LOOP ( 'NONE', ( #14701, #3122, #15670, #14482, #9686 ) ) ;
#21687=CARTESIAN_POINT ( 'NONE',  ( 6.124999911758999716, 14.37502625872000195, -0.0001546258496581000123 ) ) ;
#21689=FACE_OUTER_BOUND ( 'NONE', #13632, .T. ) ;
#21691=CARTESIAN_POINT ( 'NONE',  ( 14.30851550260190663, 1.558156080228414009, -10.24440842901224080 ) ) ;
#21692=CARTESIAN_POINT ( 'NONE',  ( -4.008718708443686829, 13.84443620156353383, 4.855404245198969626 ) ) ;
#21693=CARTESIAN_POINT ( 'NONE',  ( -4.550974324282003103, 12.30365742415998831, 1.872281734269997999 ) ) ;
#21694=ADVANCED_FACE ( 'NONE', ( #14563 ), #15178, .F. ) ;
#21698=ADVANCED_FACE ( 'NONE', ( #9826 ), #2687, .F. ) ;
#21702=CARTESIAN_POINT ( 'NONE',  ( 6.046348537316000638, 14.51594544156001731, 1.039485355375998843 ) ) ;
#21703=CARTESIAN_POINT ( 'NONE',  ( 11.90008533511925570, 4.641570061506223865, -12.50003962888440867 ) ) ;
#21705=CARTESIAN_POINT ( 'NONE',  ( 13.49999999999999822, -3.814422028142153920, 9.637201378805430707 ) ) ;
#21708=VERTEX_POINT ( 'NONE', #20854 ) ;
#21709=DIRECTION ( 'NONE',  ( -0.000000000000000000, 1.000000000000000000, 0.000000000000000000 ) ) ;
#21710=CARTESIAN_POINT ( 'NONE',  ( -14.00000000000000000, 15.45000000000000107, 0.000000000000000000 ) ) ;
#21713=CARTESIAN_POINT ( 'NONE',  ( -20.77592263693000163, -9.968135545850000057, -3.872507180638000257 ) ) ;
#21715=CARTESIAN_POINT ( 'NONE',  ( 14.88795491433943141, 10.27596259119593469, -1.066310422897988053 ) ) ;
#21717=CARTESIAN_POINT ( 'NONE',  ( 23.17123256445000123, -6.909033356756999922, -8.914582262144000069 ) ) ;
#21720=B_SPLINE_CURVE_WITH_KNOTS ( 'NONE', 3,
 ( #22566, #279, #163, #4049 ),
 .UNSPECIFIED., .F., .F.,
 ( 4, 4 ),
 ( 0.000000000000000000, 0.2414086770563061979 ),
 .UNSPECIFIED. ) ;
#21721=CARTESIAN_POINT ( 'NONE',  ( 0.3622508839787001444, 11.63016099405998816, -4.759913996260000779 ) ) ;
#21725=DIRECTION ( 'NONE',  ( -1.000000000000000000, 0.000000000000000000, 0.000000000000000000 ) ) ;
#21726=PLANE ( 'NONE',  #1099 ) ;
#21727=ORIENTED_EDGE ( 'NONE', *, *, #14895, .F. ) ;
#21730=DIRECTION ( 'NONE',  ( 1.000000000000000000, 0.000000000000000000, 0.000000000000000000 ) ) ;
#21731=CARTESIAN_POINT ( 'NONE',  ( 17.39987535718000089, -10.66748124715000046, -3.050476693690000296 ) ) ;
#21734=CARTESIAN_POINT ( 'NONE',  ( -11.64012149292000053, 14.44913244472000002, -1.408148137578000059 ) ) ;
#21735=B_SPLINE_CURVE_WITH_KNOTS ( 'NONE', 3,
 ( #20609, #11412, #6188, #18785, #10073 ),
 .UNSPECIFIED., .F., .F.,
 ( 4, 1, 4 ),
 ( 0.000000000000000000, 0.5000000000000000000, 1.000000000000000000 ),
 .UNSPECIFIED. ) ;
#21738=CARTESIAN_POINT ( 'NONE',  ( 11.32654380052929532, 12.11008572906302660, 4.024656720653348785 ) ) ;
#21739=CARTESIAN_POINT ( 'NONE',  ( 20.91152651491986703, -9.035863455013506851, 5.423255042272778326 ) ) ;
#21740=CARTESIAN_POINT ( 'NONE',  ( -14.00000000000000178, 4.694743687854951553, 8.221477620564558109 ) ) ;
#21741=CARTESIAN_POINT ( 'NONE',  ( 16.27872609588940023, 0.07001526935372526239, -10.36642397399645255 ) ) ;
#21742=CARTESIAN_POINT ( 'NONE',  ( -18.62749591150999962, 2.262565266096000283, -10.88529173890999857 ) ) ;
#21745=CARTESIAN_POINT ( 'NONE',  ( -18.39867747026000089, -7.918532069388001027, -5.797808426274999150 ) ) ;
#21747=ORIENTED_EDGE ( 'NONE', *, *, #11448, .T. ) ;
#21748=CARTESIAN_POINT ( 'NONE',  ( -23.86847083086815147, -5.679235826686364064, 12.50000000000278533 ) ) ;
#21749=CARTESIAN_POINT ( 'NONE',  ( 23.81066487044000013, 11.42980371577000120, -1.209163809909999943 ) ) ;
#21751=CARTESIAN_POINT ( 'NONE',  ( -12.25000000000000000, 15.45000000000000107, 0.000000000000000000 ) ) ;
#21753=CARTESIAN_POINT ( 'NONE',  ( -4.900699999999999612, 1.284663064832999817E-14, 0.000000000000000000 ) ) ;
#21755=CARTESIAN_POINT ( 'NONE',  ( -3.242527372584000034, 11.89078663977000616, -3.603690374931001195 ) ) ;
#21757=CARTESIAN_POINT ( 'NONE',  ( -6.042815832213999983, 16.39253418350000047, -0.9999999878869999526 ) ) ;
#21760=DIRECTION ( 'NONE',  ( 0.000000000000000000, 0.8660254037844288266, -0.5000000000000169864 ) ) ;
#21766=CARTESIAN_POINT ( 'NONE',  ( -3.711347484313542999, 14.46588732160023483, -4.873238578355667983 ) ) ;
#21767=CARTESIAN_POINT ( 'NONE',  ( -21.75873182887000112, -6.211188989293999541, 8.644182252947999245 ) ) ;
#21768=EDGE_CURVE ( 'NONE', #12558, #12473, #16116, .T. ) ;
#21769=CARTESIAN_POINT ( 'NONE',  ( -17.18320679392000017, 4.803081678427999712, 8.519217971866998695 ) ) ;
#21770=CARTESIAN_POINT ( 'NONE',  ( -5.666264227037997259, 14.58672067372999770, -4.744312203209001488 ) ) ;
#21771=CARTESIAN_POINT ( 'NONE',  ( -23.54679585804987951, 0.2324833852550877988, 10.57975454153479866 ) ) ;
#21776=CARTESIAN_POINT ( 'NONE',  ( 23.86147274828209675, -7.124683383478932264, 6.063353310551788056 ) ) ;
#21781=CARTESIAN_POINT ( 'NONE',  ( -3.166937750419610342, 11.90469789891420760, 3.644469328947587350 ) ) ;
#21782=ORIENTED_EDGE ( 'NONE', *, *, #16471, .T. ) ;
#21784=CARTESIAN_POINT ( 'NONE',  ( 4.632870948126061705, 12.36824807791137104, -1.431490575886223748 ) ) ;
#21787=CARTESIAN_POINT ( 'NONE',  ( 6.125000000000000000, 21.50000000000000000, 0.000000000000000000 ) ) ;
#21790=CARTESIAN_POINT ( 'NONE',  ( 16.79343892131000260, -7.329510781495000238, 6.390029238976000059 ) ) ;
#21791=CARTESIAN_POINT ( 'NONE',  ( 18.81675108960719456, 6.131865051825325708, 8.439018125457318220 ) ) ;
#21792=EDGE_CURVE ( 'NONE', #3147, #17, #6994, .T. ) ;
#21793=ORIENTED_EDGE ( 'NONE', *, *, #13937, .F. ) ;
#21795=DIRECTION ( 'NONE',  ( 0.000000000000000000, 1.000000000000000000, 0.000000000000000000 ) ) ;
#21796=CARTESIAN_POINT ( 'NONE',  ( -12.50116661936999840, 6.705358320533000516, -5.997050322680999912 ) ) ;
#21797=CARTESIAN_POINT ( 'NONE',  ( 13.50000000000000355, -6.133804904974399008, 8.162014436799776007 ) ) ;
#21799=FACE_OUTER_BOUND ( 'NONE', #10151, .T. ) ;
#21801=DIRECTION ( 'NONE',  ( 1.000000000000000000, 0.000000000000000000, 0.000000000000000000 ) ) ;
#21802=CARTESIAN_POINT ( 'NONE',  ( 13.50000000000000000, -4.865356088987999428, 9.073685197596999430 ) ) ;
#21803=FACE_OUTER_BOUND ( 'NONE', #22978, .T. ) ;
#21804=CARTESIAN_POINT ( 'NONE',  ( -4.101460439749002873, 12.21661303934001097, 2.777632186137001913 ) ) ;
#21805=ADVANCED_FACE ( 'NONE', ( #7144 ), #6844, .T. ) ;
#21806=CARTESIAN_POINT ( 'NONE',  ( -19.47031957961999638, -4.572788659038001136, 10.04465920712000049 ) ) ;
#21807=VERTEX_POINT ( 'NONE', #10562 ) ;
#21808=CARTESIAN_POINT ( 'NONE',  ( -14.65021834701999204, -8.903882834198213914, -1.852295623008597625 ) ) ;
#21813=CARTESIAN_POINT ( 'NONE',  ( 11.18529249867571806, 1.746922494874735499, -12.50002083036462430 ) ) ;
#21814=AXIS2_PLACEMENT_3D ( 'NONE', #17245, #2114, #22925 ) ;
#21815=DIRECTION ( 'NONE',  ( 0.000000000000000000, 1.000000000000000000, 0.000000000000000000 ) ) ;
#21817=EDGE_CURVE ( 'NONE', #12435, #20353, #4370, .T. ) ;
#21819=ORIENTED_EDGE ( 'NONE', *, *, #17867, .F. ) ;
#21820=FACE_OUTER_BOUND ( 'NONE', #13579, .T. ) ;
#21823=EDGE_CURVE ( 'NONE', #837, #10482, #7282, .T. ) ;
#21825=CARTESIAN_POINT ( 'NONE',  ( -19.23362201646000003, -8.964731209158999903, 5.752370880095000416 ) ) ;
#21827=CARTESIAN_POINT ( 'NONE',  ( 14.54008231524181483, 2.694371657221933170, -9.964067780447548373 ) ) ;
#21830=CARTESIAN_POINT ( 'NONE',  ( 19.72076563415999928, 4.999595931465999676, -10.00405158629999924 ) ) ;
#21832=CARTESIAN_POINT ( 'NONE',  ( 13.60227460879853112, 6.956803079665641931, -5.741568056601168202 ) ) ;
#21833=CARTESIAN_POINT ( 'NONE',  ( -4.754932747674998517, 12.62052246796000965, -0.7944665464532989496 ) ) ;
#21837=AXIS2_PLACEMENT_3D ( 'NONE', #17616, #19679, #1145 ) ;
#21841=CARTESIAN_POINT ( 'NONE',  ( 11.66614181938224704, -12.78577920080955899, -2.854240613922053083 ) ) ;
#21843=CIRCLE ( 'NONE', #9851, 10.59999999999999964 ) ;
#21844=CARTESIAN_POINT ( 'NONE',  ( 16.13671907226000002, 6.387739664468999656, -9.029444740878000530 ) ) ;
#21845=ORIENTED_EDGE ( 'NONE', *, *, #20089, .T. ) ;
#21846=B_SPLINE_CURVE_WITH_KNOTS ( 'NONE', 3,
 ( #15507, #21089, #8259, #21218 ),
 .UNSPECIFIED., .F., .F.,
 ( 4, 4 ),
 ( 0.000000000000000000, 1.000000000000000000 ),
 .UNSPECIFIED. ) ;
#21847=CARTESIAN_POINT ( 'NONE',  ( -9.996213638770001353, -8.329006823806000881, 12.73688500997000084 ) ) ;
#21848=CARTESIAN_POINT ( 'NONE',  ( 13.50000000000000000, 2.048741218006000064, 10.08990150394999930 ) ) ;
#21849=FACE_BOUND ( 'NONE', #19436, .T. ) ;
#21853=CARTESIAN_POINT ( 'NONE',  ( 20.82328275621039282, -6.980445704735060986, 7.888708581122024555 ) ) ;
#21854=CARTESIAN_POINT ( 'NONE',  ( -13.99999999999999822, 5.300363432082431103, 7.769144702572521766 ) ) ;
#21855=CARTESIAN_POINT ( 'NONE',  ( 16.02407758412532601, -7.929595264181977576, -6.665930917639996345 ) ) ;
#21856=CARTESIAN_POINT ( 'NONE',  ( -16.64019944616000046, 7.976360620752999786, -7.666729674259999960 ) ) ;
#21857=CARTESIAN_POINT ( 'NONE',  ( -14.45960639177118701, -12.05326364612463408, 4.123067891182932598 ) ) ;
#21859=CARTESIAN_POINT ( 'NONE',  ( -13.72667946694999941, 4.336095440212999641, 8.658528082053999597 ) ) ;
#21862=ORIENTED_EDGE ( 'NONE', *, *, #2289, .F. ) ;
#21863=CARTESIAN_POINT ( 'NONE',  ( 23.51329488828995551, -5.702615401652804117, 7.418699527094694268 ) ) ;
#21864=ADVANCED_FACE ( 'NONE', ( #1701 ), #2981, .F. ) ;
#21865=CARTESIAN_POINT ( 'NONE',  ( 19.41967423818407923, -10.43171934178962879, 1.169883962161388569 ) ) ;
#21867=ORIENTED_EDGE ( 'NONE', *, *, #4667, .T. ) ;
#21868=CARTESIAN_POINT ( 'NONE',  ( 24.36165043081784276, -9.237917109185875830, -8.999458210778742639 ) ) ;
#21869=CARTESIAN_POINT ( 'NONE',  ( -12.25000000000000000, 13.75000000000000000, 0.000000000000000000 ) ) ;
#21870=CARTESIAN_POINT ( 'NONE',  ( -2.168383903499000898, 11.64268071799000559, -4.342811940312000019 ) ) ;
#21871=EDGE_LOOP ( 'NONE', ( #10215, #3887, #7478, #20972, #23723 ) ) ;
#21877=DIRECTION ( 'NONE',  ( 1.000000000000000000, 0.000000000000000000, 0.000000000000000000 ) ) ;
#21879=CARTESIAN_POINT ( 'NONE',  ( -15.19472087121333637, -7.246037513405295449, 5.568446011427537812 ) ) ;
#21880=CARTESIAN_POINT ( 'NONE',  ( -21.70673924429999957, -9.986630310228999718, -1.660063458803999970 ) ) ;
#21882=CARTESIAN_POINT ( 'NONE',  ( 19.05504166666666066, 7.325075730494997828, -5.629504654586422241 ) ) ;
#21883=CARTESIAN_POINT ( 'NONE',  ( -23.98429299575930074, 10.59045595307713228, 0.3598248026102631725 ) ) ;
#21885=CARTESIAN_POINT ( 'NONE',  ( -5.330039164744003521, 15.50911245456000032, 2.864231857536000625 ) ) ;
#21887=FACE_OUTER_BOUND ( 'NONE', #23785, .T. ) ;
#21888=ORIENTED_EDGE ( 'NONE', *, *, #23015, .F. ) ;
#21890=CARTESIAN_POINT ( 'NONE',  ( 4.829988586904999437, 14.79876397742000016, 3.766541904039999888 ) ) ;
#21895=CARTESIAN_POINT ( 'NONE',  ( 1.772600511826058822, 11.61607745207374975, 4.480042189610983883 ) ) ;
#21896=EDGE_LOOP ( 'NONE', ( #156, #7778, #2720, #17950, #8107 ) ) ;
#21898=CARTESIAN_POINT ( 'NONE',  ( -1.981777970230752084, 11.64981023145996453, -4.391405225778299837 ) ) ;
#21901=EDGE_LOOP ( 'NONE', ( #1562, #22499, #9848 ) ) ;
#21905=CARTESIAN_POINT ( 'NONE',  ( 16.35468892131000018, 6.000265896171000257, 7.637201470843999473 ) ) ;
#21906=CARTESIAN_POINT ( 'NONE',  ( 18.85894798992291399, 4.799130230538453112, 9.275998069617465092 ) ) ;
#21909=CARTESIAN_POINT ( 'NONE',  ( 17.29108580085999947, -6.112256495352999863, 9.625372826315000907 ) ) ;
#21910=CARTESIAN_POINT ( 'NONE',  ( 13.49999999999999467, -6.881482076045544183, 7.468481572847831096 ) ) ;
#21911=EDGE_LOOP ( 'NONE', ( #1644, #3468 ) ) ;
#21913=CARTESIAN_POINT ( 'NONE',  ( 24.46803514405999991, 6.544162614452000426, 8.648843365141001271 ) ) ;
#21914=CARTESIAN_POINT ( 'NONE',  ( -24.46466276874232904, 5.021295921611101498, -9.004480667326742349 ) ) ;
#21916=CARTESIAN_POINT ( 'NONE',  ( 24.50000000000000000, -8.246372141814999779, 6.625187740483999832 ) ) ;
#21917=CARTESIAN_POINT ( 'NONE',  ( -3.862330210613311721, 14.00496637028538593, 4.847486289291174977 ) ) ;
#21918=CARTESIAN_POINT ( 'NONE',  ( -4.911810085394003877, 12.43822141189999542, -0.1532012021291000170 ) ) ;
#21919=CARTESIAN_POINT ( 'NONE',  ( -23.81451776991000102, 9.879857505359000314, -5.177521040838999333 ) ) ;
#21920=ORIENTED_EDGE ( 'NONE', *, *, #6829, .F. ) ;
#21925=ADVANCED_FACE ( 'NONE', ( #5458 ), #7261, .F. ) ;
#21927=CARTESIAN_POINT ( 'NONE',  ( 5.057845774443002540, 14.83209949158001884, 3.474588151562001404 ) ) ;
#21928=CARTESIAN_POINT ( 'NONE',  ( 4.155001577763409948, 13.38046536914801266, 5.412598244128762559 ) ) ;
#21932=CARTESIAN_POINT ( 'NONE',  ( -17.78928642635000301, 9.027876325972000515, -3.804579355723999967 ) ) ;
#21933=CARTESIAN_POINT ( 'NONE',  ( -7.834000000000000519, 1.320585629393000037E-14, 0.000000000000000000 ) ) ;
#21935=DIRECTION ( 'NONE',  ( 1.000000000000000000, 0.000000000000000000, 0.000000000000000000 ) ) ;
#21938=CARTESIAN_POINT ( 'NONE',  ( -10.88471959503360331, 15.34845819752904461, -1.727494947682089999 ) ) ;
#21941=CARTESIAN_POINT ( 'NONE',  ( 14.63547441700031548, 5.828595367498566659, -8.523805803212322729 ) ) ;
#21943=CARTESIAN_POINT ( 'NONE',  ( 24.05204201319999768, 10.75388736322999961, 3.479171898811000307 ) ) ;
#21945=CARTESIAN_POINT ( 'NONE',  ( 14.07248325032791314, 5.273353179838896843, 7.334521014497600078 ) ) ;
#21946=CARTESIAN_POINT ( 'NONE',  ( -12.00000000000000000, 1.371604415045000054E-14, 0.000000000000000000 ) ) ;
#21949=CARTESIAN_POINT ( 'NONE',  ( -14.95696059356579433, -8.969510928318662479, -1.518716752286801031 ) ) ;
#21955=CARTESIAN_POINT ( 'NONE',  ( 11.18529249867709474, -9.951874339551746829, -7.762889674110271976 ) ) ;
#21956=AXIS2_PLACEMENT_3D ( 'NONE', #17279, #21030, #22839 ) ;
#21957=CARTESIAN_POINT ( 'NONE',  ( 21.75799770046333137, 1.208283319978225689, 9.229634816791103091 ) ) ;
#21958=CARTESIAN_POINT ( 'NONE',  ( 18.48258074425000075, 7.027092927644000397, 8.624643700690000969 ) ) ;
#21959=CARTESIAN_POINT ( 'NONE',  ( -14.19545626576198138, -2.703128947221847156, 9.988535580370172084 ) ) ;
#21960=ORIENTED_EDGE ( 'NONE', *, *, #20208, .F. ) ;
#21961=CARTESIAN_POINT ( 'NONE',  ( -12.04003756584999962, 8.646183865892000497, -12.09541814886999944 ) ) ;
#21962=DIRECTION ( 'NONE',  ( -1.000000000000000000, 0.000000000000000000, 0.000000000000000000 ) ) ;
#21963=CARTESIAN_POINT ( 'NONE',  ( -14.43045961913871089, -12.44097983993757595, -3.451577511306503698 ) ) ;
#21964=VERTEX_POINT ( 'NONE', #14882 ) ;
#21966=CARTESIAN_POINT ( 'NONE',  ( 20.41147854889662838, 6.791870828880062660, 8.042442484653800960 ) ) ;
#21968=CARTESIAN_POINT ( 'NONE',  ( 16.10246075293501633, -5.923530797957349492, -8.502184744949477846 ) ) ;
#21970=B_SPLINE_CURVE_WITH_KNOTS ( 'NONE', 3,
 ( #19193, #10117, #21136, #17506, #22938, #3107, #23187, #4548, #16027, #19570, #13865, #2856, #900, #2974, #1025, #4795, #17993, #15551, #12179, #4915, #2735, #6355, #13987, #10365, #15666, #1158, #23421, #21378, #12062, #10239, #19692, #8302, #15796, #17754, #8551, #10491, #12302, #6481, #14232, #23056 ),
 .UNSPECIFIED., .F., .F.,
 ( 4, 2, 2, 1, 1, 2, 2, 2, 2, 2, 2, 2, 2, 1, 2, 2, 2, 2, 1, 2, 2, 4 ),
 ( 0.000000000000000000, 0.1250000000000027478, 0.1875000000000036637, 0.2187500000000025258, 0.2343750000000018319, 0.2421875000000017764, 0.2500000000000017208, 0.3125000000000177081, 0.3437500000000245359, 0.3593750000000291989, 0.3750000000000339173, 0.4375000000000564548, 0.4687500000000697775, 0.4843750000000763833, 0.4921875000000776601, 0.5000000000000789369, 0.6250000000000606182, 0.6875000000000502931, 0.7187500000000442979, 0.7343750000000424105, 0.7500000000000406342, 1.000000000000000000 ),
 .UNSPECIFIED. ) ;
#21971=CARTESIAN_POINT ( 'NONE',  ( -18.94199577250666167, 4.611708388952700410, 8.001634414202589696 ) ) ;
#21973=CARTESIAN_POINT ( 'NONE',  ( -16.57050433853000015, -7.584645295112999897, -6.147042915735999813 ) ) ;
#21974=EDGE_CURVE ( 'NONE', #6021, #21466, #11099, .T. ) ;
#21975=AXIS2_PLACEMENT_3D ( 'NONE', #4765, #8025, #20137 ) ;
#21977=EDGE_LOOP ( 'NONE', ( #14818, #23688, #8677, #4826, #9232 ) ) ;
#21979=CARTESIAN_POINT ( 'NONE',  ( 20.10063544609122843, 6.579109543901849655, -8.200420943266742313 ) ) ;
#21980=DIRECTION ( 'NONE',  ( 1.000000000000000000, 0.000000000000000000, 0.000000000000000000 ) ) ;
#21983=CARTESIAN_POINT ( 'NONE',  ( 24.45564077607145492, -9.795255522623715905, -8.034119761694611839 ) ) ;
#21984=CARTESIAN_POINT ( 'NONE',  ( -14.25243324638999809, -7.716878364870000340, -11.63397459621999985 ) ) ;
#21987=CARTESIAN_POINT ( 'NONE',  ( 4.838659373281001486, 12.42377767764999419, -0.1101032568685000185 ) ) ;
#21994=EDGE_CURVE ( 'NONE', #5259, #12884, #11331, .T. ) ;
#21995=CARTESIAN_POINT ( 'NONE',  ( 22.85395603379666341, 4.662265998550135571, -8.089352615493318410 ) ) ;
#21998=CARTESIAN_POINT ( 'NONE',  ( -22.83084603907999721, 8.452768372852000667, -5.626295165922000407 ) ) ;
#21999=CARTESIAN_POINT ( 'NONE',  ( -20.43329236144000305, -6.491487173960999613, 6.361872185110000189 ) ) ;
#22000=CARTESIAN_POINT ( 'NONE',  ( -4.850028262036998328, 13.70733162851999865, -4.729463290261002761 ) ) ;
#22001=CARTESIAN_POINT ( 'NONE',  ( -23.13503384608747027, -10.42901907143014739, 1.748523312326609513 ) ) ;
#22006=VERTEX_POINT ( 'NONE', #14763 ) ;
#22007=CARTESIAN_POINT ( 'NONE',  ( -17.23547087121333732, -1.193091500503335789, 9.113577864919761851 ) ) ;
#22008=CARTESIAN_POINT ( 'NONE',  ( 3.952348409963450049, 14.44207180802359147, 4.679171297609252989 ) ) ;
#22013=CIRCLE ( 'NONE', #14659, 0.5000000000000004441 ) ;
#22014=CARTESIAN_POINT ( 'NONE',  ( 1.268068893756492344, 11.54954083627711192, 4.648988597672141232 ) ) ;
#22016=CARTESIAN_POINT ( 'NONE',  ( -3.428826227638388957, 11.97595429753372009, -3.402799634008572660 ) ) ;
#22017=CARTESIAN_POINT ( 'NONE',  ( -10.51102833032320483, 15.52504438449052060, 1.381747433397627178 ) ) ;
#22018=CIRCLE ( 'NONE', #20464, 15.43375672974000068 ) ;
#22019=PLANE ( 'NONE',  #5674 ) ;
#22021=EDGE_CURVE ( 'NONE', #19135, #14395, #2202, .T. ) ;
#22023=CARTESIAN_POINT ( 'NONE',  ( -16.44184587121332441, -2.380011688135305281, -8.856588498222468075 ) ) ;
#22024=CARTESIAN_POINT ( 'NONE',  ( 11.85750142130999940, -4.891210171397999851, -8.253706317253998392 ) ) ;
#22025=CARTESIAN_POINT ( 'NONE',  ( 18.58429248281415624, 10.33569022815195027, 1.375693033861695280 ) ) ;
#22028=CARTESIAN_POINT ( 'NONE',  ( -24.46742986863897329, 1.281690452090803456, 12.50000620969185938 ) ) ;
#22030=CARTESIAN_POINT ( 'NONE',  ( -12.49274363707000113, 6.877373328682999443, -5.798644816960000448 ) ) ;
#22031=CARTESIAN_POINT ( 'NONE',  ( 13.50000000000000000, -9.115747871093871524, 3.863369538079849619 ) ) ;
#22032=AXIS2_PLACEMENT_3D ( 'NONE', #3833, #23932, #7340 ) ;
#22034=VECTOR ( 'NONE', #5669, 1000.000000000000227 ) ;
#22035=CARTESIAN_POINT ( 'NONE',  ( -24.47970833437436156, 11.33727345181091550, 5.363206565949876214 ) ) ;
#22036=CARTESIAN_POINT ( 'NONE',  ( 19.77050301799999943, -3.010326857828999891, -10.83590067529000045 ) ) ;
#22037=CARTESIAN_POINT ( 'NONE',  ( -24.15753426113404956, 8.341958059169604311, 5.501469373877088564 ) ) ;
#22040=CARTESIAN_POINT ( 'NONE',  ( 4.698522026118003403, 12.42251073348998425, 1.557367633878998348 ) ) ;
#22043=ORIENTED_EDGE ( 'NONE', *, *, #5972, .T. ) ;
#22047=CARTESIAN_POINT ( 'NONE',  ( 6.112958255465001045, 13.74060334821000318, 1.425172817424000149 ) ) ;
#22048=CARTESIAN_POINT ( 'NONE',  ( 11.12576011241567109, -1.246535810014351764, -12.50000754954019833 ) ) ;
#22050=DIRECTION ( 'NONE',  ( 1.000000000000000000, 0.000000000000000000, 0.000000000000000000 ) ) ;
#22051=CARTESIAN_POINT ( 'NONE',  ( 18.27225174930999785, 9.757448129154999705, -4.584997352848999341 ) ) ;
#22054=CARTESIAN_POINT ( 'NONE',  ( -18.19554712229000160, -2.285746783449999597, -9.537972663088998715 ) ) ;
#22055=DIRECTION ( 'NONE',  ( 0.000000000000000000, 1.000000000000000000, 0.000000000000000000 ) ) ;
#22058=CARTESIAN_POINT ( 'NONE',  ( -20.67707759490999919, -0.1471764284891000085, -11.21320839060999930 ) ) ;
#22060=CARTESIAN_POINT ( 'NONE',  ( 14.65172699290454972, 6.282441235618426489, -8.192983905010713386 ) ) ;
#22061=DIRECTION ( 'NONE',  ( 1.000000000000000000, 0.000000000000000000, 0.000000000000000000 ) ) ;
#22062=CARTESIAN_POINT ( 'NONE',  ( 24.78622986507000192, -10.15669625742000015, 2.982069395447000115 ) ) ;
#22063=EDGE_CURVE ( 'NONE', #18634, #4798, #15942, .T. ) ;
#22065=CARTESIAN_POINT ( 'NONE',  ( 14.09167841898807438, 4.781097061663486691, 7.663137420670809163 ) ) ;
#22066=CARTESIAN_POINT ( 'NONE',  ( 1.385371806688001639, 11.73739883782001314, -4.651319360739003095 ) ) ;
#22069=CARTESIAN_POINT ( 'NONE',  ( -14.67092228382045782, -3.603863581076387490, -8.324530791617933190 ) ) ;
#22070=DIRECTION ( 'NONE',  ( -1.000000000000000000, 0.000000000000000000, 0.000000000000000000 ) ) ;
#22071=VERTEX_POINT ( 'NONE', #19958 ) ;
#22073=CARTESIAN_POINT ( 'NONE',  ( 11.36448692219090084, -9.446283672508670293, -8.638507912415571255 ) ) ;
#22076=CARTESIAN_POINT ( 'NONE',  ( 13.42244730194000013, 3.896089010268000141, 9.766325367788999401 ) ) ;
#22077=CARTESIAN_POINT ( 'NONE',  ( -16.37253276963559756, 8.717735455328519123, 5.679932193535492502 ) ) ;
#22080=CARTESIAN_POINT ( 'NONE',  ( -9.283456138769999200, 6.248931676845000283, -13.87633134369000132 ) ) ;
#22081=CARTESIAN_POINT ( 'NONE',  ( 13.49999999999999289, 9.584200888098308724, 0.3179355005750706953 ) ) ;
#22082=CARTESIAN_POINT ( 'NONE',  ( -14.37382028566586101, -13.01774735371480318, -2.452106660102837843 ) ) ;
#22083=ORIENTED_EDGE ( 'NONE', *, *, #18884, .T. ) ;
#22084=CARTESIAN_POINT ( 'NONE',  ( 23.05879131019755235, -8.652720740703848890, -6.105659068090134589 ) ) ;
#22085=CARTESIAN_POINT ( 'NONE',  ( 24.37173283531060619, 9.297778257491829734, -8.895775660514537719 ) ) ;
#22086=CARTESIAN_POINT ( 'NONE',  ( 16.16828646285382476, -3.839896425325243889, -9.652464845986353126 ) ) ;
#22087=CARTESIAN_POINT ( 'NONE',  ( -15.88350446789000081, -7.863141422307999839, 7.753313641256998956 ) ) ;
#22090=CARTESIAN_POINT ( 'NONE',  ( -17.83004450757999848, 9.857337362280999216, 3.100493417357999881 ) ) ;
#22092=VERTEX_POINT ( 'NONE', #12804 ) ;
#22094=CARTESIAN_POINT ( 'NONE',  ( 21.32069094358849526, -10.50854990665072997, -1.992772991833056562 ) ) ;
#22096=EDGE_LOOP ( 'NONE', ( #6486, #4746, #18220, #13479, #18567 ) ) ;
#22097=CARTESIAN_POINT ( 'NONE',  ( 24.07420734439622123, -5.678657336859300742, 12.50000000000000355 ) ) ;
#22098=CARTESIAN_POINT ( 'NONE',  ( 4.856921901366256122, 14.53926045619292751, -3.784552473569310571 ) ) ;
#22099=EDGE_CURVE ( 'NONE', #20167, #9887, #13029, .T. ) ;
#22100=CARTESIAN_POINT ( 'NONE',  ( -4.856048418805002598, 12.41684859253000361, -0.7982404537521002874 ) ) ;
#22101=ORIENTED_EDGE ( 'NONE', *, *, #14737, .T. ) ;
#22102=CARTESIAN_POINT ( 'NONE',  ( 14.13450125731000107, 8.592455601080001060, 3.130286720869000394 ) ) ;
#22104=CARTESIAN_POINT ( 'NONE',  ( -4.972490738245377351, 15.85507734270906077, 3.578469026183233037 ) ) ;
#22106=ADVANCED_FACE ( 'NONE', ( #3253 ), #5188, .F. ) ;
#22107=CARTESIAN_POINT ( 'NONE',  ( -7.034000000000000696, -11.50000000000000000, 0.000000000000000000 ) ) ;
#22109=CARTESIAN_POINT ( 'NONE',  ( -23.39536544476928981, -2.238522300281205801, -9.155022575166720245 ) ) ;
#22111=CARTESIAN_POINT ( 'NONE',  ( -25.18765372902999999, 0.3463529480658999460, -9.692089422165000911 ) ) ;
#22112=EDGE_CURVE ( 'NONE', #11620, #2581, #19703, .T. ) ;
#22113=CARTESIAN_POINT ( 'NONE',  ( 11.78693030655906782, -8.669062849295544382, -9.984739426234524373 ) ) ;
#22114=CARTESIAN_POINT ( 'NONE',  ( -4.012811773491001155, 13.17015569023999610, -4.696507356432001679 ) ) ;
#22115=EDGE_CURVE ( 'NONE', #2581, #4204, #36, .T. ) ;
#22116=CARTESIAN_POINT ( 'NONE',  ( -24.44752525921816044, 0.002284610134966501369, -10.60947411550792729 ) ) ;
#22118=CARTESIAN_POINT ( 'NONE',  ( 16.33404166666666057, -7.269238015384150486, 5.586593178390435455 ) ) ;
#22121=ORIENTED_EDGE ( 'NONE', *, *, #11448, .F. ) ;
#22122=DIRECTION ( 'NONE',  ( 0.000000000000000000, -0.5000000000000169864, -0.8660254037844288266 ) ) ;
#22124=CARTESIAN_POINT ( 'NONE',  ( -21.07269641591645026, -10.52253052917413001, -0.05638204554735719992 ) ) ;
#22126=EDGE_CURVE ( 'NONE', #10277, #11958, #10485, .T. ) ;
#22128=FACE_OUTER_BOUND ( 'NONE', #16639, .T. ) ;
#22129=ORIENTED_EDGE ( 'NONE', *, *, #15154, .T. ) ;
#22130=CARTESIAN_POINT ( 'NONE',  ( -4.194936859874647261, 12.21355901615086559, -2.415068615545117758 ) ) ;
#22133=ORIENTED_EDGE ( 'NONE', *, *, #10473, .T. ) ;
#22134=CARTESIAN_POINT ( 'NONE',  ( 11.77156519342000074, 1.080486702797000030E-14, 0.000000000000000000 ) ) ;
#22135=CARTESIAN_POINT ( 'NONE',  ( 18.46518908530999781, 4.839936825908999651, 9.065913725881001639 ) ) ;
#22136=CARTESIAN_POINT ( 'NONE',  ( 18.58923523000861877, 10.30907166458805690, 1.558049498255399845 ) ) ;
#22137=EDGE_CURVE ( 'NONE', #6064, #17452, #11025, .T. ) ;
#22141=CARTESIAN_POINT ( 'NONE',  ( 18.30671080085999947, 9.244294984138999638, -6.722868547277000673 ) ) ;
#22142=CARTESIAN_POINT ( 'NONE',  ( 13.49999999999999289, -8.867844327939206295, 4.500207874338363112 ) ) ;
#22144=VERTEX_POINT ( 'NONE', #16126 ) ;
#22146=CARTESIAN_POINT ( 'NONE',  ( 20.21885669234999838, 3.601023353282000183, -10.10703359440999982 ) ) ;
#22147=CARTESIAN_POINT ( 'NONE',  ( -24.05515809193239818, 4.205914552781904625, 8.947780035611691218 ) ) ;
#22149=CARTESIAN_POINT ( 'NONE',  ( 24.49999999999999645, -5.925652364458730226, 8.763099245663633852 ) ) ;
#22150=CARTESIAN_POINT ( 'NONE',  ( 24.50000000000000355, 6.882980620445878550, 7.423222315167702590 ) ) ;
#22151=CARTESIAN_POINT ( 'NONE',  ( 3.409885634504002283, 11.93905035093000677, 3.554569955099000200 ) ) ;
#22153=FACE_OUTER_BOUND ( 'NONE', #15949, .T. ) ;
#22154=ORIENTED_EDGE ( 'NONE', *, *, #14309, .T. ) ;
#22159=CARTESIAN_POINT ( 'NONE',  ( 6.265492238153998805, 13.70414734520999112, 0.3873945776806000940 ) ) ;
#22160=CARTESIAN_POINT ( 'NONE',  ( 11.85409292834066264, -4.507814091389457545, -12.50002426122858168 ) ) ;
#22161=CARTESIAN_POINT ( 'NONE',  ( 19.05233531832000082, -1.887707665395999879, 10.26617185442000135 ) ) ;
#22163=CARTESIAN_POINT ( 'NONE',  ( 17.83350174931000254, -4.076359992019000344, -9.968186170592000295 ) ) ;
#22165=CARTESIAN_POINT ( 'NONE',  ( -17.38302573041000088, 5.218320932965999859, 8.277968099418000492 ) ) ;
#22167=LINE ( 'NONE', #8748, #17098 ) ;
#22169=CARTESIAN_POINT ( 'NONE',  ( -10.68259645647714429, 15.42389723940939739, -1.538719359861782099 ) ) ;
#22171=CARTESIAN_POINT ( 'NONE',  ( 14.77189528956980347, 9.067954214462249141, -4.942123315334161049 ) ) ;
#22173=CARTESIAN_POINT ( 'NONE',  ( 22.91383486932000224, -6.129809015165000652, 9.458891919796998948 ) ) ;
#22175=CARTESIAN_POINT ( 'NONE',  ( 14.10179216132728719, 4.514300806135581823, 7.822680230860565409 ) ) ;
#22176=CARTESIAN_POINT ( 'NONE',  ( -6.634681955164054123, 15.38524051851555363, -1.622884314630087754 ) ) ;
#22177=CARTESIAN_POINT ( 'NONE',  ( -6.781029893680056375, 15.33022057605113631, 1.804325008919367201 ) ) ;
#22178=CARTESIAN_POINT ( 'NONE',  ( 11.31235608930338721, 12.07787442524536026, -4.080443649690880470 ) ) ;
#22179=ORIENTED_EDGE ( 'NONE', *, *, #16075, .T. ) ;
#22181=DIRECTION ( 'NONE',  ( -1.000000000000000000, 0.000000000000000000, 0.000000000000000000 ) ) ;
#22184=CARTESIAN_POINT ( 'NONE',  ( 21.98474770046333049, -5.675527994026910328, 7.385375838905533286 ) ) ;
#22185=CARTESIAN_POINT ( 'NONE',  ( 18.02019104568000429, -6.876349436605000420, -8.728898656365000619 ) ) ;
#22186=CARTESIAN_POINT ( 'NONE',  ( -6.250000012226999857, 15.73199627394999922, 1.185103398761000015 ) ) ;
#22190=CARTESIAN_POINT ( 'NONE',  ( -11.42910256584999829, -0.5664460622508999954, 14.85721958263000175 ) ) ;
#22192=AXIS2_PLACEMENT_3D ( 'NONE', #13499, #2734, #17505 ) ;
#22194=ORIENTED_EDGE ( 'NONE', *, *, #2067, .T. ) ;
#22195=CARTESIAN_POINT ( 'NONE',  ( -24.33938584176032904, 9.417644943808182845, 8.688014043592605873 ) ) ;
#22196=CARTESIAN_POINT ( 'NONE',  ( 19.49962637556187772, -6.917197816422240741, -7.905051631841183202 ) ) ;
#22197=CARTESIAN_POINT ( 'NONE',  ( 24.40278699097224546, 9.495349905928280876, -8.553571527287482823 ) ) ;
#22198=CARTESIAN_POINT ( 'NONE',  ( 15.92969900157650187, -9.688817912527115439, -3.663007575884178024 ) ) ;
#22199=CARTESIAN_POINT ( 'NONE',  ( -19.10140242030999858, -4.547125262218999708, -10.15970676401999917 ) ) ;
#22201=CARTESIAN_POINT ( 'NONE',  ( -16.40813207178999988, 5.092047131649000136, -8.946165747030999427 ) ) ;
#22203=ORIENTED_EDGE ( 'NONE', *, *, #23312, .T. ) ;
#22205=CARTESIAN_POINT ( 'NONE',  ( 22.39887952277467420, 7.496365056892780210, 7.455554306885533222 ) ) ;
#22207=EDGE_LOOP ( 'NONE', ( #17868, #11726, #858, #20260 ) ) ;
#22208=CARTESIAN_POINT ( 'NONE',  ( -5.147747017024999039, 14.44777671499001315, 4.022432192786999927 ) ) ;
#22209=CARTESIAN_POINT ( 'NONE',  ( 17.92129166666665085, -1.195141376095407493, 9.131177378213125806 ) ) ;
#22210=EDGE_CURVE ( 'NONE', #14425, #3901, #16498, .T. ) ;
#22211=CARTESIAN_POINT ( 'NONE',  ( 14.24418875730999900, 6.821019272440999259, 6.095525253705999624 ) ) ;
#22212=EDGE_LOOP ( 'NONE', ( #20686, #11618, #2049 ) ) ;
#22214=CARTESIAN_POINT ( 'NONE',  ( -14.45561360440065890, -2.584657965311079941, -12.49996445837131276 ) ) ;
#22217=CARTESIAN_POINT ( 'NONE',  ( 4.222040842892996970, 12.42583961254000968, 2.326471633585998067 ) ) ;
#22219=EDGE_CURVE ( 'NONE', #10732, #19490, #8714, .T. ) ;
#22220=CARTESIAN_POINT ( 'NONE',  ( 11.48696334737605085, -9.189637287600886495, -9.082924181340967351 ) ) ;
#22221=CARTESIAN_POINT ( 'NONE',  ( 18.41258333333331620, -8.905845225604863913, -2.393249065827368405 ) ) ;
#22222=DIRECTION ( 'NONE',  ( 0.000000000000000000, 0.000000000000000000, 1.000000000000000000 ) ) ;
#22223=CARTESIAN_POINT ( 'NONE',  ( -23.74465998031000069, 13.93375672974000068, 0.8660254037843999608 ) ) ;
#22229=CARTESIAN_POINT ( 'NONE',  ( 22.87997594487999820, 7.046585999850999649, -6.898543380703000771 ) ) ;
#22231=CARTESIAN_POINT ( 'NONE',  ( -23.88421579307469855, 10.09359931140187783, -3.213991999759431728 ) ) ;
#22234=CARTESIAN_POINT ( 'NONE',  ( 3.258516839496470752, 11.92856103705473636, 3.566823035891872440 ) ) ;
#22236=EDGE_CURVE ( 'NONE', #14845, #9831, #3082, .T. ) ;
#22237=CARTESIAN_POINT ( 'NONE',  ( -4.794898800817616547, 12.42857861981699941, -0.8372831007215363330 ) ) ;
#22238=CARTESIAN_POINT ( 'NONE',  ( -5.194121241777001075, -12.44999999999999929, 0.000000000000000000 ) ) ;
#22242=CARTESIAN_POINT ( 'NONE',  ( 13.85831408531000086, -6.842896344163999167, -7.504413997217999288 ) ) ;
#22243=CARTESIAN_POINT ( 'NONE',  ( 18.03882547314998774, -1.826631431717876675, -10.26437193003392245 ) ) ;
#22247=CARTESIAN_POINT ( 'NONE',  ( 17.69733580085999947, -10.50304813760000044, -4.466741093449000388 ) ) ;
#22249=B_SPLINE_CURVE_WITH_KNOTS ( 'NONE', 3,
 ( #10429, #3283, #16222, #4981, #22118, #5637, #10665, #1339, #16090, #16660, #21568, #18053, #12904, #20304, #7450, #18483, #19756, #3832 ),
 .UNSPECIFIED., .F., .F.,
 ( 4, 2, 2, 2, 2, 2, 2, 2, 4 ),
 ( 0.000000000000000000, 0.1249999999999999722, 0.2500000000000000000, 0.3750000000000000000, 0.5000000000000001110, 0.6250000000000001110, 0.7500000000000000000, 0.8750000000000000000, 1.000000000000000000 ),
 .UNSPECIFIED. ) ;
#22250=ORIENTED_EDGE ( 'NONE', *, *, #6277, .F. ) ;
#22252=CARTESIAN_POINT ( 'NONE',  ( 18.88525750721999685, 2.047957541271999915, 10.33960724111999951 ) ) ;
#22255=CARTESIAN_POINT ( 'NONE',  ( 13.72309434659665683, -9.869885134801844373, 3.116967400436540636 ) ) ;
#22257=CARTESIAN_POINT ( 'NONE',  ( -4.621291600221002049, 12.34015603868000710, 1.443184655503999547 ) ) ;
#22259=CARTESIAN_POINT ( 'NONE',  ( -20.47282685430000271, 1.064915000120000066, -11.01223998885000022 ) ) ;
#22260=ORIENTED_EDGE ( 'NONE', *, *, #17403, .F. ) ;
#22261=DIRECTION ( 'NONE',  ( -1.000000000000000000, 0.000000000000000000, 0.000000000000000000 ) ) ;
#22262=ORIENTED_EDGE ( 'NONE', *, *, #23079, .F. ) ;
#22266=CARTESIAN_POINT ( 'NONE',  ( 6.543402445986997051, 13.52098819050001133, 1.162556828447999901 ) ) ;
#22273=CARTESIAN_POINT ( 'NONE',  ( 14.10412674931000154, -7.190271978224999749, -7.885398697387000944 ) ) ;
#22279=CARTESIAN_POINT ( 'NONE',  ( -18.73259798496000172, -8.620928137991000995, 3.072238420002000314 ) ) ;
#22282=CARTESIAN_POINT ( 'NONE',  ( 14.73749136213059785, 8.405818844597368056, -6.030319882502336526 ) ) ;
#22283=CARTESIAN_POINT ( 'NONE',  ( -18.48259587121333425, -7.991236091536491060, -4.606005739639033258 ) ) ;
#22284=CARTESIAN_POINT ( 'NONE',  ( 23.28092879524999859, -10.85541562098999968, -3.071221882731999919 ) ) ;
#22286=CARTESIAN_POINT ( 'NONE',  ( 14.31728336214042230, -1.911400327409435551, 8.862201799975091276 ) ) ;
#22287=CARTESIAN_POINT ( 'NONE',  ( 3.779846905083999342, 12.27705807091000700, -3.020046618730999555 ) ) ;
#22288=AXIS2_PLACEMENT_3D ( 'NONE', #16198, #15705, #5082 ) ;
#22291=CARTESIAN_POINT ( 'NONE',  ( 11.29022434643809270, 9.635153832122318462, -8.311371697084542376 ) ) ;
#22297=CARTESIAN_POINT ( 'NONE',  ( 22.87199999999999989, 9.258222311379999070, 0.000000000000000000 ) ) ;
#22298=DIRECTION ( 'NONE',  ( 0.000000000000000000, 0.000000000000000000, -1.000000000000000000 ) ) ;
#22299=AXIS2_PLACEMENT_3D ( 'NONE', #22939, #17507, #6483 ) ;
#22300=CARTESIAN_POINT ( 'NONE',  ( 17.51266765309999940, -10.43854800410000117, 3.769063558861000196 ) ) ;
#22301=CARTESIAN_POINT ( 'NONE',  ( 13.50000000000000000, 4.517872873748999929, -7.804362139085999850 ) ) ;
#22307=CARTESIAN_POINT ( 'NONE',  ( -10.60714863877000091, 13.96228639389999948, -6.054349922818000884 ) ) ;
#22308=CARTESIAN_POINT ( 'NONE',  ( 11.00000000000000000, 10.59999999999999964, 0.000000000000000000 ) ) ;
#22311=CARTESIAN_POINT ( 'NONE',  ( -24.48376588670982912, 10.31426502621302710, 7.135315508360969616 ) ) ;
#22312=CARTESIAN_POINT ( 'NONE',  ( 20.14674727276818800, 10.50482826883816578, -0.4971117468655986138 ) ) ;
#22313=LINE ( 'NONE', #9017, #14157 ) ;
#22314=CARTESIAN_POINT ( 'NONE',  ( 15.89284332445408943, -10.06731258041612165, -2.433320157096150460 ) ) ;
#22315=CARTESIAN_POINT ( 'NONE',  ( -18.19808584514999694, 4.666018550332999837, 10.07846247694000041 ) ) ;
#22317=CARTESIAN_POINT ( 'NONE',  ( -13.19880458549999958, -0.9434914505904000714, -10.69878979702999899 ) ) ;
#22320=ORIENTED_EDGE ( 'NONE', *, *, #13816, .T. ) ;
#22321=TOROIDAL_SURFACE ( 'NONE', #17711, 4.649999999999999467, 0.1000000000000000056 ) ;
#22323=CARTESIAN_POINT ( 'NONE',  ( 20.89509018864575296, -2.982496466438095517, 10.10845216425653881 ) ) ;
#22324=CARTESIAN_POINT ( 'NONE',  ( 4.816302164864996627, 14.93028961201002147, -3.795745731844999415 ) ) ;
#22325=ORIENTED_EDGE ( 'NONE', *, *, #1343, .T. ) ;
#22326=CARTESIAN_POINT ( 'NONE',  ( -23.74465998031000069, -7.716878364870000340, 11.63397459621999985 ) ) ;
#22327=CARTESIAN_POINT ( 'NONE',  ( -4.498662548786000137, 15.01211498829999869, 3.843732114414002865 ) ) ;
#22328=CARTESIAN_POINT ( 'NONE',  ( 18.18583333333330998, -7.984581761151016366, 4.602170423446800385 ) ) ;
#22329=CARTESIAN_POINT ( 'NONE',  ( 13.03762625731000036, -8.686210121801000383, 2.766264305181999728 ) ) ;
#22332=CARTESIAN_POINT ( 'NONE',  ( -4.623317570261906262, 15.59290886452487968, 4.017537324272654864 ) ) ;
#22334=CARTESIAN_POINT ( 'NONE',  ( -14.25243324638999809, 6.216878364870000340, -12.50000000000000000 ) ) ;
#22336=CARTESIAN_POINT ( 'NONE',  ( -23.13361993687182760, 5.790620044384096055, -7.422872665018464211 ) ) ;
#22337=CARTESIAN_POINT ( 'NONE',  ( 1.591886459334999726, 11.74621052866999449, 4.486094747653003978 ) ) ;
#22338=CARTESIAN_POINT ( 'NONE',  ( -23.26061350940999972, 3.997618465669000365, -8.779111753320000489 ) ) ;
#22339=CARTESIAN_POINT ( 'NONE',  ( -14.41332696916413525, 9.018101604870871313, -9.380024591087739338 ) ) ;
#22340=CARTESIAN_POINT ( 'NONE',  ( -4.696142548075968648, 13.41911879355214410, 5.316338907189500418 ) ) ;
#22341=CARTESIAN_POINT ( 'NONE',  ( -19.73799724739764727, -5.961347995097865393, 8.625741937770200707 ) ) ;
#22348=CARTESIAN_POINT ( 'NONE',  ( -18.14837077250665942, -7.306469912381244214, -5.615206019344828547 ) ) ;
#22349=CARTESIAN_POINT ( 'NONE',  ( 24.47854514379999813, -6.961171424654001072, -6.740760433291000275 ) ) ;
#22351=CARTESIAN_POINT ( 'NONE',  ( 4.750000000000000000, 22.00000000000000000, 0.000000000000000000 ) ) ;
#22353=CARTESIAN_POINT ( 'NONE',  ( -23.40224104270576433, 2.202070123285927217, 10.35029114405029915 ) ) ;
#22356=CARTESIAN_POINT ( 'NONE',  ( 3.126566019963172405, 11.89425924942375090, 3.678199694141997877 ) ) ;
#22359=VECTOR ( 'NONE', #15340, 1000.000000000000114 ) ;
#22360=CARTESIAN_POINT ( 'NONE',  ( -2.274037557443177260, 11.70145862779804347, -4.252662107751031151 ) ) ;
#22361=ADVANCED_FACE ( 'NONE', ( #16487 ), #14215, .F. ) ;
#22367=AXIS2_PLACEMENT_3D ( 'NONE', #5143, #3665, #9350 ) ;
#22368=CARTESIAN_POINT ( 'NONE',  ( 13.74862658530999937, -9.135377135809001459, -4.430325866828999537 ) ) ;
#22371=CARTESIAN_POINT ( 'NONE',  ( 18.57801537305999773, 8.813863540509998984, -6.409915686984000160 ) ) ;
#22373=ORIENTED_EDGE ( 'NONE', *, *, #16778, .F. ) ;
#22375=CARTESIAN_POINT ( 'NONE',  ( 23.40574053114000108, -10.02401005856000005, -4.063832034710999963 ) ) ;
#22377=EDGE_CURVE ( 'NONE', #16006, #6468, #18238, .T. ) ;
#22380=CARTESIAN_POINT ( 'NONE',  ( 18.22028936713000036, -1.652712406954000013, 8.988165862088999702 ) ) ;
#22381=CARTESIAN_POINT ( 'NONE',  ( 24.50000000000000000, 8.054858440593999802, 5.882793087032000656 ) ) ;
#22382=CARTESIAN_POINT ( 'NONE',  ( 4.796469116184001180, 12.40727786077000161, 0.6646592000246001053 ) ) ;
#22384=CARTESIAN_POINT ( 'NONE',  ( -21.76857732275000146, 2.577874773493999516, 10.79524278768000123 ) ) ;
#22386=B_SPLINE_CURVE_WITH_KNOTS ( 'NONE', 3,
 ( #8448, #3917, #5845, #11425, #14916, #18798, #18685, #4148, #15155, #22549 ),
 .UNSPECIFIED., .F., .F.,
 ( 4, 2, 2, 2, 4 ),
 ( 0.000000000000000000, 0.2500000000000000000, 0.5000000000000000000, 0.7500000000000000000, 1.000000000000000000 ),
 .UNSPECIFIED. ) ;
#22388=AXIS2_PLACEMENT_3D ( 'NONE', #15559, #15803, #13746 ) ;
#22389=ORIENTED_EDGE ( 'NONE', *, *, #16712, .T. ) ;
#22391=CARTESIAN_POINT ( 'NONE',  ( 5.818048057449997756, 13.71143573768000223, 3.214928120249999299 ) ) ;
#22394=CARTESIAN_POINT ( 'NONE',  ( 15.90028936713000185, 9.079314476020000413, 0.000000000000000000 ) ) ;
#22399=CARTESIAN_POINT ( 'NONE',  ( -16.04262945707999677, 5.313593037366000082, 9.424424275870000756 ) ) ;
#22401=DIRECTION ( 'NONE',  ( -1.000000000000000000, 0.000000000000000000, 0.000000000000000000 ) ) ;
#22402=CONICAL_SURFACE ( 'NONE', #16219, 7.249999994591000529, 0.7853981633972997312 ) ;
#22403=EDGE_CURVE ( 'NONE', #9506, #9908, #10349, .T. ) ;
#22404=CARTESIAN_POINT ( 'NONE',  ( -14.47158022755693985, -2.069973096218738373, 12.49996948346097092 ) ) ;
#22406=CARTESIAN_POINT ( 'NONE',  ( -10.53831236658635007, 15.50609459400975609, -1.406661532941654080 ) ) ;
#22408=CARTESIAN_POINT ( 'NONE',  ( 14.37355788048617100, -3.089454521824534616, -9.852699315173421013 ) ) ;
#22410=CARTESIAN_POINT ( 'NONE',  ( 21.66593149462999790, -1.098770618442999947, -11.18333031146000067 ) ) ;
#22413=CARTESIAN_POINT ( 'NONE',  ( 14.08726172903277707, 4.895756663341041204, 7.589951152256699807 ) ) ;
#22414=ADVANCED_FACE ( 'NONE', ( #17243 ), #12286, .T. ) ;
#22415=CARTESIAN_POINT ( 'NONE',  ( 17.87679683445078638, -0.5884589777194313420, -10.44048563999592538 ) ) ;
#22417=CARTESIAN_POINT ( 'NONE',  ( 11.48696334737753055, 12.46086172548929838, -3.416997251963662219 ) ) ;
#22419=CARTESIAN_POINT ( 'NONE',  ( 13.50000000000000000, 0.000000000000000000, 0.000000000000000000 ) ) ;
#22423=ADVANCED_FACE ( 'NONE', ( #19310, #2964 ), #17368, .T. ) ;
#22426=CARTESIAN_POINT ( 'NONE',  ( 17.15176585740999826, 0.2857122287928000048, 11.08459265502000157 ) ) ;
#22429=ORIENTED_EDGE ( 'NONE', *, *, #14246, .T. ) ;
#22430=ORIENTED_EDGE ( 'NONE', *, *, #21571, .F. ) ;
#22431=CARTESIAN_POINT ( 'NONE',  ( -9.683372211694999621, -6.488719643906999401, -14.15222824137000046 ) ) ;
#22433=CARTESIAN_POINT ( 'NONE',  ( 18.05162270046333717, 3.606460571753791644, 8.497838180424565735 ) ) ;
#22434=VERTEX_POINT ( 'NONE', #643 ) ;
#22435=CARTESIAN_POINT ( 'NONE',  ( -14.49863740983932914, 10.56606202786612059, 6.698971014615676900 ) ) ;
#22436=CARTESIAN_POINT ( 'NONE',  ( 19.79377223792668161, 3.114699025246350672, -10.03687850954299243 ) ) ;
#22438=CARTESIAN_POINT ( 'NONE',  ( 15.75498143486384706, -10.05429136305618165, 2.469775658380014782 ) ) ;
#22439=CARTESIAN_POINT ( 'NONE',  ( -18.23212756329999706, 9.685834697697000450, 5.436217751806999843 ) ) ;
#22441=CARTESIAN_POINT ( 'NONE',  ( -18.92721240987999920, -2.665110294750000275, -11.12003873501999962 ) ) ;
#22443=ORIENTED_EDGE ( 'NONE', *, *, #14408, .F. ) ;
#22445=CARTESIAN_POINT ( 'NONE',  ( -24.50000000000000000, -3.090136434824279466, -10.17978739575026381 ) ) ;
#22446=CARTESIAN_POINT ( 'NONE',  ( 4.649999999999999467, 20.10000000000000142, -5.428584221033999407E-09 ) ) ;
#22449=CARTESIAN_POINT ( 'NONE',  ( -4.810176010396001622, 16.11838285530999926, 3.920675986495997911 ) ) ;
#22452=DIRECTION ( 'NONE',  ( 0.000000000000000000, -0.8660254037844288266, 0.5000000000000169864 ) ) ;
#22453=CARTESIAN_POINT ( 'NONE',  ( 11.31918875731000007, -8.923818741964000267, -0.1967739533420000131 ) ) ;
#22455=FACE_OUTER_BOUND ( 'NONE', #4937, .T. ) ;
#22458=DIRECTION ( 'NONE',  ( 0.000000000000000000, 1.000000000000000000, 0.000000000000000000 ) ) ;
#22460=CARTESIAN_POINT ( 'NONE',  ( -1.915921331177998788, 11.82052783618998681, 4.443859913084001967 ) ) ;
#22461=CIRCLE ( 'NONE', #17050, 12.44999999999999929 ) ;
#22462=CARTESIAN_POINT ( 'NONE',  ( 12.00000000000000000, 0.4049267614696120399, -9.310983403904009137 ) ) ;
#22464=CARTESIAN_POINT ( 'NONE',  ( -5.062275720949998004, 15.74663350384999028, -2.895383246133002242 ) ) ;
#22466=CARTESIAN_POINT ( 'NONE',  ( 5.205597908719371780, 13.92591030125720231, -4.046157760719942154 ) ) ;
#22470=CARTESIAN_POINT ( 'NONE',  ( -17.35474577250666783, 8.879308410214960645, 2.386378174953934561 ) ) ;
#22472=CARTESIAN_POINT ( 'NONE',  ( 4.335853037485340344, 13.43036814054341122, -5.287594306914102482 ) ) ;
#22474=CARTESIAN_POINT ( 'NONE',  ( -21.09947279093694661, -10.48387386659816656, 0.9232800561193126310 ) ) ;
#22476=CARTESIAN_POINT ( 'NONE',  ( 12.50000000000000000, 13.93375672974000068, 0.000000000000000000 ) ) ;
#22478=CARTESIAN_POINT ( 'NONE',  ( -17.74018339386138265, -5.574914795658462374, 8.993144632062060495 ) ) ;
#22481=ORIENTED_EDGE ( 'NONE', *, *, #1069, .F. ) ;
#22482=EDGE_CURVE ( 'NONE', #16467, #6064, #21123, .T. ) ;
#22483=DIRECTION ( 'NONE',  ( -0.9996708941621513800, 0.02565352539212875996, -2.108144717745900797E-14 ) ) ;
#22484=CARTESIAN_POINT ( 'NONE',  ( 15.83268908530999930, -1.865934471007999917, -10.03576702404999921 ) ) ;
#22486=DIRECTION ( 'NONE',  ( 0.9996708941621511579, -0.02565352539213875543, 2.155425419848895702E-14 ) ) ;
#22487=CARTESIAN_POINT ( 'NONE',  ( 15.73426537305999950, -5.346007409990000347, 9.405856311918000756 ) ) ;
#22489=DIRECTION ( 'NONE',  ( -2.979866527141999703E-10, 1.005728194337683875E-23, 1.000000000000000000 ) ) ;
#22490=CARTESIAN_POINT ( 'NONE',  ( 24.73933971626999906, 6.229381467500999747, 8.232746011927000396 ) ) ;
#22491=TOROIDAL_SURFACE ( 'NONE', #15522, 14.44999999999999929, 2.000000000000000000 ) ;
#22492=CARTESIAN_POINT ( 'NONE',  ( 23.99895687519700616, 13.93375672973999890, 0.3849913041842834560 ) ) ;
#22494=CARTESIAN_POINT ( 'NONE',  ( 12.15527934810000055, -8.048449879512999061, -4.237977357754999730 ) ) ;
#22496=CARTESIAN_POINT ( 'NONE',  ( -3.969064160570000777, 12.18274565056999847, 2.680101174410998155 ) ) ;
#22498=CARTESIAN_POINT ( 'NONE',  ( -24.27484550945999686, 5.445138765948000170, -9.749175221210998998 ) ) ;
#22499=ORIENTED_EDGE ( 'NONE', *, *, #7717, .T. ) ;
#22500=CARTESIAN_POINT ( 'NONE',  ( -18.94247183136150525, -9.023122249501957626, 3.215535042062015680 ) ) ;
#22502=ORIENTED_EDGE ( 'NONE', *, *, #7163, .F. ) ;
#22503=CARTESIAN_POINT ( 'NONE',  ( 15.48458103379664941, 1.186956113863779416, -9.068646580869270224 ) ) ;
#22504=CARTESIAN_POINT ( 'NONE',  ( 6.633606867079997471, 13.50105012196000231, 0.4122077612039000694 ) ) ;
#22506=DIRECTION ( 'NONE',  ( 0.000000000000000000, 1.000000000000000000, 0.000000000000000000 ) ) ;
#22507=DIRECTION ( 'NONE',  ( 0.000000000000000000, 0.000000000000000000, 1.000000000000000000 ) ) ;
#22508=CARTESIAN_POINT ( 'NONE',  ( 17.06568924931000097, -1.008082813539000089, 10.70191082552000061 ) ) ;
#22509=EDGE_CURVE ( 'NONE', #9620, #5222, #18462, .T. ) ;
#22511=CARTESIAN_POINT ( 'NONE',  ( -15.23010806520000138, -8.044096712135001326, -7.201187562783000651 ) ) ;
#22514=CARTESIAN_POINT ( 'NONE',  ( -14.25243324638999809, -6.216878364870000340, 12.50000000000000000 ) ) ;
#22515=ORIENTED_EDGE ( 'NONE', *, *, #20442, .T. ) ;
#22518=CARTESIAN_POINT ( 'NONE',  ( 13.84684978381418041, -8.707682685158594893, 5.508672335018611754 ) ) ;
#22519=DIRECTION ( 'NONE',  ( 1.000000000000000000, 0.000000000000000000, 0.000000000000000000 ) ) ;
#22521=SHAPE_REPRESENTATION ( 'MAS-673 Main Body', ( #4390 ), #7088 ) ;
#22524=CARTESIAN_POINT ( 'NONE',  ( 11.22285964975863237, -2.000465806332258456, 12.49999014999633573 ) ) ;
#22526=CARTESIAN_POINT ( 'NONE',  ( -6.399639659233631761, 15.54095944911451888, 1.345865623129033795 ) ) ;
#22529=AXIS2_PLACEMENT_3D ( 'NONE', #2173, #22401, #22055 ) ;
#22530=CARTESIAN_POINT ( 'NONE',  ( 12.00000000000000000, -7.500000000000000000, 0.000000000000000000 ) ) ;
#22534=CARTESIAN_POINT ( 'NONE',  ( 24.32802197706126179, 9.050607035110887821, 9.323888775846091548 ) ) ;
#22536=ORIENTED_EDGE ( 'NONE', *, *, #21523, .F. ) ;
#22537=CARTESIAN_POINT ( 'NONE',  ( 15.16680598110999867, 6.392462273583999988, 8.993531204449999095 ) ) ;
#22541=ORIENTED_EDGE ( 'NONE', *, *, #1797, .T. ) ;
#22543=CARTESIAN_POINT ( 'NONE',  ( -24.41904027018788526, 9.801083277732518084, -8.024000955001664437 ) ) ;
#22544=CARTESIAN_POINT ( 'NONE',  ( 12.52688711657000020, 7.716878364870000340, 11.63397459621999985 ) ) ;
#22546=CARTESIAN_POINT ( 'NONE',  ( -23.86847083084956722, -7.985699633923855068, -11.16836250006485010 ) ) ;
#22548=CARTESIAN_POINT ( 'NONE',  ( -22.68728007704000049, 0.8272991724924000367, 9.664718538323999297 ) ) ;
#22549=CARTESIAN_POINT ( 'NONE',  ( 19.75000000000000000, -1.659811535170000019, 9.026773995975998943 ) ) ;
#22551=CARTESIAN_POINT ( 'NONE',  ( 6.229047772746363343, 13.74469652872262415, 1.373019302850102985 ) ) ;
#22552=CARTESIAN_POINT ( 'NONE',  ( 15.66899429073552774, -8.904753597334295279, 5.276170738670112215 ) ) ;
#22553=CARTESIAN_POINT ( 'NONE',  ( -15.55621955597000117, -10.90559009245999889, 1.677215861521999862 ) ) ;
#22555=EDGE_CURVE ( 'NONE', #17452, #10425, #20217, .T. ) ;
#22557=CARTESIAN_POINT ( 'NONE',  ( -18.27706328473999875, 10.02730951802000092, -4.225925492466999778 ) ) ;
#22562=DIRECTION ( 'NONE',  ( -4.066191827689660386E-11, -1.000000000000000000, 0.000000000000000000 ) ) ;
#22563=ORIENTED_EDGE ( 'NONE', *, *, #8627, .F. ) ;
#22565=CARTESIAN_POINT ( 'NONE',  ( -12.50000000000000000, 6.606768802097000126, -6.099810110451000966 ) ) ;
#22566=CARTESIAN_POINT ( 'NONE',  ( -23.50032910583999879, 3.801543240379000377, -8.459419100777001432 ) ) ;
#22567=EDGE_CURVE ( 'NONE', #2558, #21421, #14741, .T. ) ;
#22568=CARTESIAN_POINT ( 'NONE',  ( 14.79262625730999936, -7.984278194804999451, 4.494107504349000415 ) ) ;
#22569=ADVANCED_FACE ( 'NONE', ( #14344 ), #14223, .T. ) ;
#22574=ORIENTED_EDGE ( 'NONE', *, *, #1873, .F. ) ;
#22575=CARTESIAN_POINT ( 'NONE',  ( -16.06392920454665685, 7.937099294806711391, -4.574512672171699990 ) ) ;
#22577=CARTESIAN_POINT ( 'NONE',  ( -4.760513096662999821, 12.62269162836001435, 0.7405673987019998350 ) ) ;
#22578=CARTESIAN_POINT ( 'NONE',  ( -13.99999999999999467, -5.371542361985429892, 8.544981476852292701 ) ) ;
#22579=CARTESIAN_POINT ( 'NONE',  ( 12.00000000000000178, 2.542583502621673208, -8.834538564857254528 ) ) ;
#22581=FACE_OUTER_BOUND ( 'NONE', #4295, .T. ) ;
#22584=CARTESIAN_POINT ( 'NONE',  ( 6.243179582884000212, 13.63341776306000064, 1.952383140737000033 ) ) ;
#22589=CARTESIAN_POINT ( 'NONE',  ( -11.04281598264000053, 15.31903517202000131, -1.878299281600999793 ) ) ;
#22590=CARTESIAN_POINT ( 'NONE',  ( -0.5127195001119165818, 12.81264167692682143, -6.646073094678516924 ) ) ;
#22592=CARTESIAN_POINT ( 'NONE',  ( -21.26013104105991758, -8.417803719024050224, 6.324359816153899416 ) ) ;
#22597=CARTESIAN_POINT ( 'NONE',  ( -18.96827783194638073, -5.556685674060065416, -8.875571351387176122 ) ) ;
#22598=CARTESIAN_POINT ( 'NONE',  ( 24.36060779997411530, 9.641839768656376819, -1.940354640108606032 ) ) ;
#22603=CARTESIAN_POINT ( 'NONE',  ( 13.00000000000000000, -8.415881316778998311, -3.203269825092000200 ) ) ;
#22604=CARTESIAN_POINT ( 'NONE',  ( 14.10412674931000154, -7.190271978224999749, -7.885398697387000944 ) ) ;
#22605=CARTESIAN_POINT ( 'NONE',  ( -15.15688235000000006, 6.080933706674000128, -9.559848708078998669 ) ) ;
#22606=DIRECTION ( 'NONE',  ( 0.9996848865506517967, 0.000000000000000000, 0.02510234256419879503 ) ) ;
#22607=CARTESIAN_POINT ( 'NONE',  ( 16.14051537306000128, -10.16182289531000116, -3.745982005662999992 ) ) ;
#22608=CARTESIAN_POINT ( 'NONE',  ( -12.41173981160000039, 6.613190111079999767, -13.46349570337000046 ) ) ;
#22609=CARTESIAN_POINT ( 'NONE',  ( 0.000000000000000000, 21.50000000000000000, 0.000000000000000000 ) ) ;
#22610=CARTESIAN_POINT ( 'NONE',  ( 23.94834967554000116, -9.057010814518001496, -3.671698204039999691 ) ) ;
#22612=ORIENTED_EDGE ( 'NONE', *, *, #19884, .T. ) ;
#22615=AXIS2_PLACEMENT_3D ( 'NONE', #12480, #1337, #10298 ) ;
#22616=CARTESIAN_POINT ( 'NONE',  ( -2.670595826634000414, 11.74590557449999828, 4.055288669775002575 ) ) ;
#22617=DIRECTION ( 'NONE',  ( -1.000000000000000000, 0.000000000000000000, 0.000000000000000000 ) ) ;
#22618=CARTESIAN_POINT ( 'NONE',  ( -22.62446300055000137, -5.956939041310000071, -9.392211964618999431 ) ) ;
#22621=ORIENTED_EDGE ( 'NONE', *, *, #12341, .F. ) ;
#22622=CARTESIAN_POINT ( 'NONE',  ( -19.55887123173999953, -9.833822427806001798, 3.504477313184999776 ) ) ;
#22625=CARTESIAN_POINT ( 'NONE',  ( 15.53006424931000140, -9.332187211223001100, 5.252733788881000621 ) ) ;
#22626=CARTESIAN_POINT ( 'NONE',  ( -14.62071702128999995, 10.29594144910999809, -3.192455093500000007 ) ) ;
#22627=CARTESIAN_POINT ( 'NONE',  ( 17.75418875731000057, 8.769310764750999354, 2.911614084577999861 ) ) ;
#22632=CARTESIAN_POINT ( 'NONE',  ( 13.85149880907578357, -8.793786893394734960, 5.371349140574870340 ) ) ;
#22633=CARTESIAN_POINT ( 'NONE',  ( -0.8938142071318000426, 12.69387875947998978, -7.039327871081002996 ) ) ;
#22636=CARTESIAN_POINT ( 'NONE',  ( 12.28022044530440660, 5.662962823301384674, 12.50000000000071410 ) ) ;
#22637=CARTESIAN_POINT ( 'NONE',  ( 18.29495480302612620, 10.29737567282159105, -1.861358213112139337 ) ) ;
#22638=CARTESIAN_POINT ( 'NONE',  ( 24.50000000000000000, -8.246372141814999779, 6.625187740483999832 ) ) ;
#22640=ADVANCED_FACE ( 'NONE', ( #9126 ), #23409, .F. ) ;
#22642=ORIENTED_EDGE ( 'NONE', *, *, #646, .F. ) ;
#22646=CARTESIAN_POINT ( 'NONE',  ( -5.534675601318385318, 16.14771134836236399, -2.628939291504586162 ) ) ;
#22647=DIRECTION ( 'NONE',  ( 1.000000000000000000, 0.000000000000000000, 0.000000000000000000 ) ) ;
#22650=ORIENTED_EDGE ( 'NONE', *, *, #5719, .F. ) ;
#22651=CARTESIAN_POINT ( 'NONE',  ( 6.141065067267645894, 14.19649444987426179, -0.02421318643596113290 ) ) ;
#22652=CARTESIAN_POINT ( 'NONE',  ( -6.086257062671249329, 16.07074762286712399, 1.021981042907482040 ) ) ;
#22654=EDGE_CURVE ( 'NONE', #8639, #14252, #4027, .T. ) ;
#22655=ORIENTED_EDGE ( 'NONE', *, *, #2067, .F. ) ;
#22656=ORIENTED_EDGE ( 'NONE', *, *, #22219, .F. ) ;
#22657=CARTESIAN_POINT ( 'NONE',  ( -14.00000000000000000, -3.369147568425823636, -9.111598281861018833 ) ) ;
#22658=CARTESIAN_POINT ( 'NONE',  ( -12.13448613877000071, 13.17911648328999874, -7.610033336417999728 ) ) ;
#22662=CARTESIAN_POINT ( 'NONE',  ( -23.97728971651479313, 8.249343195704353704, 10.71120260265216118 ) ) ;
#22663=AXIS2_PLACEMENT_3D ( 'NONE', #14274, #10162, #2897 ) ;
#22665=CARTESIAN_POINT ( 'NONE',  ( 15.54280282966749915, -5.820625934528824708, 8.599006677133495202 ) ) ;
#22667=CARTESIAN_POINT ( 'NONE',  ( -15.99608434662999912, -10.91749873145000116, 1.679048479876000144 ) ) ;
#22669=CARTESIAN_POINT ( 'NONE',  ( -17.50529997408999705, -11.39253675243999986, 0.2566028257674999868 ) ) ;
#22672=ORIENTED_EDGE ( 'NONE', *, *, #16778, .T. ) ;
#22678=CARTESIAN_POINT ( 'NONE',  ( -5.606396321587005183, 15.09360509207000867, 2.791161259578001541 ) ) ;
#22680=CARTESIAN_POINT ( 'NONE',  ( -14.00000000000000000, -8.319952449050001420, 6.066771132503999020 ) ) ;
#22682=CARTESIAN_POINT ( 'NONE',  ( 15.69656392131000011, 1.888996749216000026, -9.509257592937000680 ) ) ;
#22684=DIRECTION ( 'NONE',  ( 0.000000000000000000, 1.000000000000000000, 0.000000000000000000 ) ) ;
#22685=CARTESIAN_POINT ( 'NONE',  ( 24.32802197706137903, -12.60002805950083982, 3.176111224150924173 ) ) ;
#22688=CARTESIAN_POINT ( 'NONE',  ( 11.92450592357447903, 8.469720391600080944, 10.33010329014251916 ) ) ;
#22689=CARTESIAN_POINT ( 'NONE',  ( 4.347703729989003563, 12.46533150479998930, 1.901662359772999578 ) ) ;
#22690=CARTESIAN_POINT ( 'NONE',  ( -14.00000000000000000, -1.433536925117362859, 9.728352550975314372 ) ) ;
#22691=CARTESIAN_POINT ( 'NONE',  ( 18.05533209391456495, -1.235616904331040766, -10.33763051555462198 ) ) ;
#22693=LINE ( 'NONE', #13495, #12938 ) ;
#22694=DIRECTION ( 'NONE',  ( 0.9996708941621511579, -0.02565352539213875543, 0.000000000000000000 ) ) ;
#22696=CARTESIAN_POINT ( 'NONE',  ( 6.162290176374000339, 13.65474020847999981, 2.204514988415999799 ) ) ;
#22699=CARTESIAN_POINT ( 'NONE',  ( -14.25243324638999809, -13.93375672974000068, 0.8660254037843999608 ) ) ;
#22705=CARTESIAN_POINT ( 'NONE',  ( -0.5951135560396972890, 12.81575860760598395, -6.640039254981911832 ) ) ;
#22707=CARTESIAN_POINT ( 'NONE',  ( -20.75137991567049411, -4.596998218242912770, -9.457217556533679570 ) ) ;
#22711=ORIENTED_EDGE ( 'NONE', *, *, #6245, .F. ) ;
#22712=CARTESIAN_POINT ( 'NONE',  ( -18.13094071507020288, 7.623672199478383149, 7.352634401449745560 ) ) ;
#22717=ORIENTED_EDGE ( 'NONE', *, *, #6601, .T. ) ;
#22719=CARTESIAN_POINT ( 'NONE',  ( -18.76627150799833643, -8.263409740610351051, 4.078035658106594852 ) ) ;
#22720=CARTESIAN_POINT ( 'NONE',  ( 16.51725174930999884, 10.44001970777000032, -2.498676648948999990 ) ) ;
#22721=CARTESIAN_POINT ( 'NONE',  ( -13.19328898630000069, 9.449229977676001369, -4.943757532052999615 ) ) ;
#22722=CARTESIAN_POINT ( 'NONE',  ( 0.000000000000000000, 21.50000000000000000, 0.000000000000000000 ) ) ;
#22723=CARTESIAN_POINT ( 'NONE',  ( 16.95301537306000128, 10.84929791343999916, 0.2805791889531000227 ) ) ;
#22724=CARTESIAN_POINT ( 'NONE',  ( 8.124934037954998800, -10.59999999999999964, 0.000000000000000000 ) ) ;
#22726=DIRECTION ( 'NONE',  ( -0.000000000000000000, 1.000000000000000000, 0.000000000000000000 ) ) ;
#22727=CARTESIAN_POINT ( 'NONE',  ( 22.43770138826000249, 7.394962502173999752, -7.113329243426999682 ) ) ;
#22729=ORIENTED_EDGE ( 'NONE', *, *, #3738, .T. ) ;
#22730=CARTESIAN_POINT ( 'NONE',  ( 11.87172645921999958, -2.663994189788999822, -8.934245366879000727 ) ) ;
#22732=CARTESIAN_POINT ( 'NONE',  ( 3.971078888290999309, 12.18367478550000982, 2.673022683980000647 ) ) ;
#22734=CONICAL_SURFACE ( 'NONE', #21215, 13.23032192316000000, 1.093540295016705466 ) ;
#22735=CARTESIAN_POINT ( 'NONE',  ( -21.12070208853000253, -11.05482043179000051, 0.7640197540441000523 ) ) ;
#22738=VECTOR ( 'NONE', #3650, 1000.000000000000000 ) ;
#22739=ORIENTED_EDGE ( 'NONE', *, *, #12210, .F. ) ;
#22742=CARTESIAN_POINT ( 'NONE',  ( 3.799035759646001154, 13.17963623137001505, 5.991547988457999629 ) ) ;
#22744=CARTESIAN_POINT ( 'NONE',  ( -12.25000000000000000, 15.45000000000000107, 0.000000000000000000 ) ) ;
#22745=CARTESIAN_POINT ( 'NONE',  ( 15.96881424931000026, -5.728615299830999597, -9.061514726575000012 ) ) ;
#22746=CARTESIAN_POINT ( 'NONE',  ( -17.66767224083000087, -1.527991571549000005, 10.75645198264999891 ) ) ;
#22747=CARTESIAN_POINT ( 'NONE',  ( 17.42512625730999787, 6.303186173173999762, -6.744507379544999459 ) ) ;
#22748=CARTESIAN_POINT ( 'NONE',  ( 24.36414987671881960, 12.39811243366166416, -3.525839346946420427 ) ) ;
#22749=VECTOR ( 'NONE', #15369, 1000.000000000000000 ) ;
#22751=CARTESIAN_POINT ( 'NONE',  ( 12.51793201921000076, -13.93375672974000068, -0.7216659839314999436 ) ) ;
#22753=CARTESIAN_POINT ( 'NONE',  ( 14.06984511579193331, -10.11168233347247813, -2.157631914311957999 ) ) ;
#22754=AXIS2_PLACEMENT_3D ( 'NONE', #4174, #15296, #6345 ) ;
#22755=CARTESIAN_POINT ( 'NONE',  ( 2.838808265031001810, 14.18773367037002409, -5.481123045573999875 ) ) ;
#22756=DIRECTION ( 'NONE',  ( 2.979867880226000256E-10, 9.527955641186100052E-24, -1.000000000000000000 ) ) ;
#22758=CARTESIAN_POINT ( 'NONE',  ( 11.18529249867571984, -1.746922494864825426, 12.50002083036580913 ) ) ;
#22759=CARTESIAN_POINT ( 'NONE',  ( 17.73741084492538889, -5.461382820680055872, -9.083679806854396688 ) ) ;
#22761=AXIS2_PLACEMENT_3D ( 'NONE', #6948, #21730, #12524 ) ;
#22762=CARTESIAN_POINT ( 'NONE',  ( 0.000000000000000000, -7.216878364870000340, 12.50000000000000000 ) ) ;
#22763=CARTESIAN_POINT ( 'NONE',  ( -6.046837210729000489, 16.30334039894000142, -1.000000000000000000 ) ) ;
#22764=VERTEX_POINT ( 'NONE', #22308 ) ;
#22769=CARTESIAN_POINT ( 'NONE',  ( -2.351879151723880845, 11.71687587877330117, 4.209509496448244015 ) ) ;
#22770=CARTESIAN_POINT ( 'NONE',  ( 4.749999673578000348, 12.55004296393999930, -4.341645649670000483E-06 ) ) ;
#22771=CARTESIAN_POINT ( 'NONE',  ( 24.12867869089190265, -9.461899957204449763, 0.6956614285005767728 ) ) ;
#22772=CARTESIAN_POINT ( 'NONE',  ( -20.51955273722667172, -2.691069519324763348, 8.860573964823370119 ) ) ;
#22773=CARTESIAN_POINT ( 'NONE',  ( 23.99062354302999722, -6.216878364870000340, -12.50000000000000000 ) ) ;
#22774=VERTEX_POINT ( 'NONE', #9596 ) ;
#22775=VERTEX_POINT ( 'NONE', #13111 ) ;
#22776=DIRECTION ( 'NONE',  ( -0.9999999999810907925, 6.097499773276291543E-06, 7.994200222768927623E-07 ) ) ;
#22779=CARTESIAN_POINT ( 'NONE',  ( -14.25243324638999809, -7.716878364870000340, -11.63397459621999985 ) ) ;
#22782=CARTESIAN_POINT ( 'NONE',  ( -21.14497945657000244, 8.262325765017999757, 5.001268951993999679 ) ) ;
#22784=CARTESIAN_POINT ( 'NONE',  ( 6.157064176825728374, 14.08830590709009556, 0.3628796317935392146 ) ) ;
#22785=CARTESIAN_POINT ( 'NONE',  ( 15.28176760385781385, 3.108477508404123846, 9.870308429438537701 ) ) ;
#22786=CARTESIAN_POINT ( 'NONE',  ( -17.98338081197000093, -8.100370408748000628, 7.589501626130000567 ) ) ;
#22787=CIRCLE ( 'NONE', #11211, 9.030549305585997999 ) ;
#22789=CARTESIAN_POINT ( 'NONE',  ( -21.46225067249296359, -8.457439661898087380, 6.476282215921202123 ) ) ;
#22790=AXIS2_PLACEMENT_3D ( 'NONE', #17903, #21658, #12454 ) ;
#22791=CARTESIAN_POINT ( 'NONE',  ( -16.24575980504999606, 10.15426072268999924, 3.750674035441000420 ) ) ;
#22794=ORIENTED_EDGE ( 'NONE', *, *, #8672, .T. ) ;
#22796=CARTESIAN_POINT ( 'NONE',  ( -18.63025570457361013, 10.07612922007779765, -2.841683973627437076 ) ) ;
#22798=CARTESIAN_POINT ( 'NONE',  ( 5.975665869958996623, 14.53417513656000182, -1.387968629032001910 ) ) ;
#22800=CARTESIAN_POINT ( 'NONE',  ( -20.44776253787999920, -9.196011600180998613, 0.000000000000000000 ) ) ;
#22801=CARTESIAN_POINT ( 'NONE',  ( 15.91593892131000132, 7.924234377949000319, -5.595770532261999719 ) ) ;
#22803=DIRECTION ( 'NONE',  ( 1.000000000000000000, 0.000000000000000000, 0.000000000000000000 ) ) ;
#22804=DIRECTION ( 'NONE',  ( -0.000000000000000000, 1.000000000000000000, 0.000000000000000000 ) ) ;
#22805=CARTESIAN_POINT ( 'NONE',  ( 24.50000000000000000, -10.82531754731000007, 6.250000000000000000 ) ) ;
#22810=CARTESIAN_POINT ( 'NONE',  ( 24.08830182848186041, 5.395025589383775078, 9.150520802871518811 ) ) ;
#22812=CARTESIAN_POINT ( 'NONE',  ( 18.19747459623542341, 3.794755501146056975, -9.726389436706863734 ) ) ;
#22813=AXIS2_PLACEMENT_3D ( 'NONE', #3830, #7939, #417 ) ;
#22814=CARTESIAN_POINT ( 'NONE',  ( 12.00000000000000000, -9.140869530236654938, -4.136866240621976054 ) ) ;
#22816=CARTESIAN_POINT ( 'NONE',  ( -3.412554491691996539, 13.99161680779000605, -5.089445285121002804 ) ) ;
#22824=CARTESIAN_POINT ( 'NONE',  ( 20.66608820303999750, -8.164859526374000254, 7.177460020925999551 ) ) ;
#22825=CARTESIAN_POINT ( 'NONE',  ( -3.554379017154496445, 13.22735737994497462, -5.777226003025122125 ) ) ;
#22827=CARTESIAN_POINT ( 'NONE',  ( -19.62677216480515696, -3.112713671263979354, 10.01251316358262144 ) ) ;
#22831=EDGE_CURVE ( 'NONE', #10425, #5775, #3586, .T. ) ;
#22832=CARTESIAN_POINT ( 'NONE',  ( -17.12613617482062267, -4.646914316943434820, -9.333643767870253072 ) ) ;
#22834=CARTESIAN_POINT ( 'NONE',  ( 0.000000000000000000, 7.216878364870000340, -12.50000000000000000 ) ) ;
#22839=DIRECTION ( 'NONE',  ( 0.000000000000000000, 0.9512662730843030046, -0.3083706822840010520 ) ) ;
#22840=CARTESIAN_POINT ( 'NONE',  ( 17.72381424930999927, -7.480404092888999656, -7.743571870822999692 ) ) ;
#22841=CARTESIAN_POINT ( 'NONE',  ( -14.00000000000000000, 6.995278287856000254, -5.711120943918999160 ) ) ;
#22842=CARTESIAN_POINT ( 'NONE',  ( -17.79757687361000151, -8.527194750238999532, 7.571551323727999439 ) ) ;
#22843=CARTESIAN_POINT ( 'NONE',  ( 23.92506969171387965, -8.172088213226873066, -4.569912402413578434 ) ) ;
#22844=CARTESIAN_POINT ( 'NONE',  ( 18.84931994526000310, 8.383432096882000195, -6.096962826690000448 ) ) ;
#22846=CARTESIAN_POINT ( 'NONE',  ( -12.06624327026009347, 1.368548241523999952E-14, 0.000000000000000000 ) ) ;
#22847=CARTESIAN_POINT ( 'NONE',  ( 21.02130857102000050, 8.371468613062001296, 5.866070922022999845 ) ) ;
#22853=B_SPLINE_CURVE_WITH_KNOTS ( 'NONE', 3,
 ( #12147, #14073, #21468, #19409, #19892, #15757, #19657, #2823, #10456, #1485, #23147, #3308, #6568, #13952, #17845, #21346, #23385, #12396 ),
 .UNSPECIFIED., .F., .F.,
 ( 4, 2, 2, 2, 2, 2, 2, 2, 4 ),
 ( 0.000000000000000000, 0.1250000000000000000, 0.2500000000000000000, 0.3750000000000000000, 0.5000000000000000000, 0.6250000000000000000, 0.7500000000000000000, 0.8750000000000000000, 1.000000000000000000 ),
 .UNSPECIFIED. ) ;
#22854=CARTESIAN_POINT ( 'NONE',  ( 3.310881862312000656, 11.97843584064001199, 3.462059838974000936 ) ) ;
#22856=CARTESIAN_POINT ( 'NONE',  ( -20.28527935963000317, 10.50778539144999968, -3.446350770996999824 ) ) ;
#22857=ORIENTED_EDGE ( 'NONE', *, *, #3336, .F. ) ;
#22860=CARTESIAN_POINT ( 'NONE',  ( 15.25783103379665384, -5.569620820083297730, -7.247153067674876326 ) ) ;
#22862=CARTESIAN_POINT ( 'NONE',  ( -1.703378280910000875, 12.85045892059999595, 6.244730413338999142 ) ) ;
#22864=CARTESIAN_POINT ( 'NONE',  ( -14.25546320177999959, 6.466449120341000167, 12.35591025714999880 ) ) ;
#22865=EDGE_CURVE ( 'NONE', #21237, #11791, #15944, .T. ) ;
#22867=CARTESIAN_POINT ( 'NONE',  ( -15.02697771723000031, -1.474210749020000044, -10.68967233462999999 ) ) ;
#22868=CARTESIAN_POINT ( 'NONE',  ( 17.53481375730999758, 8.357543471651000644, -3.927243979254000372 ) ) ;
#22871=CARTESIAN_POINT ( 'NONE',  ( 19.70552847921732464, -0.05221305801487967357, -10.50537839887272185 ) ) ;
#22873=CARTESIAN_POINT ( 'NONE',  ( 13.52121136864142414, 1.289066941492836849, 10.24442406412049067 ) ) ;
#22875=CARTESIAN_POINT ( 'NONE',  ( 4.878371034287997787, 14.94155586047998874, -3.715635765802999035 ) ) ;
#22876=DIRECTION ( 'NONE',  ( 0.000000000000000000, -0.8660254037844288266, -0.5000000000000169864 ) ) ;
#22879=CARTESIAN_POINT ( 'NONE',  ( 14.70899999999999963, -9.048743642952000954, 0.000000000000000000 ) ) ;
#22880=ADVANCED_FACE ( 'NONE', ( #8017 ), #17466, .F. ) ;
#22881=DIRECTION ( 'NONE',  ( -0.000000000000000000, 0.6324223201336057754, 0.7746237854577066040 ) ) ;
#22886=CARTESIAN_POINT ( 'NONE',  ( 11.45478115326693747, -12.39608915220626528, 3.529209591781598654 ) ) ;
#22887=ORIENTED_EDGE ( 'NONE', *, *, #11575, .F. ) ;
#22888=CARTESIAN_POINT ( 'NONE',  ( 12.00000000000000000, -9.392874664203999302, -3.575135015595999999 ) ) ;
#22889=CARTESIAN_POINT ( 'NONE',  ( -2.884120348847549309, 11.83272722737032190, 3.874092213913487015 ) ) ;
#22891=CARTESIAN_POINT ( 'NONE',  ( -3.224906711384808666, 13.15387152289895134, 5.942239841201511830 ) ) ;
#22892=CIRCLE ( 'NONE', #3962, 10.69999999999999929 ) ;
#22893=CARTESIAN_POINT ( 'NONE',  ( 16.93748565861000088, 10.60378489164999927, 3.221716779813999842 ) ) ;
#22898=CARTESIAN_POINT ( 'NONE',  ( -14.00000000000000178, -7.049815569282562144, -6.985318574217756371 ) ) ;
#22902=CARTESIAN_POINT ( 'NONE',  ( -18.74584515806999718, -8.073393492905999835, 5.180320272283000627 ) ) ;
#22904=CARTESIAN_POINT ( 'NONE',  ( 6.225701887381084987, 13.76125012799850467, 1.306893872209164753 ) ) ;
#22905=CARTESIAN_POINT ( 'NONE',  ( 15.66748608625431416, -8.878148344715427243, 5.320606095657832491 ) ) ;
#22906=CARTESIAN_POINT ( 'NONE',  ( -18.88669738713000257, 8.214810501480998894, -7.502223699012001035 ) ) ;
#22907=CARTESIAN_POINT ( 'NONE',  ( 4.834779662050625149, 12.44818287292682335, -0.2493690240449278894 ) ) ;
#22908=CARTESIAN_POINT ( 'NONE',  ( -20.07255388211770963, 5.526680004444125771, 8.922835914469294138 ) ) ;
#22910=CARTESIAN_POINT ( 'NONE',  ( -14.86460545047999915, 10.81390249068999942, -3.353128725732000159 ) ) ;
#22914=CARTESIAN_POINT ( 'NONE',  ( -14.54983219195056243, 2.782516519562602930, 9.977023446843118037 ) ) ;
#22915=ORIENTED_EDGE ( 'NONE', *, *, #17321, .F. ) ;
#22917=CARTESIAN_POINT ( 'NONE',  ( 5.365624983119998248, 14.28158000389998783, -2.870197123060997502 ) ) ;
#22919=CARTESIAN_POINT ( 'NONE',  ( -20.06984587121332808, -2.404380842926237882, -8.947266942397744671 ) ) ;
#22920=CARTESIAN_POINT ( 'NONE',  ( 11.56500142131000075, -9.431037050546001055, -0.2079650321152999859 ) ) ;
#22923=FACE_OUTER_BOUND ( 'NONE', #7556, .T. ) ;
#22925=DIRECTION ( 'NONE',  ( -1.000000000000000000, 0.000000000000000000, 0.000000000000000000 ) ) ;
#22928=DIRECTION ( 'NONE',  ( -1.000000000000000000, 0.000000000000000000, 0.000000000000000000 ) ) ;
#22929=CARTESIAN_POINT ( 'NONE',  ( 11.78693030655652763, 8.669062849316338415, 9.984739426213851132 ) ) ;
#22932=CARTESIAN_POINT ( 'NONE',  ( 18.38725600494685963, 8.888177610145580942, -5.441499180344855802 ) ) ;
#22933=CARTESIAN_POINT ( 'NONE',  ( -14.00000000000000000, 1.396097351027999937E-14, 0.000000000000000000 ) ) ;
#22934=B_SPLINE_CURVE_WITH_KNOTS ( 'NONE', 3,
 ( #4089, #13525, #10028, #22843, #9659, #2505 ),
 .UNSPECIFIED., .F., .F.,
 ( 4, 2, 4 ),
 ( 0.8039802372034564604, 0.9019901186017282857, 1.000000000000000000 ),
 .UNSPECIFIED. ) ;
#22935=CARTESIAN_POINT ( 'NONE',  ( -14.39391672138606637, 12.88860090843610351, -2.676267392864989603 ) ) ;
#22936=CARTESIAN_POINT ( 'NONE',  ( 19.53721867119999800, -1.916595458125999851, -11.01322041192999990 ) ) ;
#22937=CARTESIAN_POINT ( 'NONE',  ( -11.00000000000000000, 10.59999999999999964, 0.000000000000000000 ) ) ;
#22938=CARTESIAN_POINT ( 'NONE',  ( -3.755314868451799626, 14.14753470886829234, -4.866744050934065591 ) ) ;
#22939=CARTESIAN_POINT ( 'NONE',  ( -6.099196000000000062, 16.31160201366999729, -2.000000000000000000 ) ) ;
#22942=CARTESIAN_POINT ( 'NONE',  ( 20.61352647260000026, -10.32027106859000121, 0.5347350817453000449 ) ) ;
#22943=CARTESIAN_POINT ( 'NONE',  ( -3.062204858405229047, 13.12005258919790407, -6.016671387275827954 ) ) ;
#22946=CARTESIAN_POINT ( 'NONE',  ( -19.46611391468236008, -7.928063235344735560, 6.854333141353487591 ) ) ;
#22949=CARTESIAN_POINT ( 'NONE',  ( 0.3815877974581001753, 11.45498001497000118, -4.936402010209000046 ) ) ;
#22951=CARTESIAN_POINT ( 'NONE',  ( -16.84702380252937459, 5.079908938365492510, -9.198943836403035590 ) ) ;
#22958=CARTESIAN_POINT ( 'NONE',  ( 13.22662674931000204, 6.334720884006999952, 8.559150566242998082 ) ) ;
#22959=CIRCLE ( 'NONE', #22192, 15.45000000000000107 ) ;
#22960=CARTESIAN_POINT ( 'NONE',  ( -21.65013772846999984, -0.7453069750031999785, 11.13564762747999914 ) ) ;
#22961=CARTESIAN_POINT ( 'NONE',  ( -15.01980243943000026, 9.926543453055000299, 4.231053017515000292 ) ) ;
#22962=DIRECTION ( 'NONE',  ( 1.000000000000000000, 0.000000000000000000, 0.000000000000000000 ) ) ;
#22963=CARTESIAN_POINT ( 'NONE',  ( 15.87062451746000136, 7.573146751075999994, 6.130183788350000995 ) ) ;
#22965=DIRECTION ( 'NONE',  ( 0.000000000000000000, 1.000000000000000000, 0.000000000000000000 ) ) ;
#22966=CARTESIAN_POINT ( 'NONE',  ( 20.84425946885999892, 10.21728774804000039, -0.02082316127604999859 ) ) ;
#22967=ORIENTED_EDGE ( 'NONE', *, *, #5676, .F. ) ;
#22968=VECTOR ( 'NONE', #19463, 1000.000000000000000 ) ;
#22969=CARTESIAN_POINT ( 'NONE',  ( 18.43276763470113977, -1.730528564387503687, 9.411642275345988295 ) ) ;
#22971=CARTESIAN_POINT ( 'NONE',  ( -2.590695557940999816, 11.85722059114999638, 3.971571042362003645 ) ) ;
#22974=CARTESIAN_POINT ( 'NONE',  ( -14.42210300337531770, 4.045542311194462393, -8.116575561360184210 ) ) ;
#22975=CARTESIAN_POINT ( 'NONE',  ( -19.91018437026999877, -4.577733189479999965, 10.05552272314999840 ) ) ;
#22976=DIRECTION ( 'NONE',  ( -1.000000000000000000, 0.000000000000000000, 0.000000000000000000 ) ) ;
#22978=EDGE_LOOP ( 'NONE', ( #22203, #6666, #7924, #14303 ) ) ;
#22979=CARTESIAN_POINT ( 'NONE',  ( -4.900699999999999612, 1.284663064832999817E-14, 0.000000000000000000 ) ) ;
#22980=CARTESIAN_POINT ( 'NONE',  ( -4.749997084077000054, 12.55000000011000161, -4.491085162427999259E-09 ) ) ;
#22981=CARTESIAN_POINT ( 'NONE',  ( -4.276707022270998415, 13.50735784737998735, 4.819750607759997862 ) ) ;
#22984=ADVANCED_FACE ( 'NONE', ( #13458 ), #14427, .F. ) ;
#22985=CARTESIAN_POINT ( 'NONE',  ( -6.089787304710518434, 16.07459693448465998, -1.026727111026596528 ) ) ;
#22986=CARTESIAN_POINT ( 'NONE',  ( 12.92793875730999886, -7.038709952280000515, 5.788476981990000603 ) ) ;
#22988=ORIENTED_EDGE ( 'NONE', *, *, #5402, .F. ) ;
#22990=LINE ( 'NONE', #835, #15314 ) ;
#22991=CARTESIAN_POINT ( 'NONE',  ( 1.004156133560362374, 13.74043590524155611, -6.042168540479655903 ) ) ;
#22997=CARTESIAN_POINT ( 'NONE',  ( 14.40587415921926251, -4.504273601744794853, 7.838925639499337628 ) ) ;
#22998=CARTESIAN_POINT ( 'NONE',  ( 14.44790149212718156, 6.135938681383620974, -8.358155082646094414 ) ) ;
#22999=CARTESIAN_POINT ( 'NONE',  ( -4.364381710089920929, 13.57203098063190438, 4.996831629903377703 ) ) ;
#23006=CARTESIAN_POINT ( 'NONE',  ( 11.78924557933399875, -8.668821331392315699, 9.985146724267631058 ) ) ;
#23007=ORIENTED_EDGE ( 'NONE', *, *, #5844, .F. ) ;
#23008=CARTESIAN_POINT ( 'NONE',  ( -9.042815982636001948, 20.50000000000000000, 55.76088950527000065 ) ) ;
#23010=CARTESIAN_POINT ( 'NONE',  ( 2.490045692465482574, 13.01343478852942326, 6.243790476444181614 ) ) ;
#23012=CARTESIAN_POINT ( 'NONE',  ( 6.146720786676755033, 14.15407065691313093, -0.1974862381914592735 ) ) ;
#23013=CARTESIAN_POINT ( 'NONE',  ( -5.790975589382995281, 15.02417427529998939, -3.017301706163999953 ) ) ;
#23015=EDGE_CURVE ( 'NONE', #7090, #1524, #8874, .T. ) ;
#23024=CARTESIAN_POINT ( 'NONE',  ( 6.159835994203606724, 14.07226188649447707, 0.4016429018227478109 ) ) ;
#23025=CARTESIAN_POINT ( 'NONE',  ( 15.16948588246496854, 6.616435942061880127, 7.943911616450581192 ) ) ;
#23026=CARTESIAN_POINT ( 'NONE',  ( -15.45409440152999991, 1.691041824560000073, -10.90062380652000051 ) ) ;
#23027=AXIS2_PLACEMENT_3D ( 'NONE', #11689, #23050, #17251 ) ;
#23029=CARTESIAN_POINT ( 'NONE',  ( -20.45858076833473049, 9.968623160409832096, -3.311721528445693785 ) ) ;
#23035=CARTESIAN_POINT ( 'NONE',  ( -16.22830427515723883, -2.009085296611893945, 10.21346353486777048 ) ) ;
#23037=DIRECTION ( 'NONE',  ( 1.000000000000000000, 0.000000000000000000, 0.000000000000000000 ) ) ;
#23038=CARTESIAN_POINT ( 'NONE',  ( 6.118390120404000321, 14.49807793005001777, -0.4535226805296005415 ) ) ;
#23039=CARTESIAN_POINT ( 'NONE',  ( -4.820914651057999656, 13.20110358116999905, -5.836454220812999694 ) ) ;
#23041=CARTESIAN_POINT ( 'NONE',  ( 16.13531392131000075, 9.604728693984000643, 1.402583754804999971 ) ) ;
#23048=CARTESIAN_POINT ( 'NONE',  ( 21.58708333333332163, -2.414572076269414946, 8.985188864258029540 ) ) ;
#23049=CARTESIAN_POINT ( 'NONE',  ( -23.22511994411532754, 9.140896836353345378, -1.774683072962275121 ) ) ;
#23050=DIRECTION ( 'NONE',  ( 1.000000000000000000, 0.000000000000000000, 0.000000000000000000 ) ) ;
#23051=CARTESIAN_POINT ( 'NONE',  ( 16.89463950886860744, 8.818331488848656363, 5.668027532568643778 ) ) ;
#23052=DIRECTION ( 'NONE',  ( 0.000000000000000000, 0.000000000000000000, 1.000000000000000000 ) ) ;
#23053=CARTESIAN_POINT ( 'NONE',  ( -14.49284524109528682, 11.34356441105102320, -5.352320976844095135 ) ) ;
#23054=FACE_OUTER_BOUND ( 'NONE', #21224, .T. ) ;
#23056=CARTESIAN_POINT ( 'NONE',  ( -4.544340308300998998, 13.49051417780999884, -5.132142894851999593 ) ) ;
#23057=CYLINDRICAL_SURFACE ( 'NONE', #22299, 1.000000000000000222 ) ;
#23059=VERTEX_POINT ( 'NONE', #21710 ) ;
#23060=CARTESIAN_POINT ( 'NONE',  ( 20.03377367193000325, 4.847508016323000213, 9.108486939822999062 ) ) ;
#23061=CARTESIAN_POINT ( 'NONE',  ( 23.67568178759826836, 5.018981409586317000, -9.344864196030615133 ) ) ;
#23064=CARTESIAN_POINT ( 'NONE',  ( -23.99212502904755340, -13.39645431917461771, -1.796660477931302680 ) ) ;
#23065=CARTESIAN_POINT ( 'NONE',  ( -0.6109688586221994067, 11.46768424835998168, -4.905989630836000259 ) ) ;
#23066=ORIENTED_EDGE ( 'NONE', *, *, #20459, .T. ) ;
#23067=CARTESIAN_POINT ( 'NONE',  ( -15.78639678782281131, -9.050916927008973545, 5.383602120784745537 ) ) ;
#23071=B_SPLINE_CURVE_WITH_KNOTS ( 'NONE', 3,
 ( #22186, #5600, #17093, #7526, #490, #7892, #9239, #13331, #20730, #22652, #26, #16726 ),
 .UNSPECIFIED., .F., .F.,
 ( 4, 2, 2, 2, 2, 4 ),
 ( 0.000000000000000000, 0.2499999999999920064, 0.3749999999999807931, 0.4374999999999751865, 0.4999999999999695799, 1.000000000000000000 ),
 .UNSPECIFIED. ) ;
#23074=ORIENTED_EDGE ( 'NONE', *, *, #9654, .T. ) ;
#23077=CARTESIAN_POINT ( 'NONE',  ( 15.96881424931000026, -5.728615299830999597, -9.061514726575000012 ) ) ;
#23078=CARTESIAN_POINT ( 'NONE',  ( -23.52518536351999856, -7.578138410264999791, 7.542607835675000594 ) ) ;
#23079=EDGE_CURVE ( 'NONE', #7890, #15169, #1358, .T. ) ;
#23080=CARTESIAN_POINT ( 'NONE',  ( -14.27333148495000081, -7.281001511342000576, -7.192128478635999578 ) ) ;
#23081=CARTESIAN_POINT ( 'NONE',  ( -6.332330438508005699, 16.43030572369001874, 1.007229720589999378 ) ) ;
#23082=CARTESIAN_POINT ( 'NONE',  ( 14.04249951745999958, 7.822669716756000646, 5.722386861447000150 ) ) ;
#23084=DIRECTION ( 'NONE',  ( -0.000000000000000000, 1.000000000000000000, 0.000000000000000000 ) ) ;
#23089=CONICAL_SURFACE ( 'NONE', #20022, 7.249999994591000529, 0.7853981633972997312 ) ;
#23090=CARTESIAN_POINT ( 'NONE',  ( -2.630645692287001847, 11.80156308281999067, 4.013429856067998180 ) ) ;
#23091=CARTESIAN_POINT ( 'NONE',  ( -19.39549577250665280, 8.011803281376410624, -4.617569357475225011 ) ) ;
#23092=CARTESIAN_POINT ( 'NONE',  ( -14.36261680801592000, 5.626503938841797670, -7.110814111431843720 ) ) ;
#23094=CARTESIAN_POINT ( 'NONE',  ( -22.08228346541999798, 8.068880685816999687, 7.633144572907999859 ) ) ;
#23095=AXIS2_PLACEMENT_3D ( 'NONE', #4324, #4444, #11715 ) ;
#23097=EDGE_LOOP ( 'NONE', ( #1194, #19762, #17929, #12144 ) ) ;
#23099=CARTESIAN_POINT ( 'NONE',  ( 4.647821725315998798, 14.83942339102000041, 4.018338400731999549 ) ) ;
#23102=CARTESIAN_POINT ( 'NONE',  ( -9.988839711695000290, -15.41946301301999966, 2.151533345712000056 ) ) ;
#23104=AXIS2_PLACEMENT_3D ( 'NONE', #2170, #16943, #10048 ) ;
#23105=AXIS2_PLACEMENT_3D ( 'NONE', #8415, #10598, #17983 ) ;
#23106=CARTESIAN_POINT ( 'NONE',  ( 12.05043875730999936, 7.573215573255999367, -5.027566056405999184 ) ) ;
#23107=CARTESIAN_POINT ( 'NONE',  ( 24.48327518124253643, 1.286795374954478932, 12.49999999999999822 ) ) ;
#23108=ADVANCED_FACE ( 'NONE', ( #8747 ), #6925, .F. ) ;
#23109=ORIENTED_EDGE ( 'NONE', *, *, #21823, .F. ) ;
#23113=CARTESIAN_POINT ( 'NONE',  ( -2.865402830231887243, 14.08554499887472566, -5.425456058132048121 ) ) ;
#23118=CARTESIAN_POINT ( 'NONE',  ( 14.47577869003221451, 6.916416855222763616, -7.723673430031631426 ) ) ;
#23119=CARTESIAN_POINT ( 'NONE',  ( -4.510025733234193979, 13.50215798145615942, 5.101579666907003485 ) ) ;
#23120=CARTESIAN_POINT ( 'NONE',  ( -21.13391243917332218, 8.973862284426854075, -2.411528142513474915 ) ) ;
#23122=CARTESIAN_POINT ( 'NONE',  ( 0.000000000000000000, 21.50000000000000000, 0.000000000000000000 ) ) ;
#23125=FACE_OUTER_BOUND ( 'NONE', #9526, .T. ) ;
#23130=CARTESIAN_POINT ( 'NONE',  ( -0.8063831873887827850, 12.82547172164913718, 6.621239620338749354 ) ) ;
#23131=DIRECTION ( 'NONE',  ( 0.000000000000000000, 1.000000000000000000, 0.000000000000000000 ) ) ;
#23132=DIRECTION ( 'NONE',  ( -1.000000000000000000, 0.000000000000000000, 0.000000000000000000 ) ) ;
#23133=ADVANCED_FACE ( 'NONE', ( #23746 ), #12735, .F. ) ;
#23134=CIRCLE ( 'NONE', #2253, 7.000000000000000000 ) ;
#23138=CARTESIAN_POINT ( 'NONE',  ( -14.00000000000000000, -10.27687089286999900, -0.6428416445564000270 ) ) ;
#23139=CIRCLE ( 'NONE', #18893, 4.750000000000000000 ) ;
#23141=FACE_OUTER_BOUND ( 'NONE', #5953, .T. ) ;
#23142=EDGE_CURVE ( 'NONE', #11779, #3740, #22892, .T. ) ;
#23143=ORIENTED_EDGE ( 'NONE', *, *, #6587, .T. ) ;
#23144=CARTESIAN_POINT ( 'NONE',  ( -20.36066747213000028, -5.792492153153000700, -8.346631074955999097 ) ) ;
#23147=CARTESIAN_POINT ( 'NONE',  ( 20.52891666666666026, -2.407698974803198055, -8.958643823178077170 ) ) ;
#23148=CARTESIAN_POINT ( 'NONE',  ( 15.21050474296684740, 5.394461060204293723, 8.833667902654472215 ) ) ;
#23150=CARTESIAN_POINT ( 'NONE',  ( -16.17674766165999856, -7.868860569998000543, 7.758953960773999903 ) ) ;
#23152=CARTESIAN_POINT ( 'NONE',  ( -22.56483322422616311, -4.636276520427093928, 8.029449324473102223 ) ) ;
#23153=CARTESIAN_POINT ( 'NONE',  ( -4.720309893115999245, 12.53493801369999616, 0.1499651499519998876 ) ) ;
#23154=CARTESIAN_POINT ( 'NONE',  ( -14.45834475453999879, 5.064797291421999859, 10.11313827054000036 ) ) ;
#23155=AXIS2_PLACEMENT_3D ( 'NONE', #9362, #16735, #146 ) ;
#23157=EDGE_CURVE ( 'NONE', #8416, #1912, #13235, .T. ) ;
#23159=CARTESIAN_POINT ( 'NONE',  ( -6.042815432463000569, 16.37762245475000000, 0.9999999720525000191 ) ) ;
#23160=CARTESIAN_POINT ( 'NONE',  ( -15.27331153816034970, 3.763286766049342091, -9.840476004715160485 ) ) ;
#23161=VECTOR ( 'NONE', #15303, 1000.000000000000000 ) ;
#23164=CARTESIAN_POINT ( 'NONE',  ( 6.641840470203004720, 13.49927717272000294, -0.1936058750606000356 ) ) ;
#23165=CARTESIAN_POINT ( 'NONE',  ( 11.99999999999999822, 0.8847351093544478795, -8.935637287590818545 ) ) ;
#23167=CARTESIAN_POINT ( 'NONE',  ( 24.07420734439638821, 5.678657336858167426, -12.50000000000000355 ) ) ;
#23168=CARTESIAN_POINT ( 'NONE',  ( 13.39312642131000075, -9.609817522467999140, -0.6894128909195000876 ) ) ;
#23172=SURFACE_STYLE_USAGE ( .BOTH. , #16139 ) ;
#23173=CIRCLE ( 'NONE', #23952, 0.9999999999999991118 ) ;
#23176=CARTESIAN_POINT ( 'NONE',  ( -12.50000000000000000, 6.790122574649000597, -5.897138879738999862 ) ) ;
#23177=CARTESIAN_POINT ( 'NONE',  ( 11.43887872962561048, 9.287405149887408840, 8.913622445536628192 ) ) ;
#23179=CARTESIAN_POINT ( 'NONE',  ( -14.00000000000000000, 8.507292963980999545, 3.029321241734000303 ) ) ;
#23180=AXIS2_PLACEMENT_3D ( 'NONE', #6868, #5071, #14140 ) ;
#23181=CARTESIAN_POINT ( 'NONE',  ( 16.27717232079294263, 0.01447902640547235782, -10.36628560847415059 ) ) ;
#23182=CONICAL_SURFACE ( 'NONE', #4630, 9.152445778720998959, 0.02565634000431304615 ) ;
#23183=CARTESIAN_POINT ( 'NONE',  ( 12.00000000000000355, -4.925392270767085634, -8.318283231588928572 ) ) ;
#23184=CARTESIAN_POINT ( 'NONE',  ( -14.48633711635906174, 11.53909476760598807, -5.013715100885117515 ) ) ;
#23185=CARTESIAN_POINT ( 'NONE',  ( 20.27140652306000135, 7.802973122706000630, 8.032991296161000605 ) ) ;
#23187=CARTESIAN_POINT ( 'NONE',  ( -3.796676405536449028, 14.08940060151082108, -4.856290979845076627 ) ) ;
#23190=VERTEX_POINT ( 'NONE', #16704 ) ;
#23191=CARTESIAN_POINT ( 'NONE',  ( 21.43909193728000062, 4.096243081809999964, -10.09291015812000047 ) ) ;
#23192=CARTESIAN_POINT ( 'NONE',  ( 23.53381486928319077, 0.02178524961730664289, -10.60783701616260721 ) ) ;
#23194=CIRCLE ( 'NONE', #3821, 5.625000000000000000 ) ;
#23196=CARTESIAN_POINT ( 'NONE',  ( -23.74465998031000069, -13.93375672974000068, -0.8660254037843999608 ) ) ;
#23199=CARTESIAN_POINT ( 'NONE',  ( -14.13963379130298037, -4.565423490151436781, 9.281307119413254370 ) ) ;
#23201=B_SPLINE_CURVE_WITH_KNOTS ( 'NONE', 3,
 ( #11452, #1651, #7809, #20766 ),
 .UNSPECIFIED., .F., .F.,
 ( 4, 4 ),
 ( 0.000000000000000000, 1.000000000000000000 ),
 .UNSPECIFIED. ) ;
#23205=ORIENTED_EDGE ( 'NONE', *, *, #18856, .T. ) ;
#23206=CARTESIAN_POINT ( 'NONE',  ( -19.10300673838166574, 0.5074784849211602111, 9.209648430438782896 ) ) ;
#23207=CARTESIAN_POINT ( 'NONE',  ( -4.622988392615989817, 15.59405543785941006, -4.019176710598885371 ) ) ;
#23208=CARTESIAN_POINT ( 'NONE',  ( -23.09541789318999960, -10.91273857643000156, 2.518621640306000220 ) ) ;
#23209=CARTESIAN_POINT ( 'NONE',  ( -18.74219914028000034, 5.524159514902000190, 8.762982706192000038 ) ) ;
#23210=CARTESIAN_POINT ( 'NONE',  ( -6.214960006199002684, 16.43302743514002628, 1.007233960737000222 ) ) ;
#23211=CARTESIAN_POINT ( 'NONE',  ( 18.10499951746000136, -5.256258768401999681, 8.277723090073999757 ) ) ;
#23213=FACE_BOUND ( 'NONE', #10956, .T. ) ;
#23214=CARTESIAN_POINT ( 'NONE',  ( 5.315020105233999814, 13.91583881926999844, -3.802361444130999857 ) ) ;
#23215=ORIENTED_EDGE ( 'NONE', *, *, #17869, .F. ) ;
#23216=CARTESIAN_POINT ( 'NONE',  ( -2.126245409042402112, 13.91230505524877614, 5.744102105465449526 ) ) ;
#23219=CARTESIAN_POINT ( 'NONE',  ( -14.51410574374127904, 1.264063492210389716, -8.954773398761787462 ) ) ;
#23220=CARTESIAN_POINT ( 'NONE',  ( -23.25187528588000063, -11.01077565003999936, 1.685400950775999940 ) ) ;
#23221=CARTESIAN_POINT ( 'NONE',  ( 4.750000000000000000, 22.00000000000000000, 0.000000000000000000 ) ) ;
#23225=CARTESIAN_POINT ( 'NONE',  ( 1.999318247333280896, 11.65229316158473694, -4.385180337949393881 ) ) ;
#23226=CARTESIAN_POINT ( 'NONE',  ( 1.963372574454999464, 13.97765948033002026, 5.856068077966999574 ) ) ;
#23227=CARTESIAN_POINT ( 'NONE',  ( 11.77933705839073752, -1.226278748475006397, -8.915936121416093485 ) ) ;
#23228=CARTESIAN_POINT ( 'NONE',  ( -14.25243324638999809, 6.216878364870000340, 12.50000000000000000 ) ) ;
#23229=CARTESIAN_POINT ( 'NONE',  ( -11.31253221169000156, -12.85060658243000020, -8.789246050924999665 ) ) ;
#23230=CARTESIAN_POINT ( 'NONE',  ( -7.834000000000000519, 1.320585629393000037E-14, 0.000000000000000000 ) ) ;
#23231=CARTESIAN_POINT ( 'NONE',  ( 18.32906392130999862, 1.076221949391999999, 9.704785274157000430 ) ) ;
#23232=CARTESIAN_POINT ( 'NONE',  ( 18.92316945876704182, 2.674257117273544093, 10.08631798118172718 ) ) ;
#23237=CARTESIAN_POINT ( 'NONE',  ( 2.062592510876792851, 13.89940162384647948, -5.767274509907090341 ) ) ;
#23239=EDGE_LOOP ( 'NONE', ( #19863, #6879, #17229, #8291 ) ) ;
#23243=CARTESIAN_POINT ( 'NONE',  ( -5.372793533988000192, 16.07374366253000275, 2.940837684191000001 ) ) ;
#23245=CARTESIAN_POINT ( 'NONE',  ( 15.89751578318907299, -6.116246800416883289, -8.419007581516531502 ) ) ;
#23247=DIRECTION ( 'NONE',  ( 0.000000000000000000, 1.000000000000000000, 0.000000000000000000 ) ) ;
#23248=DIRECTION ( 'NONE',  ( -1.000000000000000000, 0.000000000000000000, 0.000000000000000000 ) ) ;
#23251=CARTESIAN_POINT ( 'NONE',  ( 11.09594815122425437, -11.32305097984590425, 5.387897831760633416 ) ) ;
#23252=ORIENTED_EDGE ( 'NONE', *, *, #2903, .T. ) ;
#23255=FACE_OUTER_BOUND ( 'NONE', #12241, .T. ) ;
#23256=CARTESIAN_POINT ( 'NONE',  ( 0.1121017584363108860, 12.80188320469649454, 6.666875631454949769 ) ) ;
#23258=FACE_OUTER_BOUND ( 'NONE', #4373, .T. ) ;
#23260=ORIENTED_EDGE ( 'NONE', *, *, #7066, .T. ) ;
#23262=CARTESIAN_POINT ( 'NONE',  ( -11.09999999999999964, 6.613190111079999767, -13.46349570337000046 ) ) ;
#23264=VERTEX_POINT ( 'NONE', #4112 ) ;
#23266=CARTESIAN_POINT ( 'NONE',  ( -19.06225528084999965, -10.03758185236999978, -0.2302352342852000133 ) ) ;
#23268=CARTESIAN_POINT ( 'NONE',  ( 15.18932757003898715, 6.036209813893644416, 8.395765448665670760 ) ) ;
#23271=CARTESIAN_POINT ( 'NONE',  ( -22.64045740894113834, -2.421573919205059156, 9.009506293889163686 ) ) ;
#23272=CARTESIAN_POINT ( 'NONE',  ( -4.503312502202000189, 12.37293047922001499, -1.619280038292999269 ) ) ;
#23274=CYLINDRICAL_SURFACE ( 'NONE', #7531, 3.000000000000000000 ) ;
#23278=ORIENTED_EDGE ( 'NONE', *, *, #4833, .T. ) ;
#23280=CARTESIAN_POINT ( 'NONE',  ( -16.80708775212494288, 10.12209424226509746, -2.478698942612353573 ) ) ;
#23283=CARTESIAN_POINT ( 'NONE',  ( 4.825493926286998914, 14.15457440094998987, -4.012025319334002305 ) ) ;
#23284=CARTESIAN_POINT ( 'NONE',  ( 11.99999999999999822, -6.567735135913689071, -6.123476794215256369 ) ) ;
#23285=CARTESIAN_POINT ( 'NONE',  ( 17.72694785191000122, -6.871380090573000032, -8.722589323108000059 ) ) ;
#23287=CARTESIAN_POINT ( 'NONE',  ( 16.16175158531000022, 8.345400111538999965, -5.893156809269999741 ) ) ;
#23289=CARTESIAN_POINT ( 'NONE',  ( -8.890913992921001707, 5.961159121560999807, -13.23730574134999927 ) ) ;
#23290=CARTESIAN_POINT ( 'NONE',  ( 24.50000000000000000, 0.000000000000000000, 0.000000000000000000 ) ) ;
#23291=ORIENTED_EDGE ( 'NONE', *, *, #19656, .F. ) ;
#23293=CARTESIAN_POINT ( 'NONE',  ( 8.124934037954998800, 1.125145054518999965E-14, 0.000000000000000000 ) ) ;
#23294=CARTESIAN_POINT ( 'NONE',  ( -18.13088126894000141, 1.446686056264999920E-14, 0.000000000000000000 ) ) ;
#23296=CARTESIAN_POINT ( 'NONE',  ( -14.00000000000000533, 5.593944997764537241, 7.525645797716226326 ) ) ;
#23297=CARTESIAN_POINT ( 'NONE',  ( 16.51941598158408553, 7.761714885866147995, -6.948838952575716377 ) ) ;
#23298=CARTESIAN_POINT ( 'NONE',  ( -5.618694691383806727, 14.59993743893240037, 4.601122152415220157 ) ) ;
#23299=CARTESIAN_POINT ( 'NONE',  ( -14.47158023610679933, 11.86027760101404738, -4.457335568564616324 ) ) ;
#23305=CARTESIAN_POINT ( 'NONE',  ( 19.84052273837000158, 9.448312643429998658, 4.133039138847000693 ) ) ;
#23306=CARTESIAN_POINT ( 'NONE',  ( 22.93797381236814559, -9.336338345241010472, 4.991623801638819025 ) ) ;
#23307=DIRECTION ( 'NONE',  ( 0.9999999999999997780, -2.086377177501379609E-08, -3.558922666258043983E-16 ) ) ;
#23309=ADVANCED_FACE ( 'NONE', ( #11275 ), #17516, .T. ) ;
#23312=EDGE_CURVE ( 'NONE', #4978, #15509, #15003, .T. ) ;
#23314=CARTESIAN_POINT ( 'NONE',  ( 4.917038878626002862, 12.44025957970000462, -0.1120513407610999462 ) ) ;
#23315=EDGE_LOOP ( 'NONE', ( #12635, #5558, #20229, #12526 ) ) ;
#23316=CARTESIAN_POINT ( 'NONE',  ( -15.95386421119776976, -4.621354449514186058, 9.465521188640689587 ) ) ;
#23317=CARTESIAN_POINT ( 'NONE',  ( 12.49102043323999922, -6.966913015870999537, -12.06696729233999932 ) ) ;
#23318=ORIENTED_EDGE ( 'NONE', *, *, #18533, .T. ) ;
#23324=ADVANCED_FACE ( 'NONE', ( #9332 ), #11335, .F. ) ;
#23326=CARTESIAN_POINT ( 'NONE',  ( -23.57717794809000011, 3.577206651746999810, 10.62669505086999955 ) ) ;
#23327=CARTESIAN_POINT ( 'NONE',  ( -14.61354174348999990, -2.554879995948999838, 10.47217342617999947 ) ) ;
#23328=CARTESIAN_POINT ( 'NONE',  ( 22.22954166666665543, -5.679568043481586059, -7.390219731457483121 ) ) ;
#23329=CARTESIAN_POINT ( 'NONE',  ( 17.42744494526000310, 7.698988374779999866, 6.881885182000000434 ) ) ;
#23333=CARTESIAN_POINT ( 'NONE',  ( 15.12470833333332720, -1.186001144903460203, -9.059411538103518069 ) ) ;
#23334=ORIENTED_EDGE ( 'NONE', *, *, #16060, .T. ) ;
#23339=CARTESIAN_POINT ( 'NONE',  ( -20.43190095651000249, 10.51156571426000141, -3.447590974849000123 ) ) ;
#23340=CARTESIAN_POINT ( 'NONE',  ( -3.789523947482483113, 12.08245691660683363, 3.002800408178633251 ) ) ;
#23344=CARTESIAN_POINT ( 'NONE',  ( 1.306883166391199058, 11.55337411466912378, -4.639543142079135762 ) ) ;
#23346=CARTESIAN_POINT ( 'NONE',  ( -20.71230420454666898, -5.655640480365105027, 7.359084460172671704 ) ) ;
#23347=AXIS2_PLACEMENT_3D ( 'NONE', #18676, #2321, #14791 ) ;
#23350=CARTESIAN_POINT ( 'NONE',  ( 17.34187642131000118, -3.686089773936000125, -9.013740861256998471 ) ) ;
#23351=CARTESIAN_POINT ( 'NONE',  ( -23.68078907432000335, -9.459496811531000304, -9.754788243598999975E-09 ) ) ;
#23352=VERTEX_POINT ( 'NONE', #11066 ) ;
#23353=CARTESIAN_POINT ( 'NONE',  ( -22.22922847155658843, -5.637976605639000383, 7.349597483169831413 ) ) ;
#23355=AXIS2_PLACEMENT_3D ( 'NONE', #19531, #17467, #19777 ) ;
#23356=CARTESIAN_POINT ( 'NONE',  ( -14.86049577250666687, -7.910114609640821470, 4.558959672250926687 ) ) ;
#23357=CARTESIAN_POINT ( 'NONE',  ( 3.079268300026640315, 14.15153817426477012, -5.294691079465464689 ) ) ;
#23360=CARTESIAN_POINT ( 'NONE',  ( -23.86847083087676324, -13.66493546063248132, 1.331637500039342115 ) ) ;
#23361=CARTESIAN_POINT ( 'NONE',  ( 6.086261285717811553, 14.38442930254080210, 0.7146526165609166092 ) ) ;
#23363=CARTESIAN_POINT ( 'NONE',  ( 16.48293693919926284, 10.26475150931634417, -1.776896041145952454 ) ) ;
#23364=DIRECTION ( 'NONE',  ( 1.000000000000000000, 0.000000000000000000, 0.000000000000000000 ) ) ;
#23365=CARTESIAN_POINT ( 'NONE',  ( -4.085036808003000175, 12.14322947999000135, 2.749988504941001999 ) ) ;
#23366=CARTESIAN_POINT ( 'NONE',  ( -12.25000000000000000, 6.489681479813073750, -13.21205004727046095 ) ) ;
#23367=ORIENTED_EDGE ( 'NONE', *, *, #6395, .F. ) ;
#23368=CARTESIAN_POINT ( 'NONE',  ( -14.67977372642998546, -9.047993639170183400, -0.9263344474169592502 ) ) ;
#23370=B_SPLINE_CURVE_WITH_KNOTS ( 'NONE', 3,
 ( #21168, #17536, #4580, #3137, #23214, #11971 ),
 .UNSPECIFIED., .F., .F.,
 ( 4, 1, 1, 4 ),
 ( 0.000000000000000000, 0.3333333333333000081, 0.6666666666667000474, 1.000000000000000000 ),
 .UNSPECIFIED. ) ;
#23371=ORIENTED_EDGE ( 'NONE', *, *, #19797, .T. ) ;
#23377=DIRECTION ( 'NONE',  ( -1.000000000000000000, 0.000000000000000000, 0.000000000000000000 ) ) ;
#23384=CARTESIAN_POINT ( 'NONE',  ( -23.59031210023999847, 7.092207792705000458, 8.788782243285998774 ) ) ;
#23385=CARTESIAN_POINT ( 'NONE',  ( 20.18879166666666336, -9.189365897221289714, -1.202758235422014543 ) ) ;
#23386=CARTESIAN_POINT ( 'NONE',  ( 15.08199357210373392, 8.700070515883242095, 5.582766916463140383 ) ) ;
#23388=CARTESIAN_POINT ( 'NONE',  ( -16.81976253787999909, -9.102909969768001375, 0.000000000000000000 ) ) ;
#23389=ADVANCED_FACE ( 'NONE', ( #15816 ), #18301, .T. ) ;
#23391=CARTESIAN_POINT ( 'NONE',  ( -18.73259798496000172, -8.620928137991000995, 3.072238420002000314 ) ) ;
#23392=CARTESIAN_POINT ( 'NONE',  ( 4.720309713848997113, 12.53493730558998998, 0.1499515764287999986 ) ) ;
#23394=CARTESIAN_POINT ( 'NONE',  ( -14.66147510250999808, 10.41001213865000175, 4.437054729469999792 ) ) ;
#23399=CARTESIAN_POINT ( 'NONE',  ( -16.89390527367012851, 8.934894438370687197, -5.364026527456945637 ) ) ;
#23401=CARTESIAN_POINT ( 'NONE',  ( 18.33699999999999974, -9.141845273363999880, 1.095420050962999850E-14 ) ) ;
#23402=CARTESIAN_POINT ( 'NONE',  ( 11.31235608933160819, -9.572705071928648835, -8.419524251220471101 ) ) ;
#23403=ADVANCED_FACE ( 'NONE', ( #10514 ), #2638, .F. ) ;
#23404=CARTESIAN_POINT ( 'NONE',  ( 12.00000000000000000, 3.198220168757963666, -8.391080537878064405 ) ) ;
#23405=CARTESIAN_POINT ( 'NONE',  ( 13.61040650243000094, -10.56087978152000062, 3.045457193391999606 ) ) ;
#23406=CARTESIAN_POINT ( 'NONE',  ( 14.07768908531000207, 0.2086024747513000044, -10.15948369482999958 ) ) ;
#23408=CARTESIAN_POINT ( 'NONE',  ( -10.01096149291999815, 13.11075716299000149, 6.234477108572999526 ) ) ;
#23409=PLANE ( 'NONE',  #11706 ) ;
#23412=CARTESIAN_POINT ( 'NONE',  ( -23.37274701946999755, 6.125680067344999813, -7.545173917617000292 ) ) ;
#23413=DIRECTION ( 'NONE',  ( -1.000000000000000000, 0.000000000000000000, 0.000000000000000000 ) ) ;
#23414=CARTESIAN_POINT ( 'NONE',  ( 22.52932875793747769, -3.641196223536565135, 9.931222262582332760 ) ) ;
#23416=CARTESIAN_POINT ( 'NONE',  ( -6.182361223440762110, 15.05471004068462193, -3.405165877464595869 ) ) ;
#23417=CARTESIAN_POINT ( 'NONE',  ( 17.14672531740638917, 1.317997890521231952, 10.34275493089012876 ) ) ;
#23418=CARTESIAN_POINT ( 'NONE',  ( -18.97978743917332878, 5.628138328197398010, 7.323710967538636929 ) ) ;
#23419=EDGE_CURVE ( 'NONE', #11805, #12236, #14034, .T. ) ;
#23421=CARTESIAN_POINT ( 'NONE',  ( -4.062644810066652568, 13.79322630918717962, -4.866505382640951005 ) ) ;
#23424=CARTESIAN_POINT ( 'NONE',  ( 23.75882644412315869, -9.280857264428881592, 0.6076903218426756847 ) ) ;
#23425=CARTESIAN_POINT ( 'NONE',  ( 11.66614181937085704, 8.864734480583086551, -9.645689288095473657 ) ) ;
#23428=B_SPLINE_CURVE_WITH_KNOTS ( 'NONE', 3,
 ( #3726, #11244, #3613, #2029, #4085, #9181 ),
 .UNSPECIFIED., .F., .F.,
 ( 4, 1, 1, 4 ),
 ( 0.000000000000000000, 0.3333333333333000081, 0.6666666666667000474, 1.000000000000000000 ),
 .UNSPECIFIED. ) ;
#23432=CARTESIAN_POINT ( 'NONE',  ( 23.77835672501372599, -9.281039036324623126, -1.918975276430111748E-05 ) ) ;
#23436=EDGE_LOOP ( 'NONE', ( #7363, #19804, #17156, #16687, #8260, #17955, #2815 ) ) ;
#23437=CARTESIAN_POINT ( 'NONE',  ( -14.50247987528135774, 7.489765101905747180, 7.283635598514888621 ) ) ;
#23438=DIRECTION ( 'NONE',  ( 0.9996708941621507138, 0.02565352539215873945, 0.000000000000000000 ) ) ;
#23442=EDGE_CURVE ( 'NONE', #16718, #12435, #22386, .T. ) ;
#23443=CARTESIAN_POINT ( 'NONE',  ( -14.37382046148723802, -4.385283933000476253, -12.49975322911771514 ) ) ;
#23445=CARTESIAN_POINT ( 'NONE',  ( -19.50708901484166446, 9.171872063609672665, 1.069867623823596459 ) ) ;
#23446=CARTESIAN_POINT ( 'NONE',  ( -4.536289218716924587, 15.51665606200187497, -4.115569062310257209 ) ) ;
#23447=CARTESIAN_POINT ( 'NONE',  ( -22.88283862364999877, -1.372540388790000065, -10.58604782883999995 ) ) ;
#23448=EDGE_CURVE ( 'NONE', #7987, #22092, #1031, .T. ) ;
#23449=CARTESIAN_POINT ( 'NONE',  ( -18.94532948824999963, 9.886987204373001603, 3.109815198001999903 ) ) ;
#23450=CARTESIAN_POINT ( 'NONE',  ( -6.323124832514003479, 16.13723008609998999, 0.9717865035293998810 ) ) ;
#23451=ADVANCED_FACE ( 'NONE', ( #11664 ), #19458, .F. ) ;
#23452=CARTESIAN_POINT ( 'NONE',  ( 18.51124951746000136, -9.033937733188000863, -3.841755647517000050 ) ) ;
#23458=ORIENTED_EDGE ( 'NONE', *, *, #12245, .F. ) ;
#23459=CARTESIAN_POINT ( 'NONE',  ( -17.19767920454667021, -2.385323164064429680, 8.875382679229677052 ) ) ;
#23460=CARTESIAN_POINT ( 'NONE',  ( 0.3879374145667575102, 13.69591497976315608, 6.116692095101760707 ) ) ;
#23464=CARTESIAN_POINT ( 'NONE',  ( -20.57852255339999914, 10.51534603707000137, -3.448831178700999978 ) ) ;
#23465=EDGE_CURVE ( 'NONE', #13026, #10425, #7682, .T. ) ;
#23468=CARTESIAN_POINT ( 'NONE',  ( -1.983357808483588114, 11.65004507716673210, 4.390781508571285130 ) ) ;
#23469=ORIENTED_EDGE ( 'NONE', *, *, #23900, .T. ) ;
#23470=CONICAL_SURFACE ( 'NONE', #15724, 13.23032192316000000, 1.235249617460683957 ) ;
#23471=LINE ( 'NONE', #6880, #12253 ) ;
#23472=CARTESIAN_POINT ( 'NONE',  ( 3.895813302869969519, 12.11565003950416397, -2.865938779683453230 ) ) ;
#23473=CARTESIAN_POINT ( 'NONE',  ( 24.03164415829611400, -5.349159599255311370, -7.707290229052887298 ) ) ;
#23474=CARTESIAN_POINT ( 'NONE',  ( 23.99062354302999722, -13.93375672974000068, -0.8660254037843999608 ) ) ;
#23475=EDGE_LOOP ( 'NONE', ( #23732, #20658, #11207, #8001 ) ) ;
#23477=CARTESIAN_POINT ( 'NONE',  ( -6.052215895878795493, 16.24384873199515411, -0.9999999999999972244 ) ) ;
#23479=CARTESIAN_POINT ( 'NONE',  ( 13.72218892130999990, -3.391610850449999770, -9.027048835217000189 ) ) ;
#23480=CARTESIAN_POINT ( 'NONE',  ( 18.45312019494581790, 9.917877877953065635, -3.199893147332716126 ) ) ;
#23481=EDGE_LOOP ( 'NONE', ( #23638, #7797, #3501, #22536, #13687, #12456, #8835, #22541, #11319, #10579 ) ) ;
#23482=CARTESIAN_POINT ( 'NONE',  ( -22.72066361546963620, 8.032224500089185426, 4.638484310570157199 ) ) ;
#23485=CARTESIAN_POINT ( 'NONE',  ( 13.49999999999999822, -6.476318932888407431, 7.855616484088395524 ) ) ;
#23486=AXIS2_PLACEMENT_3D ( 'NONE', #733, #19644, #8139 ) ;
#23487=ORIENTED_EDGE ( 'NONE', *, *, #23900, .F. ) ;
#23489=CARTESIAN_POINT ( 'NONE',  ( -24.16119556693467985, -12.87912905764661531, 2.692171137954526117 ) ) ;
#23490=CARTESIAN_POINT ( 'NONE',  ( 5.975075284666832687, 14.41257202741255128, 1.359510027979535574 ) ) ;
#23491=CARTESIAN_POINT ( 'NONE',  ( -23.69684149972337295, -9.477051524790651271, 0.8648883612165714219 ) ) ;
#23492=CONICAL_SURFACE ( 'NONE', #10364, 12.68487026514999982, 0.6105562205522639951 ) ;
#23493=CARTESIAN_POINT ( 'NONE',  ( 14.36426989841201518, 3.489952449228996390, -9.755240512065860514 ) ) ;
#23494=DIRECTION ( 'NONE',  ( 0.000000000000000000, -1.000000000000000000, 0.000000000000000000 ) ) ;
#23495=CARTESIAN_POINT ( 'NONE',  ( -3.293058160344002339, 11.97730948580998067, 3.707778763315998649 ) ) ;
#23498=EDGE_LOOP ( 'NONE', ( #13352, #9830, #9743, #15959 ) ) ;
#23499=ADVANCED_FACE ( 'NONE', ( #17342 ), #12027, .T. ) ;
#23503=ORIENTED_EDGE ( 'NONE', *, *, #18408, .F. ) ;
#23505=CARTESIAN_POINT ( 'NONE',  ( 5.905044978160000291, 14.55306956897999981, 1.663656914930999209 ) ) ;
#23507=VECTOR ( 'NONE', #13269, 1000.000000000000000 ) ;
#23508=CONICAL_SURFACE ( 'NONE', #9582, 9.136555860486998526, 0.02565634000431304615 ) ;
#23509=CARTESIAN_POINT ( 'NONE',  ( 19.70783333333331910, -0.3412242520863046913, 9.268130979224045163 ) ) ;
#23511=ORIENTED_EDGE ( 'NONE', *, *, #7750, .T. ) ;
#23517=CARTESIAN_POINT ( 'NONE',  ( -24.48886857509999970, -10.34867540887999837, -0.7644260386628000115 ) ) ;
#23519=CARTESIAN_POINT ( 'NONE',  ( 14.89266383929930093, 10.29194843803560744, -0.9031650063429182973 ) ) ;
#23520=FACE_OUTER_BOUND ( 'NONE', #7046, .T. ) ;
#23522=CARTESIAN_POINT ( 'NONE',  ( -22.79170577837355438, 2.421737280725368091, 9.013834718038792104 ) ) ;
#23523=CARTESIAN_POINT ( 'NONE',  ( 3.721017143809998373, 12.17176577897999579, -2.946712179682002386 ) ) ;
#23524=ORIENTED_EDGE ( 'NONE', *, *, #15881, .F. ) ;
#23530=VERTEX_POINT ( 'NONE', #12146 ) ;
#23533=CARTESIAN_POINT ( 'NONE',  ( 16.56079166666665969, -9.096264266808555377, -1.190571260499436512 ) ) ;
#23534=PLANE ( 'NONE',  #22761 ) ;
#23536=CARTESIAN_POINT ( 'NONE',  ( 18.78333224065999829, -3.764053801582000425, 9.968462294195999718 ) ) ;
#23539=CARTESIAN_POINT ( 'NONE',  ( -9.705493992920999347, -2.207063777844999741, 14.34885109169999851 ) ) ;
#23540=CIRCLE ( 'NONE', #22367, 10.59999999999999964 ) ;
#23541=CARTESIAN_POINT ( 'NONE',  ( 13.50000000000000000, 7.742518136641512783, 6.218115689482817565 ) ) ;
#23545=CARTESIAN_POINT ( 'NONE',  ( 11.07373617191558957, 11.07537056389167063, 5.816824279998757063 ) ) ;
#23546=CARTESIAN_POINT ( 'NONE',  ( 21.02918485986734254, -10.44527410498406006, 1.391412801358522522 ) ) ;
#23547=CARTESIAN_POINT ( 'NONE',  ( -14.00000000000000355, 7.297470702052054392, 5.625831777954100943 ) ) ;
#23548=CARTESIAN_POINT ( 'NONE',  ( 17.38903384696896026, -6.833465684892690462, 7.891901893606365626 ) ) ;
#23549=CARTESIAN_POINT ( 'NONE',  ( -19.09316243917332656, 8.004926875064779068, 4.613896613807892066 ) ) ;
#23550=CONICAL_SURFACE ( 'NONE', #5749, 13.23032192316000000, 1.235249617460683957 ) ;
#23557=ORIENTED_EDGE ( 'NONE', *, *, #13827, .T. ) ;
#23558=CARTESIAN_POINT ( 'NONE',  ( 11.97297107869919586, 13.24884602490437935, -2.052424400535973970 ) ) ;
#23559=CARTESIAN_POINT ( 'NONE',  ( 23.87429547323717927, 9.821396689478271824, -4.029826075455165579 ) ) ;
#23564=CARTESIAN_POINT ( 'NONE',  ( 4.877087740424957296, 14.45533858427638840, -3.799144659019715764 ) ) ;
#23565=CARTESIAN_POINT ( 'NONE',  ( -3.633619105303003138, 12.00370723790998539, -3.205740308949000639 ) ) ;
#23566=ORIENTED_EDGE ( 'NONE', *, *, #1275, .T. ) ;
#23567=VECTOR ( 'NONE', #19389, 1000.000000000000114 ) ;
#23569=CARTESIAN_POINT ( 'NONE',  ( 12.50898080071999985, -7.466894666658999924, -11.77830275166999918 ) ) ;
#23573=CIRCLE ( 'NONE', #4241, 6.125000000000002665 ) ;
#23578=CIRCLE ( 'NONE', #2695, 9.287173237303996132 ) ;
#23579=CARTESIAN_POINT ( 'NONE',  ( -4.252372020903545824, 15.23278328154970218, -4.409552293429433334 ) ) ;
#23580=CARTESIAN_POINT ( 'NONE',  ( -20.79521171905999921, 7.755012229217999931, -7.253067937808999943 ) ) ;
#23582=CARTESIAN_POINT ( 'NONE',  ( -18.40198888174000302, -9.811392118899000536, 0.2208054555764999982 ) ) ;
#23584=CARTESIAN_POINT ( 'NONE',  ( -24.47326038496474965, -0.9464271205007054322, -10.56558464230831618 ) ) ;
#23590=CARTESIAN_POINT ( 'NONE',  ( 4.701602651720952153, 14.74110825330134844, 3.931159545749582040 ) ) ;
#23594=CARTESIAN_POINT ( 'NONE',  ( -24.50000000000000000, -8.081477262649000792, -6.807253044743999837 ) ) ;
#23600=CARTESIAN_POINT ( 'NONE',  ( 4.825047752666590029, 12.44037768847285363, -0.5059731828766852457 ) ) ;
#23601=CARTESIAN_POINT ( 'NONE',  ( 24.21257416121859407, 4.458793670155209554, -8.532776386654354894 ) ) ;
#23602=CARTESIAN_POINT ( 'NONE',  ( -21.35476253787999923, 9.219287007783998789, 0.000000000000000000 ) ) ;
#23604=CARTESIAN_POINT ( 'NONE',  ( -10.04281598263999875, 20.50000000000000000, 1.000000000000000000 ) ) ;
#23605=CARTESIAN_POINT ( 'NONE',  ( 15.47718892131000068, -5.177634673800000975, -8.189908713891000502 ) ) ;
#23606=CARTESIAN_POINT ( 'NONE',  ( 18.47504315980862444, 10.13530769844259360, -2.440014412375295816 ) ) ;
#23607=ORIENTED_EDGE ( 'NONE', *, *, #1873, .T. ) ;
#23615=CARTESIAN_POINT ( 'NONE',  ( -24.50000000000292033, -11.08154813082897228, 5.806195610894957504 ) ) ;
#23620=LINE ( 'NONE', #7251, #10418 ) ;
#23621=CARTESIAN_POINT ( 'NONE',  ( 19.94399770046332421, 1.202189832516935564, 9.183084001584736811 ) ) ;
#23628=CARTESIAN_POINT ( 'NONE',  ( 5.752994088155999108, 14.16261243406998993, 1.981461215821998190 ) ) ;
#23629=CARTESIAN_POINT ( 'NONE',  ( 11.06626444616513005, -0.2510812432905764058, -12.49999588481644075 ) ) ;
#23630=ADVANCED_FACE ( 'NONE', ( #6567 ), #13951, .F. ) ;
#23631=CARTESIAN_POINT ( 'NONE',  ( 6.223219914810721676, 13.77310067638714663, -1.261352567770426480 ) ) ;
#23634=ORIENTED_EDGE ( 'NONE', *, *, #16504, .F. ) ;
#23635=CARTESIAN_POINT ( 'NONE',  ( -18.03317485555000133, 9.527592921995999831, -4.015252424095000272 ) ) ;
#23636=AXIS2_PLACEMENT_3D ( 'NONE', #19239, #9678, #11623 ) ;
#23637=DIRECTION ( 'NONE',  ( -1.000000000000000000, 0.000000000000000000, 0.000000000000000000 ) ) ;
#23638=ORIENTED_EDGE ( 'NONE', *, *, #6717, .F. ) ;
#23640=CARTESIAN_POINT ( 'NONE',  ( -19.40498875207000040, -4.215398836441999642, 9.787615664903000834 ) ) ;
#23643=CARTESIAN_POINT ( 'NONE',  ( 14.50354924558716796, 1.418337556017691181, -10.23477940919253548 ) ) ;
#23645=CARTESIAN_POINT ( 'NONE',  ( 23.75879881943000171, 10.74622900717000107, 3.476693416134999826 ) ) ;
#23647=CARTESIAN_POINT ( 'NONE',  ( 13.60029401354574219, 6.915711735797342108, -5.790824394749706450 ) ) ;
#23648=CARTESIAN_POINT ( 'NONE',  ( -4.459918930441997276, 12.50682294446000142, -1.621453085808000516 ) ) ;
#23655=CARTESIAN_POINT ( 'NONE',  ( 11.32654380052867005, -12.11008572905893566, -4.024656720663734255 ) ) ;
#23657=CARTESIAN_POINT ( 'NONE',  ( 14.51266099164999979, 10.53307723766999970, -3.225898445907000145 ) ) ;
#23659=CARTESIAN_POINT ( 'NONE',  ( -11.82901863877000004, 11.07399071560000081, 10.43874032931999984 ) ) ;
#23660=CARTESIAN_POINT ( 'NONE',  ( 13.49999999999999822, 9.484469744014797143, -1.016853796975950575 ) ) ;
#23663=CARTESIAN_POINT ( 'NONE',  ( 22.26459748180845111, 5.667341905249820400, 8.925277597039414701 ) ) ;
#23665=CARTESIAN_POINT ( 'NONE',  ( 15.91794248114183574, -9.831652891108184633, -3.269710195000794961 ) ) ;
#23666=CARTESIAN_POINT ( 'NONE',  ( -16.82086276118999990, 1.975286977287000090, -10.89076854460999932 ) ) ;
#23670=CARTESIAN_POINT ( 'NONE',  ( -15.75798294665000121, 9.136783202530001091, 3.374990494159999965 ) ) ;
#23672=ORIENTED_EDGE ( 'NONE', *, *, #4821, .F. ) ;
#23673=CARTESIAN_POINT ( 'NONE',  ( 23.39997263175174425, -2.403873558705119429, 8.975496745306065449 ) ) ;
#23674=CARTESIAN_POINT ( 'NONE',  ( 11.78693030656032725, 12.98156941793456376, -2.515258941385983160 ) ) ;
#23675=CARTESIAN_POINT ( 'NONE',  ( 20.72484988667089212, 3.141094275043142314, 10.05519821595702901 ) ) ;
#23677=AXIS2_PLACEMENT_3D ( 'NONE', #3764, #1603, #23862 ) ;
#23679=CARTESIAN_POINT ( 'NONE',  ( -12.50000000000000000, 6.992973968623999781, -5.709239639804999378 ) ) ;
#23680=CARTESIAN_POINT ( 'NONE',  ( -14.25547544441000092, -7.466299210344000237, -11.77864653853000121 ) ) ;
#23681=CARTESIAN_POINT ( 'NONE',  ( 4.548030535609999703, 12.31234507743998563, -1.688239928504997600 ) ) ;
#23682=ORIENTED_EDGE ( 'NONE', *, *, #4667, .F. ) ;
#23683=CARTESIAN_POINT ( 'NONE',  ( 16.43793875730999687, -4.200504661774999704, 8.191206307881000015 ) ) ;
#23687=CARTESIAN_POINT ( 'NONE',  ( -14.49863740500227216, 0.5184489068879251095, -12.49996363569464819 ) ) ;
#23688=ORIENTED_EDGE ( 'NONE', *, *, #10769, .T. ) ;
#23690=CARTESIAN_POINT ( 'NONE',  ( -19.99227829421999658, -4.688870380650000058, 9.502835446995000268 ) ) ;
#23692=CARTESIAN_POINT ( 'NONE',  ( 18.37479166666664909, -9.142815082014921657, -1.196664747960725084 ) ) ;
#23693=CARTESIAN_POINT ( 'NONE',  ( -24.37031988197636423, 2.803527235482467628, -10.22615976150734340 ) ) ;
#23695=DIRECTION ( 'NONE',  ( -1.000000000000000000, 0.000000000000000000, 0.000000000000000000 ) ) ;
#23699=DIRECTION ( 'NONE',  ( 0.000000000000000000, -0.9925668416490733836, -0.1217007183987965646 ) ) ;
#23700=DIRECTION ( 'NONE',  ( -1.000000000000000000, 0.000000000000000000, 0.000000000000000000 ) ) ;
#23704=CARTESIAN_POINT ( 'NONE',  ( 4.492058920961061297, 12.31709606397016898, 1.815161732821968021 ) ) ;
#23707=CARTESIAN_POINT ( 'NONE',  ( 0.3616284121818696962, 11.48838882713601883, -4.797856110140303443 ) ) ;
#23709=CARTESIAN_POINT ( 'NONE',  ( -10.33761176360648371, 15.67664585749226802, 1.227329692040328490 ) ) ;
#23712=FACE_OUTER_BOUND ( 'NONE', #9427, .T. ) ;
#23715=CARTESIAN_POINT ( 'NONE',  ( 14.38031392131000175, 9.076879665875999592, 3.306787424407999776 ) ) ;
#23716=CARTESIAN_POINT ( 'NONE',  ( 18.45488575664959896, 9.937485657898088576, -3.138395590753138009 ) ) ;
#23720=CARTESIAN_POINT ( 'NONE',  ( 18.71296080085999947, 8.147654916100000477, 8.033579312641000669 ) ) ;
#23721=CARTESIAN_POINT ( 'NONE',  ( 13.50000000000000178, -9.655853724928261883, 1.323126653348174697 ) ) ;
#23723=ORIENTED_EDGE ( 'NONE', *, *, #13824, .T. ) ;
#23724=CARTESIAN_POINT ( 'NONE',  ( -24.50000000000000000, 10.82531754731000007, 6.250000000000000000 ) ) ;
#23725=CARTESIAN_POINT ( 'NONE',  ( 23.93688783760000049, 6.590125990732999206, -8.595340802195000407 ) ) ;
#23728=DIRECTION ( 'NONE',  ( -0.000000000000000000, 0.8660254037844288266, 0.5000000000000169864 ) ) ;
#23729=CARTESIAN_POINT ( 'NONE',  ( -4.071056736052401703, 13.78562280736089107, 4.868570922598909334 ) ) ;
#23730=CARTESIAN_POINT ( 'NONE',  ( 3.799177505463000593, 12.12209995490999326, 3.177317162311001031 ) ) ;
#23732=ORIENTED_EDGE ( 'NONE', *, *, #13487, .T. ) ;
#23733=FACE_OUTER_BOUND ( 'NONE', #4146, .T. ) ;
#23738=EDGE_CURVE ( 'NONE', #16256, #8876, #21846, .T. ) ;
#23739=CARTESIAN_POINT ( 'NONE',  ( 11.66614181937909578, -3.921044720226404046, -12.49992990204019527 ) ) ;
#23740=CARTESIAN_POINT ( 'NONE',  ( 6.224373531547387373, 13.76762753968859165, -1.282219680938367690 ) ) ;
#23742=DIRECTION ( 'NONE',  ( 0.000000000000000000, -1.000000000000000000, 0.000000000000000000 ) ) ;
#23744=ORIENTED_EDGE ( 'NONE', *, *, #23419, .F. ) ;
#23746=FACE_OUTER_BOUND ( 'NONE', #4173, .T. ) ;
#23749=ORIENTED_EDGE ( 'NONE', *, *, #23015, .T. ) ;
#23750=CARTESIAN_POINT ( 'NONE',  ( -10.83930303495209380, 15.36257445830826285, -1.684799336714881468 ) ) ;
#23752=CARTESIAN_POINT ( 'NONE',  ( 14.42261690652483352, -1.401882518806423228, -10.22223842188914311 ) ) ;
#23753=CARTESIAN_POINT ( 'NONE',  ( 8.124934037954998800, 0.000000000000000000, 0.000000000000000000 ) ) ;
#23754=CARTESIAN_POINT ( 'NONE',  ( 21.15221597181999869, -10.99634298136000154, -2.244525743171999821 ) ) ;
#23757=CARTESIAN_POINT ( 'NONE',  ( 13.80186061669689224, 9.025291446785679739, 0.005808137674083918567 ) ) ;
#23758=EDGE_CURVE ( 'NONE', #9908, #19829, #4779, .T. ) ;
#23759=CARTESIAN_POINT ( 'NONE',  ( -1.421060907519000382, 11.74865550866998731, -4.622470049807997583 ) ) ;
#23761=ORIENTED_EDGE ( 'NONE', *, *, #168, .F. ) ;
#23762=CONICAL_SURFACE ( 'NONE', #13304, 14.15464499511999996, 0.6126053401530057174 ) ;
#23768=CARTESIAN_POINT ( 'NONE',  ( 21.64462270046331938, 4.646871317838020765, 8.062138474834723567 ) ) ;
#23770=CARTESIAN_POINT ( 'NONE',  ( 13.42995560457999993, -6.779495263956999196, 8.645408472313999226 ) ) ;
#23773=CARTESIAN_POINT ( 'NONE',  ( -10.61452256585000065, 4.516066062789000135, -14.16555620123000026 ) ) ;
#23774=CARTESIAN_POINT ( 'NONE',  ( 13.49999999999999822, 6.231970360783858354, -6.769108791265136205 ) ) ;
#23777=CARTESIAN_POINT ( 'NONE',  ( 21.97045161944091873, 10.72494003805814344, -0.1196986000478276607 ) ) ;
#23779=CARTESIAN_POINT ( 'NONE',  ( 16.10619618340015791, -5.817247716720235218, -8.575685592426966153 ) ) ;
#23780=CARTESIAN_POINT ( 'NONE',  ( -18.26616928144000340, 11.03552772663999981, -1.267153208245000107 ) ) ;
#23782=VECTOR ( 'NONE', #16831, 1000.000000000000000 ) ;
#23783=CARTESIAN_POINT ( 'NONE',  ( -18.73722805020999616, -7.945584595330000610, 4.815966472443999891 ) ) ;
#23785=EDGE_LOOP ( 'NONE', ( #12083, #12521, #9546, #22915, #10344 ) ) ;
#23786=CARTESIAN_POINT ( 'NONE',  ( 23.24887628969795372, 2.425622639895666399, 9.025022120430918449 ) ) ;
#23787=CARTESIAN_POINT ( 'NONE',  ( 20.18575559708055778, 8.684556385100460574, -5.939556492853414582 ) ) ;
#23790=CARTESIAN_POINT ( 'NONE',  ( 12.50898179946000077, 6.466848119989000665, 12.35567989459000060 ) ) ;
#23791=CYLINDRICAL_SURFACE ( 'NONE', #13130, 13.93375672974000068 ) ;
#23792=CARTESIAN_POINT ( 'NONE',  ( 3.211718233129003508, 11.87833580068998351, -3.657054441831002034 ) ) ;
#23793=VERTEX_POINT ( 'NONE', #11773 ) ;
#23801=CARTESIAN_POINT ( 'NONE',  ( -15.42147087121333371, -1.186998013042046773, 9.067027049713395570 ) ) ;
#23803=CARTESIAN_POINT ( 'NONE',  ( -20.10087239461999786, -8.560891429069998892, 5.321486511249999829 ) ) ;
#23805=CARTESIAN_POINT ( 'NONE',  ( -4.771218631688002532, 13.11106448824000026, -5.073972735316997884 ) ) ;
#23806=CARTESIAN_POINT ( 'NONE',  ( -23.21223922333086875, -9.596433927533320585, 4.441285397424103998 ) ) ;
#23808=CARTESIAN_POINT ( 'NONE',  ( -5.824604845557002974, 16.40175155375999339, 2.021265510678000421 ) ) ;
#23809=CONICAL_SURFACE ( 'NONE', #199, 9.157130689899000586, 0.02565634000431304615 ) ;
#23811=CARTESIAN_POINT ( 'NONE',  ( -17.12209587121333954, -4.588422834071612222, 7.960729490015661547 ) ) ;
#23812=CARTESIAN_POINT ( 'NONE',  ( 3.779214145209469855, 14.37913731383023297, 4.820907688989376716 ) ) ;
#23813=CARTESIAN_POINT ( 'NONE',  ( 14.77567797042977027, -6.635935015099072132, 6.230487974134251594 ) ) ;
#23814=CARTESIAN_POINT ( 'NONE',  ( 5.819228265851155157, 14.45505663675167796, -1.911080848660286158 ) ) ;
#23817=ORIENTED_EDGE ( 'NONE', *, *, #12889, .T. ) ;
#23818=CARTESIAN_POINT ( 'NONE',  ( -2.695181268941200692, 11.78983089400772855, -4.000416410329833639 ) ) ;
#23821=ORIENTED_EDGE ( 'NONE', *, *, #5402, .T. ) ;
#23824=CARTESIAN_POINT ( 'NONE',  ( -16.17730420454665463, 5.584121353372251129, -7.266021601655057616 ) ) ;
#23827=CARTESIAN_POINT ( 'NONE',  ( 11.52843892131000025, -9.307182416847998851, 0.9706197651944000748 ) ) ;
#23828=CARTESIAN_POINT ( 'NONE',  ( 18.45819154983377786, 9.973350390120506503, -3.023520947057698915 ) ) ;
#23833=ORIENTED_EDGE ( 'NONE', *, *, #21015, .F. ) ;
#23835=CARTESIAN_POINT ( 'NONE',  ( 22.78033775462999699, -7.550126252767999979, 8.445756667117999328 ) ) ;
#23836=EDGE_CURVE ( 'NONE', #10709, #11527, #6215, .T. ) ;
#23837=CARTESIAN_POINT ( 'NONE',  ( -24.00397000733149966, 1.618184422371759856, 9.698553049397601100 ) ) ;
#23839=CARTESIAN_POINT ( 'NONE',  ( 13.86248033612164754, -10.18903838342320611, -1.816066799785956087 ) ) ;
#23841=CARTESIAN_POINT ( 'NONE',  ( 4.103561096572000189, 12.21754528531001149, 2.770293696547999840 ) ) ;
#23843=CARTESIAN_POINT ( 'NONE',  ( -12.25000000000000000, 11.84440073488268652, -9.209314101129749019 ) ) ;
#23850=CARTESIAN_POINT ( 'NONE',  ( 6.140636424933997972, 13.62023824745998901, 2.542827786053999617 ) ) ;
#23851=CARTESIAN_POINT ( 'NONE',  ( 11.78924557931654249, -4.312980057965595471, -12.49999285599341547 ) ) ;
#23852=DIRECTION ( 'NONE',  ( 0.000000000000000000, 8.881784197001252323E-16, 1.000000000000000000 ) ) ;
#23854=CARTESIAN_POINT ( 'NONE',  ( 18.60131424931000055, 8.248882947719001990, 6.955037127929000640 ) ) ;
#23855=EDGE_CURVE ( 'NONE', #1933, #17483, #3299, .T. ) ;
#23856=DIRECTION ( 'NONE',  ( 0.000000000000000000, 0.000000000000000000, 1.000000000000000000 ) ) ;
#23859=CARTESIAN_POINT ( 'NONE',  ( -18.80493816619999947, -6.461643014194000223, 6.332623921217999552 ) ) ;
#23862=DIRECTION ( 'NONE',  ( 0.000000000000000000, 0.9981468999026679167, -0.06085035919937799298 ) ) ;
#23863=ORIENTED_EDGE ( 'NONE', *, *, #16439, .T. ) ;
#23864=CARTESIAN_POINT ( 'NONE',  ( -10.51126211288548795, 15.52477961147895158, -1.382190245016840846 ) ) ;
#23866=CARTESIAN_POINT ( 'NONE',  ( 14.52769910616910032, 2.258345615986147248, -10.08167035404599687 ) ) ;
#23867=CARTESIAN_POINT ( 'NONE',  ( -18.25584587121333868, -2.392196265530771360, -8.901927720310109038 ) ) ;
#23868=CARTESIAN_POINT ( 'NONE',  ( 18.97390937112000131, 0.006297815236294000002, 10.66796791185999993 ) ) ;
#23869=CARTESIAN_POINT ( 'NONE',  ( -24.50000000000000000, 3.293267271483000247, -9.759323269498999309 ) ) ;
#23870=ADVANCED_FACE ( 'NONE', ( #6795 ), #2829, .F. ) ;
#23871=CARTESIAN_POINT ( 'NONE',  ( 13.79933150931701213, 9.025147458263377942, -0.07313042455966387023 ) ) ;
#23872=CARTESIAN_POINT ( 'NONE',  ( -6.406436833942142250, 15.54626959098088612, -1.355418181164619762 ) ) ;
#23873=CARTESIAN_POINT ( 'NONE',  ( -22.07280420454664949, -7.387003317728245477, -5.677096218463232091 ) ) ;
#23874=EDGE_LOOP ( 'NONE', ( #17371, #3955, #12492, #13932, #11355, #5462, #21449, #3623, #20244, #756, #16895, #3415 ) ) ;
#23875=CARTESIAN_POINT ( 'NONE',  ( -14.79391872048465295, -6.742496754366980483, -6.069009251390668602 ) ) ;
#23876=CARTESIAN_POINT ( 'NONE',  ( -7.834000000000000519, 1.320585629393000037E-14, 0.000000000000000000 ) ) ;
#23877=EDGE_CURVE ( 'NONE', #14911, #17463, #21587, .T. ) ;
#23880=CARTESIAN_POINT ( 'NONE',  ( 16.82533333333332237, -4.584587517879673335, -7.954075159630586533 ) ) ;
#23881=CIRCLE ( 'NONE', #5329, 10.69999999999999929 ) ;
#23884=CARTESIAN_POINT ( 'NONE',  ( 15.56153707775999884, -10.50595843275999997, 3.407448292006999946 ) ) ;
#23885=CARTESIAN_POINT ( 'NONE',  ( -14.36292368913682793, 3.214461816234695846, 9.839097687039936702 ) ) ;
#23886=EDGE_CURVE ( 'NONE', #18634, #4204, #1231, .T. ) ;
#23890=CARTESIAN_POINT ( 'NONE',  ( -9.494475065846000206, -14.25618727434000022, -4.221251427306000004 ) ) ;
#23891=CARTESIAN_POINT ( 'NONE',  ( 13.50000000000000355, 7.849402262525473795, -4.941025682226755755 ) ) ;
#23894=CARTESIAN_POINT ( 'NONE',  ( 22.41167041299115681, 0.6016933124379368891, 10.56272183056112368 ) ) ;
#23895=CARTESIAN_POINT ( 'NONE',  ( 24.50000000000000000, 10.82531754731000007, -6.250000000000000000 ) ) ;
#23896=CARTESIAN_POINT ( 'NONE',  ( 15.96138423613740365, -9.219108122161413732, -4.736901002440107256 ) ) ;
#23897=VECTOR ( 'NONE', #4073, 1000.000000000000000 ) ;
#23898=CARTESIAN_POINT ( 'NONE',  ( -17.14814767310999599, -4.781802597067000171, -9.992171950030998673 ) ) ;
#23900=EDGE_CURVE ( 'NONE', #11139, #6021, #1108, .T. ) ;
#23906=CARTESIAN_POINT ( 'NONE',  ( 20.80997003765781983, 0.08280392278151330054, 10.53160635407974155 ) ) ;
#23909=CARTESIAN_POINT ( 'NONE',  ( 12.49102043339000012, 6.966815666558000331, 12.06702349699999921 ) ) ;
#23910=CARTESIAN_POINT ( 'NONE',  ( -5.966156734610001955, 14.84369745517001249, 4.200616803647995390 ) ) ;
#23911=CARTESIAN_POINT ( 'NONE',  ( 0.3761184368515001486, 11.43848625460998214, -4.857791548063001841 ) ) ;
#23914=CARTESIAN_POINT ( 'NONE',  ( 13.36668875730999950, -6.148145076040000490, -6.742444596879999530 ) ) ;
#23918=CARTESIAN_POINT ( 'NONE',  ( -14.49454881829679920, 0.9069790026173082387, -12.49996723895875839 ) ) ;
#23919=CONICAL_SURFACE ( 'NONE', #13471, 13.23032192316000000, 1.093540295016705466 ) ;
#23921=CARTESIAN_POINT ( 'NONE',  ( 22.66499770046333495, -1.211330063708917493, -9.252910224394478078 ) ) ;
#23922=VECTOR ( 'NONE', #6020, 1000.000000000000000 ) ;
#23924=CARTESIAN_POINT ( 'NONE',  ( -24.43671288875999892, 10.10651051612000018, 1.358723590744000065 ) ) ;
#23925=CARTESIAN_POINT ( 'NONE',  ( -15.35503366218999943, 4.356420647583999717, 8.699100579126000099 ) ) ;
#23926=CARTESIAN_POINT ( 'NONE',  ( -5.606472695148997154, 15.09370601804999623, -2.790885761882998750 ) ) ;
#23927=EDGE_CURVE ( 'NONE', #2037, #3147, #15956, .T. ) ;
#23929=CARTESIAN_POINT ( 'NONE',  ( -24.13870375024561454, 9.298829860497594524, -5.090628969465328169 ) ) ;
#23931=CIRCLE ( 'NONE', #3451, 7.500000000000000000 ) ;
#23932=DIRECTION ( 'NONE',  ( -0.000000000000000000, 0.5000000000000169864, 0.8660254037844288266 ) ) ;
#23935=CARTESIAN_POINT ( 'NONE',  ( 4.230504193311618977, 14.54539643883826372, 4.442872086443444779 ) ) ;
#23936=CARTESIAN_POINT ( 'NONE',  ( 4.698364960988029360, 13.53628448261239470, -5.010774751729513810 ) ) ;
#23938=CARTESIAN_POINT ( 'NONE',  ( -24.31263779340282483, -2.333065073542751833, -10.34449948205211633 ) ) ;
#23941=CARTESIAN_POINT ( 'NONE',  ( 3.525966305170764148, 12.00356175602403930, 3.304555447279709401 ) ) ;
#23942=ORIENTED_EDGE ( 'NONE', *, *, #17403, .T. ) ;
#23943=B_SPLINE_CURVE_WITH_KNOTS ( 'NONE', 3,
 ( #15953, #17918, #12583, #12700, #3266, #23227, #16076, #14035, #21428, #4842, #19968, #19850, #10650, #12225, #19616, #7005 ),
 .UNSPECIFIED., .F., .F.,
 ( 4, 2, 2, 2, 2, 2, 2, 4 ),
 ( 0.000000000000000000, 0.2500000000000000555, 0.3750000000000001110, 0.5000000000000001110, 0.6250000000000001110, 0.7500000000000000000, 0.8750000000000000000, 1.000000000000000000 ),
 .UNSPECIFIED. ) ;
#23944=CARTESIAN_POINT ( 'NONE',  ( -4.229965536171357066, 12.22545598775685072, -2.353907750527997056 ) ) ;
#23945=DIRECTION ( 'NONE',  ( 1.000000000000000000, 0.000000000000000000, 0.000000000000000000 ) ) ;
#23947=FACE_OUTER_BOUND ( 'NONE', #8614, .T. ) ;
#23950=CARTESIAN_POINT ( 'NONE',  ( 12.98081408531000136, 6.028018288394999757, 8.144720004203000130 ) ) ;
#23951=CARTESIAN_POINT ( 'NONE',  ( 18.81919638685927865, 6.056488561384143487, 8.493049548664323822 ) ) ;
#23952=AXIS2_PLACEMENT_3D ( 'NONE', #2316, #16723, #3903 ) ;
#23959=AXIS2_PLACEMENT_3D ( 'NONE', #21599, #13956, #17724 ) ;
#23961=CARTESIAN_POINT ( 'NONE',  ( 19.59345391583999785, -8.694423010569000354, -7.125817356098999689 ) ) ;
#23962=CARTESIAN_POINT ( 'NONE',  ( -24.29403582007070739, 10.10213813269781014, -1.507518411738413944 ) ) ;
#23964=CYLINDRICAL_SURFACE ( 'NONE', #15693, 15.45000000000000107 ) ;
#23965=CARTESIAN_POINT ( 'NONE',  ( -1.099784704884000375, 11.50157083293000504, 4.823590451572001392 ) ) ;
#23968=CARTESIAN_POINT ( 'NONE',  ( 17.94318924931000225, -0.08898103000111000360, -10.77198407497000154 ) ) ;
ENDSEC;
END-ISO-10303-21;
